ISO-10303-21;
HEADER;
/* Generated by software containing ST-Developer
 * from STEP Tools, Inc. (www.steptools.com) 
 */

FILE_DESCRIPTION(
/* description */ (''),
/* implementation_level */ '2;1');

FILE_NAME(
/* name */ 'Screw.step',
/* time_stamp */ '2026-10-04T22:13:49-07:00',
/* author */ (''),
/* organization */ (''),
/* preprocessor_version */ 'ST-DEVELOPER v20.2',
/* originating_system */ 'Autodesk Translation Framework v15.15.0.0',
/* authorisation */ '');

FILE_SCHEMA (('AUTOMOTIVE_DESIGN { 1 0 10303 214 3 1 1 }'));
ENDSEC;

DATA;
#10=MECHANICAL_DESIGN_GEOMETRIC_PRESENTATION_REPRESENTATION('',(#367),#40734);
#45=B_SPLINE_SURFACE_WITH_KNOTS('',3,3,((#19059,#19060,#19061,#19062,#19063,
#19064,#19065,#19066,#19067,#19068,#19069,#19070,#19071,#19072,#19073,#19074,
#19075,#19076,#19077,#19078,#19079,#19080,#19081,#19082,#19083,#19084,#19085,
#19086,#19087,#19088,#19089,#19090,#19091,#19092,#19093,#19094,#19095,#19096,
#19097,#19098,#19099,#19100,#19101,#19102,#19103,#19104,#19105,#19106,#19107,
#19108,#19109,#19110,#19111,#19112,#19113,#19114,#19115,#19116,#19117,#19118,
#19119,#19120,#19121,#19122,#19123,#19124,#19125,#19126,#19127,#19128,#19129,
#19130,#19131,#19132,#19133,#19134,#19135,#19136,#19137,#19138,#19139,#19140,
#19141,#19142,#19143,#19144,#19145,#19146,#19147,#19148,#19149,#19150,#19151,
#19152,#19153,#19154,#19155,#19156,#19157,#19158,#19159,#19160,#19161,#19162,
#19163,#19164,#19165,#19166,#19167,#19168,#19169,#19170,#19171,#19172,#19173,
#19174,#19175,#19176,#19177,#19178,#19179,#19180,#19181,#19182,#19183,#19184,
#19185,#19186,#19187,#19188,#19189,#19190,#19191,#19192,#19193,#19194,#19195,
#19196),(#19197,#19198,#19199,#19200,#19201,#19202,#19203,#19204,#19205,
#19206,#19207,#19208,#19209,#19210,#19211,#19212,#19213,#19214,#19215,#19216,
#19217,#19218,#19219,#19220,#19221,#19222,#19223,#19224,#19225,#19226,#19227,
#19228,#19229,#19230,#19231,#19232,#19233,#19234,#19235,#19236,#19237,#19238,
#19239,#19240,#19241,#19242,#19243,#19244,#19245,#19246,#19247,#19248,#19249,
#19250,#19251,#19252,#19253,#19254,#19255,#19256,#19257,#19258,#19259,#19260,
#19261,#19262,#19263,#19264,#19265,#19266,#19267,#19268,#19269,#19270,#19271,
#19272,#19273,#19274,#19275,#19276,#19277,#19278,#19279,#19280,#19281,#19282,
#19283,#19284,#19285,#19286,#19287,#19288,#19289,#19290,#19291,#19292,#19293,
#19294,#19295,#19296,#19297,#19298,#19299,#19300,#19301,#19302,#19303,#19304,
#19305,#19306,#19307,#19308,#19309,#19310,#19311,#19312,#19313,#19314,#19315,
#19316,#19317,#19318,#19319,#19320,#19321,#19322,#19323,#19324,#19325,#19326,
#19327,#19328,#19329,#19330,#19331,#19332,#19333,#19334),(#19335,#19336,
#19337,#19338,#19339,#19340,#19341,#19342,#19343,#19344,#19345,#19346,#19347,
#19348,#19349,#19350,#19351,#19352,#19353,#19354,#19355,#19356,#19357,#19358,
#19359,#19360,#19361,#19362,#19363,#19364,#19365,#19366,#19367,#19368,#19369,
#19370,#19371,#19372,#19373,#19374,#19375,#19376,#19377,#19378,#19379,#19380,
#19381,#19382,#19383,#19384,#19385,#19386,#19387,#19388,#19389,#19390,#19391,
#19392,#19393,#19394,#19395,#19396,#19397,#19398,#19399,#19400,#19401,#19402,
#19403,#19404,#19405,#19406,#19407,#19408,#19409,#19410,#19411,#19412,#19413,
#19414,#19415,#19416,#19417,#19418,#19419,#19420,#19421,#19422,#19423,#19424,
#19425,#19426,#19427,#19428,#19429,#19430,#19431,#19432,#19433,#19434,#19435,
#19436,#19437,#19438,#19439,#19440,#19441,#19442,#19443,#19444,#19445,#19446,
#19447,#19448,#19449,#19450,#19451,#19452,#19453,#19454,#19455,#19456,#19457,
#19458,#19459,#19460,#19461,#19462,#19463,#19464,#19465,#19466,#19467,#19468,
#19469,#19470,#19471,#19472),(#19473,#19474,#19475,#19476,#19477,#19478,
#19479,#19480,#19481,#19482,#19483,#19484,#19485,#19486,#19487,#19488,#19489,
#19490,#19491,#19492,#19493,#19494,#19495,#19496,#19497,#19498,#19499,#19500,
#19501,#19502,#19503,#19504,#19505,#19506,#19507,#19508,#19509,#19510,#19511,
#19512,#19513,#19514,#19515,#19516,#19517,#19518,#19519,#19520,#19521,#19522,
#19523,#19524,#19525,#19526,#19527,#19528,#19529,#19530,#19531,#19532,#19533,
#19534,#19535,#19536,#19537,#19538,#19539,#19540,#19541,#19542,#19543,#19544,
#19545,#19546,#19547,#19548,#19549,#19550,#19551,#19552,#19553,#19554,#19555,
#19556,#19557,#19558,#19559,#19560,#19561,#19562,#19563,#19564,#19565,#19566,
#19567,#19568,#19569,#19570,#19571,#19572,#19573,#19574,#19575,#19576,#19577,
#19578,#19579,#19580,#19581,#19582,#19583,#19584,#19585,#19586,#19587,#19588,
#19589,#19590,#19591,#19592,#19593,#19594,#19595,#19596,#19597,#19598,#19599,
#19600,#19601,#19602,#19603,#19604,#19605,#19606,#19607,#19608,#19609,#19610)),
 .UNSPECIFIED.,.F.,.F.,.F.,(4,4),(4,1,1,1,1,1,1,1,1,1,1,1,1,1,1,1,1,1,1,
1,1,1,1,1,1,1,1,1,1,1,1,1,1,1,1,1,1,1,1,1,1,1,1,1,1,1,1,1,1,1,1,1,1,1,1,
1,1,1,1,1,1,1,1,1,1,1,1,1,1,1,1,1,1,1,1,1,1,1,1,1,1,1,1,1,1,1,1,1,1,1,1,
1,1,1,1,1,1,1,1,1,1,1,1,1,1,1,1,1,1,1,1,1,1,1,1,1,1,1,1,1,1,1,1,1,1,1,1,
1,1,1,1,1,1,1,1,4),(-0.000231142210478152,0.0332102052225793),(8.30203615430837,
9.29477737004237,10.2875185857764,11.2802598015104,12.2730010172444,13.2657422329784,
14.2584834487124,15.2512246644464,16.2439658801804,17.2367070959144,18.2294483116484,
19.2221895273825,20.2149307431165,21.2076719588505,22.2004131745845,23.1931543903185,
24.1858956060525,25.1786368217865,26.1713780375205,27.1641192532545,28.1568604689885,
29.1496016847225,30.1423429004565,31.1350841161905,32.1278253319246,33.1205665476586,
34.1133077633926,35.1060489791266,36.0987901948606,37.0915314105946,38.0842726263286,
39.0770138420626,40.0697550577966,41.0624962735306,42.0552374892646,43.0479787049986,
44.0407199207326,45.0334611364667,46.0262023522007,47.0189435679347,48.0116847836687,
49.0044259994027,49.9971672151367,50.9899084308707,51.9826496466047,52.9753908623387,
53.9681320780727,54.9608732938067,55.9536145095407,56.9463557252747,57.9390969410088,
58.9318381567428,59.9245793724768,60.9173205882108,61.9100618039448,62.9028030196788,
63.8955442354128,64.8882854511468,65.8810266668808,66.8737678826148,67.8665090983488,
68.8592503140828,69.8519915298168,70.8447327455509,71.8374739612849,72.8302151770189,
73.8229563927529,74.8156976084869,75.8084388242209,76.8011800399549,77.7939212556889,
78.7866624714229,79.7794036871569,80.7721449028909,81.7648861186249,82.7576273343589,
83.750368550093,84.743109765827,85.735850981561,86.728592197295,87.721333413029,
88.714074628763,89.706815844497,90.699557060231,91.692298275965,92.685039491699,
93.677780707433,94.670521923167,95.663263138901,96.6560043546351,97.6487455703691,
98.6414867861031,99.6342280018371,100.626969217571,101.619710433305,102.612451649039,
103.605192864773,104.597934080507,105.590675296241,106.583416511975,107.576157727709,
108.568898943443,109.561640159177,110.554381374911,111.547122590645,112.539863806379,
113.532605022113,114.525346237847,115.518087453581,116.510828669315,117.503569885049,
118.496311100783,119.489052316517,120.481793532251,121.474534747985,122.467275963719,
123.460017179453,124.452758395187,125.445499610921,126.438240826655,127.430982042389,
128.423723258123,129.416464473857,130.409205689591,131.401946905325,132.394688121059,
133.387429336793,134.380170552527,135.372911768261,136.365652983995,137.358394199729,
138.351135415463,139.343876631197,140.336617846931,141.329359062665,142.322331420609),
 .UNSPECIFIED.);
#46=B_SPLINE_SURFACE_WITH_KNOTS('',3,3,((#19774,#19775,#19776,#19777,#19778,
#19779,#19780,#19781,#19782,#19783,#19784,#19785,#19786,#19787,#19788,#19789,
#19790,#19791,#19792,#19793,#19794,#19795,#19796,#19797,#19798,#19799,#19800,
#19801,#19802,#19803,#19804,#19805,#19806,#19807,#19808,#19809,#19810,#19811,
#19812,#19813,#19814,#19815,#19816,#19817,#19818,#19819,#19820,#19821,#19822,
#19823,#19824,#19825,#19826,#19827,#19828,#19829,#19830,#19831,#19832,#19833,
#19834,#19835,#19836,#19837,#19838,#19839,#19840,#19841,#19842,#19843,#19844,
#19845,#19846,#19847,#19848,#19849,#19850,#19851,#19852,#19853,#19854,#19855,
#19856,#19857,#19858,#19859,#19860,#19861,#19862,#19863,#19864,#19865,#19866,
#19867,#19868,#19869,#19870,#19871,#19872,#19873,#19874,#19875,#19876,#19877,
#19878,#19879,#19880,#19881,#19882,#19883,#19884,#19885,#19886,#19887,#19888,
#19889,#19890,#19891,#19892,#19893,#19894,#19895,#19896,#19897,#19898,#19899,
#19900,#19901,#19902,#19903,#19904,#19905,#19906,#19907,#19908,#19909,#19910,
#19911),(#19912,#19913,#19914,#19915,#19916,#19917,#19918,#19919,#19920,
#19921,#19922,#19923,#19924,#19925,#19926,#19927,#19928,#19929,#19930,#19931,
#19932,#19933,#19934,#19935,#19936,#19937,#19938,#19939,#19940,#19941,#19942,
#19943,#19944,#19945,#19946,#19947,#19948,#19949,#19950,#19951,#19952,#19953,
#19954,#19955,#19956,#19957,#19958,#19959,#19960,#19961,#19962,#19963,#19964,
#19965,#19966,#19967,#19968,#19969,#19970,#19971,#19972,#19973,#19974,#19975,
#19976,#19977,#19978,#19979,#19980,#19981,#19982,#19983,#19984,#19985,#19986,
#19987,#19988,#19989,#19990,#19991,#19992,#19993,#19994,#19995,#19996,#19997,
#19998,#19999,#20000,#20001,#20002,#20003,#20004,#20005,#20006,#20007,#20008,
#20009,#20010,#20011,#20012,#20013,#20014,#20015,#20016,#20017,#20018,#20019,
#20020,#20021,#20022,#20023,#20024,#20025,#20026,#20027,#20028,#20029,#20030,
#20031,#20032,#20033,#20034,#20035,#20036,#20037,#20038,#20039,#20040,#20041,
#20042,#20043,#20044,#20045,#20046,#20047,#20048,#20049),(#20050,#20051,
#20052,#20053,#20054,#20055,#20056,#20057,#20058,#20059,#20060,#20061,#20062,
#20063,#20064,#20065,#20066,#20067,#20068,#20069,#20070,#20071,#20072,#20073,
#20074,#20075,#20076,#20077,#20078,#20079,#20080,#20081,#20082,#20083,#20084,
#20085,#20086,#20087,#20088,#20089,#20090,#20091,#20092,#20093,#20094,#20095,
#20096,#20097,#20098,#20099,#20100,#20101,#20102,#20103,#20104,#20105,#20106,
#20107,#20108,#20109,#20110,#20111,#20112,#20113,#20114,#20115,#20116,#20117,
#20118,#20119,#20120,#20121,#20122,#20123,#20124,#20125,#20126,#20127,#20128,
#20129,#20130,#20131,#20132,#20133,#20134,#20135,#20136,#20137,#20138,#20139,
#20140,#20141,#20142,#20143,#20144,#20145,#20146,#20147,#20148,#20149,#20150,
#20151,#20152,#20153,#20154,#20155,#20156,#20157,#20158,#20159,#20160,#20161,
#20162,#20163,#20164,#20165,#20166,#20167,#20168,#20169,#20170,#20171,#20172,
#20173,#20174,#20175,#20176,#20177,#20178,#20179,#20180,#20181,#20182,#20183,
#20184,#20185,#20186,#20187),(#20188,#20189,#20190,#20191,#20192,#20193,
#20194,#20195,#20196,#20197,#20198,#20199,#20200,#20201,#20202,#20203,#20204,
#20205,#20206,#20207,#20208,#20209,#20210,#20211,#20212,#20213,#20214,#20215,
#20216,#20217,#20218,#20219,#20220,#20221,#20222,#20223,#20224,#20225,#20226,
#20227,#20228,#20229,#20230,#20231,#20232,#20233,#20234,#20235,#20236,#20237,
#20238,#20239,#20240,#20241,#20242,#20243,#20244,#20245,#20246,#20247,#20248,
#20249,#20250,#20251,#20252,#20253,#20254,#20255,#20256,#20257,#20258,#20259,
#20260,#20261,#20262,#20263,#20264,#20265,#20266,#20267,#20268,#20269,#20270,
#20271,#20272,#20273,#20274,#20275,#20276,#20277,#20278,#20279,#20280,#20281,
#20282,#20283,#20284,#20285,#20286,#20287,#20288,#20289,#20290,#20291,#20292,
#20293,#20294,#20295,#20296,#20297,#20298,#20299,#20300,#20301,#20302,#20303,
#20304,#20305,#20306,#20307,#20308,#20309,#20310,#20311,#20312,#20313,#20314,
#20315,#20316,#20317,#20318,#20319,#20320,#20321,#20322,#20323,#20324,#20325)),
 .UNSPECIFIED.,.F.,.F.,.F.,(4,4),(4,1,1,1,1,1,1,1,1,1,1,1,1,1,1,1,1,1,1,
1,1,1,1,1,1,1,1,1,1,1,1,1,1,1,1,1,1,1,1,1,1,1,1,1,1,1,1,1,1,1,1,1,1,1,1,
1,1,1,1,1,1,1,1,1,1,1,1,1,1,1,1,1,1,1,1,1,1,1,1,1,1,1,1,1,1,1,1,1,1,1,1,
1,1,1,1,1,1,1,1,1,1,1,1,1,1,1,1,1,1,1,1,1,1,1,1,1,1,1,1,1,1,1,1,1,1,1,1,
1,1,1,1,1,1,1,1,4),(-0.000203358763107571,0.0332327300170814),(11.6157025853675,
12.6086809632344,13.6014221789684,14.5941633947024,15.5869046104364,16.5796458261704,
17.5723870419044,18.5651282576385,19.5578694733725,20.5506106891065,21.5433519048405,
22.5360931205745,23.5288343363085,24.5215755520425,25.5143167677765,26.5070579835105,
27.4997991992445,28.4925404149785,29.4852816307125,30.4780228464465,31.4707640621806,
32.4635052779146,33.4562464936486,34.4489877093826,35.4417289251166,36.4344701408506,
37.4272113565846,38.4199525723186,39.4126937880526,40.4054350037866,41.3981762195206,
42.3909174352546,43.3836586509887,44.3763998667227,45.3691410824567,46.3618822981907,
47.3546235139247,48.3473647296587,49.3401059453927,50.3328471611267,51.3255883768607,
52.3183295925947,53.3110708083287,54.3038120240627,55.2965532397967,56.2892944555308,
57.2820356712648,58.2747768869988,59.2675181027328,60.2602593184668,61.2530005342008,
62.2457417499348,63.2384829656688,64.2312241814028,65.2239653971368,66.2167066128708,
67.2094478286048,68.2021890443388,69.1949302600729,70.1876714758069,71.1804126915409,
72.1731539072749,73.1658951230089,74.1586363387429,75.1513775544769,76.1441187702109,
77.1368599859449,78.1296012016789,79.1223424174129,80.1150836331469,81.107824848881,
82.100566064615,83.093307280349,84.086048496083,85.078789711817,86.071530927551,
87.064272143285,88.057013359019,89.049754574753,90.042495790487,91.035237006221,
92.027978221955,93.020719437689,94.0134606534231,95.0062018691571,95.9989430848911,
96.9916843006251,97.9844255163591,98.9771667320931,99.9699079478271,100.962649163561,
101.955390379295,102.948131595029,103.940872810763,104.933614026497,105.926355242231,
106.919096457965,107.911837673699,108.904578889433,109.897320105167,110.890061320901,
111.882802536635,112.875543752369,113.868284968103,114.861026183837,115.853767399571,
116.846508615305,117.839249831039,118.831991046773,119.824732262507,120.817473478241,
121.810214693975,122.802955909709,123.795697125443,124.788438341177,125.781179556911,
126.773920772645,127.766661988379,128.759403204113,129.752144419847,130.744885635581,
131.737626851315,132.730368067049,133.723109282783,134.715850498517,135.708591714251,
136.701332929985,137.694074145719,138.686815361453,139.679556577187,140.672297792921,
141.665039008655,142.657780224389,143.650521440123,144.643262655857,145.636003871591),
 .UNSPECIFIED.);
#83=B_SPLINE_CURVE_WITH_KNOTS('',3,(#6490,#6491,#6492,#6493,#6494,#6495,
#6496,#6497,#6498,#6499,#6500,#6501,#6502,#6503,#6504,#6505,#6506,#6507,
#6508,#6509,#6510,#6511,#6512,#6513,#6514,#6515,#6516,#6517,#6518,#6519,
#6520,#6521,#6522,#6523,#6524,#6525,#6526,#6527,#6528,#6529,#6530,#6531,
#6532,#6533,#6534,#6535,#6536,#6537,#6538,#6539,#6540,#6541,#6542,#6543,
#6544,#6545,#6546,#6547,#6548,#6549,#6550,#6551,#6552,#6553,#6554,#6555,
#6556,#6557,#6558,#6559,#6560,#6561,#6562,#6563,#6564,#6565,#6566,#6567,
#6568,#6569,#6570,#6571,#6572,#6573,#6574,#6575,#6576,#6577,#6578,#6579,
#6580,#6581,#6582,#6583,#6584,#6585,#6586,#6587,#6588,#6589,#6590,#6591,
#6592,#6593),.UNSPECIFIED.,.F.,.F.,(4,2,2,2,2,2,2,2,2,2,2,2,2,2,2,2,2,2,
2,2,2,2,2,2,2,2,2,2,2,2,2,2,2,2,2,2,2,2,2,2,2,2,2,2,2,2,2,2,2,2,2,4),(-0.388514427190929,
-0.368221310937293,-0.346791783756936,-0.343842853532956,-0.342674543962951,
-0.341819510444399,-0.340868810709443,-0.339445697276287,-0.335398541529993,
-0.32895292619097,-0.314550516013459,-0.291050761397792,-0.286392135096329,
-0.284273066173644,-0.282636675189563,-0.28086450600946,-0.278021181417783,
-0.267979780725477,-0.234896592289182,-0.227511697807702,-0.225702799566772,
-0.22465610901148,-0.223829575858867,-0.222664975514512,-0.22025973306123,
-0.217050085148467,-0.208937459508696,-0.185148325978312,-0.171212712264527,
-0.167979267254765,-0.166089040079341,-0.164449928003969,-0.162431611861429,
-0.158497993283455,-0.136834284450073,-0.112966254746684,-0.109341869582915,
-0.107941242202741,-0.106991115318562,-0.106014115977095,-0.104509334881813,
-0.100096609042361,-0.0928656015424145,-0.0773124844305157,-0.0560252071051106,
-0.0528876958272259,-0.0508429216859864,-0.0491823720855215,-0.0472669220909674,
-0.0438997461789251,-0.0262185413838201,-0.00172224983852417),
 .UNSPECIFIED.);
#84=B_SPLINE_CURVE_WITH_KNOTS('',3,(#6596,#6597,#6598,#6599,#6600,#6601,
#6602,#6603,#6604,#6605,#6606,#6607,#6608,#6609,#6610,#6611,#6612,#6613,
#6614,#6615,#6616,#6617,#6618,#6619,#6620,#6621,#6622,#6623,#6624,#6625,
#6626,#6627,#6628,#6629,#6630,#6631,#6632,#6633,#6634,#6635,#6636,#6637,
#6638,#6639,#6640,#6641,#6642,#6643,#6644,#6645,#6646,#6647,#6648,#6649,
#6650),.UNSPECIFIED.,.F.,.F.,(4,3,3,3,3,3,3,3,3,3,3,3,3,3,3,3,3,3,4),(11.6159397475004,
11.7400323994672,11.862567028973,11.985074843802,12.1075982462362,12.2328689254857,
12.3556466736646,12.4821638184495,12.6086809632344,12.7327736152012,12.8511026178218,
12.9692968137257,13.0874111577251,13.2055004593513,13.323702607504,13.4419711806477,
13.560458265704,13.6014221789684,13.6623817597106),.UNSPECIFIED.);
#85=B_SPLINE_CURVE_WITH_KNOTS('',3,(#6655,#6656,#6657,#6658,#6659,#6660,
#6661,#6662,#6663,#6664,#6665,#6666,#6667,#6668,#6669,#6670,#6671,#6672,
#6673,#6674,#6675,#6676,#6677,#6678,#6679,#6680,#6681,#6682,#6683,#6684,
#6685,#6686,#6687,#6688,#6689,#6690,#6691,#6692,#6693,#6694,#6695,#6696,
#6697,#6698,#6699,#6700,#6701,#6702,#6703,#6704,#6705,#6706,#6707,#6708,
#6709,#6710,#6711,#6712,#6713,#6714,#6715,#6716,#6717,#6718,#6719,#6720,
#6721,#6722,#6723,#6724,#6725,#6726,#6727,#6728,#6729,#6730,#6731,#6732,
#6733,#6734,#6735,#6736,#6737,#6738,#6739,#6740,#6741,#6742,#6743,#6744,
#6745,#6746,#6747,#6748,#6749,#6750,#6751,#6752,#6753,#6754,#6755,#6756,
#6757,#6758,#6759,#6760,#6761,#6762,#6763,#6764,#6765,#6766,#6767,#6768,
#6769,#6770,#6771,#6772,#6773,#6774,#6775,#6776,#6777,#6778,#6779,#6780,
#6781,#6782,#6783,#6784,#6785,#6786,#6787,#6788,#6789,#6790,#6791,#6792,
#6793,#6794,#6795,#6796,#6797,#6798,#6799,#6800,#6801,#6802,#6803,#6804,
#6805,#6806,#6807,#6808,#6809,#6810,#6811,#6812,#6813,#6814,#6815,#6816,
#6817,#6818,#6819,#6820,#6821,#6822,#6823,#6824,#6825,#6826,#6827,#6828,
#6829,#6830,#6831,#6832,#6833,#6834,#6835,#6836,#6837,#6838,#6839,#6840,
#6841,#6842,#6843,#6844,#6845,#6846,#6847,#6848,#6849,#6850,#6851,#6852,
#6853,#6854,#6855,#6856,#6857,#6858,#6859,#6860,#6861,#6862,#6863,#6864,
#6865,#6866,#6867,#6868,#6869,#6870,#6871,#6872,#6873,#6874),
 .UNSPECIFIED.,.F.,.F.,(4,2,2,2,2,2,2,2,2,2,2,2,2,2,2,2,2,2,2,2,2,2,2,2,
2,2,2,2,2,2,2,2,2,2,2,2,2,2,2,2,2,2,2,2,2,2,2,2,2,2,2,2,2,2,2,2,2,2,2,2,
2,2,2,2,2,2,2,2,2,2,2,2,2,2,2,2,2,2,2,2,2,2,2,2,2,2,2,2,2,2,2,2,2,2,2,2,
2,2,2,2,2,2,2,2,2,2,2,2,2,4),(-1.13034213650894,-1.11820041556272,-1.11177497333452,
-1.10702526459189,-1.10485747823376,-1.10320963951788,-1.10142274079296,
-1.09855015211907,-1.08933196811893,-1.05797328810593,-1.05142615478228,
-1.04732838922035,-1.04589136802156,-1.0449329513895,-1.04407836063236,
-1.04291101850557,-1.03996504071417,-1.01856767427725,-1.00089023061501,
-0.99451631738985,-0.989795890656017,-0.987633536452375,-0.985986620994032,
-0.98419760350581,-0.981314703344727,-0.971997099803371,-0.947031836916508,
-0.931352399734769,-0.929260956228999,-0.92816043504425,-0.92724610555965,
-0.926096197724991,-0.9242738535319,-0.913860420219523,-0.905378302347292,
-0.890964824454125,-0.874929853182554,-0.871673834827296,-0.869803389415422,
-0.868171797855497,-0.86615043382999,-0.863027939613639,-0.840359212284697,
-0.823002803884699,-0.816814311731417,-0.812878535714292,-0.811463204754879,
-0.810509129265617,-0.809649936427881,-0.808466211197927,-0.805458770482397,
-0.786547298096331,-0.76780885711994,-0.757118941048501,-0.754204369043874,
-0.752407656370931,-0.750761548758316,-0.748647663602783,-0.744071461326168,
-0.718193708769564,-0.703313973227802,-0.69863965860383,-0.695437100124942,
-0.694131129064522,-0.693198150743625,-0.692315151393086,-0.690773485775082,
-0.686249583783698,-0.678509337501351,-0.662821909200767,-0.640915208090116,
-0.637783632906045,-0.63576056827369,-0.634130361513526,-0.632264549260561,
-0.629024566980841,-0.613288092327909,-0.590011639141079,-0.5796148181095,
-0.577793949130371,-0.576644953121554,-0.575731081854003,-0.57463079288496,
-0.572540081175855,-0.556898177806101,-0.532038487071388,-0.52257177098094,
-0.519669399877649,-0.517875386921876,-0.516228573833571,-0.5140731795945,
-0.509395587447883,-0.503096525912975,-0.485779367623905,-0.463858351648118,
-0.460944071181973,-0.459775085167193,-0.458918891001253,-0.457955454832381,
-0.456509464126,-0.452374802532125,-0.445751668633164,-0.412950832225143,
-0.405181758156097,-0.402475709624456,-0.400721473034683,-0.399053286009071,
-0.396780642755917,-0.391448996417024,-0.388514427190929),.UNSPECIFIED.);
#86=B_SPLINE_CURVE_WITH_KNOTS('',3,(#6876,#6877,#6878,#6879,#6880,#6881,
#6882,#6883,#6884,#6885,#6886,#6887,#6888,#6889,#6890,#6891,#6892,#6893,
#6894,#6895,#6896,#6897,#6898,#6899,#6900,#6901,#6902,#6903,#6904,#6905,
#6906,#6907,#6908,#6909,#6910,#6911,#6912,#6913,#6914,#6915,#6916,#6917,
#6918,#6919,#6920,#6921,#6922,#6923,#6924,#6925,#6926,#6927,#6928,#6929,
#6930),.UNSPECIFIED.,.F.,.F.,(4,3,3,3,3,3,3,3,3,3,3,3,3,3,3,3,3,3,4),(13.6623817597106,
13.7822439330251,13.9019593887874,14.0215805270642,14.141159596228,14.2608366137815,
14.380560216883,14.5005136928787,14.5941633947024,14.7182560466692,14.838053126636,
14.9577353493353,15.0773549872691,15.1969642038554,15.3166972037048,15.4365049949453,
15.5565283172486,15.5869046104364,15.7079632679489),.UNSPECIFIED.);
#87=B_SPLINE_CURVE_WITH_KNOTS('',3,(#6931,#6932,#6933,#6934,#6935,#6936,
#6937,#6938,#6939,#6940,#6941,#6942,#6943,#6944,#6945,#6946,#6947,#6948,
#6949,#6950,#6951,#6952,#6953,#6954,#6955,#6956,#6957,#6958,#6959,#6960,
#6961,#6962,#6963,#6964,#6965,#6966,#6967,#6968,#6969,#6970,#6971,#6972,
#6973,#6974,#6975,#6976,#6977,#6978,#6979,#6980,#6981,#6982,#6983,#6984,
#6985,#6986,#6987,#6988,#6989,#6990,#6991,#6992,#6993,#6994,#6995,#6996,
#6997,#6998,#6999,#7000,#7001,#7002,#7003,#7004,#7005,#7006,#7007,#7008,
#7009,#7010,#7011,#7012,#7013,#7014,#7015,#7016,#7017,#7018,#7019,#7020,
#7021,#7022,#7023,#7024,#7025,#7026,#7027,#7028,#7029,#7030,#7031,#7032,
#7033,#7034,#7035,#7036,#7037,#7038,#7039,#7040,#7041,#7042,#7043,#7044,
#7045,#7046,#7047,#7048,#7049,#7050,#7051,#7052,#7053,#7054,#7055,#7056,
#7057,#7058,#7059,#7060,#7061,#7062,#7063,#7064,#7065,#7066,#7067,#7068,
#7069,#7070,#7071,#7072,#7073,#7074,#7075,#7076,#7077,#7078),
 .UNSPECIFIED.,.F.,.F.,(4,2,2,2,2,2,2,2,2,2,2,2,2,2,2,2,2,2,2,2,2,2,2,2,
2,2,2,2,2,2,2,2,2,2,2,2,2,2,2,2,2,2,2,2,2,2,2,2,2,2,2,2,2,2,2,2,2,2,2,2,
2,2,2,2,2,2,2,2,2,2,2,2,2,4),(-1.4842126102915,-1.45130207338096,-1.44653130870228,
-1.44276869942762,-1.44080057054265,-1.43934051164438,-1.43751243817818,
-1.4344104257189,-1.42265854661368,-1.39703504888428,-1.38855781433865,
-1.38526210078702,-1.38285473389067,-1.38168740855745,-1.38078564426567,
-1.37972798915731,-1.37788809376559,-1.37017195385148,-1.36675056177856,
-1.3445160894195,-1.32824044125102,-1.32496817415823,-1.32309142791469,
-1.3214560273151,-1.31943202057342,-1.31630906073201,-1.29380089136102,
-1.27658693263777,-1.27035072447172,-1.26639114431749,-1.26496911456164,
-1.26401104340175,-1.26315131940477,-1.26196698062992,-1.2589596710476,
-1.24090131187391,-1.22086735295395,-1.21057179383267,-1.2076926130244,
-1.20590414969959,-1.20425655965863,-1.20212813564549,-1.19746864097054,
-1.17384809453591,-1.16461532130469,-1.15161192875772,-1.14877183895778,
-1.14752773246244,-1.14660501956323,-1.14556920533366,-1.14377563658134,
-1.1369004973678,-1.13034372480405,-1.12505514274365,-1.1113946695191,-1.0999270589011,
-1.09505136269905,-1.09121913384257,-1.08922918810993,-1.0877587552546,
-1.08592503317702,-1.08283083981542,-1.0712707980281,-1.04563535180211,
-1.03715357075267,-1.03224704240593,-1.03071241032682,-1.02973378947652,
-1.02879532618135,-1.02763142312175,-1.024737534062,-1.00239397536905,-0.985353888275223,
-0.983952824113294),.UNSPECIFIED.);
#88=B_SPLINE_CURVE_WITH_KNOTS('',3,(#7084,#7085,#7086,#7087,#7088,#7089,
#7090,#7091,#7092,#7093,#7094,#7095,#7096,#7097,#7098,#7099,#7100,#7101,
#7102,#7103,#7104,#7105,#7106,#7107,#7108,#7109,#7110,#7111,#7112,#7113,
#7114,#7115,#7116,#7117,#7118,#7119,#7120,#7121,#7122,#7123,#7124,#7125,
#7126,#7127,#7128,#7129,#7130,#7131,#7132,#7133,#7134,#7135,#7136,#7137,
#7138,#7139,#7140,#7141,#7142,#7143,#7144,#7145,#7146,#7147,#7148,#7149,
#7150,#7151,#7152,#7153,#7154,#7155,#7156,#7157,#7158,#7159,#7160,#7161,
#7162,#7163,#7164,#7165,#7166,#7167,#7168,#7169,#7170,#7171,#7172,#7173,
#7174,#7175,#7176,#7177,#7178,#7179,#7180,#7181,#7182,#7183,#7184,#7185,
#7186,#7187,#7188,#7189,#7190,#7191,#7192,#7193,#7194,#7195,#7196,#7197,
#7198,#7199,#7200,#7201,#7202,#7203,#7204,#7205,#7206,#7207,#7208,#7209,
#7210,#7211,#7212,#7213,#7214,#7215,#7216,#7217,#7218,#7219,#7220,#7221,
#7222,#7223,#7224,#7225,#7226,#7227,#7228,#7229,#7230,#7231,#7232,#7233,
#7234,#7235,#7236,#7237,#7238,#7239,#7240,#7241),.UNSPECIFIED.,.F.,.F.,
(4,2,2,2,2,2,2,2,2,2,2,2,2,2,2,2,2,2,2,2,2,2,2,2,2,2,2,2,2,2,2,2,2,2,2,
2,2,2,2,2,2,2,2,2,2,2,2,2,2,2,2,2,2,2,2,2,2,2,2,2,2,2,2,2,2,2,2,2,2,2,2,
2,2,2,2,2,2,2,4),(-0.50063650275462,-0.497024637327494,-0.495221469099781,
-0.494172101298276,-0.493343476842378,-0.492172717878405,-0.489733842655887,
-0.48646488791054,-0.478116602320491,-0.453224652532998,-0.440866015760715,
-0.437708521725177,-0.43585911919942,-0.434388009039503,-0.432412512068425,
-0.428660542059646,-0.423915850114574,-0.412918930263119,-0.390000903402408,
-0.380088751451523,-0.378118092411696,-0.377030712610813,-0.37611507727911,
-0.374947899808193,-0.372527524358872,-0.369290559832854,-0.361065820328322,
-0.336791511166343,-0.323720090478632,-0.320552077568326,-0.318682313840578,
-0.317050171360907,-0.315026639774005,-0.311037965859611,-0.305908604171269,
-0.293519775473539,-0.275504200391794,-0.263046350866745,-0.261149301146257,
-0.259976754628464,-0.259060776951206,-0.257977550615054,-0.255969559166934,
-0.243626994095386,-0.218649328115914,-0.20638912865002,-0.203238106878432,
-0.201390134617007,-0.199918875936053,-0.197941519525203,-0.194180385200166,
-0.189420928527075,-0.178372117169142,-0.15215115604119,-0.145266667814842,
-0.143470367067601,-0.142432885763339,-0.141508973714647,-0.14030975903304,
-0.137650977813546,-0.133944521184283,-0.123810489935291,-0.09795895259853,
-0.0886339571623371,-0.0857493870782382,-0.0839594152448264,-0.0823116697759282,
-0.080148292349025,-0.0757326145299565,-0.0592212029193365,-0.0449233210994165,
-0.0286365008532833,-0.0267014876391612,-0.0255176528208188,-0.0246007846056997,
-0.0235257826118716,-0.0223781926196326,-0.0205714060941184,-0.000340550666543722),
 .UNSPECIFIED.);
#89=B_SPLINE_CURVE_WITH_KNOTS('',3,(#7242,#7243,#7244,#7245,#7246,#7247,
#7248,#7249,#7250,#7251,#7252,#7253,#7254,#7255,#7256,#7257,#7258,#7259,
#7260,#7261,#7262,#7263,#7264,#7265,#7266,#7267,#7268,#7269,#7270,#7271,
#7272,#7273,#7274,#7275,#7276,#7277,#7278,#7279,#7280,#7281,#7282,#7283,
#7284,#7285,#7286,#7287,#7288,#7289,#7290,#7291,#7292,#7293,#7294,#7295,
#7296,#7297,#7298,#7299,#7300,#7301,#7302,#7303,#7304,#7305,#7306,#7307,
#7308,#7309,#7310,#7311,#7312,#7313),.UNSPECIFIED.,.F.,.F.,(4,2,2,2,2,2,
2,2,2,2,2,2,2,2,2,2,2,2,2,2,2,2,2,2,2,2,2,2,2,2,2,2,2,2,2,4),(-1.37194901085214,
-1.34536824511777,-1.34239661910496,-1.34044614178634,-1.33857827078369,
-1.33694682595166,-1.33492292119506,-1.33179126924952,-1.31125702746167,
-1.29365158861557,-1.28627394289529,-1.28185440494781,-1.28040102360935,
-1.279419129298,-1.27848200570107,-1.27732337203004,-1.27446076747013,-1.25172253860903,
-1.23493567505875,-1.22564933688806,-1.22293752234361,-1.22114898911913,
-1.21950187176284,-1.21737481149489,-1.21272137552847,-1.18903102983852,
-1.17492030217937,-1.16853475121453,-1.16450967889086,-1.16308248541461,
-1.16212619743274,-1.1612698733031,-1.16009582551167,-1.15714334193878,
-1.13613143610354,-1.13034213650894),.UNSPECIFIED.);
#90=B_SPLINE_CURVE_WITH_KNOTS('',3,(#7314,#7315,#7316,#7317,#7318,#7319,
#7320,#7321,#7322,#7323,#7324,#7325,#7326,#7327,#7328,#7329,#7330,#7331,
#7332,#7333,#7334,#7335,#7336,#7337,#7338,#7339,#7340,#7341,#7342,#7343,
#7344,#7345,#7346,#7347,#7348,#7349,#7350,#7351,#7352,#7353,#7354,#7355,
#7356,#7357,#7358,#7359,#7360,#7361,#7362,#7363,#7364,#7365,#7366,#7367,
#7368,#7369,#7370,#7371,#7372,#7373,#7374,#7375,#7376,#7377,#7378,#7379,
#7380,#7381,#7382,#7383,#7384,#7385,#7386,#7387,#7388,#7389,#7390,#7391,
#7392,#7393,#7394,#7395,#7396,#7397,#7398,#7399,#7400,#7401,#7402,#7403,
#7404,#7405,#7406,#7407,#7408,#7409,#7410,#7411,#7412,#7413,#7414,#7415,
#7416,#7417,#7418,#7419,#7420,#7421,#7422,#7423,#7424,#7425,#7426,#7427,
#7428,#7429,#7430,#7431,#7432,#7433,#7434,#7435,#7436,#7437,#7438,#7439,
#7440,#7441,#7442,#7443,#7444,#7445,#7446,#7447,#7448,#7449,#7450,#7451,
#7452,#7453,#7454,#7455,#7456,#7457,#7458,#7459,#7460,#7461,#7462,#7463,
#7464,#7465,#7466,#7467,#7468,#7469,#7470,#7471,#7472,#7473,#7474,#7475,
#7476,#7477,#7478,#7479,#7480,#7481,#7482,#7483,#7484,#7485,#7486,#7487,
#7488,#7489,#7490,#7491,#7492,#7493,#7494,#7495,#7496,#7497,#7498,#7499,
#7500,#7501,#7502,#7503,#7504,#7505,#7506,#7507,#7508,#7509,#7510,#7511,
#7512,#7513,#7514,#7515,#7516,#7517,#7518,#7519,#7520,#7521,#7522,#7523,
#7524,#7525),.UNSPECIFIED.,.F.,.F.,(4,2,2,2,2,2,2,2,2,2,2,2,2,2,2,2,2,2,
2,2,2,2,2,2,2,2,2,2,2,2,2,2,2,2,2,2,2,2,2,2,2,2,2,2,2,2,2,2,2,2,2,2,2,2,
2,2,2,2,2,2,2,2,2,2,2,2,2,2,2,2,2,2,2,2,2,2,2,2,2,2,2,2,2,2,2,2,2,2,2,2,
2,2,2,2,2,2,2,2,2,2,2,2,2,2,2,4),(-0.983952824113294,-0.979112457342209,
-0.974467210153396,-0.972318108599363,-0.970672559708975,-0.968876428169694,
-0.965962748639736,-0.956367956378335,-0.925454067561909,-0.918936148615411,
-0.914851190701928,-0.9134154210932,-0.912456926202318,-0.911601816724087,
-0.910432824749628,-0.907510684142617,-0.885735684430236,-0.868321864233186,
-0.86200269440527,-0.857313497744151,-0.855156830607735,-0.85351072917423,
-0.851719152654242,-0.848824455782848,-0.839402772390256,-0.814521718062078,
-0.798874004326344,-0.796783280196324,-0.79568299312694,-0.794768810212375,
-0.793619032069579,-0.79179674190767,-0.781378236929632,-0.772879384216026,
-0.758416439463654,-0.742455947614859,-0.739242432341524,-0.737362976429339,
-0.735732756192979,-0.733724939901887,-0.729811076664254,-0.710344793261954,
-0.690555130412554,-0.681441642654773,-0.679514134972561,-0.678436812333014,
-0.677520688410213,-0.676341400787479,-0.673856830254932,-0.657571990761665,
-0.629363875052377,-0.6235329308949,-0.621118517170292,-0.619596915814238,
-0.617917721693957,-0.615563096914216,-0.609697241792277,-0.576305668323957,
-0.56441144503393,-0.562535875829102,-0.561369872435618,-0.560454549203759,
-0.559366831544476,-0.557336714035062,-0.544267051131203,-0.514184662095057,
-0.506800394592969,-0.504150088099636,-0.502584971541169,-0.500936077963987,
-0.498760679712532,-0.493968522749452,-0.487467358485707,-0.456539253956947,
-0.446978560843,-0.445026777089898,-0.443943845995054,-0.443028155468029,
-0.441856051730323,-0.439409069944889,-0.419040355454601,-0.392865542696693,
-0.388307656442141,-0.386197810391775,-0.38455302103317,-0.382755916582182,
-0.379836636757588,-0.369081443983243,-0.350140703300661,-0.346589037711122,
-0.330038268487219,-0.328103777119719,-0.326920315779717,-0.326003760019795,
-0.324929152495716,-0.322960633236989,-0.311703117048912,-0.295885020599676,
-0.2739338284628,-0.270791465048754,-0.268764127147645,-0.26713218555787,
-0.265266227696324,-0.26203065701868,-0.246426662707309,-0.242036404917214),
 .UNSPECIFIED.);
#91=B_SPLINE_CURVE_WITH_KNOTS('',3,(#7530,#7531,#7532,#7533,#7534,#7535,
#7536,#7537,#7538,#7539,#7540,#7541,#7542,#7543,#7544,#7545,#7546,#7547,
#7548,#7549,#7550,#7551,#7552,#7553,#7554,#7555,#7556,#7557,#7558,#7559,
#7560,#7561,#7562,#7563,#7564,#7565,#7566,#7567,#7568,#7569,#7570,#7571,
#7572,#7573,#7574,#7575,#7576,#7577,#7578,#7579,#7580,#7581,#7582,#7583,
#7584,#7585,#7586,#7587,#7588,#7589,#7590,#7591,#7592,#7593,#7594,#7595,
#7596,#7597,#7598,#7599,#7600,#7601,#7602,#7603,#7604,#7605,#7606,#7607,
#7608,#7609,#7610,#7611,#7612,#7613,#7614,#7615,#7616,#7617,#7618,#7619,
#7620,#7621,#7622,#7623,#7624,#7625,#7626,#7627,#7628,#7629,#7630,#7631,
#7632,#7633,#7634,#7635,#7636,#7637,#7638,#7639,#7640,#7641,#7642,#7643,
#7644,#7645,#7646,#7647,#7648,#7649,#7650,#7651,#7652,#7653,#7654,#7655,
#7656,#7657,#7658,#7659,#7660,#7661,#7662,#7663,#7664,#7665,#7666,#7667,
#7668,#7669,#7670,#7671,#7672,#7673,#7674,#7675,#7676,#7677,#7678,#7679,
#7680,#7681,#7682,#7683,#7684,#7685,#7686,#7687,#7688,#7689,#7690,#7691,
#7692,#7693,#7694,#7695,#7696,#7697,#7698,#7699,#7700,#7701,#7702,#7703,
#7704,#7705,#7706,#7707,#7708,#7709,#7710,#7711,#7712,#7713,#7714,#7715,
#7716,#7717,#7718,#7719,#7720,#7721,#7722,#7723,#7724,#7725,#7726,#7727,
#7728,#7729,#7730,#7731,#7732,#7733,#7734,#7735,#7736,#7737,#7738,#7739,
#7740,#7741,#7742,#7743,#7744,#7745,#7746,#7747),.UNSPECIFIED.,.F.,.F.,
(4,2,2,2,2,2,2,2,2,2,2,2,2,2,2,2,2,2,2,2,2,2,2,2,2,2,2,2,2,2,2,2,2,2,2,
2,2,2,2,2,2,2,2,2,2,2,2,2,2,2,2,2,2,2,2,2,2,2,2,2,2,2,2,2,2,2,2,2,2,2,2,
2,2,2,2,2,2,2,2,2,2,2,2,2,2,2,2,2,2,2,2,2,2,2,2,2,2,2,2,2,2,2,2,2,2,2,2,
2,4),(-1.24264336813119,-1.22712387526997,-1.20979043909343,-1.20357483124483,
-1.19962660535392,-1.19820958233988,-1.1972552015808,-1.19639682159987,
-1.19521511959944,-1.19221789981971,-1.17284850970692,-1.15440534164446,
-1.14380788165375,-1.14090173994353,-1.13910723124616,-1.13746117927735,
-1.13534465337651,-1.13075179952556,-1.10523906071215,-1.09828730208679,
-1.08489208712552,-1.082010351588,-1.08075827738038,-1.07983359958038,-1.07879956122474,
-1.07701855233006,-1.07030705950698,-1.06487313487277,-1.05809892239603,
-1.03713163172408,-1.0301386978465,-1.02507180193962,-1.0228476100675,-1.0211908289725,
-1.01963932991833,-1.01706257980809,-1.0102055054726,-0.979647202704972,
-0.970596590982185,-0.967150237728209,-0.964609930994401,-0.963419792553165,
-0.962502395743958,-0.961431833346224,-0.959535718783307,-0.950962199086458,
-0.919101737246764,-0.912525607385185,-0.907690497674577,-0.905507030483104,
-0.90385655098092,-0.902075736918723,-0.899232529315944,-0.890304074065052,
-0.864995358738982,-0.849182001509665,-0.847087495813602,-0.845986080348796,
-0.845071433052295,-0.843921636805775,-0.842100360838026,-0.831724092395496,
-0.829243987775399,-0.823742451505518,-0.809999637397287,-0.798595745451111,
-0.793735794587718,-0.789912071538546,-0.787921891398305,-0.786291819411394,
-0.784396573813481,-0.781116074382432,-0.766029631183796,-0.742162358302822,
-0.731835197619737,-0.730015707904923,-0.72886641777491,-0.727951734275185,
-0.726849742074642,-0.724752694641456,-0.708790487399557,-0.683089422239272,
-0.674617375026131,-0.671828296225942,-0.670059129977536,-0.668404071696104,
-0.666191366279745,-0.661191239826731,-0.654318641261029,-0.634045211892259,
-0.631755811411363,-0.614811879826588,-0.612876358682872,-0.611692393317409,
-0.610775533046097,-0.609700661792849,-0.607731841359522,-0.596477892339598,
-0.580653748784753,-0.558696996926903,-0.555554343478411,-0.553526596051362,
-0.551894177024496,-0.550027508688503,-0.546790271736406,-0.531166267807641,
-0.508897535085186,-0.504245027562709,-0.50063650275462),.UNSPECIFIED.);
#92=B_SPLINE_CURVE_WITH_KNOTS('',3,(#7749,#7750,#7751,#7752,#7753,#7754,
#7755,#7756,#7757,#7758,#7759,#7760,#7761,#7762,#7763,#7764,#7765,#7766,
#7767,#7768,#7769,#7770,#7771,#7772,#7773,#7774,#7775,#7776,#7777,#7778,
#7779,#7780,#7781,#7782,#7783,#7784,#7785,#7786,#7787,#7788,#7789,#7790,
#7791,#7792,#7793,#7794,#7795,#7796,#7797,#7798,#7799,#7800,#7801,#7802,
#7803,#7804,#7805,#7806,#7807,#7808,#7809,#7810,#7811,#7812,#7813,#7814,
#7815,#7816,#7817,#7818,#7819,#7820),.UNSPECIFIED.,.F.,.F.,(4,2,2,2,2,2,
2,2,2,2,2,2,2,2,2,2,2,2,2,2,2,2,2,2,2,2,2,2,2,2,2,2,2,2,2,4),(-0.242036404917214,
-0.224304689154436,-0.219081814344386,-0.212217338264901,-0.210423145404613,
-0.209386338842877,-0.208462666703193,-0.207216708244654,-0.204369011382599,
-0.191299921640434,-0.173017733276505,-0.156535286804907,-0.153193752754875,
-0.151285062299865,-0.149671724073372,-0.147705565778639,-0.144195939889097,
-0.139707951364804,-0.129590328758661,-0.10074616488669,-0.0948246251316918,
-0.0931187066129743,-0.0921012994788982,-0.0911712853451696,-0.0902432979436676,
-0.0880087333420003,-0.0730617412361167,-0.0581265465350124,-0.0394301049462768,
-0.0363181880100623,-0.0342999386601178,-0.0326684507778004,-0.0307954762365262,
-0.0288378594984424,-0.0258493948732865,-0.000340914984294712),
 .UNSPECIFIED.);
#93=B_SPLINE_CURVE_WITH_KNOTS('',3,(#7821,#7822,#7823,#7824,#7825,#7826,
#7827,#7828,#7829,#7830,#7831,#7832,#7833,#7834,#7835,#7836,#7837,#7838,
#7839,#7840,#7841,#7842,#7843,#7844,#7845,#7846,#7847,#7848,#7849,#7850,
#7851,#7852,#7853,#7854,#7855,#7856,#7857,#7858,#7859,#7860,#7861,#7862,
#7863,#7864,#7865,#7866,#7867,#7868,#7869,#7870,#7871,#7872,#7873,#7874,
#7875,#7876,#7877,#7878,#7879,#7880,#7881,#7882,#7883,#7884,#7885,#7886,
#7887,#7888,#7889,#7890,#7891,#7892,#7893,#7894,#7895,#7896,#7897,#7898,
#7899,#7900,#7901,#7902,#7903,#7904,#7905,#7906,#7907,#7908,#7909,#7910,
#7911,#7912,#7913,#7914,#7915,#7916,#7917,#7918,#7919,#7920,#7921,#7922,
#7923,#7924,#7925,#7926,#7927,#7928,#7929,#7930,#7931,#7932,#7933,#7934,
#7935,#7936,#7937,#7938,#7939,#7940,#7941,#7942,#7943,#7944,#7945,#7946,
#7947,#7948,#7949,#7950,#7951,#7952,#7953,#7954,#7955,#7956,#7957,#7958,
#7959,#7960,#7961,#7962,#7963,#7964,#7965,#7966,#7967,#7968,#7969,#7970,
#7971,#7972),.UNSPECIFIED.,.F.,.F.,(4,2,2,2,2,2,2,2,2,2,2,2,2,2,2,2,2,2,
2,2,2,2,2,2,2,2,2,2,2,2,2,2,2,2,2,2,2,2,2,2,2,2,2,2,2,2,2,2,2,2,2,2,2,2,
2,2,2,2,2,2,2,2,2,2,2,2,2,2,2,2,2,2,2,2,2,4),(-1.48452552344657,-1.46324998878013,
-1.46143255545788,-1.46028067119404,-1.45920273036994,-1.45828632138,-1.4571069253181,
-1.45518665640661,-1.43747892874884,-1.4195484851468,-1.40579231336392,
-1.40277758422884,-1.40090018600885,-1.39926894611929,-1.39725627461905,
-1.39416297392096,-1.37632827098489,-1.35346024078587,-1.34764165979955,
-1.34389961524338,-1.34254176559955,-1.34158318422872,-1.34072820483503,
-1.33956018512919,-1.33661235638184,-1.31524838903706,-1.29753439872821,
-1.291151877532,-1.28642611251312,-1.284262256449,-1.28261457971463,-1.28082510845336,
-1.27794230562532,-1.26863301093611,-1.24364684020745,-1.22795675751151,
-1.22586436687754,-1.22476337146837,-1.22384867599427,-1.22269833317034,
-1.22087531287728,-1.2104578294475,-1.20197289382995,-1.18755111677402,
-1.17151975238591,-1.16826324412659,-1.16639238783583,-1.16476036438029,
-1.16273837365398,-1.15961475105383,-1.13692504794917,-1.1195456143468,
-1.11336704461743,-1.10943558579736,-1.10802075636541,-1.10706674800836,
-1.10620784428835,-1.10502434185619,-1.10201679037227,-1.08363569870297,
-1.06722778238116,-1.05398717427103,-1.05088339342619,-1.04904563885963,
-1.04740919216897,-1.04533716553315,-1.04110214661615,-1.01139413227062,
-0.998975792054699,-0.994771046868928,-0.991813620582064,-0.990548338519137,
-0.989621606801628,-0.988593758881314,-0.986841354122029,-0.984153281563999),
 .UNSPECIFIED.);
#94=B_SPLINE_CURVE_WITH_KNOTS('',3,(#7978,#7979,#7980,#7981,#7982,#7983,
#7984,#7985,#7986,#7987,#7988,#7989,#7990,#7991,#7992,#7993,#7994,#7995,
#7996,#7997,#7998,#7999,#8000,#8001,#8002,#8003,#8004,#8005,#8006,#8007,
#8008,#8009,#8010,#8011,#8012,#8013,#8014,#8015,#8016,#8017,#8018,#8019,
#8020,#8021,#8022,#8023,#8024,#8025,#8026,#8027,#8028,#8029,#8030,#8031,
#8032,#8033,#8034,#8035,#8036,#8037,#8038,#8039,#8040,#8041,#8042,#8043,
#8044,#8045,#8046,#8047,#8048,#8049,#8050,#8051,#8052,#8053,#8054,#8055,
#8056,#8057,#8058,#8059,#8060,#8061,#8062,#8063,#8064,#8065,#8066,#8067,
#8068,#8069,#8070,#8071,#8072,#8073,#8074,#8075,#8076,#8077,#8078,#8079,
#8080,#8081,#8082,#8083,#8084,#8085,#8086,#8087,#8088,#8089,#8090,#8091,
#8092,#8093,#8094,#8095,#8096,#8097,#8098,#8099,#8100,#8101,#8102,#8103,
#8104,#8105,#8106,#8107,#8108,#8109,#8110,#8111,#8112,#8113,#8114,#8115,
#8116,#8117,#8118,#8119,#8120,#8121,#8122,#8123,#8124,#8125,#8126,#8127,
#8128,#8129),.UNSPECIFIED.,.F.,.F.,(4,2,2,2,2,2,2,2,2,2,2,2,2,2,2,2,2,2,
2,2,2,2,2,2,2,2,2,2,2,2,2,2,2,2,2,2,2,2,2,2,2,2,2,2,2,2,2,2,2,2,2,2,2,2,
2,2,2,2,2,2,2,2,2,2,2,2,2,2,2,2,2,2,2,2,2,4),(-0.500930905015856,-0.489414795378476,
-0.480595938752729,-0.477758763458719,-0.47597915635434,-0.474328044687318,
-0.472141138444648,-0.467287443190145,-0.460677618302062,-0.428398008132838,
-0.420227150845221,-0.418356128387158,-0.41729118119917,-0.416381572424069,
-0.415187698266216,-0.412628080405464,-0.393583200777573,-0.366105453164573,
-0.362080450391464,-0.360024535264082,-0.358496781341437,-0.356822075232639,
-0.354494845907435,-0.348807714003998,-0.340652043927438,-0.310642109202778,
-0.302892970599045,-0.301050213958518,-0.299991670589847,-0.299164427617486,
-0.298006775734322,-0.295635711675723,-0.292483681190909,-0.284583105366693,
-0.261147446158963,-0.246876973565852,-0.243636361419123,-0.241749920146631,
-0.240118931306484,-0.238116888669093,-0.234235985029833,-0.229283045541622,
-0.217545063671744,-0.195864794956641,-0.185881639625283,-0.184077288804618,
-0.182932472356574,-0.18201780299577,-0.180911543136154,-0.178794560374685,
-0.161526427743071,-0.132184626026053,-0.127403791955138,-0.125395489751191,
-0.123727408204824,-0.122047612538427,-0.119598017667965,-0.116786128127286,
-0.11165441678592,-0.0992575921436533,-0.0811582678166073,-0.0687842506521004,
-0.0668904483073508,-0.0657187973444854,-0.0648027827936573,-0.063718642147186,
-0.0617067190957231,-0.0492496180350549,-0.0183593721448643,-0.0110826221428734,
-0.00844911783150569,-0.00688674173760558,-0.00531457785453973,-0.0037118314827622,
-0.00203881054937059,-0.000340422350922375),.UNSPECIFIED.);
#95=B_SPLINE_CURVE_WITH_KNOTS('',3,(#8130,#8131,#8132,#8133,#8134,#8135,
#8136,#8137,#8138,#8139,#8140,#8141,#8142,#8143,#8144,#8145,#8146,#8147,
#8148,#8149,#8150,#8151,#8152,#8153,#8154,#8155,#8156,#8157,#8158,#8159,
#8160,#8161,#8162,#8163,#8164,#8165,#8166,#8167,#8168,#8169,#8170,#8171,
#8172,#8173,#8174,#8175,#8176,#8177,#8178,#8179,#8180,#8181,#8182,#8183,
#8184,#8185,#8186,#8187,#8188,#8189,#8190,#8191,#8192,#8193,#8194,#8195,
#8196,#8197,#8198,#8199,#8200,#8201,#8202,#8203,#8204,#8205,#8206,#8207),
 .UNSPECIFIED.,.F.,.F.,(4,2,2,2,2,2,2,2,2,2,2,2,2,2,2,2,2,2,2,2,2,2,2,2,
2,2,2,2,2,2,2,2,2,2,2,2,2,2,4),(-1.48418639400976,-1.48017874309778,-1.44813213191569,
-1.43936492498694,-1.43434588509554,-1.43279727926195,-1.43181461792903,
-1.43087752427373,-1.42971972877046,-1.42686314038833,-1.40400822573636,
-1.38250883373378,-1.37870546308272,-1.3764143956616,-1.37442443659962,
-1.3743926974679,-1.37435948447998,-1.37432460331821,-1.37275532211427,
-1.37096702527161,-1.36808897032653,-1.35882224098135,-1.33380902979447,
-1.3181100726536,-1.31601778901592,-1.31491689621603,-1.31400230905884,
-1.31285211772264,-1.311029356812,-1.3006132149743,-1.29213604341452,-1.27772466985114,
-1.2616891893659,-1.25843285733839,-1.25656218084475,-1.25493035618873,
-1.25290866190645,-1.2497855829382,-1.24264336813119),.UNSPECIFIED.);
#96=B_SPLINE_CURVE_WITH_KNOTS('',3,(#8208,#8209,#8210,#8211,#8212,#8213,
#8214,#8215,#8216,#8217,#8218,#8219,#8220,#8221,#8222,#8223,#8224,#8225,
#8226,#8227,#8228,#8229,#8230,#8231,#8232,#8233,#8234,#8235,#8236,#8237,
#8238,#8239,#8240,#8241,#8242,#8243,#8244,#8245,#8246,#8247,#8248,#8249,
#8250,#8251,#8252,#8253,#8254,#8255,#8256,#8257,#8258,#8259,#8260,#8261,
#8262,#8263,#8264,#8265,#8266,#8267,#8268,#8269,#8270,#8271,#8272,#8273,
#8274,#8275,#8276,#8277,#8278,#8279,#8280,#8281,#8282,#8283,#8284,#8285,
#8286,#8287,#8288,#8289,#8290,#8291,#8292,#8293,#8294,#8295,#8296,#8297,
#8298,#8299,#8300,#8301,#8302,#8303,#8304,#8305,#8306,#8307,#8308,#8309,
#8310,#8311,#8312,#8313,#8314,#8315,#8316,#8317,#8318,#8319,#8320,#8321,
#8322,#8323,#8324,#8325,#8326,#8327,#8328,#8329,#8330,#8331,#8332,#8333,
#8334,#8335,#8336,#8337,#8338,#8339,#8340,#8341,#8342,#8343,#8344,#8345,
#8346,#8347,#8348,#8349,#8350,#8351,#8352,#8353,#8354,#8355,#8356,#8357,
#8358,#8359,#8360,#8361,#8362,#8363,#8364,#8365,#8366,#8367,#8368,#8369,
#8370,#8371,#8372,#8373,#8374,#8375,#8376,#8377,#8378,#8379,#8380,#8381,
#8382,#8383,#8384,#8385,#8386,#8387,#8388,#8389,#8390,#8391,#8392,#8393,
#8394,#8395,#8396,#8397,#8398,#8399,#8400,#8401,#8402,#8403,#8404,#8405,
#8406,#8407,#8408,#8409,#8410,#8411,#8412,#8413,#8414,#8415,#8416,#8417),
 .UNSPECIFIED.,.F.,.F.,(4,2,2,2,2,2,2,2,2,2,2,2,2,2,2,2,2,2,2,2,2,2,2,2,
2,2,2,2,2,2,2,2,2,2,2,2,2,2,2,2,2,2,2,2,2,2,2,2,2,2,2,2,2,2,2,2,2,2,2,2,
2,2,2,2,2,2,2,2,2,2,2,2,2,2,2,2,2,2,2,2,2,2,2,2,2,2,2,2,2,2,2,2,2,2,2,2,
2,2,2,2,2,2,2,2,4),(-0.984153281563999,-0.980446617635857,-0.949083063846512,
-0.936591368536691,-0.933537702523708,-0.931710902589926,-0.930072520691694,
-0.927982019546928,-0.923650764903865,-0.894761695085295,-0.881852713101108,
-0.877549109366779,-0.874539290610191,-0.873265118657313,-0.872337057184719,
-0.871313400710301,-0.869579882426399,-0.863383163621796,-0.837874039499182,
-0.821409270227159,-0.817122453290162,-0.815040464802325,-0.81340300398146,
-0.811571257252587,-0.808494949596129,-0.797217304573491,-0.771318938491924,
-0.762792088943186,-0.7594773133826,-0.757012183290362,-0.755836340574079,
-0.754920092276665,-0.753839269750242,-0.751897874311517,-0.742542281486401,
-0.728504517050363,-0.704707562090513,-0.700054589302537,-0.697927004308375,
-0.696279176879146,-0.694489573228853,-0.691606626505655,-0.681277053976863,
-0.661140117196513,-0.643143298927895,-0.640120276386359,-0.638934177437661,
-0.638074599347353,-0.637121288783701,-0.635709964603215,-0.631804037019758,
-0.625681908418129,-0.60818730993821,-0.585548075802756,-0.582424636816855,
-0.580402655879584,-0.578770581989299,-0.576899603585641,-0.57364272427195,
-0.557608573605474,-0.54317306108342,-0.534678952657553,-0.524257815881781,
-0.522434485016907,-0.521284032655635,-0.520369300741631,-0.519268317035172,
-0.51717611250087,-0.501489747364672,-0.476508929189119,-0.467211192134723,
-0.464329542869904,-0.462540255681777,-0.460892390730031,-0.458727765152341,
-0.45399821087008,-0.447608380182307,-0.429860312323292,-0.408515568527029,
-0.405575784391122,-0.404403626315586,-0.403547572696955,-0.402590166129962,
-0.401159011280747,-0.397107348330107,-0.390664890546024,-0.373598181545457,
-0.351047533758038,-0.347921737886868,-0.345899064831565,-0.344266973291212,
-0.342396567963362,-0.339142225044656,-0.323161567880343,-0.308687691348596,
-0.300177412819621,-0.289754124345347,-0.287930737351276,-0.28678028110471,
-0.285865567874966,-0.28476463283225,-0.28267259205122,-0.266993032297975,
-0.242029482469724,-0.241988514754038),.UNSPECIFIED.);
#97=B_SPLINE_CURVE_WITH_KNOTS('',3,(#8422,#8423,#8424,#8425,#8426,#8427,
#8428,#8429,#8430,#8431,#8432,#8433,#8434,#8435,#8436,#8437,#8438,#8439,
#8440,#8441,#8442,#8443,#8444,#8445,#8446,#8447,#8448,#8449,#8450,#8451,
#8452,#8453,#8454,#8455,#8456,#8457,#8458,#8459,#8460,#8461,#8462,#8463,
#8464,#8465,#8466,#8467,#8468,#8469,#8470,#8471,#8472,#8473,#8474,#8475,
#8476,#8477,#8478,#8479,#8480,#8481,#8482,#8483,#8484,#8485,#8486,#8487,
#8488,#8489,#8490,#8491,#8492,#8493,#8494,#8495,#8496,#8497,#8498,#8499,
#8500,#8501,#8502,#8503,#8504,#8505,#8506,#8507,#8508,#8509,#8510,#8511,
#8512,#8513,#8514,#8515,#8516,#8517,#8518,#8519,#8520,#8521,#8522,#8523,
#8524,#8525,#8526,#8527,#8528,#8529,#8530,#8531,#8532,#8533,#8534,#8535,
#8536,#8537,#8538,#8539,#8540,#8541,#8542,#8543,#8544,#8545,#8546,#8547,
#8548,#8549,#8550,#8551,#8552,#8553,#8554,#8555,#8556,#8557,#8558,#8559,
#8560,#8561,#8562,#8563,#8564,#8565,#8566,#8567,#8568,#8569,#8570,#8571,
#8572,#8573,#8574,#8575,#8576,#8577,#8578,#8579,#8580,#8581,#8582,#8583,
#8584,#8585,#8586,#8587,#8588,#8589,#8590,#8591,#8592,#8593,#8594,#8595,
#8596,#8597,#8598,#8599,#8600,#8601,#8602,#8603,#8604,#8605,#8606,#8607,
#8608,#8609,#8610,#8611,#8612,#8613,#8614,#8615,#8616,#8617,#8618,#8619,
#8620,#8621,#8622,#8623,#8624,#8625,#8626,#8627,#8628,#8629,#8630,#8631,
#8632,#8633,#8634,#8635,#8636,#8637,#8638,#8639,#8640,#8641),
 .UNSPECIFIED.,.F.,.F.,(4,2,2,2,2,2,2,2,2,2,2,2,2,2,2,2,2,2,2,2,2,2,2,2,
2,2,2,2,2,2,2,2,2,2,2,2,2,2,2,2,2,2,2,2,2,2,2,2,2,2,2,2,2,2,2,2,2,2,2,2,
2,2,2,2,2,2,2,2,2,2,2,2,2,2,2,2,2,2,2,2,2,2,2,2,2,2,2,2,2,2,2,2,2,2,2,2,
2,2,2,2,2,2,2,2,2,2,2,2,2,4),(-1.24309113755231,-1.24126632442143,-1.23926693276646,
-1.23818551144056,-1.23726931749502,-1.23609426338528,-1.23418889070891,
-1.22070590490734,-1.20365940695935,-1.19133512542798,-1.18622278579794,
-1.18224411471887,-1.18022252406742,-1.17859044478126,-1.17671910482104,
-1.17354442737101,-1.16041497062373,-1.13617349906431,-1.12795365152909,
-1.12471798954741,-1.12229851255801,-1.12113146376042,-1.12030323585615,
-1.1192512898428,-1.11743710707711,-1.11007707877698,-1.07700856402774,
-1.07034271672478,-1.06545718590742,-1.06326463847935,-1.06161268595253,
-1.06005198049401,-1.05742696370277,-1.05023108217569,-1.01996261489869,
-1.011014805984,-1.00759389292042,-1.00506801745253,-1.00388055851729,-1.00296334148134,
-1.00189079039497,-0.999986105325724,-0.991285744971732,-0.962219334169995,
-0.950029067899264,-0.946996787179803,-0.94517463843108,-0.943535289520301,
-0.941436438524951,-0.937061427575507,-0.908584851671165,-0.895426743947146,
-0.891074050475468,-0.888038379096605,-0.886759841993951,-0.88583109090128,
-0.884809376542716,-0.883084673218698,-0.876978109408967,-0.851427419565153,
-0.834915369678608,-0.830622566689491,-0.828539422348956,-0.826901825757826,
-0.825070727683588,-0.8219974302899,-0.810758391755525,-0.781563306750961,
-0.775161278486433,-0.771128184394633,-0.769699464254831,-0.768742529345625,
-0.767885987986307,-0.766712021933907,-0.763761749195055,-0.74268854491404,
-0.71816638474444,-0.713534668857383,-0.711410893274628,-0.709763583211138,
-0.707972100616846,-0.705080685803936,-0.694656025852426,-0.67416984738979,
-0.666168391592487,-0.662640378933236,-0.654752555190516,-0.652900405974989,
-0.651839801655332,-0.651012996072326,-0.649858599354989,-0.647503607729981,
-0.644378949607415,-0.636580779371404,-0.613342325985203,-0.598757587071977,
-0.595500471328468,-0.593610442358724,-0.591979933870467,-0.589983012305076,
-0.586126567446377,-0.563670628477222,-0.538968082207945,-0.536170996631755,
-0.534946939717794,-0.534023014778787,-0.532985361727387,-0.531188471005012,
-0.523278635959589,-0.500930905015856),.UNSPECIFIED.);
#98=B_SPLINE_CURVE_WITH_KNOTS('',3,(#8643,#8644,#8645,#8646,#8647,#8648,
#8649,#8650,#8651,#8652,#8653,#8654,#8655,#8656,#8657,#8658,#8659,#8660,
#8661,#8662,#8663,#8664,#8665,#8666,#8667,#8668,#8669,#8670,#8671,#8672,
#8673,#8674,#8675,#8676,#8677,#8678,#8679,#8680,#8681,#8682,#8683,#8684,
#8685,#8686,#8687,#8688,#8689,#8690,#8691,#8692,#8693,#8694,#8695,#8696,
#8697,#8698,#8699,#8700,#8701,#8702,#8703,#8704,#8705,#8706,#8707,#8708,
#8709,#8710,#8711,#8712,#8713,#8714,#8715,#8716),.UNSPECIFIED.,.F.,.F.,
(4,2,2,2,2,2,2,2,2,2,2,2,2,2,2,2,2,2,2,2,2,2,2,2,2,2,2,2,2,2,2,2,2,2,2,
2,4),(-0.241988514754038,-0.232712639227085,-0.229829016152512,-0.228039324207548,
-0.226391634885176,-0.224228041812203,-0.219504030892733,-0.213123918449792,
-0.195422977376067,-0.17401126592963,-0.17106329479951,-0.16989529214844,
-0.169040282082338,-0.168081604915298,-0.166644328235717,-0.162546644592089,
-0.156001480166582,-0.124671258454934,-0.115424722653325,-0.112548598795624,
-0.110760591377874,-0.109185782200507,-0.109157460453551,-0.109130732410267,
-0.10712992737639,-0.104851867839005,-0.101080791656546,-0.0809630231652105,
-0.0564594984009954,-0.053641854435739,-0.0524142889581039,-0.0514899538839555,
-0.0504544029297609,-0.0486667149753297,-0.0408919222111806,-0.00875195972409242,
-0.000340782874575415),.UNSPECIFIED.);
#99=B_SPLINE_CURVE_WITH_KNOTS('',3,(#8717,#8718,#8719,#8720,#8721,#8722,
#8723,#8724,#8725,#8726,#8727,#8728,#8729,#8730,#8731,#8732,#8733,#8734,
#8735,#8736,#8737,#8738,#8739,#8740,#8741,#8742,#8743,#8744,#8745,#8746,
#8747,#8748,#8749,#8750,#8751,#8752,#8753,#8754,#8755,#8756,#8757,#8758,
#8759,#8760,#8761,#8762,#8763,#8764,#8765,#8766,#8767,#8768,#8769,#8770,
#8771,#8772,#8773,#8774,#8775,#8776,#8777,#8778,#8779,#8780,#8781,#8782,
#8783,#8784,#8785,#8786,#8787,#8788,#8789,#8790,#8791,#8792,#8793,#8794,
#8795,#8796,#8797,#8798,#8799,#8800,#8801,#8802,#8803,#8804,#8805,#8806,
#8807,#8808,#8809,#8810,#8811,#8812,#8813,#8814,#8815,#8816,#8817,#8818,
#8819,#8820,#8821,#8822,#8823,#8824,#8825,#8826,#8827,#8828,#8829,#8830,
#8831,#8832,#8833,#8834,#8835,#8836,#8837,#8838,#8839,#8840,#8841,#8842,
#8843,#8844,#8845,#8846,#8847,#8848,#8849,#8850,#8851,#8852,#8853,#8854,
#8855,#8856,#8857,#8858,#8859,#8860,#8861,#8862,#8863,#8864,#8865,#8866),
 .UNSPECIFIED.,.F.,.F.,(4,2,2,2,2,2,2,2,2,2,2,2,2,2,2,2,2,2,2,2,2,2,2,2,
2,2,2,2,2,2,2,2,2,2,2,2,2,2,2,2,2,2,2,2,2,2,2,2,2,2,2,2,2,2,2,2,2,2,2,2,
2,2,2,2,2,2,2,2,2,2,2,2,2,2,4),(-1.48412001715137,-1.48190965603259,-1.47983659088756,
-1.47821563782734,-1.47666047664527,-1.47491530913237,-1.47223351354066,
-1.46458778411192,-1.434944769811,-1.42176781561533,-1.41973510949454,-1.41864711061999,
-1.41773226021195,-1.41656776312692,-1.41469626621342,-1.40289891138794,
-1.36951389790073,-1.36549205973259,-1.36311358723029,-1.36097061927544,
-1.35935005515891,-1.35758157780193,-1.3547914425417,-1.3462989039611,-1.31205232442885,
-1.30411659550579,-1.30231887845869,-1.30128152637233,-1.30035841499434,
-1.29913618082103,-1.29634635071621,-1.27162529681923,-1.25609533368068,
-1.2501881548139,-1.24573650734627,-1.24362399052763,-1.24198390753885,
-1.24017105395127,-1.23717796753591,-1.22680454173612,-1.1967129446604,
-1.19024934602209,-1.18618921672579,-1.184757430969,-1.18380027507081,-1.18294496095465,
-1.18177447330326,-1.17884223239724,-1.1573354928398,-1.139736836888,-1.13337936496933,
-1.12866837701041,-1.12650784113347,-1.12486129200661,-1.12307167744254,
-1.12018560251057,-1.11083640832922,-1.07962041459186,-1.07308229491254,
-1.06898866688826,-1.06755232586779,-1.06659414786319,-1.06573948144598,
-1.06457183281278,-1.06162488567421,-1.0402706189335,-1.02256290960806,
-1.01618274884087,-1.01145875357087,-1.00929572808906,-1.0076486919997,
-1.00585992449612,-1.0029782730818,-0.99367286509119,-0.983793564935614),
 .UNSPECIFIED.);
#100=B_SPLINE_CURVE_WITH_KNOTS('',3,(#8872,#8873,#8874,#8875,#8876,#8877,
#8878,#8879,#8880,#8881,#8882,#8883,#8884,#8885,#8886,#8887,#8888,#8889,
#8890,#8891,#8892,#8893,#8894,#8895,#8896,#8897,#8898,#8899,#8900,#8901,
#8902,#8903,#8904,#8905,#8906,#8907,#8908,#8909,#8910,#8911,#8912,#8913,
#8914,#8915,#8916,#8917,#8918,#8919,#8920,#8921,#8922,#8923,#8924,#8925,
#8926,#8927,#8928,#8929,#8930,#8931,#8932,#8933,#8934,#8935,#8936,#8937,
#8938,#8939,#8940,#8941,#8942,#8943,#8944,#8945,#8946,#8947,#8948,#8949,
#8950,#8951,#8952,#8953,#8954,#8955,#8956,#8957,#8958,#8959,#8960,#8961,
#8962,#8963,#8964,#8965,#8966,#8967,#8968,#8969,#8970,#8971,#8972,#8973,
#8974,#8975,#8976,#8977,#8978,#8979,#8980,#8981,#8982,#8983,#8984,#8985,
#8986,#8987,#8988,#8989,#8990,#8991,#8992,#8993,#8994,#8995,#8996,#8997,
#8998,#8999,#9000,#9001,#9002,#9003,#9004,#9005,#9006,#9007,#9008,#9009,
#9010,#9011,#9012,#9013,#9014,#9015),.UNSPECIFIED.,.F.,.F.,(4,2,2,2,2,2,
2,2,2,2,2,2,2,2,2,2,2,2,2,2,2,2,2,2,2,2,2,2,2,2,2,2,2,2,2,2,2,2,2,2,2,2,
2,2,2,2,2,2,2,2,2,2,2,2,2,2,2,2,2,2,2,2,2,2,2,2,2,2,2,2,2,4),(-0.500819173945887,
-0.493777206906728,-0.479351861776628,-0.470865801088027,-0.46044512596012,
-0.458621959504854,-0.457471604552115,-0.456556942202042,-0.45545601971394,
-0.45336385714678,-0.437669222525489,-0.412663201038334,-0.403404091249994,
-0.400526694865227,-0.398738425051046,-0.39709040679574,-0.394923978418504,
-0.3901838706952,-0.383775228035058,-0.365932818995212,-0.344738336504506,
-0.341783031791153,-0.340613829838816,-0.339758555185984,-0.338800324047081,
-0.337364989287407,-0.333281494086993,-0.32676777916111,-0.29591966733786,
-0.286246301329913,-0.283324121186216,-0.281526137556155,-0.279881133613596,
-0.277735991188525,-0.27311239074608,-0.266907954555483,-0.25004233161852,
-0.227383301044488,-0.22451310642436,-0.223352907767055,-0.222415134207218,
-0.221433302782806,-0.219888710254711,-0.214906469089431,-0.206235806671276,
-0.17915184505782,-0.169099215949359,-0.166134623139714,-0.164327402676302,
-0.162684900855216,-0.160558631331137,-0.156036957893393,-0.150009388874568,
-0.133951888692588,-0.110018687787216,-0.107175144709924,-0.106053229930523,
-0.105125192411495,-0.104146874338745,-0.102648556808029,-0.100813822341213,
-0.0972150595024378,-0.0875372674535842,-0.0783689936404857,-0.054706126379121,
-0.0500515005800035,-0.0479237987091279,-0.0462761366731087,-0.0444869649045571,
-0.0416052648876107,-0.0312863423734425,-0.000340942165246433),
 .UNSPECIFIED.);
#101=B_SPLINE_CURVE_WITH_KNOTS('',3,(#9016,#9017,#9018,#9019,#9020,#9021,
#9022,#9023,#9024,#9025,#9026,#9027,#9028,#9029,#9030,#9031,#9032,#9033,
#9034,#9035,#9036,#9037,#9038,#9039,#9040,#9041,#9042,#9043,#9044,#9045,
#9046,#9047,#9048,#9049,#9050,#9051,#9052,#9053,#9054,#9055,#9056,#9057,
#9058,#9059,#9060,#9061,#9062,#9063,#9064,#9065,#9066,#9067,#9068,#9069,
#9070,#9071,#9072,#9073,#9074,#9075,#9076,#9077,#9078,#9079,#9080,#9081,
#9082,#9083,#9084,#9085,#9086,#9087,#9088,#9089,#9090,#9091),
 .UNSPECIFIED.,.F.,.F.,(4,2,2,2,2,2,2,2,2,2,2,2,2,2,2,2,2,2,2,2,2,2,2,2,
2,2,2,2,2,2,2,2,2,2,2,2,2,4),(-1.48462944420424,-1.47854706264515,-1.47522746968644,
-1.47396875633596,-1.47304062285797,-1.47216955552764,-1.4711705878605,
-1.46954819973224,-1.46438832786397,-1.45664645350163,-1.44275484241869,
-1.42063070257591,-1.41669766923023,-1.41468548338647,-1.41305434599212,
-1.41117673959019,-1.40797348414356,-1.39435211355748,-1.3618191261588,
-1.35889281860234,-1.35730422023743,-1.35594276665795,-1.35500797741246,
-1.35414906110552,-1.35296547144243,-1.34995731772499,-1.33148899974201,
-1.31239607042987,-1.30523902346609,-1.30008214116386,-1.29784236701082,
-1.2961829427663,-1.29442385838963,-1.29168153576673,-1.28359941082173,
-1.27740114420268,-1.25334811321103,-1.24309113755231),.UNSPECIFIED.);
#102=B_SPLINE_CURVE_WITH_KNOTS('',3,(#9092,#9093,#9094,#9095,#9096,#9097,
#9098,#9099,#9100,#9101,#9102,#9103,#9104,#9105,#9106,#9107,#9108,#9109,
#9110,#9111,#9112,#9113,#9114,#9115,#9116,#9117,#9118,#9119,#9120,#9121,
#9122,#9123,#9124,#9125,#9126,#9127,#9128,#9129,#9130,#9131,#9132,#9133,
#9134,#9135,#9136,#9137,#9138,#9139,#9140,#9141,#9142,#9143,#9144,#9145,
#9146,#9147,#9148,#9149,#9150,#9151,#9152,#9153,#9154,#9155,#9156,#9157,
#9158,#9159,#9160,#9161,#9162,#9163,#9164,#9165,#9166,#9167,#9168,#9169,
#9170,#9171,#9172,#9173,#9174,#9175,#9176,#9177,#9178,#9179,#9180,#9181,
#9182,#9183,#9184,#9185,#9186,#9187,#9188,#9189,#9190,#9191,#9192,#9193,
#9194,#9195,#9196,#9197,#9198,#9199,#9200,#9201,#9202,#9203,#9204,#9205,
#9206,#9207,#9208,#9209,#9210,#9211,#9212,#9213,#9214,#9215,#9216,#9217,
#9218,#9219,#9220,#9221,#9222,#9223,#9224,#9225,#9226,#9227,#9228,#9229,
#9230,#9231,#9232,#9233,#9234,#9235,#9236,#9237,#9238,#9239,#9240,#9241,
#9242,#9243,#9244,#9245,#9246,#9247,#9248,#9249,#9250,#9251,#9252,#9253,
#9254,#9255,#9256,#9257,#9258,#9259,#9260,#9261,#9262,#9263,#9264,#9265,
#9266,#9267,#9268,#9269,#9270,#9271,#9272,#9273,#9274,#9275,#9276,#9277,
#9278,#9279,#9280,#9281,#9282,#9283,#9284,#9285,#9286,#9287,#9288,#9289,
#9290,#9291,#9292,#9293,#9294,#9295,#9296,#9297,#9298,#9299,#9300,#9301,
#9302,#9303,#9304,#9305,#9306,#9307),.UNSPECIFIED.,.F.,.F.,(4,2,2,2,2,2,
2,2,2,2,2,2,2,2,2,2,2,2,2,2,2,2,2,2,2,2,2,2,2,2,2,2,2,2,2,2,2,2,2,2,2,2,
2,2,2,2,2,2,2,2,2,2,2,2,2,2,2,2,2,2,2,2,2,2,2,2,2,2,2,2,2,2,2,2,2,2,2,2,
2,2,2,2,2,2,2,2,2,2,2,2,2,2,2,2,2,2,2,2,2,2,2,2,2,2,2,2,2,4),(-0.983793564935614,
-0.968696261868599,-0.953012236160266,-0.950920660055713,-0.949820093400412,
-0.948905754416435,-0.947755860133233,-0.94593355059917,-0.935520123495261,
-0.927038511042748,-0.912622359712589,-0.896597264859473,-0.893342027870717,
-0.891471901615443,-0.889840514812668,-0.887819312617179,-0.884696907671688,
-0.862006562726232,-0.84461534549455,-0.838456713890232,-0.83453482699478,
-0.833121656489663,-0.832168248187483,-0.831309478421971,-0.83012564474862,
-0.827114483444018,-0.80896740956612,-0.788966357616482,-0.778676332009486,
-0.775797756300876,-0.774009570297988,-0.772362179491771,-0.770233937309615,
-0.76557450857,-0.742147073738758,-0.719937075314893,-0.717037065860415,
-0.715871903558975,-0.714932951359228,-0.713953374336011,-0.712418376972951,
-0.707519867930903,-0.699062837519007,-0.673570092699887,-0.661895314942863,
-0.658784935592021,-0.656946187079544,-0.655474223034174,-0.653485438433571,
-0.649666558844556,-0.628488494720904,-0.605952493049906,-0.600576136686598,
-0.598928918820536,-0.597924571068326,-0.596989138598303,-0.595669372942323,
-0.592379584239752,-0.587534244208183,-0.571664837309244,-0.547185012169975,
-0.542553243950537,-0.540429926712259,-0.538783175839867,-0.536992509009948,
-0.53410288231899,-0.523690579447275,-0.503245278973118,-0.49561067002373,
-0.490805137257805,-0.483680188068646,-0.481864029236699,-0.480822423448885,
-0.479900000765593,-0.478663191227497,-0.475867189104592,-0.463284699551626,
-0.441127668571468,-0.427682290649862,-0.42449054103066,-0.422615744908427,
-0.420984667879787,-0.418969499525952,-0.415020622489202,-0.391301557665565,
-0.368192272870674,-0.365345349402046,-0.364189279578466,-0.363252698628978,
-0.362269478355352,-0.360718098347127,-0.355672958115622,-0.346838923238608,
-0.317118075265111,-0.309394102414707,-0.306698136847339,-0.304949386529126,
-0.303285762257949,-0.30101843144945,-0.295695787017629,-0.269354114211768,
-0.251184887950499,-0.24817287021915,-0.24698881359996,-0.246129927382777,
-0.245176433937095,-0.243763221929403,-0.241871924735937),.UNSPECIFIED.);
#103=B_SPLINE_CURVE_WITH_KNOTS('',3,(#9312,#9313,#9314,#9315,#9316,#9317,
#9318,#9319,#9320,#9321,#9322,#9323,#9324,#9325,#9326,#9327,#9328,#9329,
#9330,#9331,#9332,#9333,#9334,#9335,#9336,#9337,#9338,#9339,#9340,#9341,
#9342,#9343,#9344,#9345,#9346,#9347,#9348,#9349,#9350,#9351,#9352,#9353,
#9354,#9355,#9356,#9357,#9358,#9359,#9360,#9361,#9362,#9363,#9364,#9365,
#9366,#9367,#9368,#9369,#9370,#9371,#9372,#9373,#9374,#9375,#9376,#9377,
#9378,#9379,#9380,#9381,#9382,#9383,#9384,#9385,#9386,#9387,#9388,#9389,
#9390,#9391,#9392,#9393,#9394,#9395,#9396,#9397,#9398,#9399,#9400,#9401,
#9402,#9403,#9404,#9405,#9406,#9407,#9408,#9409,#9410,#9411,#9412,#9413,
#9414,#9415,#9416,#9417,#9418,#9419,#9420,#9421,#9422,#9423,#9424,#9425,
#9426,#9427,#9428,#9429,#9430,#9431,#9432,#9433,#9434,#9435,#9436,#9437,
#9438,#9439,#9440,#9441,#9442,#9443,#9444,#9445,#9446,#9447,#9448,#9449,
#9450,#9451,#9452,#9453,#9454,#9455,#9456,#9457,#9458,#9459,#9460,#9461,
#9462,#9463,#9464,#9465,#9466,#9467,#9468,#9469,#9470,#9471,#9472,#9473,
#9474,#9475,#9476,#9477,#9478,#9479,#9480,#9481,#9482,#9483,#9484,#9485,
#9486,#9487,#9488,#9489,#9490,#9491,#9492,#9493,#9494,#9495,#9496,#9497,
#9498,#9499,#9500,#9501,#9502,#9503,#9504,#9505,#9506,#9507,#9508,#9509,
#9510,#9511,#9512,#9513,#9514,#9515,#9516,#9517,#9518,#9519,#9520,#9521,
#9522,#9523,#9524,#9525,#9526,#9527,#9528,#9529,#9530,#9531,#9532,#9533),
 .UNSPECIFIED.,.F.,.F.,(4,2,2,2,2,2,2,2,2,2,2,2,2,2,2,2,2,2,2,2,2,2,2,2,
2,2,2,2,2,2,2,2,2,2,2,2,2,2,2,2,2,2,2,2,2,2,2,2,2,2,2,2,2,2,2,2,2,2,2,2,
2,2,2,2,2,2,2,2,2,2,2,2,2,2,2,2,2,2,2,2,2,2,2,2,2,2,2,2,2,2,2,2,2,2,2,2,
2,2,2,2,2,2,2,2,2,2,2,2,2,2,4),(-1.2428172115265,-1.24249234473694,-1.23078262926944,
-1.22583767315457,-1.22196155341259,-1.21996074205993,-1.21833014567714,
-1.21644347476855,-1.21320076899999,-1.19888499679281,-1.17546559847501,
-1.16757628439986,-1.16442755563331,-1.1620586984377,-1.16090161783892,
-1.1600745816541,-1.15901600819455,-1.15717257801453,-1.14940924389079,
-1.11943961512502,-1.11129047521323,-1.10560639889848,-1.10327989549632,
-1.10160552361073,-1.10007794037801,-1.09802205322527,-1.09399646262687,
-1.0665154066557,-1.05272569646497,-1.04825145863456,-1.04515223747807,
-1.04386315972315,-1.04293278083638,-1.04191580163504,-1.04021226373077,
-1.03431527911758,-1.00862299086621,-0.992024560629506,-0.987720938971641,
-0.985635831704979,-0.983998149664809,-0.982168469399791,-0.979101195136434,
-0.967936794679667,-0.944515512125686,-0.93420287263835,-0.928615632696912,
-0.927007549208844,-0.926011699898189,-0.925082284623874,-0.923954855652924,
-0.92107657660576,-0.897310699738304,-0.881187617793249,-0.875145220086792,
-0.870614478764588,-0.868486417478237,-0.866843569632226,-0.865037008816023,
-0.862075896748497,-0.852060176738265,-0.827694828606197,-0.81224622831273,
-0.810158395254423,-0.809058347262913,-0.808143592794,-0.806992095849127,
-0.805165263453635,-0.794652144959133,-0.767275694831161,-0.755350953423724,
-0.752338216961626,-0.750520388425605,-0.748880210691996,-0.746773728485989,
-0.742358109158383,-0.724862609446661,-0.706516547946201,-0.70154835440642,
-0.694523523075217,-0.69271538809805,-0.69167536361139,-0.690752218469142,
-0.689511555996434,-0.686694981166887,-0.67392358609147,-0.666933433456118,
-0.640706684604885,-0.636150813889163,-0.634040978294949,-0.632395805915498,
-0.630597882793247,-0.627676358967061,-0.616901059222625,-0.597898551376377,
-0.57928969230207,-0.576276161915608,-0.57509169726426,-0.574232578310295,
-0.573278894949353,-0.571865504691222,-0.5679441006064,-0.561788004791788,
-0.544404412671272,-0.521721132984155,-0.518598128564709,-0.516576365329992,
-0.514944421395287,-0.513073538066115,-0.509816672449976,-0.500819173945887),
 .UNSPECIFIED.);
#104=B_SPLINE_CURVE_WITH_KNOTS('',3,(#9535,#9536,#9537,#9538,#9539,#9540,
#9541,#9542,#9543,#9544,#9545,#9546,#9547,#9548,#9549,#9550,#9551,#9552,
#9553,#9554,#9555,#9556,#9557,#9558,#9559,#9560,#9561,#9562,#9563,#9564,
#9565,#9566,#9567,#9568,#9569,#9570,#9571,#9572,#9573,#9574,#9575,#9576,
#9577,#9578,#9579,#9580,#9581,#9582,#9583,#9584,#9585,#9586,#9587,#9588,
#9589,#9590,#9591,#9592,#9593,#9594,#9595,#9596,#9597,#9598,#9599,#9600,
#9601,#9602,#9603,#9604,#9605,#9606,#9607,#9608,#9609,#9610),
 .UNSPECIFIED.,.F.,.F.,(4,2,2,2,2,2,2,2,2,2,2,2,2,2,2,2,2,2,2,2,2,2,2,2,
2,2,2,2,2,2,2,2,2,2,2,2,2,4),(-0.241871924735937,-0.239841673385435,-0.233684822665038,
-0.216303692719354,-0.193622004876805,-0.190499538363504,-0.18847818442888,
-0.186846614987625,-0.184976213068143,-0.181720332570845,-0.165690973487894,
-0.140556038965802,-0.132138525183534,-0.130251016583305,-0.129182537690494,
-0.128282805778212,-0.127132854326775,-0.125848452014372,-0.123703968120966,
-0.119203879859423,-0.105275452917386,-0.0780319460560208,-0.0735452913502586,
-0.0714484189340119,-0.0698052957158563,-0.0680013910808192,-0.0650514232092265,
-0.0539293515464517,-0.0259234861970813,-0.0183744785915654,-0.0141211811940812,
-0.0126154182771393,-0.0117388268599531,-0.0108674173226553,-0.00993989921184121,
-0.00868279022866366,-0.00563249670091923,-0.000340252375207522),
 .UNSPECIFIED.);
#105=B_SPLINE_CURVE_WITH_KNOTS('',3,(#9611,#9612,#9613,#9614,#9615,#9616,
#9617,#9618,#9619,#9620,#9621,#9622,#9623,#9624,#9625,#9626,#9627,#9628,
#9629,#9630,#9631,#9632,#9633,#9634,#9635,#9636,#9637,#9638,#9639,#9640,
#9641,#9642,#9643,#9644,#9645,#9646,#9647,#9648,#9649,#9650,#9651,#9652,
#9653,#9654,#9655,#9656,#9657,#9658,#9659,#9660,#9661,#9662,#9663,#9664,
#9665,#9666,#9667,#9668,#9669,#9670,#9671,#9672,#9673,#9674,#9675,#9676,
#9677,#9678,#9679,#9680,#9681,#9682,#9683,#9684,#9685,#9686,#9687,#9688,
#9689,#9690,#9691,#9692,#9693,#9694,#9695,#9696,#9697,#9698,#9699,#9700,
#9701,#9702,#9703,#9704,#9705,#9706,#9707,#9708,#9709,#9710,#9711,#9712,
#9713,#9714,#9715,#9716,#9717,#9718,#9719,#9720,#9721,#9722,#9723,#9724,
#9725,#9726,#9727,#9728,#9729,#9730,#9731,#9732,#9733,#9734,#9735,#9736,
#9737,#9738,#9739,#9740,#9741,#9742,#9743,#9744,#9745,#9746,#9747,#9748,
#9749,#9750,#9751,#9752,#9753,#9754),.UNSPECIFIED.,.F.,.F.,(4,2,2,2,2,2,
2,2,2,2,2,2,2,2,2,2,2,2,2,2,2,2,2,2,2,2,2,2,2,2,2,2,2,2,2,2,2,2,2,2,2,2,
2,2,2,2,2,2,2,2,2,2,2,2,2,2,2,2,2,2,2,2,2,2,2,2,2,2,2,2,2,4),(-1.48448022972756,
-1.45253145118343,-1.44218218330809,-1.43929849412675,-1.43750929736548,
-1.43586242197044,-1.43373687449237,-1.42909174084597,-1.40503566329731,
-1.39117708996751,-1.384849204403,-1.38213576934346,-1.38062823722837,-1.3793554103156,
-1.37842741728136,-1.37756250831909,-1.37635473994927,-1.37386053420512,
-1.34906907763824,-1.33355666097405,-1.32765311333543,-1.32320341324644,
-1.32109104869219,-1.31945075265988,-1.31763732764823,-1.31464251382629,
-1.30425463192307,-1.27417162459092,-1.26770788105642,-1.26364749278658,
-1.26221552349324,-1.2612582190253,-1.26040275212933,-1.25923203030285,
-1.25629907348894,-1.2347941477793,-1.21718886179115,-1.2108295659136,-1.20611735705056,
-1.20395638083128,-1.20230954473904,-1.20051966578124,-1.19763327014716,
-1.18828405633806,-1.15706112532489,-1.15052180244857,-1.14642744035259,
-1.14499085223529,-1.14403251230689,-1.14317770370543,-1.14200986362902,
-1.13906243745354,-1.11770396783046,-1.09999372397697,-1.09361258272429,
-1.0888878461881,-1.08672446734085,-1.08507715652161,-1.0832880851261,-1.08040593189491,
-1.07109878533898,-1.0461181513722,-1.03043155715585,-1.02833963162282,
-1.02723888075393,-1.02632438852579,-1.02517430126548,-1.02335168544546,
-1.01293649113938,-1.0044532045271,-0.990034106714849,-0.98405823001278),
 .UNSPECIFIED.);
#106=B_SPLINE_CURVE_WITH_KNOTS('',3,(#9760,#9761,#9762,#9763,#9764,#9765,
#9766,#9767,#9768,#9769,#9770,#9771,#9772,#9773,#9774,#9775,#9776,#9777,
#9778,#9779,#9780,#9781,#9782,#9783,#9784,#9785,#9786,#9787,#9788,#9789,
#9790,#9791,#9792,#9793,#9794,#9795,#9796,#9797,#9798,#9799,#9800,#9801,
#9802,#9803,#9804,#9805,#9806,#9807,#9808,#9809,#9810,#9811,#9812,#9813,
#9814,#9815,#9816,#9817,#9818,#9819,#9820,#9821,#9822,#9823,#9824,#9825,
#9826,#9827,#9828,#9829,#9830,#9831,#9832,#9833,#9834,#9835,#9836,#9837,
#9838,#9839,#9840,#9841,#9842,#9843,#9844,#9845,#9846,#9847,#9848,#9849,
#9850,#9851,#9852,#9853,#9854,#9855,#9856,#9857,#9858,#9859,#9860,#9861,
#9862,#9863,#9864,#9865,#9866,#9867,#9868,#9869,#9870,#9871,#9872,#9873,
#9874,#9875,#9876,#9877,#9878,#9879,#9880,#9881,#9882,#9883,#9884,#9885,
#9886,#9887,#9888,#9889,#9890,#9891,#9892,#9893,#9894,#9895,#9896,#9897,
#9898,#9899,#9900,#9901,#9902,#9903,#9904,#9905,#9906,#9907,#9908,#9909,
#9910,#9911),.UNSPECIFIED.,.F.,.F.,(4,2,2,2,2,2,2,2,2,2,2,2,2,2,2,2,2,2,
2,2,2,2,2,2,2,2,2,2,2,2,2,2,2,2,2,2,2,2,2,2,2,2,2,2,2,2,2,2,2,2,2,2,2,2,
2,2,2,2,2,2,2,2,2,2,2,2,2,2,2,2,2,2,2,2,2,4),(-0.500712197120109,-0.499886588927617,
-0.498155634717826,-0.497132550335824,-0.496204286833124,-0.494928847679332,
-0.49191148215954,-0.487594006162487,-0.474614145976675,-0.445876781470393,
-0.441532128751737,-0.43943907733086,-0.437800407536301,-0.435975047452157,
-0.432927988268123,-0.420531219258952,-0.389962238813033,-0.38277887871243,
-0.380978607154051,-0.379929844830267,-0.379101012200458,-0.377929061452973,
-0.375484354622653,-0.372205387236876,-0.363818660474139,-0.338725789014427,
-0.326592632820325,-0.323449679782123,-0.321603330348852,-0.32013166466181,
-0.318151563245263,-0.314377722233372,-0.309597958210389,-0.298478375150139,
-0.27580250107145,-0.265844271387734,-0.26404297498217,-0.262899131515969,
-0.261984564462171,-0.260877612020439,-0.258757038578453,-0.241186104621821,
-0.211088678604902,-0.206906604019289,-0.204844851656629,-0.203209403655764,
-0.201365249478619,-0.198232142414803,-0.184522712491843,-0.168436853651836,
-0.15024396269488,-0.14723214677337,-0.146047909429669,-0.145188801950515,
-0.144234946323207,-0.142879572072936,-0.13924028239031,-0.133634208548949,
-0.113594284681153,-0.092707884315093,-0.089566733559867,-0.0875393766573888,
-0.0859068978359904,-0.0840397526215277,-0.0810718295493039,-0.0680879069889224,
-0.0504342275555722,-0.0419858476100865,-0.0314035321927687,-0.0295737764242259,
-0.0284213811036784,-0.0275065538783484,-0.026407182221728,-0.0252248357174609,
-0.0233328873464089,-0.00034061238379718),.UNSPECIFIED.);
#107=B_SPLINE_CURVE_WITH_KNOTS('',3,(#9912,#9913,#9914,#9915,#9916,#9917,
#9918,#9919,#9920,#9921,#9922,#9923,#9924,#9925,#9926,#9927,#9928,#9929,
#9930,#9931,#9932,#9933,#9934,#9935,#9936,#9937,#9938,#9939,#9940,#9941,
#9942,#9943,#9944,#9945,#9946,#9947,#9948,#9949,#9950,#9951,#9952,#9953,
#9954,#9955,#9956,#9957,#9958,#9959,#9960,#9961,#9962,#9963,#9964,#9965,
#9966,#9967,#9968,#9969,#9970,#9971,#9972,#9973,#9974,#9975,#9976,#9977,
#9978,#9979,#9980,#9981,#9982,#9983,#9984,#9985),.UNSPECIFIED.,.F.,.F.,
(4,2,2,2,2,2,2,2,2,2,2,2,2,2,2,2,2,2,2,2,2,2,2,2,2,2,2,2,2,2,2,2,2,2,2,
2,4),(-1.48451373067849,-1.46116924777296,-1.45808400850521,-1.45608651279479,
-1.45418536159507,-1.45271924820267,-1.45080623437103,-1.44744613437415,
-1.43053270847733,-1.41672089915974,-1.40406921364431,-1.40030111634928,
-1.39700628022729,-1.39597319077417,-1.39497744950135,-1.3940481350744,
-1.39292082845391,-1.39004286185665,-1.3665419218,-1.35023558159827,-1.34415285491573,
-1.339636031179,-1.33749038448044,-1.33584536069051,-1.33404771752278,-1.33112691416296,
-1.32146605515252,-1.28852098913718,-1.28327249887088,-1.27978201788845,
-1.27843091628103,-1.27748955484114,-1.27649574954126,-1.27489698996495,
-1.26993474313087,-1.26411590652247,-1.2428172115265),.UNSPECIFIED.);
#108=B_SPLINE_CURVE_WITH_KNOTS('',3,(#9986,#9987,#9988,#9989,#9990,#9991,
#9992,#9993,#9994,#9995,#9996,#9997,#9998,#9999,#10000,#10001,#10002,#10003,
#10004,#10005,#10006,#10007,#10008,#10009,#10010,#10011,#10012,#10013,#10014,
#10015,#10016,#10017,#10018,#10019,#10020,#10021,#10022,#10023,#10024,#10025,
#10026,#10027,#10028,#10029,#10030,#10031,#10032,#10033,#10034,#10035,#10036,
#10037,#10038,#10039,#10040,#10041,#10042,#10043,#10044,#10045,#10046,#10047,
#10048,#10049,#10050,#10051,#10052,#10053,#10054,#10055,#10056,#10057,#10058,
#10059,#10060,#10061,#10062,#10063,#10064,#10065,#10066,#10067,#10068,#10069,
#10070,#10071,#10072,#10073,#10074,#10075,#10076,#10077,#10078,#10079,#10080,
#10081,#10082,#10083,#10084,#10085,#10086,#10087,#10088,#10089,#10090,#10091,
#10092,#10093,#10094,#10095,#10096,#10097,#10098,#10099,#10100,#10101,#10102,
#10103,#10104,#10105,#10106,#10107,#10108,#10109,#10110,#10111,#10112,#10113,
#10114,#10115,#10116,#10117,#10118,#10119,#10120,#10121,#10122,#10123,#10124,
#10125,#10126,#10127,#10128,#10129,#10130,#10131,#10132,#10133,#10134,#10135,
#10136,#10137,#10138,#10139,#10140,#10141,#10142,#10143,#10144,#10145,#10146,
#10147,#10148,#10149,#10150,#10151,#10152,#10153,#10154,#10155,#10156,#10157,
#10158,#10159,#10160,#10161,#10162,#10163,#10164,#10165,#10166,#10167,#10168,
#10169,#10170,#10171,#10172,#10173,#10174,#10175,#10176,#10177,#10178,#10179,
#10180,#10181,#10182,#10183,#10184,#10185,#10186,#10187,#10188,#10189,#10190,
#10191,#10192,#10193,#10194,#10195,#10196,#10197,#10198,#10199,#10200,#10201,
#10202,#10203,#10204,#10205),.UNSPECIFIED.,.F.,.F.,(4,2,2,2,2,2,2,2,2,2,
2,2,2,2,2,2,2,2,2,2,2,2,2,2,2,2,2,2,2,2,2,2,2,2,2,2,2,2,2,2,2,2,2,2,2,2,
2,2,2,2,2,2,2,2,2,2,2,2,2,2,2,2,2,2,2,2,2,2,2,2,2,2,2,2,2,2,2,2,2,2,2,2,
2,2,2,2,2,2,2,2,2,2,2,2,2,2,2,2,2,2,2,2,2,2,2,2,2,2,2,4),(-0.98405823001278,
-0.97400707104787,-0.970751322952857,-0.968880890719665,-0.967249229774399,
-0.965227678577384,-0.962104716522352,-0.939450532390953,-0.921932922739935,
-0.915825427897057,-0.911926867132361,-0.910516773785427,-0.909563886051716,
-0.908704363146824,-0.907517937650744,-0.904492041117516,-0.886581067929002,
-0.866411828836706,-0.856074473085999,-0.853191341938306,-0.851401969544046,
-0.849754583930772,-0.847627889181588,-0.842978227434208,-0.819043668860734,
-0.80509198424679,-0.798741802913096,-0.794732412670994,-0.793307140818024,
-0.79235111324414,-0.791494301057696,-0.790318609442775,-0.787356942735387,
-0.766542008679358,-0.742504085515605,-0.737493007348105,-0.735445218903251,
-0.733919759220508,-0.732243893297746,-0.729908190212917,-0.724164738818813,
-0.715899240907171,-0.684546126543545,-0.678130409343872,-0.676376224410512,
-0.675348101217621,-0.674421673710567,-0.673157589418741,-0.670206343020052,
-0.666013420097018,-0.65365123238517,-0.623883897872317,-0.619660189745749,
-0.617590579403002,-0.615954629787558,-0.61411595003376,-0.611006985416679,
-0.597680316716895,-0.581319613680652,-0.562970119972712,-0.559962101353089,
-0.558778623782255,-0.557919816092369,-0.556965997793481,-0.555551602359039,
-0.551622239650024,-0.545448648603113,-0.528082323631822,-0.505406498411675,
-0.502283657914997,-0.500262058696316,-0.498630289203212,-0.496759655680116,
-0.493503366136088,-0.477471835743734,-0.463039274916872,-0.454546891360892,
-0.444127690341879,-0.442304698911643,-0.441154460790533,-0.44023989927412,
-0.43913912072516,-0.437047306200743,-0.421363876621889,-0.396387746483833,
-0.387091702409179,-0.384210585859698,-0.382421631112915,-0.380774073440092,
-0.378609853130598,-0.373881191013549,-0.367492570217147,-0.349747903971835,
-0.328406998548195,-0.325467766644331,-0.32429582771276,-0.323439933769897,
-0.322482705334922,-0.321051815983408,-0.31700089942774,-0.310559623129661,
-0.293496097450313,-0.270949680337322,-0.267824464950883,-0.265802168162892,
-0.264170380648203,-0.262300324195541,-0.259046589473324,-0.243068950388722,
-0.242040300785714),.UNSPECIFIED.);
#109=B_SPLINE_CURVE_WITH_KNOTS('',3,(#10210,#10211,#10212,#10213,#10214,
#10215,#10216,#10217,#10218,#10219,#10220,#10221,#10222,#10223,#10224,#10225,
#10226,#10227,#10228,#10229,#10230,#10231,#10232,#10233,#10234,#10235,#10236,
#10237,#10238,#10239,#10240,#10241,#10242,#10243,#10244,#10245,#10246,#10247,
#10248,#10249,#10250,#10251,#10252,#10253,#10254,#10255,#10256,#10257,#10258,
#10259,#10260,#10261,#10262,#10263,#10264,#10265,#10266,#10267,#10268,#10269,
#10270,#10271,#10272,#10273,#10274,#10275,#10276,#10277,#10278,#10279,#10280,
#10281,#10282,#10283,#10284,#10285,#10286,#10287,#10288,#10289,#10290,#10291,
#10292,#10293,#10294,#10295,#10296,#10297,#10298,#10299,#10300,#10301,#10302,
#10303,#10304,#10305,#10306,#10307,#10308,#10309,#10310,#10311,#10312,#10313,
#10314,#10315,#10316,#10317,#10318,#10319,#10320,#10321,#10322,#10323,#10324,
#10325,#10326,#10327,#10328,#10329,#10330,#10331,#10332,#10333,#10334,#10335,
#10336,#10337,#10338,#10339,#10340,#10341,#10342,#10343,#10344,#10345,#10346,
#10347,#10348,#10349,#10350,#10351,#10352,#10353,#10354,#10355,#10356,#10357,
#10358,#10359,#10360,#10361,#10362,#10363,#10364,#10365,#10366,#10367,#10368,
#10369,#10370,#10371,#10372,#10373,#10374,#10375,#10376,#10377,#10378,#10379,
#10380,#10381,#10382,#10383,#10384,#10385,#10386,#10387,#10388,#10389,#10390,
#10391,#10392,#10393,#10394,#10395,#10396,#10397,#10398,#10399,#10400,#10401,
#10402,#10403,#10404,#10405,#10406,#10407,#10408,#10409,#10410,#10411,#10412,
#10413,#10414,#10415,#10416,#10417,#10418,#10419),.UNSPECIFIED.,.F.,.F.,
(4,2,2,2,2,2,2,2,2,2,2,2,2,2,2,2,2,2,2,2,2,2,2,2,2,2,2,2,2,2,2,2,2,2,2,
2,2,2,2,2,2,2,2,2,2,2,2,2,2,2,2,2,2,2,2,2,2,2,2,2,2,2,2,2,2,2,2,2,2,2,2,
2,2,2,2,2,2,2,2,2,2,2,2,2,2,2,2,2,2,2,2,2,2,2,2,2,2,2,2,2,2,2,2,2,4),(-1.24265200671274,
-1.22719957996762,-1.21800259183579,-1.20382165019046,-1.20176176771288,
-1.20066777501492,-1.19975295499178,-1.19859491083029,-1.19674574147489,
-1.19527393431518,-1.17407659103393,-1.1562619318333,-1.14985971710055,
-1.14512306508982,-1.14295754968399,-1.14130994991724,-1.139521864745,-1.13664417352646,
-1.12737883775365,-1.10236807716455,-1.0866709045022,-1.0845788593499,-1.08347809206551,
-1.08256360919259,-1.08141354901745,-1.0795909959997,-1.06917604326802,
-1.0606999415883,-1.04629040673359,-1.03025647923327,-1.02700050579771,
-1.02513003986385,-1.02349840154925,-1.02147694157929,-1.01835423119893,
-0.995658223040673,-0.97825456008128,-0.972107808314153,-0.968191255742003,
-0.966778688550653,-0.965825300982004,-0.964966239807481,-0.963781601828935,
-0.960766223140326,-0.942700796067431,-0.923326769326904,-0.912437615006063,
-0.909506902339477,-0.907707169076331,-0.906062861392199,-0.903957612653297,
-0.899425656055709,-0.87279334065823,-0.866955856400763,-0.856875298955461,
-0.851370175331793,-0.849770420736875,-0.848776496300703,-0.847846239855462,
-0.846715056964892,-0.843927777383174,-0.819514641309596,-0.803793839945378,
-0.797842212731947,-0.793364258774201,-0.791246225694342,-0.789604830855865,
-0.787793527369268,-0.784809967171913,-0.774545218488185,-0.742269625666963,
-0.73460858950906,-0.732772356677799,-0.731715454356179,-0.73088818939534,
-0.729728816690724,-0.727348157480081,-0.72417946655417,-0.716214982995178,
-0.692714662962205,-0.678601259858895,-0.675369880401874,-0.673485803329206,
-0.672018143879595,-0.670085991925144,-0.66654187774207,-0.641493766653995,
-0.619098326283343,-0.616205651112152,-0.615041527318315,-0.614102649424678,
-0.613122203160549,-0.611584194157185,-0.606661724495914,-0.598144730113181,
-0.572290524813978,-0.560994513900779,-0.557917033245088,-0.55608507410508,
-0.554447719210809,-0.552366265779187,-0.548082007112975,-0.531634463220765,
-0.506056827056548,-0.500712197120109),.UNSPECIFIED.);
#110=B_SPLINE_CURVE_WITH_KNOTS('',3,(#10421,#10422,#10423,#10424,#10425,
#10426,#10427,#10428,#10429,#10430,#10431,#10432,#10433,#10434,#10435,#10436,
#10437,#10438,#10439,#10440,#10441,#10442,#10443,#10444,#10445,#10446,#10447,
#10448,#10449,#10450,#10451,#10452,#10453,#10454,#10455,#10456,#10457,#10458,
#10459,#10460,#10461,#10462,#10463,#10464,#10465,#10466,#10467,#10468,#10469,
#10470,#10471,#10472,#10473,#10474,#10475,#10476,#10477,#10478,#10479,#10480,
#10481,#10482,#10483,#10484,#10485,#10486,#10487,#10488,#10489,#10490,#10491,
#10492),.UNSPECIFIED.,.F.,.F.,(4,2,2,2,2,2,2,2,2,2,2,2,2,2,2,2,2,2,2,2,
2,2,2,2,2,2,2,2,2,2,2,2,2,2,2,4),(-0.242040300785714,-0.228597739999477,
-0.220089037302706,-0.20966768651593,-0.207844639056614,-0.206694397094238,
-0.205779854275758,-0.204679124381012,-0.202587473559587,-0.18691084659806,
-0.161955516755339,-0.152637453339446,-0.149754055762204,-0.147964629307045,
-0.14631726825784,-0.144281346116536,-0.139914405248792,-0.134089246407373,
-0.118917821650194,-0.0939154634649374,-0.0909957444604389,-0.0898271140801679,
-0.0889720410306897,-0.0880137787955856,-0.0870372998373829,-0.0843343282204052,
-0.071989764230856,-0.0545185270730589,-0.0364418201534302,-0.033342502060549,
-0.0313280574066432,-0.0296967933063195,-0.0278209284362617,-0.0258592177881634,
-0.0228608516323196,-0.000340552445936415),.UNSPECIFIED.);
#111=B_SPLINE_CURVE_WITH_KNOTS('',3,(#10493,#10494,#10495,#10496,#10497,
#10498,#10499,#10500,#10501,#10502,#10503,#10504,#10505,#10506,#10507,#10508,
#10509,#10510,#10511,#10512,#10513,#10514,#10515,#10516,#10517,#10518,#10519,
#10520,#10521,#10522,#10523,#10524,#10525,#10526,#10527,#10528,#10529,#10530,
#10531,#10532,#10533,#10534,#10535,#10536,#10537,#10538,#10539,#10540,#10541,
#10542,#10543,#10544,#10545,#10546,#10547,#10548,#10549,#10550,#10551,#10552,
#10553,#10554,#10555,#10556,#10557,#10558,#10559,#10560,#10561,#10562,#10563,
#10564,#10565,#10566,#10567,#10568,#10569,#10570,#10571,#10572,#10573,#10574,
#10575,#10576,#10577,#10578,#10579,#10580,#10581,#10582,#10583,#10584,#10585,
#10586,#10587,#10588,#10589,#10590,#10591,#10592,#10593,#10594,#10595,#10596,
#10597,#10598,#10599,#10600,#10601,#10602,#10603,#10604,#10605,#10606,#10607,
#10608,#10609,#10610,#10611,#10612,#10613,#10614,#10615,#10616,#10617,#10618,
#10619,#10620,#10621,#10622,#10623,#10624,#10625,#10626,#10627,#10628,#10629,
#10630,#10631,#10632,#10633,#10634,#10635,#10636,#10637,#10638,#10639,#10640,
#10641,#10642),.UNSPECIFIED.,.F.,.F.,(4,2,2,2,2,2,2,2,2,2,2,2,2,2,2,2,2,
2,2,2,2,2,2,2,2,2,2,2,2,2,2,2,2,2,2,2,2,2,2,2,2,2,2,2,2,2,2,2,2,2,2,2,2,
2,2,2,2,2,2,2,2,2,2,2,2,2,2,2,2,2,2,2,2,2,4),(-1.48450003793453,-1.46287590279009,
-1.45982402878966,-1.45818847912071,-1.45677398097135,-1.45582014616151,
-1.45496135988593,-1.4537779697734,-1.45077043850895,-1.43245112533197,
-1.41332429557885,-1.4024311153063,-1.39961975102648,-1.39778822759921,
-1.39615100963953,-1.39406938960619,-1.38978357236929,-1.36164388380195,
-1.34813055164141,-1.34370901783773,-1.34066777723663,-1.33937093337936,
-1.33843931368745,-1.33742568729945,-1.33573713892179,-1.32998390352211,
-1.30409417468053,-1.28751148795387,-1.2832099247477,-1.28112528423152,
-1.27948773869952,-1.27765797570941,-1.27459000701043,-1.26341572476417,
-1.23742564777199,-1.22888554065074,-1.22395449314357,-1.22241558919221,
-1.2214350084424,-1.22049637956714,-1.21933298815086,-1.21644421135776,
-1.19402388573959,-1.17701973658039,-1.17078551762507,-1.16614436730831,
-1.16399596271834,-1.16235047137383,-1.16055394673447,-1.15763864382601,
-1.14803077950044,-1.12043803744325,-1.11171861793898,-1.10671770284436,
-1.10517095094971,-1.10418860508198,-1.10325107886563,-1.10209198800552,
-1.09922845709034,-1.07647851393198,-1.05968089198163,-1.05349064870514,
-1.04887464056812,-1.04673076625755,-1.04508579964447,-1.04328693390141,
-1.04036124690405,-1.03065755880463,-1.00601282647642,-0.990454733507967,
-0.988364718932059,-0.987264194398857,-0.986349438227163,-0.985198449752847,
-0.984126425382023),.UNSPECIFIED.);
#112=B_SPLINE_CURVE_WITH_KNOTS('',3,(#10648,#10649,#10650,#10651,#10652,
#10653,#10654,#10655,#10656,#10657,#10658,#10659,#10660,#10661,#10662,#10663,
#10664,#10665,#10666,#10667,#10668,#10669,#10670,#10671,#10672,#10673,#10674,
#10675,#10676,#10677,#10678,#10679,#10680,#10681,#10682,#10683,#10684,#10685,
#10686,#10687,#10688,#10689,#10690,#10691,#10692,#10693,#10694,#10695,#10696,
#10697,#10698,#10699,#10700,#10701,#10702,#10703,#10704,#10705,#10706,#10707,
#10708,#10709,#10710,#10711,#10712,#10713,#10714,#10715,#10716,#10717,#10718,
#10719,#10720,#10721,#10722,#10723,#10724,#10725,#10726,#10727,#10728,#10729,
#10730,#10731,#10732,#10733,#10734,#10735,#10736,#10737,#10738,#10739,#10740,
#10741,#10742,#10743,#10744,#10745,#10746,#10747,#10748,#10749,#10750,#10751,
#10752,#10753,#10754,#10755,#10756,#10757,#10758,#10759,#10760,#10761,#10762,
#10763,#10764,#10765,#10766,#10767,#10768,#10769,#10770,#10771,#10772,#10773,
#10774,#10775,#10776,#10777,#10778,#10779,#10780,#10781,#10782,#10783,#10784,
#10785,#10786,#10787,#10788,#10789,#10790,#10791,#10792,#10793,#10794,#10795,
#10796,#10797,#10798,#10799,#10800,#10801,#10802,#10803,#10804,#10805),
 .UNSPECIFIED.,.F.,.F.,(4,2,2,2,2,2,2,2,2,2,2,2,2,2,2,2,2,2,2,2,2,2,2,2,
2,2,2,2,2,2,2,2,2,2,2,2,2,2,2,2,2,2,2,2,2,2,2,2,2,2,2,2,2,2,2,2,2,2,2,2,
2,2,2,2,2,2,2,2,2,2,2,2,2,2,2,2,2,2,4),(-0.500854930573822,-0.486075548964709,
-0.481734828916494,-0.479642564627619,-0.478004024270296,-0.476178306202764,
-0.47312945105295,-0.460706260795896,-0.429924054507328,-0.422952536531026,
-0.421148758649097,-0.420109613554019,-0.419186103588324,-0.417943400011714,
-0.415115777483494,-0.40224200702912,-0.393704480343706,-0.36926014305392,
-0.364625685841479,-0.362501381634948,-0.360853960802749,-0.359062657667822,
-0.356172200613966,-0.345758949958123,-0.325315360564438,-0.317751558646107,
-0.312660167920223,-0.305710990210885,-0.303909110442994,-0.302870381811186,
-0.301946764313685,-0.300703268918895,-0.297871159456327,-0.284954985031877,
-0.276059760720306,-0.252042212729601,-0.247395002600144,-0.245268388807385,
-0.243620626473954,-0.241830402803363,-0.238944913963799,-0.228587769603937,
-0.208349904171972,-0.190477443323002,-0.187464749125807,-0.186280330461392,
-0.185421147783713,-0.18446727661304,-0.183053408682288,-0.179129394696484,
-0.172967935187127,-0.155586796920719,-0.132903481814581,-0.129779761096779,
-0.127757635343345,-0.126203544961513,-0.124402424605798,-0.122501968967435,
-0.119652995467467,-0.114423204676567,-0.101655907336608,-0.0830142693867631,
-0.0787861475531215,-0.071306942697782,-0.0694837304140167,-0.0684297112479054,
-0.0676018237803621,-0.0664378360264485,-0.0640341176443245,-0.0608259398031352,
-0.0527118768185914,-0.0229576793455864,-0.0143961687149711,-0.0115987725285022,
-0.00982773786947007,-0.00825972761001749,-0.00665241883828211,-0.00386429324692953,
-0.000340360607640195),.UNSPECIFIED.);
#113=B_SPLINE_CURVE_WITH_KNOTS('',3,(#10806,#10807,#10808,#10809,#10810,
#10811,#10812,#10813,#10814,#10815,#10816,#10817,#10818,#10819,#10820,#10821,
#10822,#10823,#10824,#10825,#10826,#10827,#10828,#10829,#10830,#10831,#10832,
#10833,#10834,#10835,#10836,#10837,#10838,#10839,#10840,#10841,#10842,#10843,
#10844,#10845,#10846,#10847,#10848,#10849,#10850,#10851,#10852,#10853,#10854,
#10855,#10856,#10857,#10858,#10859,#10860,#10861,#10862,#10863,#10864,#10865,
#10866,#10867,#10868,#10869,#10870,#10871,#10872,#10873,#10874,#10875,#10876,
#10877,#10878,#10879,#10880,#10881,#10882,#10883,#10884,#10885,#10886,#10887,
#10888,#10889,#10890,#10891,#10892,#10893,#10894,#10895,#10896,#10897,#10898,
#10899,#10900,#10901,#10902,#10903,#10904,#10905,#10906,#10907),
 .UNSPECIFIED.,.F.,.F.,(4,2,2,2,2,2,2,2,2,2,2,2,2,2,2,2,2,2,2,2,2,2,2,2,
2,2,2,2,2,2,2,2,2,2,2,2,2,2,2,2,2,2,2,2,2,2,2,2,2,2,4),(-1.48415514651379,
-1.45149920551291,-1.44244211629787,-1.43731255766761,-1.43575204220037,
-1.43476685356475,-1.433831635031,-1.43246270329097,-1.42986122343986,-1.4061924457234,
-1.38541357703921,-1.38163060098673,-1.37934788511961,-1.37731925181912,
-1.3772983125346,-1.37727586732553,-1.37725174788944,-1.37722575916579,
-1.37719767368199,-1.37716722436655,-1.37713409534207,-1.37709790995652,
-1.37705821505763,-1.37701446000724,-1.37696596824716,-1.37691189805811,
-1.37685118732537,-1.37678247397149,-1.37674965215004,-1.37667856265869,
-1.37508854787638,-1.37306558233999,-1.36993756341773,-1.34725092169245,
-1.32984167098033,-1.3237024152774,-1.31978941393382,-1.31837742282627,
-1.31742421890925,-1.31656516220981,-1.31538032592114,-1.31236334101688,
-1.29433178935098,-1.27425428314318,-1.26394326012941,-1.26106272044498,
-1.25927404078754,-1.25762667722671,-1.25549914243146,-1.25084401886462,
-1.24265200671274),.UNSPECIFIED.);
#114=B_SPLINE_CURVE_WITH_KNOTS('',3,(#10908,#10909,#10910,#10911,#10912,
#10913,#10914,#10915,#10916,#10917,#10918,#10919,#10920,#10921,#10922,#10923,
#10924,#10925,#10926,#10927,#10928,#10929,#10930,#10931,#10932,#10933,#10934,
#10935,#10936,#10937,#10938,#10939,#10940,#10941,#10942,#10943,#10944,#10945,
#10946,#10947,#10948,#10949,#10950,#10951,#10952,#10953,#10954,#10955,#10956,
#10957,#10958,#10959,#10960,#10961,#10962,#10963,#10964,#10965,#10966,#10967,
#10968,#10969,#10970,#10971,#10972,#10973,#10974,#10975,#10976,#10977,#10978,
#10979,#10980,#10981,#10982,#10983,#10984,#10985,#10986,#10987,#10988,#10989,
#10990,#10991,#10992,#10993,#10994,#10995,#10996,#10997,#10998,#10999,#11000,
#11001,#11002,#11003,#11004,#11005,#11006,#11007,#11008,#11009,#11010,#11011,
#11012,#11013,#11014,#11015,#11016,#11017,#11018,#11019,#11020,#11021,#11022,
#11023,#11024,#11025,#11026,#11027,#11028,#11029,#11030,#11031,#11032,#11033,
#11034,#11035,#11036,#11037,#11038,#11039,#11040,#11041,#11042,#11043,#11044,
#11045,#11046,#11047,#11048,#11049,#11050,#11051,#11052,#11053,#11054,#11055,
#11056,#11057,#11058,#11059,#11060,#11061,#11062,#11063,#11064,#11065,#11066,
#11067,#11068,#11069,#11070,#11071,#11072,#11073,#11074,#11075,#11076,#11077,
#11078,#11079,#11080,#11081,#11082,#11083,#11084,#11085,#11086,#11087,#11088,
#11089,#11090,#11091,#11092,#11093,#11094,#11095,#11096,#11097,#11098,#11099,
#11100,#11101,#11102,#11103,#11104,#11105,#11106,#11107,#11108,#11109,#11110,
#11111,#11112,#11113,#11114,#11115,#11116,#11117),.UNSPECIFIED.,.F.,.F.,
(4,2,2,2,2,2,2,2,2,2,2,2,2,2,2,2,2,2,2,2,2,2,2,2,2,2,2,2,2,2,2,2,2,2,2,
2,2,2,2,2,2,2,2,2,2,2,2,2,2,2,2,2,2,2,2,2,2,2,2,2,2,2,2,2,2,2,2,2,2,2,2,
2,2,2,2,2,2,2,2,2,2,2,2,2,2,2,2,2,2,2,2,2,2,2,2,2,2,2,2,2,2,2,2,2,4),(-0.984126425382023,
-0.983373365694033,-0.972905881216294,-0.96440508188655,-0.944486287465323,
-0.933431938592775,-0.930487001827596,-0.928683873097357,-0.92703995418775,
-0.924940004467587,-0.920438620203604,-0.893336752663696,-0.873797532864454,
-0.871327513572878,-0.870150693646636,-0.869234327455437,-0.868154122712197,
-0.86621562404796,-0.856915362097018,-0.837265444012163,-0.820172839227312,
-0.814728758241953,-0.812440769945779,-0.810773058499702,-0.809236966256497,
-0.807147299654878,-0.802985899498695,-0.778077028674095,-0.770491729308653,
-0.757142158191999,-0.754264791825363,-0.753013336330303,-0.752088605896066,
-0.751053954240847,-0.749270710216774,-0.742536657701058,-0.728157707544133,
-0.701569538465855,-0.6970339008539,-0.694927624767163,-0.69328279890119,
-0.691482791774579,-0.688552312985616,-0.677673742852565,-0.658340794028179,
-0.64016692608942,-0.637153807938739,-0.635969333996813,-0.635110150305577,
-0.634156332939673,-0.632742651598299,-0.628819870039803,-0.62266115183107,
-0.605273799859729,-0.5825841984773,-0.579460660601513,-0.577438613171592,
-0.575806484002945,-0.573935440464655,-0.570678443187492,-0.554643588932069,
-0.540207700435531,-0.531713365710718,-0.521291872639942,-0.519468479745616,
-0.51831798827299,-0.517403225285627,-0.516302204207945,-0.514209928708041,
-0.498523035351526,-0.473541380321435,-0.464243314699706,-0.46136156623328,
-0.459572217995092,-0.457924297183967,-0.455759598764231,-0.451029887520897,
-0.444639846263575,-0.426891207045569,-0.405545692995482,-0.402605810537817,
-0.401433612918007,-0.400577530298193,-0.399620091151593,-0.398188887347618,
-0.394137084093678,-0.387694401476146,-0.370627114237207,-0.348075710368098,
-0.344949807772665,-0.342927065866851,-0.341294918907402,-0.339424450217873,
-0.336169997443571,-0.320188811190221,-0.305714433171593,-0.29720386249206,
-0.286780218720869,-0.284956769767485,-0.283806274447871,-0.282891530162832,
-0.28179055775546,-0.279698446018787,-0.264018358063324,-0.241971004323415),
 .UNSPECIFIED.);
#115=B_SPLINE_CURVE_WITH_KNOTS('',3,(#11122,#11123,#11124,#11125,#11126,
#11127,#11128,#11129,#11130,#11131,#11132,#11133,#11134,#11135,#11136,#11137,
#11138,#11139,#11140,#11141,#11142,#11143,#11144,#11145,#11146,#11147,#11148,
#11149,#11150,#11151,#11152,#11153,#11154,#11155,#11156,#11157,#11158,#11159,
#11160,#11161,#11162,#11163,#11164,#11165,#11166,#11167,#11168,#11169,#11170,
#11171,#11172,#11173,#11174,#11175,#11176,#11177,#11178,#11179,#11180,#11181,
#11182,#11183,#11184,#11185,#11186,#11187,#11188,#11189,#11190,#11191,#11192,
#11193,#11194,#11195,#11196,#11197,#11198,#11199,#11200,#11201,#11202,#11203,
#11204,#11205,#11206,#11207,#11208,#11209,#11210,#11211,#11212,#11213,#11214,
#11215,#11216,#11217,#11218,#11219,#11220,#11221,#11222,#11223,#11224,#11225,
#11226,#11227,#11228,#11229,#11230,#11231,#11232,#11233,#11234,#11235,#11236,
#11237,#11238,#11239,#11240,#11241,#11242,#11243,#11244,#11245,#11246,#11247,
#11248,#11249,#11250,#11251,#11252,#11253,#11254,#11255,#11256,#11257,#11258,
#11259,#11260,#11261,#11262,#11263,#11264,#11265,#11266,#11267,#11268,#11269,
#11270,#11271,#11272,#11273,#11274,#11275,#11276,#11277,#11278,#11279,#11280,
#11281,#11282,#11283,#11284,#11285,#11286,#11287,#11288,#11289,#11290,#11291,
#11292,#11293,#11294,#11295,#11296,#11297,#11298,#11299,#11300,#11301,#11302,
#11303,#11304,#11305,#11306,#11307,#11308,#11309,#11310,#11311,#11312,#11313,
#11314,#11315,#11316,#11317,#11318,#11319,#11320,#11321,#11322,#11323,#11324,
#11325,#11326,#11327,#11328,#11329,#11330,#11331,#11332,#11333,#11334,#11335,
#11336,#11337),.UNSPECIFIED.,.F.,.F.,(4,2,2,2,2,2,2,2,2,2,2,2,2,2,2,2,2,
2,2,2,2,2,2,2,2,2,2,2,2,2,2,2,2,2,2,2,2,2,2,2,2,2,2,2,2,2,2,2,2,2,2,2,2,
2,2,2,2,2,2,2,2,2,2,2,2,2,2,2,2,2,2,2,2,2,2,2,2,2,2,2,2,2,2,2,2,2,2,2,2,
2,2,2,2,2,2,2,2,2,2,2,2,2,2,2,2,2,2,4),(-1.24288726449128,-1.24163342877597,
-1.24065148247496,-1.23971399027183,-1.23855456628014,-1.23568835295016,
-1.21300160884336,-1.19617494378115,-1.18997916861392,-1.18536022569125,
-1.18321606753075,-1.18157132481516,-1.17977313763682,-1.17684952619924,
-1.16716146154078,-1.13631403244112,-1.12979850884176,-1.12571465366471,
-1.12427931995828,-1.12332113562735,-1.12246593316861,-1.12129687952411,
-1.11834450385232,-1.09713198867436,-1.08891161571426,-1.07227074593167,
-1.06796179849435,-1.06587571137707,-1.06423796846684,-1.06240895519245,
-1.0593445658533,-1.04821575680757,-1.02477530920776,-1.00970577855156,
-1.00762561154606,-1.00652721495725,-1.00561244168765,-1.0044591642126,
-1.00262628343159,-0.991958228061934,-0.98392943416366,-0.963130008609321,
-0.956165846235589,-0.951114761823736,-0.948893279039927,-0.947236904566019,
-0.945684622485903,-0.94310382069536,-0.936219008662551,-0.905685438203178,
-0.896642236282482,-0.893197693911649,-0.890658404777163,-0.889468444510046,
-0.888559318249259,-0.887491966658089,-0.885610059085682,-0.877271087301634,
-0.847860136594266,-0.835620927876824,-0.832585251292835,-0.830762428581112,
-0.829123335681778,-0.827026007287135,-0.822658622109339,-0.794113753893987,
-0.789047536182051,-0.779575591033752,-0.774290458738673,-0.772713091474382,
-0.771723993276586,-0.77079071192917,-0.769433081074306,-0.76687557349804,
-0.742576440167406,-0.719163860961597,-0.716031534274363,-0.714006938726207,
-0.71237478398984,-0.710505931928709,-0.707258487523441,-0.691420629244765,
-0.667199684751267,-0.657762157472976,-0.655816397579372,-0.654734615219692,
-0.653818485833921,-0.652643990423514,-0.650185746470363,-0.646883203323154,
-0.638404239760665,-0.612787283335558,-0.601233334434435,-0.598136504368191,
-0.596300303557412,-0.594827344822309,-0.592833235264844,-0.588990277410438,
-0.569376559148978,-0.549534964027653,-0.540486204516383,-0.538561582925485,
-0.5374845601196,-0.536567924843716,-0.535386922748773,-0.53289477986775,
-0.514846765038427,-0.500854930573822),.UNSPECIFIED.);
#116=B_SPLINE_CURVE_WITH_KNOTS('',3,(#11339,#11340,#11341,#11342,#11343,
#11344,#11345,#11346,#11347,#11348,#11349,#11350,#11351,#11352,#11353,#11354,
#11355,#11356,#11357,#11358,#11359,#11360,#11361,#11362,#11363,#11364,#11365,
#11366,#11367,#11368,#11369,#11370,#11371,#11372,#11373,#11374,#11375,#11376,
#11377,#11378,#11379,#11380,#11381,#11382,#11383,#11384,#11385,#11386,#11387,
#11388,#11389,#11390,#11391,#11392,#11393,#11394,#11395,#11396,#11397,#11398,
#11399,#11400,#11401,#11402,#11403,#11404,#11405,#11406,#11407,#11408,#11409,
#11410,#11411,#11412,#11413,#11414),.UNSPECIFIED.,.F.,.F.,(4,2,2,2,2,2,
2,2,2,2,2,2,2,2,2,2,2,2,2,2,2,2,2,2,2,2,2,2,2,2,2,2,2,2,2,2,2,4),(-0.241971004323415,
-0.239053971418212,-0.229736799381529,-0.22685307708173,-0.22506332408183,
-0.22341557890168,-0.221251912997029,-0.216527745168172,-0.210147422237314,
-0.192445910058425,-0.171033428826221,-0.168085358638406,-0.166917316565231,
-0.166062277525162,-0.165103567731153,-0.163666241889273,-0.159568416394568,
-0.153023023648686,-0.121691640522961,-0.11244487918447,-0.109568666996894,
-0.107780600902137,-0.106201075113282,-0.106181872856666,-0.104141339135245,
-0.10185902694292,-0.0980775006358801,-0.0902103746626518,-0.076223358344637,
-0.0536758840913093,-0.0507959511513297,-0.0496340231114811,-0.0486957404565197,
-0.0477144793902815,-0.0461727153274274,-0.041216633357305,-0.0326138141010124,
-0.000340852960060052),.UNSPECIFIED.);
#117=B_SPLINE_CURVE_WITH_KNOTS('',3,(#11415,#11416,#11417,#11418,#11419,
#11420,#11421,#11422,#11423,#11424,#11425,#11426,#11427,#11428,#11429,#11430,
#11431,#11432,#11433,#11434,#11435,#11436,#11437,#11438,#11439,#11440,#11441,
#11442,#11443,#11444,#11445,#11446,#11447,#11448,#11449,#11450,#11451,#11452,
#11453,#11454,#11455,#11456,#11457,#11458,#11459,#11460,#11461,#11462,#11463,
#11464,#11465,#11466,#11467,#11468,#11469,#11470,#11471,#11472,#11473,#11474,
#11475,#11476,#11477,#11478,#11479,#11480,#11481,#11482,#11483,#11484,#11485,
#11486,#11487,#11488,#11489,#11490,#11491,#11492,#11493,#11494,#11495,#11496,
#11497,#11498,#11499,#11500,#11501,#11502,#11503,#11504,#11505,#11506,#11507,
#11508,#11509,#11510,#11511,#11512,#11513,#11514,#11515,#11516,#11517,#11518,
#11519,#11520,#11521,#11522,#11523,#11524,#11525,#11526,#11527,#11528,#11529,
#11530,#11531,#11532,#11533,#11534,#11535,#11536,#11537,#11538,#11539,#11540,
#11541,#11542,#11543,#11544,#11545,#11546,#11547,#11548,#11549,#11550,#11551,
#11552,#11553,#11554,#11555,#11556,#11557,#11558,#11559,#11560,#11561,#11562,
#11563,#11564,#11565,#11566,#11567,#11568,#11569,#11570),.UNSPECIFIED.,
 .F.,.F.,(4,2,2,2,2,2,2,2,2,2,2,2,2,2,2,2,2,2,2,2,2,2,2,2,2,2,2,2,2,2,2,
2,2,2,2,2,2,2,2,2,2,2,2,2,2,2,2,2,2,2,2,2,2,2,2,2,2,2,2,2,2,2,2,2,2,2,2,
2,2,2,2,2,2,2,2,2,2,4),(-1.48431280040011,-1.47896056546552,-1.47689292482486,
-1.47529572669305,-1.47371992892605,-1.47193220443593,-1.46905506899411,
-1.45978888255018,-1.43819039265586,-1.42492169717083,-1.42054823772937,
-1.4175020382775,-1.41622215306785,-1.41529358812556,-1.41427335838495,
-1.41255378430918,-1.40649295880256,-1.38450574218668,-1.37007018954134,
-1.36442059579054,-1.36141528466624,-1.35945096227819,-1.35805699629727,
-1.3564493497163,-1.35463627557722,-1.35164285402985,-1.34126858027713,
-1.31117265327994,-1.30470819826332,-1.30064753724468,-1.29921556738997,
-1.29825828937859,-1.2974028668826,-1.29623223184307,-1.29329962648975,
-1.27178996015631,-1.25418919766581,-1.2478309444976,-1.24311937298221,
-1.24095856523215,-1.23931180718429,-1.23752196386011,-1.23463551625966,
-1.22528507866461,-1.19406517724991,-1.18752623024879,-1.18343208354017,
-1.18199556015604,-1.18103726039389,-1.1801824852927,-1.17901468807528,
-1.17606736578505,-1.15471040666525,-1.13700043088882,-1.13061945590468,
-1.12589485831694,-1.12373155754217,-1.12208431203236,-1.12029531728363,
-1.11741330022025,-1.10810671568076,-1.0831269318708,-1.06744091024756,
-1.06534906821887,-1.06424836164924,-1.06333390643313,-1.06218386598269,
-1.06036132482472,-1.04994657472771,-1.04146389337108,-1.02704592886333,
-1.01101876958153,-1.00776311751941,-1.00589275325785,-1.0042611590973,
-1.00223970033911,-0.999116899707024,-0.983965850740792),.UNSPECIFIED.);
#118=B_SPLINE_CURVE_WITH_KNOTS('',3,(#11576,#11577,#11578,#11579,#11580,
#11581,#11582,#11583,#11584,#11585,#11586,#11587,#11588,#11589,#11590,#11591,
#11592,#11593,#11594,#11595,#11596,#11597,#11598,#11599,#11600,#11601,#11602,
#11603,#11604,#11605,#11606,#11607,#11608,#11609,#11610,#11611,#11612,#11613,
#11614,#11615,#11616,#11617,#11618,#11619,#11620,#11621,#11622,#11623,#11624,
#11625,#11626,#11627,#11628,#11629,#11630,#11631,#11632,#11633,#11634,#11635,
#11636,#11637,#11638,#11639,#11640,#11641,#11642,#11643,#11644,#11645,#11646,
#11647,#11648,#11649,#11650,#11651,#11652,#11653,#11654,#11655,#11656,#11657,
#11658,#11659,#11660,#11661,#11662,#11663,#11664,#11665,#11666,#11667,#11668,
#11669,#11670,#11671,#11672,#11673,#11674,#11675,#11676,#11677,#11678,#11679,
#11680,#11681,#11682,#11683,#11684,#11685,#11686,#11687,#11688,#11689,#11690,
#11691,#11692,#11693,#11694,#11695,#11696,#11697,#11698,#11699,#11700,#11701,
#11702,#11703,#11704,#11705,#11706,#11707,#11708,#11709,#11710,#11711,#11712,
#11713,#11714,#11715,#11716,#11717,#11718,#11719),.UNSPECIFIED.,.F.,.F.,
(4,2,2,2,2,2,2,2,2,2,2,2,2,2,2,2,2,2,2,2,2,2,2,2,2,2,2,2,2,2,2,2,2,2,2,
2,2,2,2,2,2,2,2,2,2,2,2,2,2,2,2,2,2,2,2,2,2,2,2,2,2,2,2,2,2,2,2,2,2,2,2,
4),(-0.500801107159108,-0.496719065298586,-0.482294243553749,-0.473808490442153,
-0.463388293448443,-0.461565209675061,-0.460414906796204,-0.459500285784731,
-0.458399412973998,-0.456307344596265,-0.440613399579905,-0.415608457267786,
-0.40634982463576,-0.403472564478538,-0.401684376828063,-0.400036432618386,
-0.397870099126282,-0.39313018891593,-0.386721806429579,-0.368880059124788,
-0.347686747930129,-0.344731566857804,-0.343562416108004,-0.342707179701646,
-0.341748992382079,-0.340313724936937,-0.336230432660855,-0.329717053164425,
-0.298870969127536,-0.28919746513731,-0.286275355303111,-0.284477439454449,
-0.282832513660004,-0.280687496388851,-0.276064258498405,-0.269860370559074,
-0.252996759706132,-0.230336790507938,-0.22746686859608,-0.226306747010982,
-0.22536902236462,-0.224387225669904,-0.222842659074172,-0.217860248016697,
-0.209188959324149,-0.182095666929319,-0.172053928327316,-0.169090290863669,
-0.167283331368708,-0.165640858576464,-0.163514331183331,-0.158990961236074,
-0.152960381091844,-0.13688889987488,-0.112980279065176,-0.110135095017116,
-0.109012950430518,-0.108084887205651,-0.107106739772946,-0.105622849083686,
-0.10379912883353,-0.100231194655918,-0.0906818545504389,-0.0829888986598714,
-0.0575747013332469,-0.0530377262946375,-0.0508997778988846,-0.0492506615316133,
-0.0474663484896398,-0.0446066631603827,-0.0345296234097491,-0.000340926357595197),
 .UNSPECIFIED.);
#119=B_SPLINE_CURVE_WITH_KNOTS('',3,(#11720,#11721,#11722,#11723,#11724,
#11725,#11726,#11727,#11728,#11729,#11730,#11731,#11732,#11733,#11734,#11735,
#11736,#11737,#11738,#11739,#11740,#11741,#11742,#11743,#11744,#11745,#11746,
#11747,#11748,#11749,#11750,#11751,#11752,#11753,#11754,#11755,#11756,#11757,
#11758,#11759,#11760,#11761,#11762,#11763,#11764,#11765,#11766,#11767,#11768,
#11769,#11770,#11771,#11772,#11773,#11774,#11775,#11776,#11777,#11778,#11779,
#11780,#11781,#11782,#11783,#11784,#11785,#11786,#11787,#11788,#11789,#11790,
#11791,#11792,#11793,#11794,#11795,#11796,#11797),.UNSPECIFIED.,.F.,.F.,
(4,2,2,2,2,2,2,2,2,2,2,2,2,2,2,2,2,2,2,2,2,2,2,2,2,2,2,2,2,2,2,2,2,2,2,
2,2,2,4),(-1.48440949910283,-1.4781158042,-1.47680243786291,-1.47585385357628,
-1.47499593067532,-1.47413998146761,-1.47296752304019,-1.47001584976481,
-1.46266620479669,-1.43155466603343,-1.42484447046188,-1.41993456996183,
-1.41773818743503,-1.41608612565901,-1.4145273566791,-1.41191052624761,
-1.40476913271227,-1.37446864224158,-1.36550713048265,-1.36208323358632,
-1.36031134764514,-1.35882320203303,-1.35787181397324,-1.35693581026479,
-1.35578187816802,-1.35294711884787,-1.32977967194719,-1.31326405289154,
-1.30713574232963,-1.30255564838505,-1.30041873287133,-1.29877504491022,
-1.29697353758565,-1.29403436310168,-1.28420275305495,-1.25686630998966,
-1.24817035041627,-1.2431789305523,-1.24288726449128),.UNSPECIFIED.);
#120=B_SPLINE_CURVE_WITH_KNOTS('',3,(#11798,#11799,#11800,#11801,#11802,
#11803,#11804,#11805,#11806,#11807,#11808,#11809,#11810,#11811,#11812,#11813,
#11814,#11815,#11816,#11817,#11818,#11819,#11820,#11821,#11822,#11823,#11824,
#11825,#11826,#11827,#11828,#11829,#11830,#11831,#11832,#11833,#11834,#11835,
#11836,#11837,#11838,#11839,#11840,#11841,#11842,#11843,#11844,#11845,#11846,
#11847,#11848,#11849,#11850,#11851,#11852,#11853,#11854,#11855,#11856,#11857,
#11858,#11859,#11860,#11861,#11862,#11863,#11864,#11865,#11866,#11867,#11868,
#11869,#11870,#11871,#11872,#11873,#11874,#11875,#11876,#11877,#11878,#11879,
#11880,#11881,#11882,#11883,#11884,#11885,#11886,#11887,#11888,#11889,#11890,
#11891,#11892,#11893,#11894,#11895,#11896,#11897,#11898,#11899,#11900,#11901,
#11902,#11903,#11904,#11905,#11906,#11907,#11908,#11909,#11910,#11911,#11912,
#11913,#11914,#11915,#11916,#11917,#11918,#11919,#11920,#11921,#11922,#11923,
#11924,#11925,#11926,#11927,#11928,#11929,#11930,#11931,#11932,#11933,#11934,
#11935,#11936,#11937,#11938,#11939,#11940,#11941,#11942,#11943,#11944,#11945,
#11946,#11947,#11948,#11949,#11950,#11951,#11952,#11953,#11954,#11955,#11956,
#11957,#11958,#11959,#11960,#11961,#11962,#11963,#11964,#11965,#11966,#11967,
#11968,#11969,#11970,#11971,#11972,#11973,#11974,#11975,#11976,#11977,#11978,
#11979,#11980,#11981,#11982,#11983,#11984,#11985,#11986,#11987,#11988,#11989,
#11990,#11991,#11992,#11993,#11994,#11995,#11996,#11997,#11998,#11999,#12000,
#12001,#12002,#12003,#12004,#12005,#12006,#12007,#12008,#12009,#12010,#12011,
#12012,#12013,#12014,#12015,#12016,#12017,#12018,#12019),.UNSPECIFIED.,
 .F.,.F.,(4,2,2,2,2,2,2,2,2,2,2,2,2,2,2,2,2,2,2,2,2,2,2,2,2,2,2,2,2,2,2,
2,2,2,2,2,2,2,2,2,2,2,2,2,2,2,2,2,2,2,2,2,2,2,2,2,2,2,2,2,2,2,2,2,2,2,2,
2,2,2,2,2,2,2,2,2,2,2,2,2,2,2,2,2,2,2,2,2,2,2,2,2,2,2,2,2,2,2,2,2,2,2,2,
2,2,2,2,2,2,2,4),(-0.983965850740792,-0.976428697428846,-0.959045095961489,
-0.952876404968067,-0.948949764161217,-0.947535827801338,-0.946582177705485,
-0.945723405608626,-0.944539842061414,-0.941530835141036,-0.922281673275152,
-0.903762537031074,-0.896724178341862,-0.891632474803611,-0.889404206799181,
-0.887746973845169,-0.886196914496551,-0.883626948700429,-0.876814880707329,
-0.846213007603617,-0.83715097356694,-0.833701920004943,-0.831160152720884,
-0.829969847312564,-0.829060827846964,-0.827994052118297,-0.826114188563904,
-0.817802398410004,-0.792860302132136,-0.776564021948787,-0.77329597848607,
-0.771422870431342,-0.76979143471797,-0.767773467493801,-0.764662372283216,
-0.74225374988622,-0.718463153736229,-0.714550134167476,-0.713093994412623,
-0.712227047949536,-0.71128142153802,-0.709907802106248,-0.706265635557273,
-0.7007048015412,-0.68098909362998,-0.659699936987695,-0.656561536305509,
-0.654535206144928,-0.652903074845401,-0.651035807311733,-0.647795149662252,
-0.632095427960709,-0.609174234092233,-0.604739213945095,-0.59796325257311,
-0.596176533825275,-0.595141251301399,-0.594216936000927,-0.592967396330633,
-0.590100111197881,-0.576846030924175,-0.568460602809955,-0.544317396501895,
-0.539674031624726,-0.537548345915618,-0.53590096725911,-0.534110828263999,
-0.531224746360662,-0.520857145987655,-0.500579691464689,-0.498155800088846,
-0.481347157268226,-0.479411982654054,-0.478228173420962,-0.477311400996102,
-0.476236606468444,-0.474267874747157,-0.463013411690192,-0.447187888902494,
-0.425228744858819,-0.422086261431702,-0.420058659823978,-0.418426385971435,
-0.416559917619868,-0.413323126686715,-0.397704962907729,-0.375492237198176,
-0.370616026629478,-0.363532450079602,-0.361719435784044,-0.360678368129702,
-0.359755537405875,-0.35851698649178,-0.355712159094041,-0.343050632059556,
-0.339789268291339,-0.311247873410837,-0.305737138156674,-0.303607241145018,
-0.30206118217053,-0.300401119482355,-0.298156542080228,-0.292970615229178,
-0.285759137709564,-0.26639756419925,-0.248273508693048,-0.245258751663719,
-0.244074127698381,-0.243215004790582,-0.242261459367992,-0.241913378149247),
 .UNSPECIFIED.);
#121=B_SPLINE_CURVE_WITH_KNOTS('',3,(#12024,#12025,#12026,#12027,#12028,
#12029,#12030,#12031,#12032,#12033,#12034,#12035,#12036,#12037,#12038,#12039,
#12040,#12041,#12042,#12043,#12044,#12045,#12046,#12047,#12048,#12049,#12050,
#12051,#12052,#12053,#12054,#12055,#12056,#12057,#12058,#12059,#12060,#12061,
#12062,#12063,#12064,#12065,#12066,#12067,#12068,#12069,#12070,#12071,#12072,
#12073,#12074,#12075,#12076,#12077,#12078,#12079,#12080,#12081,#12082,#12083,
#12084,#12085,#12086,#12087,#12088,#12089,#12090,#12091,#12092,#12093,#12094,
#12095,#12096,#12097,#12098,#12099,#12100,#12101,#12102,#12103,#12104,#12105,
#12106,#12107,#12108,#12109,#12110,#12111,#12112,#12113,#12114,#12115,#12116,
#12117,#12118,#12119,#12120,#12121,#12122,#12123,#12124,#12125,#12126,#12127,
#12128,#12129,#12130,#12131,#12132,#12133,#12134,#12135,#12136,#12137,#12138,
#12139,#12140,#12141,#12142,#12143,#12144,#12145,#12146,#12147,#12148,#12149,
#12150,#12151,#12152,#12153,#12154,#12155,#12156,#12157,#12158,#12159,#12160,
#12161,#12162,#12163,#12164,#12165,#12166,#12167,#12168,#12169,#12170,#12171,
#12172,#12173,#12174,#12175,#12176,#12177,#12178,#12179,#12180,#12181,#12182,
#12183,#12184,#12185,#12186,#12187,#12188,#12189,#12190,#12191,#12192,#12193,
#12194,#12195,#12196,#12197,#12198,#12199,#12200,#12201,#12202,#12203,#12204,
#12205,#12206,#12207,#12208,#12209,#12210,#12211,#12212,#12213,#12214,#12215,
#12216,#12217,#12218,#12219,#12220,#12221,#12222,#12223,#12224,#12225,#12226,
#12227,#12228,#12229,#12230,#12231,#12232,#12233,#12234,#12235,#12236,#12237,
#12238,#12239,#12240,#12241,#12242,#12243,#12244,#12245),.UNSPECIFIED.,
 .F.,.F.,(4,2,2,2,2,2,2,2,2,2,2,2,2,2,2,2,2,2,2,2,2,2,2,2,2,2,2,2,2,2,2,
2,2,2,2,2,2,2,2,2,2,2,2,2,2,2,2,2,2,2,2,2,2,2,2,2,2,2,2,2,2,2,2,2,2,2,2,
2,2,2,2,2,2,2,2,2,2,2,2,2,2,2,2,2,2,2,2,2,2,2,2,2,2,2,2,2,2,2,2,2,2,2,2,
2,2,2,2,2,2,2,4),(-1.24275875787133,-1.22762709042559,-1.22439557108871,
-1.22253040814363,-1.22089824662139,-1.21886943960928,-1.21572244605731,
-1.19377471854145,-1.1779530859873,-1.16668254077522,-1.16471331138028,
-1.1636385000826,-1.16272186196663,-1.16153841649317,-1.15960421697158,
-1.1434311354434,-1.14040894422488,-1.12013411227508,-1.11326239930923,
-1.10826253976813,-1.10605016131273,-1.10439542077469,-1.10284093033319,
-1.10024756798278,-1.09327378678655,-1.06282525540613,-1.05380937532503,
-1.04869512696797,-1.04713608115745,-1.04615109810587,-1.04521546079699,
-1.04384498891157,-1.04123808540654,-1.01765465716894,-1.00141723025515,
-0.995349644485654,-0.990804417400253,-0.988673760726219,-0.987030681099189,
-0.985225638721172,-0.982271084517546,-0.972308353985407,-0.941761417526941,
-0.935265240655457,-0.931189948491823,-0.929755678374846,-0.928797660019481,
-0.927942185370316,-0.926772233310791,-0.923845209926974,-0.902247053177529,
-0.884696379319723,-0.878347622556955,-0.873641060241546,-0.871480653994794,
-0.869833424525861,-0.868042305160197,-0.865152090496027,-0.855774016661728,
-0.830787781031016,-0.815186007645975,-0.813095244649029,-0.811994570448843,
-0.811079827689608,-0.809929016013944,-0.808104496425623,-0.79764984218356,
-0.789148471402704,-0.762083629338326,-0.75670033941679,-0.754422528616797,
-0.752756721290641,-0.751218527442592,-0.748713842179597,-0.742321661881945,
-0.732501371157368,-0.717302382328109,-0.716304926794569,-0.709948205956288,
-0.697948099926155,-0.696068579989618,-0.694901291903405,-0.693985708609038,
-0.692898547487598,-0.690871865540765,-0.677931799445221,-0.649154283611957,
-0.640627360955181,-0.637831985324643,-0.636061554521682,-0.634407203720999,
-0.632198307072287,-0.627219327042051,-0.620384717817706,-0.600321734957142,
-0.582231537016983,-0.579215353915678,-0.578030480957579,-0.577171283423045,
-0.576217775081048,-0.57480509047453,-0.570888516213993,-0.564742830092001,
-0.547349286418453,-0.524661547707217,-0.52153867618665,-0.519517001818466,
-0.517885131453972,-0.516014334483734,-0.512757624437976,-0.500801107159108),
 .UNSPECIFIED.);
#122=B_SPLINE_CURVE_WITH_KNOTS('',3,(#12247,#12248,#12249,#12250,#12251,
#12252,#12253,#12254,#12255,#12256,#12257,#12258,#12259,#12260,#12261,#12262,
#12263,#12264,#12265,#12266,#12267,#12268,#12269,#12270,#12271,#12272,#12273,
#12274,#12275,#12276,#12277,#12278,#12279,#12280,#12281,#12282,#12283,#12284,
#12285,#12286,#12287,#12288,#12289,#12290,#12291,#12292,#12293,#12294,#12295,
#12296,#12297,#12298,#12299,#12300,#12301,#12302,#12303,#12304,#12305,#12306,
#12307,#12308,#12309,#12310,#12311,#12312,#12313,#12314,#12315,#12316,#12317,
#12318,#12319,#12320,#12321,#12322),.UNSPECIFIED.,.F.,.F.,(4,2,2,2,2,2,
2,2,2,2,2,2,2,2,2,2,2,2,2,2,2,2,2,2,2,2,2,2,2,2,2,2,2,2,2,2,2,4),(-0.241913378149247,
-0.240848529093374,-0.236930072495017,-0.230780351330327,-0.213387702374564,
-0.190697843519608,-0.187574853042253,-0.185553162085369,-0.183921322020081,
-0.182050611408162,-0.178794197570654,-0.162762320117167,-0.148323804694671,
-0.131022001665608,-0.128017273181183,-0.126834312529553,-0.125975612122178,
-0.125040770468585,-0.123674078159674,-0.122081740969019,-0.119145492171102,
-0.0866091802778103,-0.0730245358674191,-0.0698237409054384,-0.0679467365411574,
-0.0663156176982367,-0.0643028117346279,-0.060366494308501,-0.0379726691064073,
-0.019855373815882,-0.0125687094178807,-0.010314958382663,-0.00916598278167907,
-0.00830796414785512,-0.00744080725723779,-0.00637243950620114,-0.00397627449831531,
-0.000340284409424339),.UNSPECIFIED.);
#123=B_SPLINE_CURVE_WITH_KNOTS('',3,(#12323,#12324,#12325,#12326,#12327,
#12328,#12329,#12330,#12331,#12332,#12333,#12334,#12335,#12336,#12337,#12338,
#12339,#12340,#12341,#12342,#12343,#12344,#12345,#12346,#12347,#12348,#12349,
#12350,#12351,#12352,#12353,#12354,#12355,#12356,#12357,#12358,#12359,#12360,
#12361,#12362,#12363,#12364,#12365,#12366,#12367,#12368,#12369,#12370,#12371,
#12372,#12373,#12374,#12375,#12376,#12377,#12378,#12379,#12380,#12381,#12382,
#12383,#12384,#12385,#12386,#12387,#12388,#12389,#12390,#12391,#12392,#12393,
#12394,#12395,#12396,#12397,#12398,#12399,#12400,#12401,#12402,#12403,#12404,
#12405,#12406,#12407,#12408,#12409,#12410,#12411,#12412,#12413,#12414,#12415,
#12416,#12417,#12418,#12419,#12420,#12421,#12422,#12423,#12424,#12425,#12426,
#12427,#12428,#12429,#12430,#12431,#12432,#12433,#12434,#12435,#12436,#12437,
#12438,#12439,#12440,#12441,#12442,#12443,#12444,#12445,#12446,#12447,#12448,
#12449,#12450,#12451,#12452,#12453,#12454,#12455,#12456,#12457,#12458,#12459,
#12460,#12461,#12462,#12463,#12464,#12465,#12466),.UNSPECIFIED.,.F.,.F.,
(4,2,2,2,2,2,2,2,2,2,2,2,2,2,2,2,2,2,2,2,2,2,2,2,2,2,2,2,2,2,2,2,2,2,2,
2,2,2,2,2,2,2,2,2,2,2,2,2,2,2,2,2,2,2,2,2,2,2,2,2,2,2,2,2,2,2,2,2,2,2,2,
4),(-1.48418159104277,-1.44929736991942,-1.43894158361684,-1.4360579623585,
-1.43426916311607,-1.43262289081551,-1.43049845413665,-1.42585712116349,
-1.40172735276898,-1.38793036424003,-1.38161779511944,-1.37890912617517,
-1.37740357484174,-1.37612666886343,-1.37520494917929,-1.37434013478619,
-1.37313204004411,-1.37063563727009,-1.34588640567838,-1.33035881398873,
-1.32445255784646,-1.32000161110428,-1.31788943205404,-1.31624961354488,
-1.31443705457726,-1.31144445990731,-1.30107279587294,-1.27098596656034,
-1.26452340553208,-1.26046392915307,-1.25903237427002,-1.2580753728876,
-1.25722019698239,-1.25604989864143,-1.25311813286199,-1.23161483158907,
-1.21401904208531,-1.207662601943,-1.20295237769528,-1.2007921912895,-1.19914590817853,
-1.19735658243439,-1.19447097258771,-1.18512327836783,-1.15391233762704,
-1.14737527465886,-1.14328230813391,-1.14184619914704,-1.1408881759123,
-1.14003364753053,-1.13886618746356,-1.13591971620666,-1.11456890259433,
-1.09686405051954,-1.09048491967064,-1.08576168707199,-1.0835990108936,
-1.08195224081831,-1.08016376225593,-1.07728257639724,-1.06797867254565,
-1.04300610243364,-1.02732460955563,-1.02523337126674,-1.02413298236893,
-1.02321879106532,-1.02206908251009,-1.02024706731368,-1.00983532228453,
-1.00135508142519,-0.986941262039221,-0.98392338245625),.UNSPECIFIED.);
#124=B_SPLINE_CURVE_WITH_KNOTS('',3,(#12472,#12473,#12474,#12475,#12476,
#12477,#12478,#12479,#12480,#12481,#12482,#12483,#12484,#12485,#12486,#12487,
#12488,#12489,#12490,#12491,#12492,#12493,#12494,#12495,#12496,#12497,#12498,
#12499,#12500,#12501,#12502,#12503,#12504,#12505,#12506,#12507,#12508,#12509,
#12510,#12511,#12512,#12513,#12514,#12515,#12516,#12517,#12518,#12519,#12520,
#12521,#12522,#12523,#12524,#12525,#12526,#12527,#12528,#12529,#12530,#12531,
#12532,#12533,#12534,#12535,#12536,#12537,#12538,#12539,#12540,#12541,#12542,
#12543,#12544,#12545,#12546,#12547,#12548,#12549,#12550,#12551,#12552,#12553,
#12554,#12555,#12556,#12557,#12558,#12559,#12560,#12561,#12562,#12563,#12564,
#12565,#12566,#12567,#12568,#12569,#12570,#12571,#12572,#12573,#12574,#12575,
#12576,#12577,#12578,#12579,#12580,#12581,#12582,#12583,#12584,#12585,#12586,
#12587,#12588,#12589,#12590,#12591,#12592,#12593,#12594,#12595,#12596,#12597,
#12598,#12599,#12600,#12601,#12602,#12603,#12604,#12605,#12606,#12607,#12608,
#12609,#12610,#12611,#12612,#12613,#12614,#12615,#12616,#12617,#12618,#12619,
#12620,#12621),.UNSPECIFIED.,.F.,.F.,(4,2,2,2,2,2,2,2,2,2,2,2,2,2,2,2,2,
2,2,2,2,2,2,2,2,2,2,2,2,2,2,2,2,2,2,2,2,2,2,2,2,2,2,2,2,2,2,2,2,2,2,2,2,
2,2,2,2,2,2,2,2,2,2,2,2,2,2,2,2,2,2,2,2,2,4),(-0.500743339736994,-0.500421455876749,
-0.499506597245934,-0.49840543860593,-0.496312827532433,-0.480614849588234,
-0.455603525682823,-0.446342355606896,-0.443464334025091,-0.44167567878242,
-0.440027307419358,-0.437860417924,-0.433119313896671,-0.426709332808253,
-0.408863275680894,-0.387663978310866,-0.38470805180707,-0.38353860100022,
-0.382683143320616,-0.381724705912274,-0.380289060085995,-0.376204665646574,
-0.36968950165102,-0.338833978450358,-0.329159255197456,-0.32623652512599,
-0.324438172499309,-0.322792810799851,-0.320647172804963,-0.316022388278023,
-0.309816286013742,-0.29294548214833,-0.270284042353455,-0.267413052528543,
-0.266252574012108,-0.265314591024113,-0.264332560995082,-0.262787692009562,
-0.257804876891455,-0.24913362992991,-0.22205701802673,-0.211989251081525,
-0.20902297549004,-0.207215138753453,-0.205572341918865,-0.203446066573736,
-0.198925841160012,-0.192901155243357,-0.176858899977733,-0.152929626487514,
-0.150341589158695,-0.148975882894424,-0.148040995266714,-0.147054229540533,
-0.145487807603155,-0.140404622250099,-0.131426679864947,-0.099285778178127,
-0.0935252617907595,-0.0911211697337286,-0.0894489453937931,-0.0877405569327365,
-0.0854750105786094,-0.0794775833616094,-0.0706309881269793,-0.0545732589707769,
-0.0359720291257095,-0.032960140758076,-0.031775904382688,-0.0309168077256966,
-0.0299629763195435,-0.0285490724174048,-0.0269145647411012,-0.0238658217156568,
-0.000340704748871543),.UNSPECIFIED.);
#125=B_SPLINE_CURVE_WITH_KNOTS('',3,(#12622,#12623,#12624,#12625,#12626,
#12627,#12628,#12629,#12630,#12631,#12632,#12633,#12634,#12635,#12636,#12637,
#12638,#12639,#12640,#12641,#12642,#12643,#12644,#12645,#12646,#12647,#12648,
#12649,#12650,#12651,#12652,#12653,#12654,#12655,#12656,#12657,#12658,#12659,
#12660,#12661,#12662,#12663,#12664,#12665,#12666,#12667,#12668,#12669,#12670,
#12671,#12672,#12673,#12674,#12675,#12676,#12677,#12678,#12679,#12680,#12681,
#12682,#12683,#12684,#12685,#12686,#12687,#12688,#12689,#12690,#12691,#12692,
#12693),.UNSPECIFIED.,.F.,.F.,(4,2,2,2,2,2,2,2,2,2,2,2,2,2,2,2,2,2,2,2,
2,2,2,2,2,2,2,2,2,2,2,2,2,2,2,4),(-1.48439292099721,-1.46367001774405,-1.46072402984557,
-1.458783958121,-1.45722482916291,-1.45559553177565,-1.45369435093942,-1.45038621433275,
-1.43466982309695,-1.42023860716416,-1.40260871447461,-1.39970369498598,
-1.39842711079842,-1.3974989050233,-1.39647683777673,-1.39474958742878,
-1.38861335916595,-1.36449168775534,-1.35154719928667,-1.34627169432974,
-1.34223098290889,-1.34025737936908,-1.33861898239508,-1.33679518963765,
-1.33375375619854,-1.32300731311845,-1.29661177082536,-1.28397018117173,
-1.28195284410562,-1.28086779668327,-1.27995223177072,-1.27878272149796,
-1.27689537761869,-1.26467333372395,-1.24314862470824,-1.24275875787133),
 .UNSPECIFIED.);
#126=B_SPLINE_CURVE_WITH_KNOTS('',3,(#12694,#12695,#12696,#12697,#12698,
#12699,#12700,#12701,#12702,#12703,#12704,#12705,#12706,#12707,#12708,#12709,
#12710,#12711,#12712,#12713,#12714,#12715,#12716,#12717,#12718,#12719,#12720,
#12721,#12722,#12723,#12724,#12725,#12726,#12727,#12728,#12729,#12730,#12731,
#12732,#12733,#12734,#12735,#12736,#12737,#12738,#12739,#12740,#12741,#12742,
#12743,#12744,#12745,#12746,#12747,#12748,#12749,#12750,#12751,#12752,#12753,
#12754,#12755,#12756,#12757,#12758,#12759,#12760,#12761,#12762,#12763,#12764,
#12765,#12766,#12767,#12768,#12769,#12770,#12771,#12772,#12773,#12774,#12775,
#12776,#12777,#12778,#12779,#12780,#12781,#12782,#12783,#12784,#12785,#12786,
#12787,#12788,#12789,#12790,#12791,#12792,#12793,#12794,#12795,#12796,#12797,
#12798,#12799,#12800,#12801,#12802,#12803,#12804,#12805,#12806,#12807,#12808,
#12809,#12810,#12811,#12812,#12813,#12814,#12815,#12816,#12817,#12818,#12819,
#12820,#12821,#12822,#12823,#12824,#12825,#12826,#12827,#12828,#12829,#12830,
#12831,#12832,#12833,#12834,#12835,#12836,#12837,#12838,#12839,#12840,#12841,
#12842,#12843,#12844,#12845,#12846,#12847,#12848,#12849,#12850,#12851,#12852,
#12853,#12854,#12855,#12856,#12857,#12858,#12859,#12860,#12861,#12862,#12863,
#12864,#12865,#12866,#12867,#12868,#12869,#12870,#12871,#12872,#12873,#12874,
#12875,#12876,#12877,#12878,#12879,#12880,#12881,#12882,#12883,#12884,#12885,
#12886,#12887,#12888,#12889,#12890,#12891,#12892,#12893,#12894,#12895,#12896,
#12897,#12898,#12899,#12900,#12901,#12902,#12903,#12904,#12905,#12906,#12907,
#12908,#12909,#12910,#12911,#12912,#12913,#12914,#12915,#12916,#12917,#12918,
#12919),.UNSPECIFIED.,.F.,.F.,(4,2,2,2,2,2,2,2,2,2,2,2,2,2,2,2,2,2,2,2,
2,2,2,2,2,2,2,2,2,2,2,2,2,2,2,2,2,2,2,2,2,2,2,2,2,2,2,2,2,2,2,2,2,2,2,2,
2,2,2,2,2,2,2,2,2,2,2,2,2,2,2,2,2,2,2,2,2,2,2,2,2,2,2,2,2,2,2,2,2,2,2,2,
2,2,2,2,2,2,2,2,2,2,2,2,2,2,2,2,2,2,2,2,4),(-0.98392338245625,-0.970918750570274,
-0.967664039126509,-0.965794214877276,-0.964163091574368,-0.96214221590316,
-0.959020315499482,-0.936334225555645,-0.918946970736374,-0.912788245005535,
-0.908866491933244,-0.907453480822628,-0.906500212350217,-0.905641593853108,
-0.904458000835556,-0.901447624246592,-0.883296323715773,-0.867241660699311,
-0.853509265326825,-0.850376134030576,-0.848532635420459,-0.846898178277098,
-0.844838229386295,-0.840661813294719,-0.810527176040019,-0.807808209204365,
-0.794190764617428,-0.791286786422429,-0.790031127090533,-0.78910621761936,
-0.788074607086689,-0.786303533793514,-0.779698445446821,-0.77309351987115,
-0.754039015969418,-0.742463178524203,-0.735286453883284,-0.732664830466287,
-0.731105251187416,-0.729453828775095,-0.727260871287469,-0.722369737277023,
-0.715692211867115,-0.682455098181662,-0.675250834469183,-0.673449353171648,
-0.672400578454938,-0.671572180997403,-0.6704014391641,-0.667961477888814,
-0.664690357240238,-0.656332468101261,-0.63138609296106,-0.619095480185138,
-0.615943131111451,-0.614095225128673,-0.612624482837142,-0.610648422290045,
-0.606891812071816,-0.602139266854766,-0.591113263942786,-0.567929528437556,
-0.558309446846038,-0.556354594489674,-0.555270966905107,-0.554355330924907,
-0.553184117199866,-0.550741768405048,-0.547466526286373,-0.539092711311397,
-0.514062657832062,-0.501866994545461,-0.498720820905074,-0.496874240061176,
-0.495403300203329,-0.49342535611242,-0.489659664291114,-0.484892526088455,
-0.473815358624704,-0.448218747985731,-0.440836754737095,-0.439021268654963,
-0.437969247007175,-0.437141381312766,-0.435975421877467,-0.433560309165682,
-0.43033218654854,-0.422140429973167,-0.398022286911143,-0.384773859320031,
-0.381594253175902,-0.379722172598729,-0.378090769949651,-0.376071730868114,
-0.372103801650872,-0.34650241058291,-0.325457552277464,-0.322505295114932,
-0.321331188708105,-0.320474780316983,-0.319518278195589,-0.318090716740568,
-0.314064244250429,-0.307677074877968,-0.293559909055934,-0.269885403914129,
-0.265230968057928,-0.263103425792196,-0.261455922618325,-0.259666962080203,
-0.256785697064329,-0.246469729589058,-0.242037410218006),.UNSPECIFIED.);
#127=B_SPLINE_CURVE_WITH_KNOTS('',3,(#12924,#12925,#12926,#12927,#12928,
#12929,#12930,#12931,#12932,#12933,#12934,#12935,#12936,#12937,#12938,#12939,
#12940,#12941,#12942,#12943,#12944,#12945,#12946,#12947,#12948,#12949,#12950,
#12951,#12952,#12953,#12954,#12955,#12956,#12957,#12958,#12959,#12960,#12961,
#12962,#12963,#12964,#12965,#12966,#12967,#12968,#12969,#12970,#12971,#12972,
#12973,#12974,#12975,#12976,#12977,#12978,#12979,#12980,#12981,#12982,#12983,
#12984,#12985,#12986,#12987,#12988,#12989,#12990,#12991,#12992,#12993,#12994,
#12995,#12996,#12997,#12998,#12999,#13000,#13001,#13002,#13003,#13004,#13005,
#13006,#13007,#13008,#13009,#13010,#13011,#13012,#13013,#13014,#13015,#13016,
#13017,#13018,#13019,#13020,#13021,#13022,#13023,#13024,#13025,#13026,#13027,
#13028,#13029,#13030,#13031,#13032,#13033,#13034,#13035,#13036,#13037,#13038,
#13039,#13040,#13041,#13042,#13043,#13044,#13045,#13046,#13047,#13048,#13049,
#13050,#13051,#13052,#13053,#13054,#13055,#13056,#13057,#13058,#13059,#13060,
#13061,#13062,#13063,#13064,#13065,#13066,#13067,#13068,#13069,#13070,#13071,
#13072,#13073,#13074,#13075,#13076,#13077,#13078,#13079,#13080,#13081,#13082,
#13083,#13084,#13085,#13086,#13087,#13088,#13089,#13090,#13091,#13092,#13093,
#13094,#13095,#13096,#13097,#13098,#13099,#13100,#13101,#13102,#13103,#13104,
#13105,#13106,#13107,#13108,#13109,#13110,#13111,#13112,#13113,#13114,#13115,
#13116,#13117,#13118,#13119,#13120,#13121,#13122,#13123,#13124,#13125,#13126,
#13127,#13128,#13129,#13130,#13131),.UNSPECIFIED.,.F.,.F.,(4,2,2,2,2,2,
2,2,2,2,2,2,2,2,2,2,2,2,2,2,2,2,2,2,2,2,2,2,2,2,2,2,2,2,2,2,2,2,2,2,2,2,
2,2,2,2,2,2,2,2,2,2,2,2,2,2,2,2,2,2,2,2,2,2,2,2,2,2,2,2,2,2,2,2,2,2,2,2,
2,2,2,2,2,2,2,2,2,2,2,2,2,2,2,2,2,2,2,2,2,2,2,2,2,4),(-1.24292430977669,
-1.22009850972989,-1.21117710213601,-1.20776282107661,-1.20524074898063,
-1.2040540418608,-1.20313692546008,-1.20206393200115,-1.20015717115628,
-1.19142022094294,-1.15971845873916,-1.15315464924074,-1.14832643144998,
-1.14614415127837,-1.14449380396601,-1.14271239640236,-1.13986663518086,
-1.13091402299806,-1.09717191663782,-1.08926948880272,-1.08747306209823,
-1.08643552429681,-1.08551158324381,-1.08428737171035,-1.0814893181499,
-1.05681554278257,-1.03442687168121,-1.03052803654771,-1.02852250440633,
-1.02689148096121,-1.02500813191233,-1.02178059200139,-1.0077440924415,
-0.984206081141666,-0.972353882315983,-0.97036242914734,-0.969282656895497,
-0.968366229833341,-0.967188777629931,-0.965275467936706,-0.951334726570139,
-0.934728329995926,-0.917880693945739,-0.91354506953747,-0.911453584049901,
-0.909814915394111,-0.907988292250247,-0.904936104965671,-0.893981686742702,
-0.867781741071759,-0.859210709444466,-0.85426725340917,-0.85272670799984,
-0.851745599744519,-0.850806907834202,-0.849643893636765,-0.846758324974834,
-0.8242946418618,-0.800006927103579,-0.796051507034116,-0.794034483656647,
-0.792402609987792,-0.790527671492334,-0.787337555593231,-0.773936388515977,
-0.751720296040212,-0.742327945440058,-0.737167921714137,-0.735545207780734,
-0.734545984105842,-0.733607309992557,-0.732271387261892,-0.728880933198242,
-0.723835784409313,-0.706744720142412,-0.683863525512931,-0.679195931896086,
-0.677065537869152,-0.675417112106932,-0.673628429504836,-0.670750439014821,
-0.660478934899834,-0.640551609385216,-0.622258878077178,-0.619249388201306,
-0.618065446390248,-0.617206340419922,-0.616252229611334,-0.614837453166633,
-0.610907346566536,-0.60473279506166,-0.587363628894845,-0.564684751763273,
-0.561561087344327,-0.559538893347397,-0.557906599438009,-0.556035312403824,
-0.552777737550461,-0.536734606063427,-0.522306323992666,-0.513818536135711,
-0.503395615840758,-0.501572057791962,-0.500743339736994),.UNSPECIFIED.);
#128=B_SPLINE_CURVE_WITH_KNOTS('',3,(#13133,#13134,#13135,#13136,#13137,
#13138,#13139,#13140,#13141,#13142,#13143,#13144,#13145,#13146,#13147,#13148,
#13149,#13150,#13151,#13152,#13153,#13154,#13155,#13156,#13157,#13158,#13159,
#13160,#13161,#13162,#13163,#13164,#13165,#13166,#13167,#13168,#13169,#13170,
#13171,#13172,#13173,#13174,#13175,#13176,#13177,#13178,#13179,#13180,#13181,
#13182,#13183,#13184,#13185,#13186,#13187,#13188,#13189,#13190,#13191,#13192,
#13193,#13194,#13195,#13196,#13197,#13198,#13199,#13200,#13201,#13202,#13203,
#13204,#13205,#13206,#13207,#13208,#13209,#13210,#13211,#13212,#13213,#13214,
#13215,#13216,#13217,#13218,#13219,#13220,#13221,#13222,#13223,#13224,#13225,
#13226,#13227,#13228,#13229,#13230,#13231,#13232,#13233,#13234,#13235,#13236,
#13237,#13238,#13239,#13240,#13241,#13242,#13243,#13244,#13245,#13246,#13247,
#13248,#13249,#13250),.UNSPECIFIED.,.F.,.F.,(4,2,2,2,2,2,2,2,2,2,2,2,2,
2,2,2,2,2,2,2,2,2,2,2,2,2,2,2,2,2,2,2,2,2,2,2,2,2,2,2,2,2,2,2,2,2,2,2,2,
2,2,2,2,2,2,2,2,2,4),(-0.242037410218006,-0.226377901503412,-0.208326430520444,
-0.205307938065085,-0.204122761128431,-0.203263550654683,-0.202310285714343,
-0.200898413453342,-0.196987019685073,-0.1908524427467,-0.173446015566506,
-0.15075166387754,-0.147628322635545,-0.145606627344241,-0.143974928387371,
-0.143947604441549,-0.143910219998259,-0.143875060873207,-0.14384198161352,
-0.143810847108984,-0.143781531857172,-0.143753919264978,-0.143727900992463,
-0.143703376333799,-0.143680251642651,-0.143658439798503,-0.143637859708992,
-0.143618435852104,-0.143600097857734,-0.143582780115167,-0.143566421414623,
-0.143550964619338,-0.143536356363321,-0.143522546769911,-0.143509489196654,
-0.143497140002465,-0.143485458325707,-0.143474405892461,-0.141501492676609,
-0.137462678591979,-0.132191756499697,-0.119265489938714,-0.0956030438442445,
-0.0890174849576289,-0.0872477763152912,-0.0862162683394732,-0.0852909391395101,
-0.0840340317944949,-0.0812441417872272,-0.0615593745656791,-0.0478414017756538,
-0.0332210227450641,-0.0299624167846491,-0.028072259689996,-0.0264420824065228,
-0.0248792806951741,-0.0229262642438582,-0.0199490446044993,-0.000340462828452178),
 .UNSPECIFIED.);
#129=B_SPLINE_CURVE_WITH_KNOTS('',3,(#13251,#13252,#13253,#13254,#13255,
#13256,#13257,#13258,#13259,#13260,#13261,#13262,#13263,#13264,#13265,#13266,
#13267,#13268,#13269,#13270,#13271,#13272,#13273,#13274,#13275,#13276,#13277,
#13278,#13279,#13280,#13281,#13282,#13283,#13284,#13285,#13286,#13287,#13288,
#13289,#13290,#13291,#13292,#13293,#13294,#13295,#13296,#13297,#13298,#13299,
#13300,#13301,#13302,#13303,#13304,#13305,#13306,#13307,#13308,#13309,#13310,
#13311,#13312,#13313,#13314,#13315,#13316,#13317,#13318,#13319,#13320,#13321,
#13322,#13323,#13324,#13325,#13326,#13327,#13328,#13329,#13330,#13331,#13332,
#13333,#13334,#13335,#13336,#13337,#13338,#13339,#13340,#13341,#13342,#13343,
#13344,#13345,#13346,#13347,#13348,#13349,#13350,#13351,#13352,#13353,#13354,
#13355,#13356,#13357,#13358,#13359,#13360,#13361,#13362,#13363,#13364,#13365,
#13366,#13367,#13368,#13369,#13370,#13371,#13372,#13373,#13374,#13375,#13376,
#13377,#13378,#13379,#13380,#13381,#13382,#13383,#13384,#13385,#13386,#13387,
#13388,#13389,#13390,#13391,#13392,#13393,#13394,#13395,#13396),
 .UNSPECIFIED.,.F.,.F.,(4,2,2,2,2,2,2,2,2,2,2,2,2,2,2,2,2,2,2,2,2,2,2,2,
2,2,2,2,2,2,2,2,2,2,2,2,2,2,2,2,2,2,2,2,2,2,2,2,2,2,2,2,2,2,2,2,2,2,2,2,
2,2,2,2,2,2,2,2,2,2,2,2,4),(-1.48433926685641,-1.45975807135474,-1.45670672976863,
-1.45507153755693,-1.45365737853428,-1.45270382492361,-1.45184533297032,
-1.4506624006039,-1.44765631229039,-1.42927933722712,-1.41475180710344,
-1.40052827236496,-1.3970514075773,-1.39544137590594,-1.39379363977833,
-1.39200704275363,-1.38913537389381,-1.37992472697872,-1.34648009397227,
-1.33860887100355,-1.33681039869128,-1.33577266208209,-1.33484924480734,
-1.33362665282004,-1.33083620409697,-1.30610364428062,-1.29057021029139,
-1.28466143703557,-1.28020851699269,-1.27809532681376,-1.27645469125338,
-1.2746411966735,-1.27164698147662,-1.26126888175128,-1.23116827023616,
-1.22470255631403,-1.22064108319677,-1.21920881525891,-1.21825133469458,
-1.21739572865764,-1.21622483926031,-1.21329158030501,-1.19177799241002,
-1.17417302845576,-1.16781332727807,-1.16310069872849,-1.16093942081488,
-1.15929231039467,-1.15750208988553,-1.15461504691953,-1.14526280523583,
-1.11403604048543,-1.10749568649636,-1.1034006612034,-1.10196383082756,
-1.10100532662837,-1.10015036944996,-1.09898232382121,-1.09603437509939,
-1.0746727870226,-1.05695908921771,-1.05057676492827,-1.04585116641477,
-1.0436874056261,-1.0420398091453,-1.04025043254736,-1.0373677988348,-1.02805920854845,
-1.00307411900119,-0.987384761064561,-0.985292473269602,-0.984191532099586,
-0.984010680622453),.UNSPECIFIED.);
#130=B_SPLINE_CURVE_WITH_KNOTS('',3,(#13402,#13403,#13404,#13405,#13406,
#13407,#13408,#13409,#13410,#13411,#13412,#13413,#13414,#13415,#13416,#13417,
#13418,#13419,#13420,#13421,#13422,#13423,#13424,#13425,#13426,#13427,#13428,
#13429,#13430,#13431,#13432,#13433,#13434,#13435,#13436,#13437,#13438,#13439,
#13440,#13441,#13442,#13443,#13444,#13445,#13446,#13447,#13448,#13449,#13450,
#13451,#13452,#13453,#13454,#13455,#13456,#13457,#13458,#13459,#13460,#13461,
#13462,#13463,#13464,#13465,#13466,#13467,#13468,#13469,#13470,#13471,#13472,
#13473,#13474,#13475,#13476,#13477,#13478,#13479,#13480,#13481,#13482,#13483,
#13484,#13485,#13486,#13487,#13488,#13489,#13490,#13491,#13492,#13493,#13494,
#13495,#13496,#13497,#13498,#13499,#13500,#13501,#13502,#13503,#13504,#13505,
#13506,#13507,#13508,#13509,#13510,#13511,#13512,#13513,#13514,#13515,#13516,
#13517,#13518,#13519,#13520,#13521,#13522,#13523,#13524,#13525,#13526,#13527,
#13528,#13529,#13530,#13531,#13532,#13533,#13534,#13535,#13536,#13537,#13538,
#13539,#13540,#13541,#13542,#13543,#13544,#13545,#13546,#13547,#13548,#13549,
#13550,#13551,#13552,#13553,#13554,#13555,#13556,#13557,#13558,#13559,#13560,
#13561),.UNSPECIFIED.,.F.,.F.,(4,2,2,2,2,2,2,2,2,2,2,2,2,2,2,2,2,2,2,2,
2,2,2,2,2,2,2,2,2,2,2,2,2,2,2,2,2,2,2,2,2,2,2,2,2,2,2,2,2,2,2,2,2,2,2,2,
2,2,2,2,2,2,2,2,2,2,2,2,2,2,2,2,2,2,2,2,2,2,2,4),(-0.500877068977447,-0.49420957397851,
-0.486243983230943,-0.483515943791592,-0.481759892900288,-0.480098968662855,
-0.477850391714746,-0.472642111419001,-0.465389743434716,-0.445822728983988,
-0.445056384759463,-0.437175356889427,-0.432966972603491,-0.425977449462116,
-0.424172203267863,-0.423132765937003,-0.422209386113219,-0.420967385311406,
-0.418143546064314,-0.405304815542059,-0.397169964439075,-0.372258221694176,
-0.368099080270406,-0.36601003283837,-0.364474158175748,-0.362806451946846,
-0.360518058034401,-0.355071007657741,-0.337852482692718,-0.317949735414949,
-0.308983947659993,-0.307063941704096,-0.305987938915715,-0.305071151693919,
-0.303888634881919,-0.301388685124148,-0.298013510633306,-0.289248655473679,
-0.26093496766503,-0.252001180990559,-0.249157279351985,-0.247376193767869,
-0.245725571351519,-0.243542077473293,-0.238707630352702,-0.232132103012891,
-0.200301395977919,-0.191673048791492,-0.18977333179338,-0.188701865905234,
-0.187784435283943,-0.186595228402586,-0.184060370545395,-0.163146355380599,
-0.137714066662209,-0.133563567964447,-0.131476569575409,-0.129941135191168,
-0.128306076750681,-0.126087476837623,-0.12360049236534,-0.119307513195447,
-0.109836791920459,-0.0941729325307969,-0.0762350431130515,-0.0732083045110218,
-0.072021527449423,-0.0711617440546169,-0.0702085423299039,-0.0687979376692082,
-0.0648975489169137,-0.0587874788908426,-0.0283441025441875,-0.0179681887086096,
-0.0148622485381598,-0.0130240025463066,-0.0114216011731331,-0.00984350975623947,
-0.00783814363815093,-0.000340318648320376),.UNSPECIFIED.);
#131=B_SPLINE_CURVE_WITH_KNOTS('',3,(#13562,#13563,#13564,#13565,#13566,
#13567,#13568,#13569,#13570,#13571,#13572,#13573,#13574,#13575,#13576,#13577,
#13578,#13579,#13580,#13581,#13582,#13583,#13584,#13585,#13586,#13587,#13588,
#13589,#13590,#13591,#13592,#13593,#13594,#13595,#13596,#13597,#13598,#13599,
#13600,#13601,#13602,#13603,#13604,#13605,#13606,#13607,#13608,#13609,#13610,
#13611,#13612,#13613,#13614,#13615,#13616,#13617,#13618,#13619,#13620,#13621,
#13622,#13623,#13624,#13625,#13626,#13627,#13628,#13629,#13630,#13631,#13632,
#13633,#13634,#13635),.UNSPECIFIED.,.F.,.F.,(4,2,2,2,2,2,2,2,2,2,2,2,2,
2,2,2,2,2,2,2,2,2,2,2,2,2,2,2,2,2,2,2,2,2,2,2,4),(-1.48451647550027,-1.453138561461,
-1.44142514844035,-1.43943890349013,-1.43836032782819,-1.43744390944019,
-1.43626517033315,-1.43434725721046,-1.4201148900124,-1.39668872794447,
-1.38876710752721,-1.38496742502763,-1.38267773562576,-1.38062685302709,
-1.38061075126092,-1.37903116612738,-1.3774642065727,-1.37480629934549,
-1.36737046093308,-1.33758067704553,-1.32851982802648,-1.32507088549672,
-1.32252908068291,-1.32133862648736,-1.32042943146041,-1.31936236402633,
-1.31748178086799,-1.30916291412439,-1.27705216305228,-1.27045655340445,
-1.26561044795672,-1.26342496301681,-1.26177412635694,-1.26021137240343,
-1.25757536252991,-1.25029959662761,-1.24292430977669),.UNSPECIFIED.);
#132=B_SPLINE_CURVE_WITH_KNOTS('',3,(#13636,#13637,#13638,#13639,#13640,
#13641,#13642,#13643,#13644,#13645,#13646,#13647,#13648,#13649,#13650,#13651,
#13652,#13653,#13654,#13655,#13656,#13657,#13658,#13659,#13660,#13661,#13662,
#13663,#13664,#13665,#13666,#13667,#13668,#13669,#13670,#13671,#13672,#13673,
#13674,#13675,#13676,#13677,#13678,#13679,#13680,#13681,#13682,#13683,#13684,
#13685,#13686,#13687,#13688,#13689,#13690,#13691,#13692,#13693,#13694,#13695,
#13696,#13697,#13698,#13699,#13700,#13701,#13702,#13703,#13704,#13705,#13706,
#13707,#13708,#13709,#13710,#13711,#13712,#13713,#13714,#13715,#13716,#13717,
#13718,#13719,#13720,#13721,#13722,#13723,#13724,#13725,#13726,#13727,#13728,
#13729,#13730,#13731,#13732,#13733,#13734,#13735,#13736,#13737,#13738,#13739,
#13740,#13741,#13742,#13743,#13744,#13745,#13746,#13747,#13748,#13749,#13750,
#13751,#13752,#13753,#13754,#13755,#13756,#13757,#13758,#13759,#13760,#13761,
#13762,#13763,#13764,#13765,#13766,#13767,#13768,#13769,#13770,#13771,#13772,
#13773,#13774,#13775,#13776,#13777,#13778,#13779,#13780,#13781,#13782,#13783,
#13784,#13785,#13786,#13787,#13788,#13789,#13790,#13791,#13792,#13793,#13794,
#13795,#13796,#13797,#13798,#13799,#13800,#13801,#13802,#13803,#13804,#13805,
#13806,#13807,#13808,#13809,#13810,#13811,#13812,#13813,#13814,#13815,#13816,
#13817,#13818,#13819,#13820,#13821,#13822,#13823,#13824,#13825,#13826,#13827,
#13828,#13829,#13830,#13831,#13832,#13833,#13834,#13835,#13836,#13837,#13838,
#13839,#13840,#13841,#13842,#13843,#13844,#13845,#13846,#13847,#13848,#13849,
#13850,#13851),.UNSPECIFIED.,.F.,.F.,(4,2,2,2,2,2,2,2,2,2,2,2,2,2,2,2,2,
2,2,2,2,2,2,2,2,2,2,2,2,2,2,2,2,2,2,2,2,2,2,2,2,2,2,2,2,2,2,2,2,2,2,2,2,
2,2,2,2,2,2,2,2,2,2,2,2,2,2,2,2,2,2,2,2,2,2,2,2,2,2,2,2,2,2,2,2,2,2,2,2,
2,2,2,2,2,2,2,2,2,2,2,2,2,2,2,2,2,2,4),(-0.984010680622453,-0.983276881955298,
-0.98212659632752,-0.980303666564888,-0.969886693743268,-0.961402172228227,
-0.946981067485029,-0.930950585751214,-0.927694244051038,-0.925823482036929,
-0.924191539989635,-0.922169649038764,-0.919046178479495,-0.896342672471697,
-0.878934906128747,-0.872784213011067,-0.868865597600561,-0.867452581316968,
-0.866498979134825,-0.865639801050707,-0.864455107846331,-0.861440165151471,
-0.843450643038574,-0.823322317990033,-0.812995416730585,-0.81011287859804,
-0.808323434641292,-0.806675689397829,-0.804548118311377,-0.799894835432268,
-0.776072670555639,-0.759683939702214,-0.754751414846854,-0.751417727830103,
-0.750090805574481,-0.749153899838092,-0.748275538754942,-0.746761208071483,
-0.742447345986866,-0.735219838592179,-0.719046110596642,-0.696853774651113,
-0.693716936107176,-0.691690971994999,-0.69005871989835,-0.68819085991827,
-0.684948001728182,-0.669207638321255,-0.645926681006725,-0.635526783116616,
-0.633704347473537,-0.632554181943724,-0.631639486098049,-0.630538314945968,
-0.628445124865518,-0.612701757282371,-0.587572878431817,-0.578447092961069,
-0.575583576041244,-0.573798270086154,-0.57214917910804,-0.569975750365758,
-0.565197208489379,-0.558720846342382,-0.540544821907918,-0.519829276205067,
-0.516862262662472,-0.515685537304518,-0.514828359157599,-0.513872383554146,
-0.512447989490181,-0.508446273233196,-0.502114318679527,-0.488240719495897,
-0.464212075387212,-0.459565066219429,-0.457438606845076,-0.455790995236776,
-0.454000969898426,-0.451115886450697,-0.440761496956498,-0.420533786818844,
-0.402644244852704,-0.399631416357241,-0.398447039642171,-0.397587920762662,
-0.396634168456819,-0.395220571811708,-0.391297949679015,-0.385139407257685,
-0.367753587181906,-0.34506576033978,-0.341942447075718,-0.339920544984728,
-0.338288533086466,-0.336417623938391,-0.333160860478709,-0.317127154123628,
-0.302692305813452,-0.294198583014737,-0.283777838649214,-0.281954576760602,
-0.280804167948434,-0.279889470685409,-0.278788528715068,-0.276696403545102,
-0.261010637430623,-0.241930398828716),.UNSPECIFIED.);
#133=B_SPLINE_CURVE_WITH_KNOTS('',3,(#13856,#13857,#13858,#13859,#13860,
#13861,#13862,#13863,#13864,#13865,#13866,#13867,#13868,#13869,#13870,#13871,
#13872,#13873,#13874,#13875,#13876,#13877,#13878,#13879,#13880,#13881,#13882,
#13883,#13884,#13885,#13886,#13887,#13888,#13889,#13890,#13891,#13892,#13893,
#13894,#13895,#13896,#13897,#13898,#13899,#13900,#13901,#13902,#13903,#13904,
#13905,#13906,#13907,#13908,#13909,#13910,#13911,#13912,#13913,#13914,#13915,
#13916,#13917,#13918,#13919,#13920,#13921,#13922,#13923,#13924,#13925,#13926,
#13927,#13928,#13929,#13930,#13931,#13932,#13933,#13934,#13935,#13936,#13937,
#13938,#13939,#13940,#13941,#13942,#13943,#13944,#13945,#13946,#13947,#13948,
#13949,#13950,#13951,#13952,#13953,#13954,#13955,#13956,#13957,#13958,#13959,
#13960,#13961,#13962,#13963,#13964,#13965,#13966,#13967,#13968,#13969,#13970,
#13971,#13972,#13973,#13974,#13975,#13976,#13977,#13978,#13979,#13980,#13981,
#13982,#13983,#13984,#13985,#13986,#13987,#13988,#13989,#13990,#13991,#13992,
#13993,#13994,#13995,#13996,#13997,#13998,#13999,#14000,#14001,#14002,#14003,
#14004,#14005,#14006,#14007,#14008,#14009,#14010,#14011,#14012,#14013,#14014,
#14015,#14016,#14017,#14018,#14019,#14020,#14021,#14022,#14023,#14024,#14025,
#14026,#14027,#14028,#14029,#14030,#14031,#14032,#14033,#14034,#14035,#14036,
#14037,#14038,#14039,#14040,#14041,#14042,#14043,#14044,#14045,#14046,#14047,
#14048,#14049,#14050,#14051,#14052,#14053,#14054,#14055,#14056,#14057,#14058,
#14059,#14060,#14061,#14062,#14063,#14064,#14065,#14066,#14067),
 .UNSPECIFIED.,.F.,.F.,(4,2,2,2,2,2,2,2,2,2,2,2,2,2,2,2,2,2,2,2,2,2,2,2,
2,2,2,2,2,2,2,2,2,2,2,2,2,2,2,2,2,2,2,2,2,2,2,2,2,2,2,2,2,2,2,2,2,2,2,2,
2,2,2,2,2,2,2,2,2,2,2,2,2,2,2,2,2,2,2,2,2,2,2,2,2,2,2,2,2,2,2,2,2,2,2,2,
2,2,2,2,2,2,2,2,2,4),(-1.24297181640774,-1.2427106352234,-1.2415244771508,
-1.23850109403567,-1.22054474535128,-1.20040417535915,-1.1900740137517,
-1.18719106031416,-1.18540143704267,-1.18375357546074,-1.18162591808405,
-1.17697268172044,-1.15315637795744,-1.14408068768981,-1.13113284813656,
-1.12829756047345,-1.12705353058867,-1.12612987531147,-1.12509148830716,
-1.12329106563629,-1.11635802555883,-1.10980684384822,-1.09226154632467,
-1.07535506155645,-1.07101218902478,-1.06891940979068,-1.06728069583163,
-1.06545502123208,-1.06240680401277,-1.05149331833715,-1.02525592379709,
-1.01668006947385,-1.01173484399188,-1.0101941708909,-1.00921308038126,
-1.00827449133722,-1.00711169498954,-1.00422711830385,-0.981756014399181,
-0.957477768123092,-0.953522707170614,-0.951505842933359,-0.949874086479932,
-0.947999269939254,-0.944809330520898,-0.931408303200817,-0.907395638602045,
-0.899223365514287,-0.896000089831674,-0.893587790363841,-0.892422135123552,
-0.891594066904416,-0.890541183317346,-0.888722921040427,-0.881309130587991,
-0.848294933610726,-0.838251876852001,-0.835395055617807,-0.833611179030274,
-0.831961552434656,-0.829821647757212,-0.82527563189193,-0.800020162397814,
-0.778892589866612,-0.776365809691835,-0.775178192494866,-0.774269262852029,
-0.773200253801601,-0.771311144490131,-0.762861625060097,-0.742599558811807,
-0.722150171937683,-0.719018622593057,-0.716994197198423,-0.715361964365038,
-0.713492787235848,-0.710244168417585,-0.694384701094228,-0.669967392019978,
-0.66072745533532,-0.658792200929812,-0.657712742348565,-0.656796310860641,
-0.655618504355478,-0.653143268783829,-0.649811239174844,-0.641217009952121,
-0.61482244656907,-0.604103548895954,-0.601063861025787,-0.599240044975084,
-0.597600950728689,-0.595504854819668,-0.591144625132405,-0.574098100995862,
-0.555399460614224,-0.549740400851259,-0.54315007293908,-0.541379696464929,
-0.54034790464077,-0.539422391453723,-0.538165316578795,-0.53525542811576,
-0.521588208206566,-0.520367955699403,-0.500877068977447),.UNSPECIFIED.);
#134=B_SPLINE_CURVE_WITH_KNOTS('',3,(#14069,#14070,#14071,#14072,#14073,
#14074,#14075,#14076,#14077,#14078,#14079,#14080,#14081,#14082,#14083,#14084,
#14085,#14086,#14087,#14088,#14089,#14090,#14091,#14092,#14093,#14094,#14095,
#14096,#14097,#14098,#14099,#14100,#14101,#14102,#14103,#14104,#14105,#14106,
#14107,#14108,#14109,#14110,#14111,#14112,#14113,#14114,#14115,#14116,#14117,
#14118,#14119,#14120,#14121,#14122,#14123,#14124,#14125,#14126,#14127,#14128,
#14129,#14130,#14131,#14132,#14133,#14134,#14135,#14136,#14137,#14138,#14139,
#14140,#14141,#14142,#14143,#14144,#14145,#14146,#14147,#14148,#14149,#14150,
#14151,#14152,#14153,#14154),.UNSPECIFIED.,.F.,.F.,(4,2,2,2,2,2,2,2,2,2,
2,2,2,2,2,2,2,2,2,2,2,2,2,2,2,2,2,2,2,2,2,2,2,2,2,2,2,2,2,2,2,2,4),(-0.241930398828716,
-0.236030777710632,-0.226733379673806,-0.223851838207649,-0.222062618520919,
-0.220414816114051,-0.218250273248799,-0.213520901960721,-0.207131320051679,
-0.189383957186124,-0.168039975130289,-0.165100303953539,-0.163928190563805,
-0.163072169454812,-0.162114799096677,-0.16068369811014,-0.156632185875177,
-0.150189965938108,-0.120410251049439,-0.109746059779745,-0.10672139934979,
-0.104900996526418,-0.103332497948253,-0.103306634631637,-0.103283079484542,
-0.103261571819152,-0.103241888231602,-0.103223836103087,-0.103207248426598,
-0.101152458394976,-0.0988694582598129,-0.0950861695135606,-0.0872136052399747,
-0.0732081983171117,-0.0506943593190284,-0.0478117360807718,-0.0466493677125125,
-0.0457109884765509,-0.0447299449399655,-0.043189075351825,-0.0382407101216464,
-0.0296575430855296,-0.000340887607588386),.UNSPECIFIED.);
#135=B_SPLINE_CURVE_WITH_KNOTS('',3,(#14155,#14156,#14157,#14158,#14159,
#14160,#14161,#14162,#14163,#14164,#14165,#14166,#14167,#14168,#14169,#14170,
#14171,#14172,#14173,#14174,#14175,#14176,#14177,#14178,#14179,#14180,#14181,
#14182,#14183,#14184,#14185,#14186,#14187,#14188,#14189,#14190,#14191,#14192,
#14193,#14194,#14195,#14196,#14197,#14198,#14199,#14200,#14201,#14202,#14203,
#14204,#14205,#14206,#14207,#14208,#14209,#14210,#14211,#14212,#14213,#14214,
#14215,#14216,#14217,#14218,#14219,#14220,#14221,#14222,#14223,#14224,#14225,
#14226,#14227,#14228,#14229,#14230,#14231,#14232,#14233,#14234,#14235,#14236,
#14237,#14238,#14239,#14240,#14241,#14242,#14243,#14244,#14245,#14246,#14247,
#14248,#14249,#14250,#14251,#14252,#14253,#14254,#14255,#14256,#14257,#14258,
#14259,#14260,#14261,#14262,#14263,#14264,#14265,#14266,#14267,#14268,#14269,
#14270,#14271,#14272,#14273,#14274,#14275,#14276,#14277,#14278,#14279,#14280,
#14281,#14282,#14283,#14284,#14285,#14286,#14287,#14288,#14289,#14290,#14291,
#14292,#14293,#14294,#14295,#14296,#14297,#14298,#14299,#14300,#14301,#14302,
#14303,#14304,#14305,#14306,#14307,#14308,#14309,#14310,#14311,#14312,#14313,
#14314,#14315,#14316,#14317,#14318,#14319,#14320,#14321,#14322),
 .UNSPECIFIED.,.F.,.F.,(4,2,2,2,2,2,2,2,2,2,2,2,2,2,2,2,2,2,2,2,2,2,2,2,
2,2,2,2,2,2,2,2,2,2,2,2,2,2,2,2,2,2,2,2,2,2,2,2,2,2,2,2,2,2,2,2,2,2,2,2,
2,2,2,2,2,2,2,2,2,2,2,2,2,2,2,2,2,2,2,2,2,2,2,4),(-1.48407147707552,-1.4790909783933,
-1.47552715703634,-1.47352482305757,-1.47194833101917,-1.47034635659878,
-1.4685079991126,-1.46539794028517,-1.45400345281321,-1.43736318535139,
-1.42229969830208,-1.41759374585316,-1.41437540724622,-1.41306733397175,
-1.41213419424307,-1.41125138989792,-1.40971269039337,-1.4052154374298,
-1.38197576830077,-1.36708654208165,-1.36132868007556,-1.35828361202568,
-1.35630302639214,-1.35444807712028,-1.35441075395009,-1.35438404447419,
-1.35434839771111,-1.35430089420225,-1.35423771987009,-1.35260070759151,
-1.35051423600606,-1.34619971912901,-1.31722927351408,-1.30438688378277,
-1.3000976789732,-1.29709594987043,-1.29582364817088,-1.29489635488629,
-1.29387289591846,-1.29213837136344,-1.28592357030251,-1.26044102864552,
-1.24400063263759,-1.23971836295991,-1.23763807212472,-1.23600171912073,
-1.23417097500079,-1.23109577963338,-1.2198137612674,-1.19068249310705,
-1.18428749829588,-1.1802582803677,-1.17883066470394,-1.17787439638152,
-1.17701840178138,-1.17584513137495,-1.17289633343534,-1.15183681683752,
-1.13393219598776,-1.12751223259252,-1.12276578595968,-1.12059886078464,
-1.11895143336478,-1.11716474983886,-1.11429201068576,-1.10506891768792,
-1.07371463983628,-1.06716795273734,-1.06307052272857,-1.06163369569907,
-1.0606754293168,-1.05982086589987,-1.05865358525953,-1.05570893263915,
-1.03427270514195,-1.01662276563985,-1.01025452117868,-1.00553732112314,
-1.00337555510661,-1.00172872608649,-0.999939449474906,-0.997055347208688,
-0.987726305082495,-0.983796640571424),.UNSPECIFIED.);
#136=B_SPLINE_CURVE_WITH_KNOTS('',3,(#14328,#14329,#14330,#14331,#14332,
#14333,#14334,#14335,#14336,#14337,#14338,#14339,#14340,#14341,#14342,#14343,
#14344,#14345,#14346,#14347,#14348,#14349,#14350,#14351,#14352,#14353,#14354,
#14355,#14356,#14357,#14358,#14359,#14360,#14361,#14362,#14363,#14364,#14365,
#14366,#14367,#14368,#14369,#14370,#14371,#14372,#14373,#14374,#14375,#14376,
#14377,#14378,#14379,#14380,#14381,#14382,#14383,#14384,#14385,#14386,#14387,
#14388,#14389,#14390,#14391,#14392,#14393,#14394,#14395,#14396,#14397,#14398,
#14399,#14400,#14401,#14402,#14403,#14404,#14405,#14406,#14407,#14408,#14409,
#14410,#14411,#14412,#14413,#14414,#14415,#14416,#14417,#14418,#14419,#14420,
#14421,#14422,#14423,#14424,#14425,#14426,#14427,#14428,#14429,#14430,#14431,
#14432,#14433,#14434,#14435,#14436,#14437,#14438,#14439,#14440,#14441,#14442,
#14443,#14444,#14445,#14446,#14447,#14448,#14449,#14450,#14451,#14452,#14453,
#14454,#14455,#14456,#14457,#14458,#14459,#14460,#14461,#14462,#14463,#14464,
#14465,#14466,#14467,#14468,#14469),.UNSPECIFIED.,.F.,.F.,(4,2,2,2,2,2,
2,2,2,2,2,2,2,2,2,2,2,2,2,2,2,2,2,2,2,2,2,2,2,2,2,2,2,2,2,2,2,2,2,2,2,2,
2,2,2,2,2,2,2,2,2,2,2,2,2,2,2,2,2,2,2,2,2,2,2,2,2,2,2,2,4),(-0.500788288135055,
-0.496909354727288,-0.478680433900642,-0.466447740647992,-0.464559682535318,
-0.463389837901927,-0.462474075256743,-0.461388860785006,-0.459371407150183,
-0.446733164115451,-0.420481786771817,-0.409606337946016,-0.406561886638268,
-0.404737161680746,-0.403098476802607,-0.401004598713318,-0.396655266018663,
-0.37969380555784,-0.361595782739146,-0.34922615319291,-0.347332784727044,
-0.346161375301015,-0.345245530777721,-0.344161568575389,-0.342149922601397,
-0.329692324407078,-0.304265428489965,-0.292514625806624,-0.289398183819507,
-0.287557806495867,-0.286085613975019,-0.284097920639864,-0.280285955260957,
-0.275444443779777,-0.264105184209276,-0.239336172959036,-0.231587122966427,
-0.229744667455211,-0.228686337190252,-0.227859286584675,-0.226701936589741,
-0.224331604643313,-0.221180620352351,-0.213283079077864,-0.189854511167829,
-0.175584056578841,-0.172344009085957,-0.170457959602764,-0.168827347211825,
-0.166825814556085,-0.162946053922135,-0.139120171130376,-0.115988816610384,
-0.11314887626941,-0.111993849950166,-0.111057381226991,-0.110097381673065,
-0.108653323487789,-0.106907414114786,-0.103555806048688,-0.0948840478971227,
-0.0677948597840799,-0.0577437969955115,-0.0547791176815606,-0.0529717654812986,
-0.0513290927820337,-0.0492025294706793,-0.0446799493256032,-0.038650987578759,
-0.0225883152000793,-0.000340897761007594),.UNSPECIFIED.);
#137=B_SPLINE_CURVE_WITH_KNOTS('',3,(#14470,#14471,#14472,#14473,#14474,
#14475,#14476,#14477,#14478,#14479,#14480,#14481,#14482,#14483,#14484,#14485,
#14486,#14487,#14488,#14489,#14490,#14491,#14492,#14493,#14494,#14495,#14496,
#14497,#14498,#14499,#14500,#14501,#14502,#14503,#14504,#14505,#14506,#14507,
#14508,#14509,#14510,#14511,#14512,#14513,#14514,#14515,#14516,#14517,#14518,
#14519,#14520,#14521,#14522,#14523,#14524,#14525,#14526,#14527,#14528,#14529,
#14530,#14531,#14532,#14533,#14534,#14535,#14536,#14537,#14538,#14539,#14540,
#14541,#14542,#14543,#14544,#14545,#14546,#14547),.UNSPECIFIED.,.F.,.F.,
(4,2,2,2,2,2,2,2,2,2,2,2,2,2,2,2,2,2,2,2,2,2,2,2,2,2,2,2,2,2,2,2,2,2,2,
2,2,2,4),(-1.48455615980153,-1.48089708969997,-1.47968395763997,-1.4787722523958,
-1.47788529481661,-1.47685546778224,-1.47509360323038,-1.46860266426421,
-1.44904999241366,-1.42643989038457,-1.42250204588403,-1.42048886317402,
-1.41885762515121,-1.41698068554125,-1.41378048487863,-1.40020837790193,
-1.36764652902101,-1.36470621038258,-1.36311232939687,-1.36174386184975,
-1.36080885508367,-1.35995009368449,-1.35876716690521,-1.35576310396599,
-1.33847287578786,-1.32405686844856,-1.30801987050693,-1.30476309763374,
-1.30289215387842,-1.30126008789132,-1.29923808401619,-1.29611450644146,
-1.2734675517998,-1.25596220523273,-1.24984023003476,-1.24593478228138,
-1.24452352177923,-1.24357022908271,-1.24297181640774),.UNSPECIFIED.);
#138=B_SPLINE_CURVE_WITH_KNOTS('',3,(#14548,#14549,#14550,#14551,#14552,
#14553,#14554,#14555,#14556,#14557,#14558,#14559,#14560,#14561,#14562,#14563,
#14564,#14565,#14566,#14567,#14568,#14569,#14570,#14571,#14572,#14573,#14574,
#14575,#14576,#14577,#14578,#14579,#14580,#14581,#14582,#14583,#14584,#14585,
#14586,#14587,#14588,#14589,#14590,#14591,#14592,#14593,#14594,#14595,#14596,
#14597,#14598,#14599,#14600,#14601,#14602,#14603,#14604,#14605,#14606,#14607,
#14608,#14609,#14610,#14611,#14612,#14613,#14614,#14615,#14616,#14617,#14618,
#14619,#14620,#14621,#14622,#14623,#14624,#14625,#14626,#14627,#14628,#14629,
#14630,#14631,#14632,#14633,#14634,#14635,#14636,#14637,#14638,#14639,#14640,
#14641,#14642,#14643,#14644,#14645,#14646,#14647,#14648,#14649,#14650,#14651,
#14652,#14653,#14654,#14655,#14656,#14657,#14658,#14659,#14660,#14661,#14662,
#14663,#14664,#14665,#14666,#14667,#14668,#14669,#14670,#14671,#14672,#14673,
#14674,#14675,#14676,#14677,#14678,#14679,#14680,#14681,#14682,#14683,#14684,
#14685,#14686,#14687,#14688,#14689,#14690,#14691,#14692,#14693,#14694,#14695,
#14696,#14697,#14698,#14699,#14700,#14701,#14702,#14703,#14704,#14705,#14706,
#14707,#14708,#14709,#14710,#14711,#14712,#14713,#14714,#14715,#14716,#14717,
#14718,#14719,#14720,#14721,#14722,#14723,#14724,#14725,#14726,#14727,#14728,
#14729,#14730,#14731,#14732,#14733,#14734,#14735,#14736,#14737,#14738,#14739,
#14740,#14741,#14742,#14743,#14744,#14745,#14746,#14747,#14748,#14749,#14750,
#14751,#14752,#14753,#14754,#14755,#14756,#14757,#14758,#14759),
 .UNSPECIFIED.,.F.,.F.,(4,2,2,2,2,2,2,2,2,2,2,2,2,2,2,2,2,2,2,2,2,2,2,2,
2,2,2,2,2,2,2,2,2,2,2,2,2,2,2,2,2,2,2,2,2,2,2,2,2,2,2,2,2,2,2,2,2,2,2,2,
2,2,2,2,2,2,2,2,2,2,2,2,2,2,2,2,2,2,2,2,2,2,2,2,2,2,2,2,2,2,2,2,2,2,2,2,
2,2,2,2,2,2,2,2,2,4),(-0.983796640571424,-0.956484794984907,-0.949944706224993,
-0.945850105421087,-0.944413564360419,-0.943455292227012,-0.942600572183522,
-0.941432888196903,-0.938485894045167,-0.917121734564788,-0.899418311752801,
-0.893038811419795,-0.88831510415133,-0.886152027165743,-0.884504877476798,
-0.882715914037039,-0.879833785882569,-0.870525286050787,-0.845548739859668,
-0.829864258257799,-0.82777253067057,-0.826671879735262,-0.82575746806048,
-0.824607478999084,-0.822785013169212,-0.81237046940453,-0.803900200100683,
-0.789504457661509,-0.773447392466685,-0.770190480607822,-0.768319900147278,
-0.76668841426212,-0.764667473836552,-0.761546211520125,-0.742126035063395,
-0.726823660385851,-0.712717872011902,-0.710802251117728,-0.709624367250383,
-0.708708248563234,-0.707629599368523,-0.705642172186622,-0.693882110996864,
-0.670390058445014,-0.65625735219468,-0.653025475071441,-0.651141589867197,
-0.649511301017205,-0.647508202153237,-0.643619083800875,-0.638652123600562,
-0.626860425760855,-0.605122493345096,-0.595277921221457,-0.593311584848066,
-0.592225386162393,-0.591309986041854,-0.590142152273994,-0.587717226415944,
-0.584472119735296,-0.576214832546439,-0.551777586066478,-0.538899720414151,
-0.535746188117545,-0.533880096667625,-0.532263729264438,-0.530244116587985,
-0.526273029294609,-0.500340623458418,-0.479655883960697,-0.476688786868871,
-0.475512217167811,-0.474655218551756,-0.47369952324976,-0.472275684724341,
-0.468276441904958,-0.461949318945634,-0.448093225921893,-0.424050549859257,
-0.419405242711111,-0.41727941243655,-0.415632226890008,-0.413842603034745,
-0.41095803020165,-0.400603862745452,-0.380372589738605,-0.362498810863909,
-0.359486817239056,-0.358302750155167,-0.357443849481546,-0.356490331972412,
-0.355077070195199,-0.351155292513191,-0.344997992333697,-0.327616840066378,
-0.304934852970566,-0.301812321839301,-0.299790926043583,-0.298159322798514,
-0.296288882116425,-0.293032934138176,-0.277003245726646,-0.262571998948119,
-0.254080382760505,-0.243662255563251,-0.24188530259165),.UNSPECIFIED.);
#139=B_SPLINE_CURVE_WITH_KNOTS('',3,(#14764,#14765,#14766,#14767,#14768,
#14769,#14770,#14771,#14772,#14773,#14774,#14775,#14776,#14777,#14778,#14779,
#14780,#14781,#14782,#14783,#14784,#14785,#14786,#14787,#14788,#14789,#14790,
#14791,#14792,#14793,#14794,#14795,#14796,#14797,#14798,#14799,#14800,#14801,
#14802,#14803,#14804,#14805,#14806,#14807,#14808,#14809,#14810,#14811,#14812,
#14813,#14814,#14815,#14816,#14817,#14818,#14819,#14820,#14821,#14822,#14823,
#14824,#14825,#14826,#14827,#14828,#14829,#14830,#14831,#14832,#14833,#14834,
#14835,#14836,#14837,#14838,#14839,#14840,#14841,#14842,#14843,#14844,#14845,
#14846,#14847,#14848,#14849,#14850,#14851,#14852,#14853,#14854,#14855,#14856,
#14857,#14858,#14859,#14860,#14861,#14862,#14863,#14864,#14865,#14866,#14867,
#14868,#14869,#14870,#14871,#14872,#14873,#14874,#14875,#14876,#14877,#14878,
#14879,#14880,#14881,#14882,#14883,#14884,#14885,#14886,#14887,#14888,#14889,
#14890,#14891,#14892,#14893,#14894,#14895,#14896,#14897,#14898,#14899,#14900,
#14901,#14902,#14903,#14904,#14905,#14906,#14907,#14908,#14909,#14910,#14911,
#14912,#14913,#14914,#14915,#14916,#14917,#14918,#14919,#14920,#14921,#14922,
#14923,#14924,#14925,#14926,#14927,#14928,#14929,#14930,#14931,#14932,#14933,
#14934,#14935,#14936,#14937,#14938,#14939,#14940,#14941,#14942,#14943,#14944,
#14945,#14946,#14947,#14948,#14949,#14950,#14951,#14952,#14953,#14954,#14955,
#14956,#14957,#14958,#14959,#14960,#14961,#14962,#14963,#14964,#14965,#14966,
#14967,#14968,#14969,#14970,#14971,#14972,#14973,#14974,#14975,#14976,#14977,
#14978,#14979),.UNSPECIFIED.,.F.,.F.,(4,2,2,2,2,2,2,2,2,2,2,2,2,2,2,2,2,
2,2,2,2,2,2,2,2,2,2,2,2,2,2,2,2,2,2,2,2,2,2,2,2,2,2,2,2,2,2,2,2,2,2,2,2,
2,2,2,2,2,2,2,2,2,2,2,2,2,2,2,2,2,2,2,2,2,2,2,2,2,2,2,2,2,2,2,2,2,2,2,2,
2,2,2,2,2,2,2,2,2,2,2,2,2,2,2,2,2,2,4),(-1.24270960294557,-1.23057108915488,
-1.22732602055169,-1.22545793559639,-1.22382609545871,-1.22180143006595,
-1.21866808826137,-1.19670716888601,-1.18091872095959,-1.16959477406654,
-1.16762361808609,-1.1665484792736,-1.16563203873022,-1.16444947668023,
-1.16251793232035,-1.14714449873207,-1.13194244786246,-1.11516132864751,
-1.11083508105137,-1.10874599200114,-1.10710826866319,-1.10528173937671,
-1.10222742295277,-1.09123775839418,-1.06179496057393,-1.05537591847317,
-1.05133551768838,-1.04990613702097,-1.04894930113395,-1.04809314592959,
-1.04692024190248,-1.04397172484588,-1.02285705837319,-1.0049812210747,
-0.998566005281528,-0.993821732748724,-0.991654546968834,-0.990006406352709,
-0.988218442563936,-0.985342508731116,-0.97609767273325,-0.951067149571288,
-0.935361831899937,-0.933269228074998,-0.932168172877487,-0.931253496325791,
-0.930103229502069,-0.928280329786855,-0.917862539400722,-0.90938655183576,
-0.894974554798651,-0.878939289563961,-0.875682893889256,-0.873812168213393,
-0.872180293451031,-0.870158528136357,-0.867035324269992,-0.844343705568824,
-0.826954044235385,-0.820789956984208,-0.816865292766497,-0.815451497226935,
-0.814497774347033,-0.813638796843363,-0.81245477007217,-0.809443611488359,
-0.79055008858818,-0.771103730870406,-0.764382522453055,-0.759466137497427,
-0.757268230294995,-0.755615560299651,-0.753840706857694,-0.751025005139501,
-0.742323621541982,-0.726847220848381,-0.701984995824586,-0.6992058495356,
-0.697985057490443,-0.697061701628054,-0.696022507756908,-0.694218220923099,
-0.686193343773232,-0.666884545894673,-0.644867787040151,-0.641736354619933,
-0.639712033490797,-0.638079902981726,-0.636210862666873,-0.632962531176757,
-0.617105597930535,-0.592701098365589,-0.58345111678198,-0.581515406698485,
-0.580435884016506,-0.579519528268489,-0.578341981854396,-0.575867831930763,
-0.572537620133231,-0.563950201397443,-0.537604989793406,-0.526838664232318,
-0.523795011014158,-0.521970419909316,-0.52033163855543,-0.518237337911599,
-0.513886018832894,-0.500788288135055),.UNSPECIFIED.);
#140=B_SPLINE_CURVE_WITH_KNOTS('',3,(#14981,#14982,#14983,#14984,#14985,
#14986,#14987,#14988,#14989,#14990,#14991,#14992,#14993,#14994,#14995,#14996,
#14997,#14998,#14999,#15000,#15001,#15002,#15003,#15004,#15005,#15006,#15007,
#15008,#15009,#15010,#15011,#15012,#15013,#15014,#15015,#15016,#15017,#15018,
#15019,#15020,#15021,#15022,#15023,#15024,#15025,#15026,#15027,#15028,#15029,
#15030,#15031,#15032,#15033,#15034,#15035,#15036,#15037,#15038,#15039,#15040,
#15041,#15042,#15043,#15044,#15045,#15046,#15047,#15048,#15049,#15050,#15051,
#15052,#15053,#15054,#15055,#15056,#15057,#15058,#15059,#15060,#15061,#15062),
 .UNSPECIFIED.,.F.,.F.,(4,2,2,2,2,2,2,2,2,2,2,2,2,2,2,2,2,2,2,2,2,2,2,2,
2,2,2,2,2,2,2,2,2,2,2,2,2,2,2,2,4),(-0.24188530259165,-0.241839450645931,
-0.240689330117789,-0.239774862237138,-0.238674196696723,-0.236582597120152,
-0.220900822173211,-0.195927396293197,-0.186632072550096,-0.183751225943813,
-0.181962448638454,-0.180315060969418,-0.178151073629708,-0.173422960231241,
-0.167035107506178,-0.149292817673318,-0.127952574016593,-0.125014146572647,
-0.123842412036512,-0.122986626178238,-0.12204872217306,-0.120665006406587,
-0.119049417498415,-0.116050969259377,-0.108718177744274,-0.0926687435394361,
-0.070491433295743,-0.0673729381326236,-0.0653527843429346,-0.063721292694102,
-0.0618500015231068,-0.0585900309526913,-0.042472028592819,-0.0142557204442416,
-0.00858106725857966,-0.00690303169297602,-0.00589177633641331,-0.00501456269788023,
-0.00409375962618727,-0.00241338029616013,-0.000340362829803059),
 .UNSPECIFIED.);
#141=B_SPLINE_CURVE_WITH_KNOTS('',3,(#15063,#15064,#15065,#15066,#15067,
#15068,#15069,#15070,#15071,#15072,#15073,#15074,#15075,#15076,#15077,#15078,
#15079,#15080,#15081,#15082,#15083,#15084,#15085,#15086,#15087,#15088,#15089,
#15090,#15091,#15092,#15093,#15094,#15095,#15096,#15097,#15098,#15099,#15100,
#15101,#15102,#15103,#15104,#15105,#15106,#15107,#15108,#15109,#15110,#15111,
#15112,#15113,#15114,#15115,#15116,#15117,#15118,#15119,#15120,#15121,#15122,
#15123,#15124,#15125,#15126,#15127,#15128,#15129,#15130,#15131,#15132,#15133,
#15134,#15135,#15136,#15137,#15138,#15139,#15140,#15141,#15142,#15143,#15144,
#15145,#15146,#15147,#15148,#15149,#15150,#15151,#15152,#15153,#15154,#15155,
#15156,#15157,#15158,#15159,#15160,#15161,#15162,#15163,#15164,#15165,#15166,
#15167,#15168,#15169,#15170,#15171,#15172,#15173,#15174,#15175,#15176,#15177),
 .UNSPECIFIED.,.F.,.F.,(4,3,3,3,3,3,3,3,3,3,3,3,3,3,3,3,3,3,3,3,3,3,3,3,
3,3,3,3,3,3,3,3,3,3,3,3,3,3,4),(128.805298797898,128.924201779237,129.04293631556,
129.161556862562,129.280117685512,129.398763030493,129.517442715942,129.636360823461,
129.752144419847,129.876237071814,129.995823262841,130.115290601643,130.234691807728,
130.354079486213,130.473588015411,130.593169388511,130.712965709663,130.744885635581,
130.868978287548,130.988564690371,131.108032242172,131.227433662028,131.346821554623,
131.466330296828,131.585911882519,131.705708413522,131.737626851315,131.861719503282,
131.981305172712,132.100771992196,132.220172682235,132.339559848936,132.45906787637,
132.578648753008,132.698444590347,132.730368067049,132.850162253262,132.969754580808,
133.043149374429),.UNSPECIFIED.);
#142=B_SPLINE_CURVE_WITH_KNOTS('',3,(#15183,#15184,#15185,#15186,#15187,
#15188,#15189,#15190,#15191,#15192,#15193,#15194,#15195,#15196,#15197,#15198,
#15199,#15200,#15201,#15202,#15203,#15204,#15205,#15206,#15207,#15208,#15209,
#15210,#15211,#15212,#15213,#15214,#15215,#15216,#15217,#15218,#15219,#15220,
#15221,#15222,#15223,#15224,#15225,#15226,#15227,#15228,#15229,#15230,#15231,
#15232,#15233,#15234,#15235,#15236,#15237,#15238,#15239,#15240,#15241,#15242,
#15243,#15244,#15245,#15246,#15247,#15248,#15249,#15250,#15251,#15252,#15253,
#15254,#15255,#15256,#15257,#15258,#15259,#15260,#15261,#15262,#15263,#15264,
#15265,#15266,#15267,#15268,#15269,#15270,#15271,#15272,#15273,#15274,#15275,
#15276,#15277,#15278,#15279,#15280,#15281,#15282,#15283,#15284,#15285,#15286,
#15287,#15288,#15289,#15290,#15291,#15292,#15293,#15294),.UNSPECIFIED.,
 .F.,.F.,(4,3,3,3,3,3,3,3,3,3,3,3,3,3,3,3,3,3,3,3,3,3,3,3,3,3,3,3,3,3,3,
3,3,3,3,3,3,4),(135.088484104826,135.235310991762,135.372911768261,135.497004420228,
135.616616883007,135.73611026417,135.855537234829,135.974950351382,136.094483653774,
136.214089438881,136.333909405395,136.365652983995,136.489745635962,136.609369624872,
136.728875103783,136.848314712737,136.967740977844,137.087288072282,137.206908039,
137.326742605226,137.358394199729,137.482486851696,137.601899867957,137.721194162145,
137.84042278402,137.959638669042,138.078977825563,138.19839104728,138.318022674585,
138.351135415463,138.472970870233,138.592784589194,138.712476256388,138.832098163482,
138.955528386017,139.075242304231,139.200530678927,139.325819053623),
 .UNSPECIFIED.);
#143=B_SPLINE_CURVE_WITH_KNOTS('',3,(#15295,#15296,#15297,#15298,#15299,
#15300,#15301,#15302,#15303,#15304,#15305,#15306,#15307,#15308,#15309,#15310,
#15311,#15312,#15313,#15314,#15315,#15316,#15317,#15318,#15319,#15320,#15321,
#15322,#15323,#15324,#15325,#15326,#15327,#15328,#15329,#15330,#15331,#15332,
#15333,#15334,#15335,#15336,#15337,#15338,#15339,#15340,#15341,#15342,#15343,
#15344,#15345,#15346,#15347,#15348,#15349,#15350,#15351,#15352,#15353,#15354,
#15355,#15356,#15357,#15358,#15359,#15360,#15361,#15362,#15363,#15364,#15365,
#15366,#15367,#15368,#15369,#15370,#15371,#15372,#15373,#15374,#15375,#15376,
#15377,#15378,#15379,#15380,#15381,#15382,#15383,#15384,#15385,#15386,#15387,
#15388,#15389,#15390,#15391,#15392,#15393,#15394,#15395,#15396,#15397,#15398),
 .UNSPECIFIED.,.F.,.F.,(4,2,2,2,2,2,2,2,2,2,2,2,2,2,2,2,2,2,2,2,2,2,2,2,
2,2,2,2,2,2,2,2,2,2,2,2,2,2,2,2,2,2,2,2,2,2,2,2,2,2,2,4),(-1.48431867888129,
-1.4667432062449,-1.46372645311139,-1.46175797776396,-1.46019207361964,
-1.45856261866385,-1.45668983668337,-1.45350196093862,-1.44009136080204,
-1.4263596585778,-1.41496328252652,-1.404029850154,-1.40203099020675,-1.40095061468933,
-1.40003509582519,-1.39886102772239,-1.39695859516784,-1.38363937752364,
-1.36747010047829,-1.35446538446697,-1.34917344444698,-1.34511944004517,
-1.34314400077368,-1.34313291116912,-1.34312119108408,-1.34310880227671,
-1.34309570394019,-1.34308185249518,-1.34306720138911,-1.34305170085914,
-1.34303529767782,-1.34301793488256,-1.34299955147528,-1.34298008210286,
-1.34295945670407,-1.34293760012776,-1.34291443172066,-1.34144236516171,
-1.3395974673014,-1.33646176715407,-1.3244389990526,-1.29922619837416,-1.29085256337213,
-1.2875770389686,-1.28513440788799,-1.28396260013633,-1.28304646209334,
-1.28196223494932,-1.28000539409258,-1.27034980175605,-1.2463741601058,
-1.24270960294557),.UNSPECIFIED.);
#144=B_SPLINE_CURVE_WITH_KNOTS('',3,(#15400,#15401,#15402,#15403,#15404,
#15405,#15406,#15407,#15408,#15409,#15410,#15411,#15412,#15413,#15414,#15415,
#15416,#15417,#15418,#15419,#15420,#15421,#15422,#15423,#15424,#15425,#15426,
#15427,#15428,#15429,#15430,#15431,#15432,#15433,#15434,#15435,#15436,#15437,
#15438,#15439,#15440,#15441,#15442,#15443,#15444,#15445,#15446,#15447,#15448,
#15449,#15450,#15451,#15452,#15453,#15454),.UNSPECIFIED.,.F.,.F.,(4,3,3,
3,3,3,3,3,3,3,3,3,3,3,3,3,3,3,4),(133.043149374429,133.162572277305,133.281959474831,
133.401451670163,133.520996801097,133.640772313025,133.723109282783,133.84720193475,
133.966789439693,134.086258097906,134.205660626244,134.325049627171,134.444559469222,
134.564142150987,134.683939761574,134.715850498517,134.851214190363,134.985564663725,
135.088484103629),.UNSPECIFIED.);
#145=B_SPLINE_CURVE_WITH_KNOTS('',3,(#15455,#15456,#15457,#15458,#15459,
#15460,#15461,#15462,#15463,#15464,#15465,#15466,#15467,#15468,#15469,#15470,
#15471,#15472,#15473,#15474,#15475,#15476,#15477,#15478,#15479,#15480,#15481,
#15482,#15483,#15484,#15485,#15486,#15487,#15488,#15489,#15490,#15491,#15492,
#15493,#15494,#15495,#15496,#15497,#15498,#15499,#15500,#15501,#15502,#15503,
#15504,#15505,#15506,#15507,#15508,#15509,#15510,#15511,#15512,#15513,#15514,
#15515,#15516,#15517,#15518,#15519,#15520,#15521,#15522,#15523,#15524,#15525,
#15526,#15527,#15528,#15529,#15530,#15531,#15532,#15533,#15534,#15535,#15536,
#15537,#15538,#15539,#15540,#15541,#15542,#15543,#15544,#15545,#15546,#15547,
#15548,#15549,#15550,#15551,#15552,#15553,#15554,#15555,#15556,#15557,#15558,
#15559,#15560,#15561,#15562,#15563,#15564,#15565,#15566,#15567,#15568,#15569,
#15570,#15571,#15572,#15573,#15574,#15575,#15576,#15577,#15578,#15579,#15580,
#15581,#15582,#15583,#15584,#15585,#15586,#15587,#15588,#15589,#15590,#15591,
#15592,#15593,#15594,#15595,#15596,#15597,#15598,#15599,#15600,#15601,#15602,
#15603,#15604,#15605,#15606,#15607,#15608,#15609,#15610,#15611,#15612,#15613,
#15614,#15615,#15616,#15617,#15618,#15619,#15620,#15621,#15622,#15623,#15624,
#15625,#15626,#15627,#15628,#15629,#15630),.UNSPECIFIED.,.F.,.F.,(4,2,2,
2,2,2,2,2,2,2,2,2,2,2,2,2,2,2,2,2,2,2,2,2,2,2,2,2,2,2,2,2,2,2,2,2,2,2,2,
2,2,2,2,2,2,2,2,2,2,2,2,2,2,2,2,2,2,2,2,2,2,2,2,2,2,2,2,2,2,2,2,2,2,2,2,
2,2,2,2,2,2,2,2,2,2,2,2,4),(0.500726922102148,0.512053449536436,0.515135237800579,
0.516968195480732,0.518441729180792,0.520440786485293,0.524307895967392,
0.529237734536915,0.540890162523225,0.559827955558004,0.563368821419012,
0.572753881272379,0.574695973166796,0.575776446253112,0.576691552793251,
0.57786488463665,0.580322056859391,0.583624206918134,0.592106616308757,
0.617744957846055,0.629294310569344,0.632388093721572,0.63422195242595,
0.635692707788795,0.63768336756942,0.641517930563704,0.646397038493051,
0.657875033052619,0.671538479196515,0.676843014242143,0.683403133368924,
0.690269330375383,0.692062247539759,0.693097959669159,0.69402122377621,
0.695266605018847,0.698111072722151,0.711150880215098,0.720448642156198,
0.743915549589254,0.748575275676725,0.750704046190909,0.75235202460641,
0.754141040194108,0.757021416462893,0.767324890412671,0.787379695059129,
0.805413291061802,0.808429734647613,0.809614810110556,0.810474230127405,
0.811427641817489,0.812840413066334,0.816758895748538,0.822910060012445,
0.8403048847854,0.862990676082221,0.866114028152321,0.868135430836476,0.869766713769115,
0.869798997363329,0.869823226361995,0.869860125153782,0.86989484839628,
0.86992752877563,0.869958290853728,0.871853904361353,0.875321569590384,
0.879661674174444,0.889288037155004,0.904766569068977,0.92261703224887,
0.925627836315947,0.926811451732629,0.927670036347477,0.928623170320318,
0.930035840011454,0.933955717604712,0.94011048814423,0.968114063101643,
0.979419476580892,0.982960671678051,0.985083168893455,0.986729295537634,
0.988255585788787,0.990013618796802,0.992513189891128,1.00100352361353),
 .UNSPECIFIED.);
#146=B_SPLINE_CURVE_WITH_KNOTS('',3,(#15636,#15637,#15638,#15639,#15640,
#15641),.UNSPECIFIED.,.F.,.F.,(4,1,1,4),(-4.09202352044853,-3.97096486293603,
-2.97822364720202,-2.0736150725356),.UNSPECIFIED.);
#147=B_SPLINE_CURVE_WITH_KNOTS('',3,(#15644,#15645,#15646,#15647,#15648),
 .UNSPECIFIED.,.F.,.F.,(4,1,4),(0.,0.992741215733998,1.12274180646084),
 .UNSPECIFIED.);
#148=B_SPLINE_CURVE_WITH_KNOTS('',3,(#15653,#15654,#15655,#15656,#15657,
#15658,#15659,#15660,#15661,#15662),.UNSPECIFIED.,.F.,.F.,(4,1,1,1,1,1,
1,4),(-10.3752088276281,-9.92741215734008,-8.93467094160607,-7.94192972587206,
-6.94918851013805,-5.95644729440404,-4.96370607867004,-4.09202352044853),
 .UNSPECIFIED.);
#149=B_SPLINE_CURVE_WITH_KNOTS('',3,(#15663,#15664,#15665,#15666,#15667,
#15668,#15669,#15670,#15671,#15672,#15673,#15674,#15675,#15676,#15677,#15678,
#15679,#15680,#15681,#15682,#15683,#15684,#15685,#15686,#15687,#15688,#15689,
#15690,#15691,#15692,#15693,#15694,#15695,#15696,#15697,#15698,#15699,#15700,
#15701,#15702,#15703,#15704,#15705,#15706,#15707,#15708,#15709,#15710,#15711,
#15712,#15713,#15714,#15715,#15716,#15717,#15718,#15719,#15720,#15721,#15722,
#15723,#15724,#15725,#15726,#15727,#15728,#15729,#15730,#15731,#15732,#15733,
#15734,#15735,#15736,#15737,#15738,#15739,#15740,#15741,#15742,#15743,#15744,
#15745,#15746,#15747,#15748,#15749,#15750,#15751,#15752,#15753,#15754,#15755,
#15756,#15757,#15758,#15759,#15760,#15761,#15762,#15763,#15764,#15765,#15766,
#15767,#15768,#15769,#15770,#15771,#15772,#15773,#15774,#15775,#15776,#15777,
#15778,#15779,#15780,#15781,#15782,#15783,#15784,#15785,#15786,#15787,#15788,
#15789,#15790,#15791,#15792,#15793,#15794,#15795,#15796,#15797,#15798,#15799,
#15800,#15801,#15802,#15803,#15804,#15805,#15806,#15807,#15808,#15809,#15810,
#15811,#15812,#15813,#15814,#15815,#15816,#15817,#15818,#15819,#15820,#15821,
#15822,#15823,#15824,#15825,#15826,#15827,#15828,#15829,#15830,#15831,#15832,
#15833,#15834),.UNSPECIFIED.,.F.,.F.,(4,3,3,3,3,3,3,3,3,3,3,3,3,3,3,3,3,
3,3,3,3,3,3,3,3,3,3,3,3,3,3,3,3,3,3,3,3,3,3,3,3,3,3,3,3,3,3,3,3,3,3,3,3,
3,3,3,3,4),(1.12274180646084,1.23343629746888,1.34399240446288,1.45445841687218,
1.56488243774564,1.67539231942886,1.78594226536294,1.89670153729216,1.98548243146801,
2.09914339557329,2.21260275597674,2.32594994134661,2.43922941306601,2.55248553226531,
2.6658428728994,2.77925047355754,2.89286747779434,2.97822364720202,3.09189566254516,
3.20537231958541,3.31874061986118,3.43204499121717,3.54532976590842,3.6587213982951,
3.77216647795867,3.8858257585652,3.97096486293603,4.08428886198503,4.19740786099008,
4.31041287767409,4.4233490066995,4.53626124008659,4.6492766385696,4.76234285582213,
4.87562368571185,4.96370607867004,5.07722135155215,5.19053517232557,5.30373703723263,
5.4168716877161,5.5299837652683,5.64319947242412,5.75646656994225,5.86994671152142,
5.95644729440405,6.06994872957337,6.1832492800824,6.29643823328387,6.40956035469253,
6.52266031031201,6.63586462950835,6.74912072961629,6.86259065731568,6.94918851013806,
7.07058093650876,7.19167798873108,7.31234457608894,7.40592711324294),
 .UNSPECIFIED.);
#150=B_SPLINE_CURVE_WITH_KNOTS('',3,(#15839,#15840,#15841,#15842,#15843,
#15844,#15845,#15846,#15847,#15848),.UNSPECIFIED.,.F.,.F.,(4,1,1,1,1,1,
1,4),(-16.6583930095603,-15.8838594517441,-14.8911182360101,-13.8983770202761,
-12.9056358045421,-11.9128945888081,-10.9201533730741,-10.3752088276281),
 .UNSPECIFIED.);
#151=B_SPLINE_CURVE_WITH_KNOTS('',3,(#15849,#15850,#15851,#15852,#15853,
#15854,#15855,#15856,#15857,#15858,#15859,#15860,#15861,#15862,#15863,#15864,
#15865,#15866,#15867,#15868,#15869,#15870,#15871,#15872,#15873,#15874,#15875,
#15876,#15877,#15878,#15879,#15880,#15881,#15882,#15883,#15884,#15885,#15886,
#15887,#15888,#15889,#15890,#15891,#15892,#15893,#15894,#15895,#15896,#15897,
#15898,#15899,#15900,#15901,#15902,#15903,#15904,#15905,#15906,#15907,#15908,
#15909,#15910,#15911,#15912,#15913,#15914,#15915,#15916,#15917,#15918,#15919,
#15920,#15921,#15922,#15923,#15924,#15925,#15926,#15927,#15928,#15929,#15930,
#15931,#15932,#15933,#15934,#15935,#15936,#15937,#15938,#15939,#15940,#15941,
#15942,#15943,#15944,#15945,#15946,#15947,#15948,#15949,#15950,#15951,#15952,
#15953,#15954,#15955,#15956,#15957,#15958,#15959,#15960,#15961,#15962,#15963,
#15964,#15965,#15966,#15967,#15968,#15969,#15970,#15971,#15972,#15973,#15974,
#15975,#15976,#15977,#15978,#15979,#15980,#15981,#15982,#15983,#15984,#15985,
#15986,#15987,#15988,#15989,#15990,#15991,#15992,#15993,#15994,#15995,#15996,
#15997,#15998,#15999,#16000,#16001,#16002,#16003,#16004,#16005,#16006,#16007,
#16008,#16009,#16010,#16011,#16012,#16013,#16014,#16015,#16016,#16017,#16018,
#16019,#16020),.UNSPECIFIED.,.F.,.F.,(4,3,3,3,3,3,3,3,3,3,3,3,3,3,3,3,3,
3,3,3,3,3,3,3,3,3,3,3,3,3,3,3,3,3,3,3,3,3,3,3,3,3,3,3,3,3,3,3,3,3,3,3,3,
3,3,3,3,4),(7.40592711364043,7.52253753703482,7.63939496513354,7.75638371478664,
7.87366366059931,7.94192972587207,8.05541582244172,8.16870031392625,8.28187277923307,
8.39497801395519,8.5080607136396,8.62124733990233,8.7344854771366,8.84793722088447,
8.93467094160608,9.04815243188051,9.16143233640877,9.2746002302422,9.38770091736713,
9.50077910174122,9.61396129959615,9.72719504990304,9.84064253031215,9.92741215734009,
10.0408880929723,10.1541622655264,10.2673243231986,10.3804190806018,10.4934912521889,
10.606667356083,10.7198949579502,10.8333362768889,10.9201533730741,11.0336337732337,
11.1469125068194,11.2600791810862,11.3731786022268,11.4862554763447,11.5994363053865,
11.7126686522404,11.8261146895023,11.9128945888081,12.0263739592526,12.1396516566805,
12.2528172916576,12.3659156722783,12.4789915065442,12.5921713051742,12.7054026252761,
12.8188476547086,12.9056358045421,13.0175005710598,13.1292059416967,13.2407992579844,
13.352877548586,13.4644294254286,13.5767709229096,13.6891124203907),
 .UNSPECIFIED.);
#152=B_SPLINE_CURVE_WITH_KNOTS('',3,(#16025,#16026,#16027,#16028,#16029,
#16030,#16031,#16032,#16033,#16034,#16035,#16036,#16037,#16038,#16039,#16040,
#16041,#16042,#16043,#16044,#16045,#16046,#16047,#16048,#16049,#16050,#16051,
#16052,#16053,#16054,#16055,#16056,#16057,#16058,#16059,#16060,#16061,#16062,
#16063,#16064,#16065,#16066,#16067,#16068,#16069,#16070,#16071,#16072,#16073,
#16074,#16075,#16076,#16077,#16078,#16079,#16080,#16081,#16082,#16083,#16084,
#16085,#16086,#16087,#16088,#16089,#16090,#16091,#16092,#16093,#16094,#16095,
#16096,#16097,#16098,#16099,#16100,#16101,#16102,#16103,#16104,#16105,#16106,
#16107,#16108,#16109,#16110,#16111,#16112,#16113,#16114,#16115,#16116,#16117,
#16118,#16119,#16120,#16121,#16122,#16123,#16124,#16125,#16126,#16127,#16128,
#16129,#16130,#16131,#16132,#16133,#16134,#16135,#16136,#16137,#16138,#16139,
#16140,#16141,#16142,#16143,#16144,#16145,#16146,#16147,#16148,#16149,#16150,
#16151,#16152,#16153,#16154,#16155,#16156,#16157,#16158,#16159,#16160,#16161,
#16162,#16163,#16164,#16165,#16166,#16167,#16168,#16169,#16170,#16171,#16172,
#16173,#16174,#16175,#16176,#16177,#16178,#16179,#16180,#16181,#16182,#16183,
#16184,#16185,#16186,#16187,#16188,#16189,#16190,#16191,#16192,#16193,#16194,
#16195,#16196),.UNSPECIFIED.,.F.,.F.,(4,3,3,3,3,3,3,3,3,3,3,3,3,3,3,3,3,
3,3,3,3,3,3,3,3,3,3,3,3,3,3,3,3,3,3,3,3,3,3,3,3,3,3,3,3,3,3,3,3,3,3,3,3,
3,3,3,3,4),(-22.9415794419873,-22.8330479618822,-22.7195687858932,-22.6062912943685,
-22.4931258721497,-22.3800277107567,-22.2669521018115,-22.1537725361979,
-22.040541453747,-21.9270966666516,-21.8403067461482,-21.7268275697863,
-21.613550077918,-21.500384655374,-21.3872864936743,-21.2742108844412,-21.1610313185711,
-21.0478002358805,-20.9343554485756,-20.8475655304142,-20.734086348015,
-20.6208088500747,-20.5076434214419,-20.3945452536477,-20.2814696383254,
-20.1682900664222,-20.0550589777206,-19.9416141845158,-19.8548243146802,
-19.7413451461789,-19.6280676621022,-19.5149022473017,-19.4018040932847,
-19.2887284916603,-19.1755489332253,-19.0623178578849,-18.9488730777009,
-18.8620830989462,-18.7486039233986,-18.6353264324728,-18.5221610109485,
-18.4090628503432,-18.2959872422765,-18.1828076776731,-18.0695765963069,
-17.9561318104028,-17.8693418832121,-17.7558626720325,-17.642585145189,
-17.5294196875997,-17.4163214908473,-17.3032458466163,-17.1900662461109,
-17.0768351289333,-16.9633903078139,-16.8766006674781,-16.7220057020924,
-16.6583941348077),.UNSPECIFIED.);
#153=B_SPLINE_CURVE_WITH_KNOTS('',3,(#16197,#16198,#16199,#16200,#16201,
#16202,#16203,#16204,#16205,#16206,#16207,#16208,#16209,#16210,#16211,#16212,
#16213,#16214,#16215,#16216,#16217,#16218,#16219,#16220,#16221,#16222,#16223,
#16224,#16225,#16226,#16227,#16228,#16229,#16230,#16231,#16232,#16233,#16234,
#16235,#16236,#16237,#16238,#16239,#16240,#16241,#16242,#16243,#16244,#16245,
#16246,#16247,#16248,#16249,#16250,#16251,#16252,#16253,#16254,#16255,#16256,
#16257,#16258,#16259,#16260,#16261,#16262,#16263,#16264,#16265,#16266,#16267,
#16268,#16269,#16270,#16271,#16272,#16273,#16274,#16275,#16276,#16277,#16278,
#16279,#16280,#16281,#16282,#16283,#16284,#16285,#16286,#16287,#16288,#16289,
#16290,#16291,#16292,#16293,#16294,#16295,#16296,#16297,#16298,#16299,#16300,
#16301,#16302,#16303,#16304,#16305,#16306,#16307,#16308,#16309,#16310,#16311,
#16312,#16313,#16314,#16315,#16316,#16317,#16318,#16319,#16320,#16321,#16322,
#16323,#16324,#16325,#16326,#16327,#16328,#16329,#16330,#16331,#16332,#16333,
#16334,#16335,#16336,#16337,#16338,#16339,#16340,#16341,#16342,#16343,#16344,
#16345,#16346,#16347,#16348,#16349,#16350,#16351,#16352,#16353,#16354,#16355,
#16356,#16357,#16358,#16359,#16360,#16361,#16362,#16363,#16364,#16365,#16366,
#16367,#16368),.UNSPECIFIED.,.F.,.F.,(4,3,3,3,3,3,3,3,3,3,3,3,3,3,3,3,3,
3,3,3,3,3,3,3,3,3,3,3,3,3,3,3,3,3,3,3,3,3,3,3,3,3,3,3,3,3,3,3,3,3,3,3,3,
3,3,3,3,4),(13.68911242082,13.84668731327,13.8983770202761,14.0118564019841,
14.125134102677,14.2382997360134,14.3513981100881,14.4644739328963,14.577653712491,
14.6908850093181,14.8043300087562,14.8911182360101,15.0045974196722,15.1178749200623,
15.2310403518703,15.3441385235596,15.4572141434919,15.5703937210833,15.6836248160808,
15.7970696165069,15.8838594517441,15.9973385684418,16.1106159990213,16.2237813593291,
16.3368794579583,16.4499550033988,16.5631345048636,16.6763655227092,16.7898102452546,
16.8766006674781,16.9900798773989,17.1033574034607,17.2165228605604,17.3296210571146,
17.4426967014383,17.5558763024844,17.6691074204524,17.7825522427601,17.8693418832121,
17.9828210580819,18.0960985485814,18.2092639698335,18.3223621303203,18.4354377384218,
18.5486173032965,18.6618483850657,18.7752931715828,18.8620830989461,18.9755622681843,
19.0888397527214,19.202005167813,19.3151033219523,19.4281789235304,19.5413584816595,
19.6545895565493,19.768034336052,19.8548243146801,19.9722977279996),
 .UNSPECIFIED.);
#154=B_SPLINE_CURVE_WITH_KNOTS('',3,(#16373,#16374,#16375,#16376,#16377,
#16378,#16379,#16380,#16381,#16382),.UNSPECIFIED.,.F.,.F.,(4,1,1,1,1,1,
1,4),(-29.2247647491669,-28.7894952562862,-27.7967540405522,-26.8040128248182,
-25.8112716090842,-24.8185303933502,-23.8257891776162,-22.9415879141924),
 .UNSPECIFIED.);
#155=B_SPLINE_CURVE_WITH_KNOTS('',3,(#16383,#16384,#16385,#16386,#16387,
#16388,#16389,#16390,#16391,#16392),.UNSPECIFIED.,.F.,.F.,(4,1,1,1,1,1,
1,4),(19.9723060732156,20.8475655304142,21.8403067461482,22.8330479618822,
23.8257891776162,24.8185303933502,25.8112716090842,26.2554830351792),
 .UNSPECIFIED.);
#156=B_SPLINE_CURVE_WITH_KNOTS('',3,(#16397,#16398,#16399,#16400,#16401,
#16402,#16403,#16404,#16405,#16406),.UNSPECIFIED.,.F.,.F.,(4,1,1,1,1,1,
1,4),(-35.5079500563465,-34.7459425506903,-33.7532013349563,-32.7604601192223,
-31.7677189034882,-30.7749776877542,-29.7822364720202,-29.2247647491669),
 .UNSPECIFIED.);
#157=B_SPLINE_CURVE_WITH_KNOTS('',3,(#16407,#16408,#16409,#16410,#16411,
#16412,#16413,#16414,#16415,#16416),.UNSPECIFIED.,.F.,.F.,(4,1,1,1,1,1,
1,4),(26.2554830351792,26.8040128248182,27.7967540405522,28.7894952562862,
29.7822364720202,30.7749776877543,31.7677189034883,32.5386675302423),
 .UNSPECIFIED.);
#158=B_SPLINE_CURVE_WITH_KNOTS('',3,(#16421,#16422,#16423,#16424,#16425,
#16426,#16427,#16428,#16429,#16430,#16431),.UNSPECIFIED.,.F.,.F.,(4,1,1,
1,1,1,1,1,4),(-41.791135363526,-41.6951310608283,-40.7023898450943,-39.7096486293603,
-38.7169074136263,-37.7241661978923,-36.7314249821583,-35.7386837664243,
-35.5079500563465),.UNSPECIFIED.);
#159=B_SPLINE_CURVE_WITH_KNOTS('',3,(#16432,#16433,#16434,#16435,#16436,
#16437,#16438,#16439,#16440,#16441,#16442,#16443,#16444,#16445,#16446,#16447,
#16448,#16449,#16450,#16451,#16452,#16453,#16454,#16455,#16456,#16457,#16458,
#16459,#16460,#16461,#16462,#16463,#16464,#16465,#16466,#16467,#16468,#16469,
#16470,#16471,#16472,#16473,#16474,#16475,#16476,#16477,#16478,#16479,#16480,
#16481,#16482,#16483,#16484,#16485,#16486,#16487,#16488,#16489,#16490,#16491,
#16492,#16493,#16494,#16495,#16496,#16497,#16498,#16499,#16500,#16501,#16502,
#16503,#16504,#16505,#16506,#16507,#16508,#16509,#16510,#16511,#16512,#16513,
#16514,#16515,#16516,#16517,#16518,#16519,#16520,#16521,#16522,#16523,#16524,
#16525,#16526,#16527,#16528,#16529,#16530,#16531,#16532,#16533,#16534,#16535,
#16536,#16537,#16538,#16539,#16540,#16541,#16542,#16543,#16544,#16545,#16546,
#16547,#16548,#16549,#16550,#16551,#16552,#16553,#16554,#16555,#16556,#16557,
#16558,#16559,#16560,#16561,#16562,#16563,#16564,#16565,#16566,#16567,#16568,
#16569,#16570,#16571,#16572,#16573,#16574,#16575,#16576,#16577,#16578,#16579,
#16580,#16581,#16582,#16583,#16584,#16585,#16586,#16587,#16588,#16589,#16590,
#16591,#16592,#16593,#16594,#16595,#16596,#16597,#16598,#16599,#16600,#16601,
#16602,#16603),.UNSPECIFIED.,.F.,.F.,(4,3,3,3,3,3,3,3,3,3,3,3,3,3,3,3,3,
3,3,3,3,3,3,3,3,3,3,3,3,3,3,3,3,3,3,3,3,3,3,3,3,3,3,3,3,3,3,3,3,3,3,3,3,
3,3,3,3,4),(32.5386683423588,32.6921491728441,32.7604601192223,32.8739392962833,
32.9872167888717,33.1003822121482,33.2134803745913,33.3265559845771,33.4397355512085,
33.5529666346662,33.6664114227379,33.7532013349563,33.8666805120183,33.9799580046077,
34.0931234278852,34.2062215903293,34.3192972003161,34.4324767669485,34.5457078504072,
34.6591526384799,34.7459425506903,34.8594217277526,34.9726992203424,35.0858646436203,
35.1989628060648,35.312038416052,35.4252179826848,35.5384490661439,35.651893854217,
35.7386837664243,35.8521629434862,35.9654404360755,36.0786058593529,36.1917040217968,
36.3047796317836,36.4179591984159,36.5311902818745,36.6446350699471,36.7314249821583,
36.8449041592204,36.9581816518098,37.0713470750875,37.1844452375316,37.2975208475185,
37.4107004141509,37.5239314976098,37.6373762856826,37.7241661978923,37.8376453749544,
37.9509228675439,38.0640882908215,38.1771864532657,38.2902620632527,38.4034416298852,
38.516672713344,38.6301175014168,38.7169074136263,38.8218536495384),
 .UNSPECIFIED.);
#160=B_SPLINE_CURVE_WITH_KNOTS('',3,(#16608,#16609,#16610,#16611,#16612,
#16613,#16614,#16615,#16616,#16617,#16618,#16619,#16620,#16621,#16622,#16623,
#16624,#16625,#16626,#16627,#16628,#16629,#16630,#16631,#16632,#16633,#16634,
#16635,#16636,#16637,#16638,#16639,#16640,#16641,#16642,#16643,#16644,#16645,
#16646,#16647,#16648,#16649,#16650,#16651,#16652,#16653,#16654,#16655,#16656,
#16657,#16658,#16659,#16660,#16661,#16662,#16663,#16664,#16665,#16666,#16667,
#16668,#16669,#16670,#16671,#16672,#16673,#16674,#16675,#16676,#16677,#16678,
#16679,#16680,#16681,#16682,#16683,#16684,#16685,#16686,#16687,#16688,#16689,
#16690,#16691,#16692,#16693,#16694,#16695,#16696,#16697,#16698,#16699,#16700,
#16701,#16702,#16703,#16704,#16705,#16706,#16707,#16708,#16709,#16710,#16711,
#16712,#16713,#16714,#16715,#16716,#16717,#16718,#16719,#16720,#16721,#16722,
#16723,#16724,#16725,#16726,#16727,#16728,#16729,#16730,#16731,#16732,#16733,
#16734,#16735,#16736,#16737,#16738,#16739,#16740,#16741,#16742,#16743,#16744,
#16745,#16746,#16747,#16748,#16749,#16750,#16751,#16752,#16753,#16754,#16755,
#16756,#16757,#16758,#16759,#16760,#16761,#16762,#16763,#16764,#16765,#16766,
#16767,#16768,#16769,#16770,#16771,#16772,#16773,#16774,#16775,#16776,#16777,
#16778,#16779),.UNSPECIFIED.,.F.,.F.,(4,3,3,3,3,3,3,3,3,3,3,3,3,3,3,3,3,
3,3,3,3,3,3,3,3,3,3,3,3,3,3,3,3,3,3,3,3,3,3,3,3,3,3,3,3,3,3,3,3,3,3,3,3,
3,3,3,3,4),(-48.0743203223387,-47.9513556297491,-47.8280197994362,-47.7041579646634,
-47.6515783552324,-47.5380991781703,-47.4248216855808,-47.3116562623032,
-47.198558099859,-47.0854824898721,-46.9723029232396,-46.8590718397807,
-46.7456270517079,-46.6588371394984,-46.5453579624364,-46.4320804698469,
-46.3189150465693,-46.2058168841252,-46.0927412741383,-45.9795617075059,
-45.8663306240471,-45.7528858359743,-45.6660959237644,-45.5526167467024,
-45.439339254113,-45.3261738308354,-45.2130756683913,-45.1000000584044,
-44.9868204917719,-44.8735894083132,-44.7601446202404,-44.6733547080304,
-44.5598755309683,-44.4465980383788,-44.3334326151012,-44.220334452657,
-44.1072588426701,-43.9940792760376,-43.8808481925788,-43.767403404506,
-43.6806134922963,-43.5671343152342,-43.4538568226448,-43.3406913993672,
-43.2275932369231,-43.1145176269361,-43.0013380603037,-42.8881069768448,
-42.774662188772,-42.6878722765623,-42.5757801624328,-42.4638771065427,
-42.3520829463607,-42.2403507815932,-42.1280469270764,-42.0162357828843,
-41.9036855732051,-41.791135363526),.UNSPECIFIED.);
#161=B_SPLINE_CURVE_WITH_KNOTS('',3,(#16780,#16781,#16782,#16783,#16784,
#16785,#16786,#16787,#16788,#16789,#16790,#16791,#16792,#16793,#16794,#16795,
#16796,#16797,#16798,#16799,#16800,#16801,#16802,#16803,#16804,#16805,#16806,
#16807,#16808,#16809,#16810,#16811,#16812,#16813,#16814,#16815,#16816,#16817,
#16818,#16819,#16820,#16821,#16822,#16823,#16824,#16825,#16826,#16827,#16828,
#16829,#16830,#16831,#16832,#16833,#16834,#16835,#16836,#16837,#16838,#16839,
#16840,#16841,#16842,#16843,#16844,#16845,#16846,#16847,#16848,#16849,#16850,
#16851,#16852,#16853,#16854,#16855,#16856,#16857,#16858,#16859,#16860,#16861,
#16862,#16863,#16864,#16865,#16866,#16867,#16868,#16869,#16870,#16871,#16872,
#16873,#16874,#16875,#16876,#16877,#16878,#16879,#16880,#16881,#16882,#16883,
#16884,#16885,#16886,#16887,#16888,#16889,#16890,#16891,#16892,#16893,#16894,
#16895,#16896,#16897,#16898,#16899,#16900,#16901,#16902,#16903,#16904,#16905,
#16906,#16907,#16908,#16909,#16910,#16911,#16912,#16913,#16914,#16915,#16916,
#16917,#16918,#16919,#16920,#16921,#16922,#16923,#16924,#16925,#16926,#16927,
#16928,#16929,#16930,#16931,#16932,#16933,#16934,#16935,#16936,#16937,#16938,
#16939,#16940,#16941,#16942,#16943,#16944,#16945,#16946,#16947,#16948,#16949,
#16950,#16951),.UNSPECIFIED.,.F.,.F.,(4,3,3,3,3,3,3,3,3,3,3,3,3,3,3,3,3,
3,3,3,3,3,3,3,3,3,3,3,3,3,3,3,3,3,3,3,3,3,3,3,3,3,3,3,3,3,3,3,3,3,3,3,3,
3,3,3,3,4),(38.8218536499681,38.9337807794497,39.0455700846134,39.1572686518211,
39.2689234195268,39.3806624113741,39.492437953727,39.6044275384719,39.7096486293603,
39.8231278064224,39.9364052990119,40.0495707222895,40.1626688847337,40.2757444947207,
40.3889240613532,40.5021551448119,40.6155999328847,40.7023898450943,40.8158690221565,
40.9291465147459,41.0423119380236,41.1554101004677,41.2684857104546,41.381665277087,
41.4948963605459,41.6083411486187,41.6951310608283,41.8086102378904,41.9218877304799,
42.0350531537575,42.1481513162015,42.2612269261883,42.3744064928208,42.4876375762796,
42.6010823643523,42.6878722765623,42.8013514536243,42.9146289462136,43.0277943694913,
43.1408925319353,43.2539681419224,43.3671477085548,43.4803787920136,43.5938235800864,
43.6806134922963,43.7940926693583,43.9073701619478,44.0205355852255,44.1336337476696,
44.2467093576563,44.3598889242888,44.4731200077475,44.5865647958202,44.6733547080304,
44.7964919319002,44.919285871168,45.0415576688195,45.1050386426266),
 .UNSPECIFIED.);
#162=B_SPLINE_CURVE_WITH_KNOTS('',3,(#16956,#16957,#16958,#16959,#16960,
#16961,#16962,#16963,#16964,#16965),.UNSPECIFIED.,.F.,.F.,(4,1,1,1,1,1,
1,4),(-54.3575059778852,-53.6080256496364,-52.6152844339024,-51.6225432181684,
-50.6298020024344,-49.6370607867004,-48.6443195709664,-48.0743206707056),
 .UNSPECIFIED.);
#163=B_SPLINE_CURVE_WITH_KNOTS('',3,(#16966,#16967,#16968,#16969,#16970,
#16971,#16972,#16973,#16974,#16975),.UNSPECIFIED.,.F.,.F.,(4,1,1,1,1,1,
1,4),(45.105038956718,45.6660959237644,46.6588371394984,47.6515783552324,
48.6443195709664,49.6370607867004,50.6298020024344,51.3882242638976),
 .UNSPECIFIED.);
#164=B_SPLINE_CURVE_WITH_KNOTS('',3,(#16980,#16981,#16982,#16983,#16984,
#16985,#16986,#16987,#16988,#16989,#16990),.UNSPECIFIED.,.F.,.F.,(4,1,1,
1,1,1,1,1,4),(-60.6406912850648,-60.5572141597745,-59.5644729440405,-58.5717317283065,
-57.5789905125725,-56.5862492968384,-55.5935080811044,-54.6007668653704,
-54.3575059778852),.UNSPECIFIED.);
#165=B_SPLINE_CURVE_WITH_KNOTS('',3,(#16991,#16992,#16993,#16994,#16995,
#16996,#16997,#16998,#16999,#17000,#17001),.UNSPECIFIED.,.F.,.F.,(4,1,1,
1,1,1,1,1,4),(51.3882242638976,51.6225432181684,52.6152844339024,53.6080256496364,
54.6007668653704,55.5935080811044,56.5862492968384,57.5789905125724,57.6714095710771),
 .UNSPECIFIED.);
#166=B_SPLINE_CURVE_WITH_KNOTS('',3,(#17006,#17007,#17008,#17009,#17010,
#17011,#17012,#17013,#17014,#17015),.UNSPECIFIED.,.F.,.F.,(4,1,1,1,1,1,
1,4),(-66.9238707158243,-66.5136614541785,-65.5209202384445,-64.5281790227105,
-63.5354378069765,-62.5426965912425,-61.5499553755085,-60.6406912850648),
 .UNSPECIFIED.);
#167=B_SPLINE_CURVE_WITH_KNOTS('',3,(#17016,#17017,#17018,#17019,#17020,
#17021,#17022,#17023,#17024,#17025,#17026,#17027,#17028,#17029,#17030,#17031,
#17032,#17033,#17034,#17035,#17036,#17037,#17038,#17039,#17040,#17041,#17042,
#17043,#17044,#17045,#17046,#17047,#17048,#17049,#17050,#17051,#17052,#17053,
#17054,#17055,#17056,#17057,#17058,#17059,#17060,#17061,#17062,#17063,#17064,
#17065,#17066,#17067,#17068,#17069,#17070,#17071,#17072,#17073,#17074,#17075,
#17076,#17077,#17078,#17079,#17080,#17081,#17082,#17083,#17084,#17085,#17086,
#17087,#17088,#17089,#17090,#17091,#17092,#17093,#17094,#17095,#17096,#17097,
#17098,#17099,#17100,#17101,#17102,#17103,#17104,#17105,#17106,#17107,#17108,
#17109,#17110,#17111,#17112,#17113,#17114,#17115,#17116,#17117,#17118,#17119,
#17120,#17121,#17122,#17123,#17124,#17125,#17126,#17127,#17128,#17129,#17130,
#17131,#17132,#17133,#17134,#17135,#17136,#17137,#17138,#17139,#17140,#17141,
#17142,#17143,#17144,#17145,#17146,#17147,#17148,#17149,#17150,#17151,#17152,
#17153,#17154,#17155,#17156,#17157,#17158,#17159,#17160,#17161,#17162,#17163,
#17164,#17165,#17166,#17167,#17168,#17169,#17170,#17171,#17172,#17173,#17174,
#17175,#17176,#17177,#17178,#17179,#17180,#17181,#17182,#17183,#17184,#17185,
#17186,#17187),.UNSPECIFIED.,.F.,.F.,(4,3,3,3,3,3,3,3,3,3,3,3,3,3,3,3,3,
3,3,3,3,3,3,3,3,3,3,3,3,3,3,3,3,3,3,3,3,3,3,3,3,3,3,3,3,3,3,3,3,3,3,3,3,
3,3,3,3,4),(57.6714095710771,57.7839498407308,57.8958482195883,58.0076522188625,
58.1194086610543,58.2324894278674,58.3443610884006,58.4580464083536,58.5717317283065,
58.6852109053686,58.798488397958,58.9116538212356,59.0247519836798,59.1378275936667,
59.2510071602991,59.3642382437579,59.4776830318307,59.5644729440405,59.6779521211026,
59.791229613692,59.9043950369696,60.0174931994137,60.1305688094004,60.2437483760328,
60.3569794594915,60.4704242475643,60.5572141597745,60.6706933368365,60.783970829426,
60.8971362527036,61.0102344151477,61.1233100251347,61.2364895917672,61.349720675226,
61.4631654632988,61.5499553755085,61.6634345525706,61.7767120451601,61.8898774684378,
62.0029756308819,62.1160512408686,62.2292308075011,62.3424618909597,62.4559066790326,
62.5426965912425,62.6561757683045,62.7694532608939,62.8826186841715,62.9957168466155,
63.1087924566024,63.2219720232348,63.3352031066935,63.4486478947663,63.5354378069765,
63.6595194390276,63.7832273544186,63.9063594692533,63.9545948779103),
 .UNSPECIFIED.);
#168=B_SPLINE_CURVE_WITH_KNOTS('',3,(#17192,#17193,#17194,#17195,#17196,
#17197,#17198,#17199,#17200,#17201,#17202,#17203,#17204,#17205,#17206,#17207,
#17208,#17209,#17210,#17211,#17212,#17213,#17214,#17215,#17216,#17217,#17218,
#17219,#17220,#17221,#17222,#17223,#17224,#17225,#17226,#17227,#17228,#17229,
#17230,#17231,#17232,#17233,#17234,#17235,#17236,#17237,#17238,#17239,#17240,
#17241,#17242,#17243,#17244,#17245,#17246,#17247,#17248,#17249,#17250,#17251,
#17252,#17253,#17254,#17255,#17256,#17257,#17258,#17259,#17260,#17261,#17262,
#17263,#17264,#17265,#17266,#17267,#17268,#17269,#17270,#17271,#17272,#17273,
#17274,#17275,#17276,#17277,#17278,#17279,#17280,#17281,#17282,#17283,#17284,
#17285,#17286,#17287,#17288,#17289,#17290,#17291,#17292,#17293,#17294,#17295,
#17296,#17297,#17298,#17299,#17300,#17301,#17302,#17303,#17304,#17305,#17306,
#17307,#17308,#17309,#17310,#17311,#17312,#17313,#17314,#17315,#17316,#17317,
#17318,#17319,#17320,#17321,#17322,#17323,#17324,#17325,#17326,#17327,#17328,
#17329,#17330,#17331,#17332,#17333,#17334,#17335,#17336,#17337,#17338,#17339,
#17340,#17341,#17342,#17343,#17344,#17345,#17346,#17347,#17348,#17349,#17350,
#17351,#17352,#17353,#17354,#17355,#17356,#17357,#17358,#17359,#17360,#17361,
#17362,#17363),.UNSPECIFIED.,.F.,.F.,(4,3,3,3,3,3,3,3,3,3,3,3,3,3,3,3,3,
3,3,3,3,3,3,3,3,3,3,3,3,3,3,3,3,3,3,3,3,3,3,3,3,3,3,3,3,3,3,3,3,3,3,3,3,
3,3,3,3,4),(-73.207061899424,-73.0950948311733,-72.9831980604613,-72.8713249933925,
-72.7593511740308,-72.6473233814792,-72.5350916115429,-72.4701087485826,
-72.3566295715204,-72.243352078931,-72.1301866556534,-72.0170884932093,
-71.9040128832223,-71.7908333165898,-71.6776022331311,-71.5641574450583,
-71.4773675328486,-71.3638883557865,-71.250610863197,-71.1374454399194,
-71.0243472774753,-70.9112716674884,-70.798092100856,-70.6848610173971,
-70.5714162293243,-70.4846263171145,-70.3711471400525,-70.2578696474631,
-70.1447042241855,-70.0316060617414,-69.9185304517545,-69.8053508851221,
-69.6921198016633,-69.5786750135905,-69.4918851013805,-69.3784059243185,
-69.2651284317291,-69.1519630084515,-69.0388648460074,-68.9257892360203,
-68.8126096693879,-68.6993785859291,-68.5859337978563,-68.4991438856465,
-68.3856647085845,-68.272387215995,-68.1592217927174,-68.0461236302732,
-67.9330480202862,-67.8198684536538,-67.7066373701951,-67.5931925821223,
-67.5064026699125,-67.3908458947149,-67.2741035690973,-67.1589453653598,
-67.0414109788021,-66.9238765922444),.UNSPECIFIED.);
#169=B_SPLINE_CURVE_WITH_KNOTS('',3,(#17364,#17365,#17366,#17367,#17368,
#17369,#17370,#17371,#17372,#17373,#17374,#17375,#17376,#17377,#17378,#17379,
#17380,#17381,#17382,#17383,#17384,#17385,#17386,#17387,#17388,#17389,#17390,
#17391,#17392,#17393,#17394,#17395,#17396,#17397,#17398,#17399,#17400,#17401,
#17402,#17403,#17404,#17405,#17406,#17407,#17408,#17409,#17410,#17411,#17412,
#17413,#17414,#17415,#17416,#17417,#17418,#17419,#17420,#17421,#17422,#17423,
#17424,#17425,#17426,#17427,#17428,#17429,#17430,#17431,#17432,#17433,#17434,
#17435,#17436,#17437,#17438,#17439,#17440,#17441,#17442,#17443,#17444,#17445,
#17446,#17447,#17448,#17449,#17450,#17451,#17452,#17453,#17454,#17455,#17456,
#17457,#17458,#17459,#17460,#17461,#17462,#17463,#17464,#17465,#17466,#17467,
#17468,#17469,#17470,#17471,#17472,#17473,#17474,#17475,#17476,#17477,#17478,
#17479,#17480,#17481,#17482,#17483,#17484,#17485,#17486,#17487,#17488,#17489,
#17490,#17491,#17492,#17493,#17494,#17495,#17496,#17497,#17498,#17499,#17500,
#17501,#17502,#17503,#17504,#17505,#17506,#17507,#17508,#17509,#17510,#17511,
#17512,#17513,#17514,#17515,#17516,#17517,#17518,#17519,#17520,#17521,#17522,
#17523,#17524,#17525,#17526,#17527,#17528,#17529,#17530,#17531,#17532,#17533,
#17534,#17535),.UNSPECIFIED.,.F.,.F.,(4,3,3,3,3,3,3,3,3,3,3,3,3,3,3,3,3,
3,3,3,3,3,3,3,3,3,3,3,3,3,3,3,3,3,3,3,3,3,3,3,3,3,3,3,3,3,3,3,3,3,3,3,3,
3,3,3,3,4),(63.9545948782567,64.0698636722457,64.1853150539345,64.3008548231996,
64.4166721465948,64.5281790227105,64.6416581997725,64.7549356923619,64.8681011156395,
64.9811992780837,65.0942748880707,65.2074544547032,65.320685538162,65.4341303262348,
65.5209202384445,65.6343994155066,65.747676908096,65.8608423313736,65.9739404938177,
66.0870161038044,66.2001956704368,66.3134267538955,66.4268715419683,66.5136614541785,
66.6271406312406,66.74041812383,66.8535835471076,66.9666817095518,67.0797573195387,
67.1929368861711,67.3061679696299,67.4196127577027,67.5064026699125,67.6198818469747,
67.7331593395641,67.8463247628417,67.9594229252858,68.0724985352727,68.1856781019051,
68.298909185364,68.4123539734367,68.4991438856465,68.6126230627086,68.725900555298,
68.8390659785756,68.9521641410198,69.0652397510066,69.1784193176391,69.2916504010978,
69.4050951891706,69.4918851013805,69.6040236394296,69.7159996034553,69.827860005518,
69.9396848486519,70.0514850869985,70.1633755926544,70.2377801854363),
 .UNSPECIFIED.);
#170=B_SPLINE_CURVE_WITH_KNOTS('',3,(#17540,#17541,#17542,#17543,#17544,
#17545,#17546,#17547,#17548,#17549,#17550),.UNSPECIFIED.,.F.,.F.,(4,1,1,
1,1,1,1,1,4),(-79.4902472066036,-79.4192972587206,-78.4265560429866,-77.4338148272526,
-76.4410736115186,-75.4483323957846,-74.4555911800506,-73.4628499643166,
-73.2070640903504),.UNSPECIFIED.);
#171=B_SPLINE_CURVE_WITH_KNOTS('',3,(#17551,#17552,#17553,#17554,#17555,
#17556,#17557,#17558,#17559,#17560,#17561),.UNSPECIFIED.,.F.,.F.,(4,1,1,
1,1,1,1,1,4),(70.2377816044152,70.4846263171145,71.4773675328486,72.4701087485826,
73.4628499643166,74.4555911800506,75.4483323957846,76.4410736115186,76.5209654926159),
 .UNSPECIFIED.);
#172=B_SPLINE_CURVE_WITH_KNOTS('',3,(#17566,#17567,#17568,#17569,#17570,
#17571,#17572,#17573,#17574,#17575),.UNSPECIFIED.,.F.,.F.,(4,1,1,1,1,1,
1,4),(-85.7734325137832,-85.3757445531247,-84.3830033373907,-83.3902621216566,
-82.3975209059226,-81.4047796901886,-80.4120384744546,-79.4902472066036),
 .UNSPECIFIED.);
#173=B_SPLINE_CURVE_WITH_KNOTS('',3,(#17576,#17577,#17578,#17579,#17580,
#17581,#17582,#17583,#17584,#17585),.UNSPECIFIED.,.F.,.F.,(4,1,1,1,1,1,
1,4),(76.5209654926159,77.4338148272526,78.4265560429866,79.4192972587206,
80.4120384744546,81.4047796901886,82.3975209059226,82.8041447673426),
 .UNSPECIFIED.);
#174=B_SPLINE_CURVE_WITH_KNOTS('',3,(#17590,#17591,#17592,#17593,#17594,
#17595,#17596,#17597,#17598,#17599),.UNSPECIFIED.,.F.,.F.,(4,1,1,1,1,1,
1,4),(-92.0566178209628,-91.3321918475287,-90.3394506317947,-89.3467094160607,
-88.3539682003267,-87.3612269845927,-86.3684857688587,-85.7734325137832),
 .UNSPECIFIED.);
#175=B_SPLINE_CURVE_WITH_KNOTS('',3,(#17600,#17601,#17602,#17603,#17604,
#17605,#17606,#17607,#17608,#17609,#17610,#17611,#17612,#17613,#17614,#17615,
#17616,#17617,#17618,#17619,#17620,#17621,#17622,#17623,#17624,#17625,#17626,
#17627,#17628,#17629,#17630,#17631,#17632,#17633,#17634,#17635,#17636,#17637,
#17638,#17639,#17640,#17641,#17642,#17643,#17644,#17645,#17646,#17647,#17648,
#17649,#17650,#17651,#17652,#17653,#17654,#17655,#17656,#17657,#17658,#17659,
#17660,#17661,#17662,#17663,#17664,#17665,#17666,#17667,#17668,#17669,#17670,
#17671,#17672,#17673,#17674,#17675,#17676,#17677,#17678,#17679,#17680,#17681,
#17682,#17683,#17684,#17685,#17686,#17687,#17688,#17689,#17690,#17691,#17692,
#17693,#17694,#17695,#17696,#17697,#17698,#17699,#17700,#17701,#17702,#17703,
#17704,#17705,#17706,#17707,#17708,#17709,#17710,#17711,#17712,#17713,#17714,
#17715,#17716,#17717,#17718,#17719,#17720,#17721,#17722,#17723,#17724,#17725,
#17726,#17727,#17728,#17729,#17730,#17731,#17732,#17733,#17734,#17735,#17736,
#17737,#17738,#17739,#17740,#17741,#17742,#17743,#17744,#17745,#17746,#17747,
#17748,#17749,#17750,#17751,#17752,#17753,#17754,#17755,#17756,#17757,#17758,
#17759,#17760,#17761,#17762,#17763,#17764,#17765,#17766,#17767,#17768,#17769,
#17770,#17771),.UNSPECIFIED.,.F.,.F.,(4,3,3,3,3,3,3,3,3,3,3,3,3,3,3,3,3,
3,3,3,3,3,3,3,3,3,3,3,3,3,3,3,3,3,3,3,3,3,3,3,3,3,3,3,3,3,3,3,3,3,3,3,3,
3,3,3,3,4),(82.8041507997955,82.9190225628796,83.0368324525739,83.1519469049723,
83.2711045133145,83.3902621216566,83.5037412987187,83.6170187913081,83.7301842145858,
83.8432823770299,83.9563579870168,84.0695375536493,84.1827686371081,84.296213425181,
84.3830033373907,84.4964825144529,84.6097600070423,84.7229254303199,84.836023592764,
84.9490992027509,85.0622787693834,85.1755098528421,85.2889546409149,85.3757445531247,
85.4892237301868,85.6025012227762,85.7156666460537,85.8287648084979,85.9418404184848,
86.0550199851172,86.168251068576,86.2816958566488,86.3684857688587,86.4819649459207,
86.5952424385102,86.7084078617878,86.8215060242319,86.9345816342187,87.0477612008512,
87.1609922843099,87.2744370723827,87.3612269845927,87.4747061616548,87.5879836542442,
87.7011490775218,87.8142472399659,87.9273228499528,88.0405024165852,88.1537335000438,
88.2671782881166,88.3539682003267,88.4662367419805,88.5783413179202,88.6903287715849,
88.8022749438312,88.914195125773,89.0261943465739,89.0873361069751),
 .UNSPECIFIED.);
#176=B_SPLINE_CURVE_WITH_KNOTS('',3,(#17776,#17777,#17778,#17779,#17780,
#17781,#17782,#17783,#17784,#17785,#17786,#17787,#17788,#17789,#17790,#17791,
#17792,#17793,#17794,#17795,#17796,#17797,#17798,#17799,#17800,#17801,#17802,
#17803,#17804,#17805,#17806,#17807,#17808,#17809,#17810,#17811,#17812,#17813,
#17814,#17815,#17816,#17817,#17818,#17819,#17820,#17821,#17822,#17823,#17824,
#17825,#17826,#17827,#17828,#17829,#17830,#17831,#17832,#17833,#17834,#17835,
#17836,#17837,#17838,#17839,#17840,#17841,#17842,#17843,#17844,#17845,#17846,
#17847,#17848,#17849,#17850,#17851,#17852,#17853,#17854,#17855,#17856,#17857,
#17858,#17859,#17860,#17861,#17862,#17863,#17864,#17865,#17866,#17867,#17868,
#17869,#17870,#17871,#17872,#17873,#17874,#17875,#17876,#17877,#17878,#17879,
#17880,#17881,#17882,#17883,#17884,#17885,#17886,#17887,#17888,#17889,#17890,
#17891,#17892,#17893,#17894,#17895,#17896,#17897,#17898,#17899,#17900,#17901,
#17902,#17903,#17904,#17905,#17906,#17907,#17908,#17909,#17910,#17911,#17912,
#17913,#17914,#17915,#17916,#17917,#17918,#17919,#17920,#17921,#17922,#17923,
#17924,#17925,#17926,#17927,#17928,#17929,#17930,#17931,#17932,#17933,#17934,
#17935,#17936,#17937,#17938,#17939,#17940,#17941,#17942,#17943,#17944,#17945,
#17946,#17947),.UNSPECIFIED.,.F.,.F.,(4,3,3,3,3,3,3,3,3,3,3,3,3,3,3,3,3,
3,3,3,3,3,3,3,3,3,3,3,3,3,3,3,3,3,3,3,3,3,3,3,3,3,3,3,3,3,3,3,3,3,3,3,3,
3,3,3,3,4),(-98.3398031281424,-98.2813803576668,-98.1679011806047,-98.0546236880152,
-97.9414582647376,-97.8283601022934,-97.7152844923065,-97.602104925674,
-97.4888738422151,-97.3754290541423,-97.2886391419328,-97.1751599648707,
-97.0618824722813,-96.9487170490037,-96.8356188865595,-96.7225432765726,
-96.6093637099401,-96.4961326264813,-96.3826878384085,-96.2958979261987,
-96.1824187491366,-96.0691412565472,-95.9559758332696,-95.8428776708254,
-95.7298020608385,-95.616622494206,-95.5033914107472,-95.3899466226744,
-95.3031567104647,-95.1896775334027,-95.0764000408133,-94.9632346175357,
-94.8501364550915,-94.7370608451047,-94.6238812784722,-94.5106501950134,
-94.3972054069406,-94.3104154947307,-94.1969363176686,-94.0836588250792,
-93.9704934018016,-93.8573952393575,-93.7443196293706,-93.6311400627381,
-93.5179089792793,-93.4044641912065,-93.3176742789967,-93.2041951019346,
-93.0909176093452,-92.9777521860676,-92.8646540236235,-92.7515784136366,
-92.6383988470042,-92.5251677635454,-92.4117229754726,-92.3249330632627,
-92.182832718097,-92.0566180325444),.UNSPECIFIED.);
#177=B_SPLINE_CURVE_WITH_KNOTS('',3,(#17948,#17949,#17950,#17951,#17952,
#17953,#17954,#17955,#17956,#17957,#17958,#17959,#17960,#17961,#17962,#17963,
#17964,#17965,#17966,#17967,#17968,#17969,#17970,#17971,#17972,#17973,#17974,
#17975,#17976,#17977,#17978,#17979,#17980,#17981,#17982,#17983,#17984,#17985,
#17986,#17987,#17988,#17989,#17990,#17991,#17992,#17993,#17994,#17995,#17996,
#17997,#17998,#17999,#18000,#18001,#18002,#18003,#18004,#18005,#18006,#18007,
#18008,#18009,#18010,#18011,#18012,#18013,#18014,#18015,#18016,#18017,#18018,
#18019,#18020,#18021,#18022,#18023,#18024,#18025,#18026,#18027,#18028,#18029,
#18030,#18031,#18032,#18033,#18034,#18035,#18036,#18037,#18038,#18039,#18040,
#18041,#18042,#18043,#18044,#18045,#18046,#18047,#18048,#18049,#18050,#18051,
#18052,#18053,#18054,#18055,#18056,#18057,#18058,#18059,#18060,#18061,#18062,
#18063,#18064,#18065,#18066,#18067,#18068,#18069,#18070,#18071,#18072,#18073,
#18074,#18075,#18076,#18077,#18078,#18079,#18080,#18081,#18082,#18083,#18084,
#18085,#18086,#18087,#18088,#18089,#18090,#18091,#18092,#18093,#18094,#18095,
#18096,#18097,#18098,#18099,#18100,#18101,#18102,#18103,#18104,#18105,#18106,
#18107,#18108,#18109,#18110,#18111,#18112,#18113,#18114,#18115,#18116,#18117,
#18118,#18119),.UNSPECIFIED.,.F.,.F.,(4,3,3,3,3,3,3,3,3,3,3,3,3,3,3,3,3,
3,3,3,3,3,3,3,3,3,3,3,3,3,3,3,3,3,3,3,3,3,3,3,3,3,3,3,3,3,3,3,3,3,3,3,3,
3,3,3,3,4),(89.0873361076021,89.2312652478392,89.3467094160607,89.4601885931227,
89.5734660857121,89.6866315089897,89.7997296714338,89.9128052814207,90.0259848480531,
90.1392159315119,90.2526607195846,90.3394506317947,90.4529298088568,90.5662073014462,
90.6793727247238,90.792470887168,90.9055464971549,91.0187260637874,91.1319571472462,
91.245401935319,91.3321918475287,91.4456710245907,91.5589485171802,91.6721139404578,
91.7852121029019,91.8982877128888,92.0114672795212,92.12469836298,92.2381431510528,
92.3249330632627,92.4384122403248,92.5516897329142,92.6648551561918,92.777953318636,
92.8910289286228,93.0042084952553,93.1174395787141,93.2308843667869,93.3176742789967,
93.4311534560588,93.5444309486482,93.6575963719258,93.7706945343699,93.8837701443568,
93.9969497109893,94.1101807944481,94.2236255825209,94.3104154947307,94.4238946717928,
94.5371721643822,94.6503375876597,94.7634357501038,94.8765113600907,94.9896909267232,
95.1029220101819,95.2163667982547,95.3031567104647,95.3705214141547),
 .UNSPECIFIED.);
#178=B_SPLINE_CURVE_WITH_KNOTS('',3,(#18124,#18125,#18126,#18127,#18128,
#18129,#18130,#18131,#18132,#18133),.UNSPECIFIED.,.F.,.F.,(4,1,1,1,1,1,
1,4),(-104.622988435322,-104.237827652071,-103.245086436337,-102.252345220603,
-101.259604004869,-100.266862789135,-99.2741215734008,-98.3398097557481),
 .UNSPECIFIED.);
#179=B_SPLINE_CURVE_WITH_KNOTS('',3,(#18134,#18135,#18136,#18137,#18138,
#18139,#18140,#18141,#18142,#18143),.UNSPECIFIED.,.F.,.F.,(4,1,1,1,1,1,
1,4),(95.3705286189736,96.2958979261987,97.2886391419327,98.2813803576667,
99.2741215734008,100.266862789135,101.259604004869,101.653706721334),
 .UNSPECIFIED.);
#180=B_SPLINE_CURVE_WITH_KNOTS('',3,(#18148,#18149,#18150,#18151,#18152,
#18153,#18154,#18155,#18156,#18157),.UNSPECIFIED.,.F.,.F.,(4,1,1,1,1,1,
1,4),(-110.906173742502,-110.194274946475,-109.201533730741,-108.208792515007,
-107.216051299273,-106.223310083539,-105.230568867805,-104.622988435322),
 .UNSPECIFIED.);
#181=B_SPLINE_CURVE_WITH_KNOTS('',3,(#18158,#18159,#18160,#18161,#18162,
#18163,#18164,#18165,#18166,#18167),.UNSPECIFIED.,.F.,.F.,(4,1,1,1,1,1,
1,4),(101.653706721334,102.252345220603,103.245086436337,104.237827652071,
105.230568867805,106.223310083539,107.216051299273,107.936892028514),
 .UNSPECIFIED.);
#182=B_SPLINE_CURVE_WITH_KNOTS('',3,(#18172,#18173,#18174,#18175,#18176,
#18177,#18178,#18179,#18180,#18181,#18182),.UNSPECIFIED.,.F.,.F.,(4,1,1,
1,1,1,1,1,4),(-117.189359049681,-117.143463456613,-116.150722240879,-115.157981025145,
-114.165239809411,-113.172498593677,-112.179757377943,-111.187016162209,
-110.906173742502),.UNSPECIFIED.);
#183=B_SPLINE_CURVE_WITH_KNOTS('',3,(#18183,#18184,#18185,#18186,#18187,
#18188,#18189,#18190,#18191,#18192,#18193,#18194,#18195,#18196,#18197,#18198,
#18199,#18200,#18201,#18202,#18203,#18204,#18205,#18206,#18207,#18208,#18209,
#18210,#18211,#18212,#18213,#18214,#18215,#18216,#18217,#18218,#18219,#18220,
#18221,#18222,#18223,#18224,#18225,#18226,#18227,#18228,#18229,#18230,#18231,
#18232,#18233,#18234,#18235,#18236,#18237,#18238,#18239,#18240,#18241,#18242,
#18243,#18244,#18245,#18246,#18247,#18248,#18249,#18250,#18251,#18252,#18253,
#18254,#18255,#18256,#18257,#18258,#18259,#18260,#18261,#18262,#18263,#18264,
#18265,#18266,#18267,#18268,#18269,#18270,#18271,#18272,#18273,#18274,#18275,
#18276,#18277,#18278,#18279,#18280,#18281,#18282,#18283,#18284,#18285,#18286,
#18287,#18288,#18289,#18290,#18291,#18292,#18293,#18294,#18295,#18296,#18297,
#18298,#18299,#18300,#18301,#18302,#18303,#18304,#18305,#18306,#18307,#18308,
#18309,#18310,#18311,#18312,#18313,#18314,#18315,#18316,#18317,#18318,#18319,
#18320,#18321,#18322,#18323,#18324,#18325,#18326,#18327,#18328,#18329,#18330,
#18331,#18332,#18333,#18334,#18335,#18336,#18337,#18338,#18339,#18340,#18341,
#18342,#18343,#18344,#18345,#18346,#18347,#18348,#18349,#18350,#18351,#18352,
#18353,#18354),.UNSPECIFIED.,.F.,.F.,(4,3,3,3,3,3,3,3,3,3,3,3,3,3,3,3,3,
3,3,3,3,3,3,3,3,3,3,3,3,3,3,3,3,3,3,3,3,3,3,3,3,3,3,3,3,3,3,3,3,3,3,3,3,
3,3,3,3,4),(107.936892258894,108.078296789096,108.208792515007,108.322271691942,
108.435549184406,108.548714607559,108.661812769879,108.774888379744,108.888067946257,
109.001299029598,109.114743817557,109.201533730741,109.315012907634,109.428290400052,
109.541455823156,109.654553985425,109.767629595236,109.880809161693,109.994040244975,
110.107485032873,110.194274946475,110.307754124348,110.421031617749,110.534197041838,
110.647295205093,110.760370815887,110.873550383317,110.986781467567,111.100226256415,
111.187016162209,111.300495338197,111.413772829721,111.526938251939,111.640036413331,
111.753112022276,111.866291587889,111.979522670339,112.092967457434,112.179757377943,
112.293236554304,112.406514046172,112.519679468715,112.632777630414,112.745853239646,
112.859032805516,112.972263888206,113.08570867551,113.172498593677,113.28597777608,
113.399255274024,113.512420702661,113.625518870459,113.738594485786,113.851774057693,
113.965005146398,114.078449939607,114.165239809411,114.220077335693),
 .UNSPECIFIED.);
#184=B_SPLINE_CURVE_WITH_KNOTS('',3,(#18359,#18360,#18361,#18362,#18363,
#18364,#18365,#18366,#18367,#18368,#18369,#18370,#18371,#18372,#18373,#18374,
#18375,#18376,#18377,#18378,#18379,#18380,#18381,#18382,#18383,#18384,#18385,
#18386,#18387,#18388,#18389,#18390,#18391,#18392,#18393,#18394,#18395,#18396,
#18397,#18398,#18399,#18400,#18401,#18402,#18403,#18404,#18405,#18406,#18407,
#18408,#18409,#18410,#18411,#18412,#18413,#18414,#18415,#18416,#18417,#18418,
#18419,#18420,#18421,#18422,#18423,#18424,#18425,#18426,#18427,#18428,#18429,
#18430,#18431,#18432,#18433,#18434,#18435,#18436,#18437,#18438,#18439,#18440,
#18441,#18442,#18443,#18444,#18445,#18446,#18447,#18448,#18449,#18450,#18451,
#18452,#18453,#18454,#18455,#18456,#18457,#18458,#18459,#18460,#18461,#18462,
#18463,#18464,#18465,#18466,#18467,#18468,#18469,#18470,#18471,#18472,#18473,
#18474,#18475,#18476,#18477,#18478,#18479,#18480,#18481,#18482,#18483,#18484,
#18485,#18486,#18487,#18488,#18489,#18490,#18491,#18492,#18493,#18494,#18495,
#18496,#18497,#18498,#18499,#18500,#18501,#18502,#18503,#18504,#18505,#18506,
#18507,#18508,#18509,#18510,#18511,#18512,#18513,#18514,#18515,#18516,#18517,
#18518,#18519,#18520,#18521,#18522,#18523,#18524,#18525,#18526,#18527,#18528,
#18529,#18530),.UNSPECIFIED.,.F.,.F.,(4,3,3,3,3,3,3,3,3,3,3,3,3,3,3,3,3,
3,3,3,3,3,3,3,3,3,3,3,3,3,3,3,3,3,3,3,3,3,3,3,3,3,3,3,3,3,3,3,3,3,3,3,3,
3,3,3,3,4),(-123.472543894631,-123.345471929838,-123.217419424173,-123.099910751017,
-122.986430351432,-122.873151618431,-122.759984944753,-122.646885524206,
-122.533808650684,-122.420627822239,-122.307395475983,-122.193949439312,
-122.107169535283,-121.993690164857,-121.880412467451,-121.767246832498,
-121.654148451904,-121.541072617666,-121.427892819067,-121.314661498998,
-121.2012164696,-121.114428319549,-121.000949591505,-120.887672559457,-120.774507603421,
-120.661409914069,-120.548334782179,-120.435155697601,-120.321925099137,
-120.208480794843,-120.121687103815,-120.008207722219,-119.89493002164,
-119.781764388419,-119.66866601446,-119.555590191769,-119.442410412291,
-119.329179115581,-119.215734116259,-119.128945888081,-119.015466704413,
-118.902189204017,-118.789023772204,-118.675925600509,-118.562849980572,
-118.449670402976,-118.336439307975,-118.222994507545,-118.136204672347,
-118.017848969514,-117.905379929234,-117.793018557627,-117.680718733564,
-117.568434433619,-117.45604635478,-117.343597808392,-117.230956823491,
-117.189359049681),.UNSPECIFIED.);
#185=B_SPLINE_CURVE_WITH_KNOTS('',3,(#18531,#18532,#18533,#18534,#18535,
#18536,#18537,#18538,#18539,#18540,#18541,#18542,#18543,#18544,#18545,#18546,
#18547,#18548,#18549,#18550,#18551,#18552,#18553,#18554,#18555,#18556,#18557,
#18558,#18559,#18560,#18561,#18562,#18563,#18564,#18565,#18566,#18567,#18568,
#18569,#18570,#18571,#18572,#18573,#18574,#18575,#18576,#18577,#18578,#18579,
#18580,#18581,#18582,#18583,#18584,#18585,#18586,#18587,#18588,#18589,#18590,
#18591,#18592,#18593,#18594,#18595,#18596,#18597,#18598,#18599,#18600,#18601,
#18602,#18603,#18604,#18605,#18606,#18607,#18608,#18609,#18610,#18611,#18612,
#18613,#18614,#18615,#18616,#18617,#18618,#18619,#18620,#18621,#18622,#18623,
#18624,#18625,#18626,#18627,#18628,#18629,#18630,#18631,#18632,#18633,#18634,
#18635,#18636,#18637,#18638,#18639,#18640,#18641,#18642,#18643,#18644,#18645,
#18646,#18647,#18648,#18649,#18650,#18651,#18652,#18653,#18654,#18655,#18656,
#18657,#18658,#18659,#18660,#18661,#18662,#18663,#18664,#18665,#18666,#18667,
#18668,#18669,#18670,#18671,#18672,#18673,#18674,#18675,#18676,#18677,#18678,
#18679,#18680,#18681,#18682,#18683,#18684,#18685,#18686,#18687,#18688,#18689,
#18690,#18691,#18692,#18693,#18694,#18695,#18696,#18697,#18698,#18699,#18700,
#18701,#18702),.UNSPECIFIED.,.F.,.F.,(4,3,3,3,3,3,3,3,3,3,3,3,3,3,3,3,3,
3,3,3,3,3,3,3,3,3,3,3,3,3,3,3,3,3,3,3,3,3,3,3,3,3,3,3,3,3,3,3,3,3,3,3,3,
3,3,3,3,4),(114.220077336354,114.337315297453,114.449646955625,114.561876294682,
114.674049601546,114.786213071814,114.898486989919,115.010826666534,115.123361222514,
115.157981025145,115.27146020069,115.384737691613,115.497903113135,115.611001273738,
115.724076881802,115.837256446402,115.950487527766,116.063932313667,116.150722240879,
116.26420145208,116.377478978945,116.490644436556,116.60374263333,116.716818277582,
116.829997878109,116.943228995308,117.056673816448,117.143463456613,117.256942568207,
117.370219995584,117.483385353854,117.596483451607,117.709558997331,117.822738500867,
117.935969521779,118.049414248978,118.136204672347,118.249683861986,118.362961366126,
118.476126800321,118.589224973036,118.702300592636,118.815480167802,118.928711259209,
119.042156054185,119.128945888081,119.24242527583,119.355702980313,119.468868616061,
119.581966991173,119.695042813645,119.808222590789,119.921453883988,120.034898877917,
120.121687103815,120.249019489535,120.376140840035,120.503262190536),
 .UNSPECIFIED.);
#186=B_SPLINE_CURVE_WITH_KNOTS('',3,(#18707,#18708,#18709,#18710,#18711,
#18712,#18713,#18714,#18715,#18716),.UNSPECIFIED.,.F.,.F.,(4,1,1,1,1,1,
1,4),(-129.75572966404,-129.056358045421,-128.063616829687,-127.070875613953,
-126.078134398219,-125.085393182485,-124.092651966751,-123.472544356861),
 .UNSPECIFIED.);
#187=B_SPLINE_CURVE_WITH_KNOTS('',3,(#18717,#18718,#18719,#18720,#18721,
#18722,#18723,#18724,#18725,#18726),.UNSPECIFIED.,.F.,.F.,(4,1,1,1,1,1,
1,4),(120.503262642873,121.114428319549,122.107169535283,123.099910751017,
124.092651966751,125.085393182485,126.078134398219,126.786447950053),
 .UNSPECIFIED.);
#188=B_SPLINE_CURVE_WITH_KNOTS('',3,(#18729,#18730,#18731,#18732,#18733,
#18734,#18735,#18736,#18737),.UNSPECIFIED.,.F.,.F.,(4,1,1,1,1,1,4),(126.786447950053,
127.070875613953,128.063616829687,129.056358045421,130.049099261155,131.041840476889,
131.946449082288),.UNSPECIFIED.);
#189=B_SPLINE_CURVE_WITH_KNOTS('',3,(#18740,#18741,#18742,#18743,#18744,
#18745,#18746,#18747),.UNSPECIFIED.,.F.,.F.,(4,1,1,1,1,4),(-134.020064124091,
-133.027322908357,-132.034581692623,-131.041840476889,-130.049099261155,
-129.75572966404),.UNSPECIFIED.);
#190=B_SPLINE_CURVE_WITH_KNOTS('',3,(#18750,#18751,#18752,#18753,#18754,
#18755,#18756,#18757,#18758,#18759,#18760,#18761,#18762,#18763,#18764,#18765,
#18766,#18767,#18768,#18769,#18770,#18771,#18772,#18773,#18774,#18775,#18776,
#18777,#18778,#18779,#18780,#18781,#18782,#18783,#18784,#18785,#18786,#18787,
#18788,#18789,#18790,#18791,#18792,#18793,#18794,#18795,#18796,#18797,#18798,
#18799,#18800,#18801,#18802,#18803,#18804,#18805,#18806,#18807,#18808,#18809,
#18810,#18811,#18812,#18813,#18814,#18815,#18816,#18817,#18818,#18819,#18820,
#18821,#18822,#18823,#18824,#18825,#18826,#18827,#18828,#18829,#18830,#18831,
#18832,#18833,#18834,#18835,#18836,#18837,#18838,#18839,#18840,#18841,#18842,
#18843,#18844,#18845,#18846,#18847,#18848,#18849,#18850,#18851,#18852,#18853,
#18854,#18855,#18856,#18857,#18858,#18859,#18860,#18861,#18862,#18863,#18864,
#18865,#18866,#18867,#18868,#18869,#18870,#18871,#18872,#18873,#18874,#18875,
#18876,#18877,#18878,#18879,#18880,#18881,#18882,#18883,#18884,#18885,#18886,
#18887,#18888,#18889,#18890,#18891,#18892,#18893,#18894,#18895,#18896,#18897,
#18898,#18899,#18900,#18901,#18902,#18903,#18904,#18905,#18906,#18907,#18908,
#18909,#18910,#18911,#18912,#18913,#18914,#18915,#18916,#18917,#18918,#18919,
#18920,#18921,#18922,#18923,#18924,#18925,#18926,#18927,#18928,#18929,#18930,
#18931,#18932,#18933,#18934,#18935,#18936,#18937,#18938,#18939,#18940,#18941,
#18942,#18943,#18944,#18945,#18946,#18947,#18948,#18949,#18950,#18951,#18952,
#18953,#18954,#18955,#18956,#18957,#18958,#18959,#18960,#18961,#18962,#18963,
#18964,#18965,#18966,#18967,#18968,#18969),.UNSPECIFIED.,.F.,.F.,(4,2,2,
2,2,2,2,2,2,2,2,2,2,2,2,2,2,2,2,2,2,2,2,2,2,2,2,2,2,2,2,2,2,2,2,2,2,2,2,
2,2,2,2,2,2,2,2,2,2,2,2,2,2,2,2,2,2,2,2,2,2,2,2,2,2,2,2,2,2,2,2,2,2,2,2,
2,2,2,2,2,2,2,2,2,2,2,2,2,2,2,2,2,2,2,2,2,2,2,2,2,2,2,2,2,2,2,2,2,2,4),
(0.00177133348906076,0.0332939428224796,0.0446468589001284,0.0476492977162608,
0.0494853420994853,0.0511583358113068,0.0532949673361036,0.0578790368847078,
0.0813213073966685,0.0895856412014572,0.0990580205537023,0.102622914444339,
0.105242464183177,0.106418036567059,0.106425319281184,0.106432688952577,
0.106440148378348,0.106447700458387,0.106455348206415,0.106463094739559,
0.106470943300493,0.106478897255693,0.10648696010216,0.106495135472981,
0.106503427147395,0.106511839057682,0.106520375300179,0.10652904013602,
0.106537838004738,0.106546773541824,0.106555851576764,0.106565077148689,
0.106574455519887,0.106583992185623,0.106593692889877,0.106603563639179,
0.106613610715625,0.106623840698047,0.10663426047506,0.106644877266566,
0.106655698639468,0.106666732539314,0.10667798730311,0.106686051022993,
0.10669489762429,0.106704614123707,0.106715299378267,0.106727066141351,
0.106740043560568,0.106754380232775,0.106770247990901,0.10678784660648,
0.106807409704104,0.106829212253955,0.106853419150707,0.106897105788926,
0.107816294099124,0.109081163064197,0.111910851100339,0.135116451326652,
0.158532048225741,0.162482297374512,0.164503661603351,0.166142589934801,
0.168029653860336,0.17125042402507,0.184976326644695,0.208927063192172,
0.220978798931431,0.222978304221318,0.224059923343987,0.224972713857167,
0.226139316161746,0.228029587104807,0.240500208304931,0.261844348980189,
0.277340634958833,0.280555592843824,0.282408559802314,0.284028276391786,
0.286039067649986,0.289152481512839,0.308939925241119,0.335665513235547,
0.339541664253455,0.340941482759423,0.341887494004219,0.342746628886886,
0.343931091601083,0.346949519411781,0.366240512633496,0.384771895284079,
0.395407454452054,0.398321699095411,0.400120964557772,0.401771292687552,
0.403893311497895,0.408498954083469,0.433359934700143,0.44083891144931,
0.454104461318418,0.456976778935707,0.458230446940733,0.459157967202875,
0.460195667052555,0.461989925851204,0.468838101212243,0.475410570919698,
0.50070097981199,0.500726922102148),.UNSPECIFIED.);
#191=B_SPLINE_CURVE_WITH_KNOTS('',3,(#18973,#18974,#18975,#18976,#18977,
#18978,#18979,#18980,#18981,#18982,#18983,#18984,#18985,#18986,#18987,#18988,
#18989,#18990,#18991,#18992,#18993,#18994,#18995,#18996,#18997),
 .UNSPECIFIED.,.F.,.F.,(4,3,3,3,3,3,3,3,4),(141.371669412113,141.493776626037,
141.615676098753,141.737414642623,141.859038816202,141.980634322619,142.102203953115,
142.223875192913,142.322100278399),.UNSPECIFIED.);
#192=B_SPLINE_CURVE_WITH_KNOTS('',3,(#18998,#18999,#19000,#19001,#19002,
#19003,#19004,#19005,#19006,#19007,#19008,#19009,#19010,#19011,#19012,#19013,
#19014,#19015,#19016,#19017,#19018,#19019,#19020,#19021,#19022,#19023,#19024,
#19025,#19026,#19027,#19028,#19029,#19030,#19031,#19032,#19033,#19034,#19035,
#19036,#19037,#19038,#19039,#19040,#19041,#19042,#19043,#19044,#19045,#19046,
#19047,#19048,#19049,#19050,#19051,#19052,#19053,#19054,#19055,#19056,#19057,
#19058),.UNSPECIFIED.,.F.,.F.,(4,3,3,3,3,3,3,3,3,3,3,3,3,3,3,3,3,3,3,3,
4),(139.325819053623,139.343876631197,139.467969283164,139.587740756953,
139.707395900858,139.826987018576,139.946566302737,140.066267437187,140.186042193601,
140.306031049809,140.336617846931,140.460710498898,140.578991514728,140.697156542209,
140.815260477709,140.933358102547,141.051596289664,141.16991700588,141.288479603891,
141.329359062665,141.371669411541),.UNSPECIFIED.);
#193=B_SPLINE_CURVE_WITH_KNOTS('',3,(#19611,#19612,#19613,#19614,#19615,
#19616,#19617,#19618,#19619,#19620,#19621,#19622,#19623,#19624,#19625,#19626,
#19627,#19628,#19629,#19630,#19631,#19632,#19633,#19634,#19635,#19636,#19637,
#19638,#19639,#19640,#19641,#19642,#19643,#19644,#19645,#19646,#19647,#19648,
#19649,#19650,#19651,#19652,#19653,#19654,#19655,#19656,#19657,#19658,#19659,
#19660,#19661,#19662,#19663,#19664,#19665,#19666,#19667,#19668,#19669,#19670,
#19671,#19672,#19673,#19674,#19675,#19676,#19677,#19678,#19679,#19680,#19681,
#19682,#19683,#19684,#19685,#19686,#19687,#19688,#19689),.UNSPECIFIED.,
 .F.,.F.,(4,3,3,3,3,3,3,3,3,3,3,3,3,3,3,3,3,3,3,3,3,3,3,3,3,3,4),(0.,0.0128630913698734,
0.030173607454054,0.0476766315161026,0.0523696650465307,0.0555715997243662,
0.0588510993424858,0.0758834917292733,0.0926337870888054,0.10745987033467,
0.111898493425318,0.128068424972759,0.144019690384188,0.151482256100753,
0.158624488771535,0.162483307325829,0.16875922376809,0.184724176101981,
0.200705370878488,0.205805249761507,0.211151080047986,0.214604616888512,
0.230111410594562,0.242198197870331,0.246866765408764,0.261749278560737,
0.27663179171271),.UNSPECIFIED.);
#194=B_SPLINE_CURVE_WITH_KNOTS('',3,(#19691,#19692,#19693,#19694,#19695,
#19696,#19697,#19698,#19699,#19700,#19701,#19702,#19703,#19704,#19705,#19706,
#19707,#19708,#19709,#19710,#19711,#19712,#19713,#19714,#19715,#19716,#19717,
#19718,#19719,#19720,#19721,#19722,#19723,#19724,#19725,#19726,#19727,#19728,
#19729,#19730,#19731,#19732,#19733,#19734,#19735,#19736,#19737,#19738,#19739,
#19740,#19741,#19742,#19743,#19744,#19745,#19746,#19747,#19748,#19749,#19750,
#19751,#19752,#19753,#19754,#19755,#19756,#19757,#19758,#19759,#19760,#19761,
#19762,#19763,#19764,#19765,#19766,#19767,#19768,#19769),.UNSPECIFIED.,
 .F.,.F.,(4,3,3,3,3,3,3,3,3,3,3,3,3,3,3,3,3,3,3,3,3,3,3,3,3,3,4),(0.,0.0104682740580808,
0.0251836130964161,0.0388969524160199,0.0444857430892301,0.0491054717138812,
0.0584413971085396,0.0740336439398356,0.0898096170712714,0.0952778368687677,
0.0982274123820461,0.114504809333193,0.130605059063041,0.136378173267175,
0.141969801169779,0.145794135544524,0.148768119797174,0.16481698689922,
0.181420617025118,0.198000402839796,0.201209381411116,0.218350668985889,
0.232526805791533,0.236420955594387,0.242939799192087,0.260349393962725,
0.275362278356888),.UNSPECIFIED.);
#195=B_SPLINE_CURVE_WITH_KNOTS('',3,(#19770,#19771,#19772,#19773),
 .UNSPECIFIED.,.F.,.F.,(4,4),(-0.01194426971835,0.),.UNSPECIFIED.);
#196=B_SPLINE_CURVE_WITH_KNOTS('',3,(#20327,#20328,#20329,#20330,#20331,
#20332,#20333,#20334,#20335,#20336,#20337,#20338,#20339,#20340,#20341,#20342,
#20343,#20344,#20345,#20346,#20347,#20348,#20349,#20350,#20351,#20352,#20353,
#20354,#20355,#20356,#20357,#20358,#20359,#20360,#20361,#20362,#20363,#20364,
#20365,#20366,#20367,#20368,#20369,#20370,#20371,#20372,#20373,#20374,#20375,
#20376,#20377,#20378,#20379,#20380,#20381,#20382,#20383,#20384,#20385,#20386,
#20387,#20388,#20389,#20390,#20391,#20392,#20393,#20394,#20395,#20396,#20397,
#20398,#20399,#20400,#20401,#20402,#20403,#20404,#20405),.UNSPECIFIED.,
 .F.,.F.,(4,3,3,3,3,3,3,3,3,3,3,3,3,3,3,3,3,3,3,3,3,3,3,3,3,3,4),(0.,0.0104682740580829,
0.0250094730845676,0.0400379756695705,0.0464362531658784,0.0494477396468055,
0.0648452005482684,0.0806255921987773,0.0952778402954169,0.0982274132155018,
0.114504810108782,0.130605060062163,0.136378173267178,0.141969800959009,
0.145794134531399,0.148768118134835,0.164776942997393,0.181333154791539,
0.193217549992342,0.198000400400437,0.201209379964382,0.218350667946125,
0.232526805152432,0.236420954197035,0.24018725862019,0.257774768488541,
0.275362278356893),.UNSPECIFIED.);
#197=B_SPLINE_CURVE_WITH_KNOTS('',3,(#20406,#20407,#20408,#20409),
 .UNSPECIFIED.,.F.,.F.,(4,4),(0.,0.0121610650312646),.UNSPECIFIED.);
#198=B_SPLINE_CURVE_WITH_KNOTS('',3,(#20410,#20411,#20412,#20413,#20414,
#20415,#20416,#20417,#20418,#20419,#20420,#20421,#20422,#20423,#20424,#20425,
#20426,#20427,#20428,#20429,#20430,#20431,#20432,#20433,#20434,#20435,#20436,
#20437,#20438,#20439,#20440,#20441,#20442,#20443,#20444,#20445,#20446,#20447,
#20448,#20449,#20450,#20451,#20452,#20453,#20454,#20455,#20456,#20457,#20458,
#20459,#20460,#20461,#20462,#20463,#20464,#20465,#20466,#20467,#20468,#20469,
#20470,#20471,#20472,#20473,#20474,#20475,#20476,#20477,#20478,#20479,#20480,
#20481,#20482),.UNSPECIFIED.,.F.,.F.,(4,3,3,3,3,3,3,3,3,3,3,3,3,3,3,3,3,
3,3,3,3,3,3,3,4),(0.,0.0128630913698816,0.0301736075898532,0.0476766317653969,
0.0523696653091531,0.0557875908672854,0.0588510996533798,0.0758834920598313,
0.0926337883448894,0.107459871004135,0.111898493425658,0.128218441979264,
0.144019692909864,0.151482256100771,0.160181367556473,0.163702575469109,
0.179617427500875,0.195596970381227,0.211151080173894,0.214604616819749,
0.230040863840438,0.242198197759019,0.246866765353746,0.261749278533234,
0.276631791712723),.UNSPECIFIED.);
#350=SHAPE_REPRESENTATION_RELATIONSHIP('SRR','None',#40771,#358);
#358=ADVANCED_BREP_SHAPE_REPRESENTATION('',(#376),#40731);
#367=STYLED_ITEM('',(#40815),#376);
#376=MANIFOLD_SOLID_BREP('Body1',#3172);
#415=PLANE('',#3400);
#416=PLANE('',#3401);
#473=FACE_OUTER_BOUND('',#641,.T.);
#474=FACE_OUTER_BOUND('',#642,.T.);
#475=FACE_OUTER_BOUND('',#643,.T.);
#476=FACE_OUTER_BOUND('',#644,.T.);
#477=FACE_OUTER_BOUND('',#645,.T.);
#478=FACE_OUTER_BOUND('',#646,.T.);
#479=FACE_OUTER_BOUND('',#647,.T.);
#480=FACE_OUTER_BOUND('',#648,.T.);
#481=FACE_OUTER_BOUND('',#649,.T.);
#482=FACE_OUTER_BOUND('',#650,.T.);
#483=FACE_OUTER_BOUND('',#651,.T.);
#484=FACE_OUTER_BOUND('',#652,.T.);
#485=FACE_OUTER_BOUND('',#653,.T.);
#486=FACE_OUTER_BOUND('',#654,.T.);
#487=FACE_OUTER_BOUND('',#655,.T.);
#488=FACE_OUTER_BOUND('',#656,.T.);
#489=FACE_OUTER_BOUND('',#657,.T.);
#490=FACE_OUTER_BOUND('',#658,.T.);
#491=FACE_OUTER_BOUND('',#659,.T.);
#492=FACE_OUTER_BOUND('',#660,.T.);
#493=FACE_OUTER_BOUND('',#661,.T.);
#494=FACE_OUTER_BOUND('',#662,.T.);
#495=FACE_OUTER_BOUND('',#663,.T.);
#496=FACE_OUTER_BOUND('',#664,.T.);
#497=FACE_OUTER_BOUND('',#665,.T.);
#498=FACE_OUTER_BOUND('',#666,.T.);
#499=FACE_OUTER_BOUND('',#667,.T.);
#500=FACE_OUTER_BOUND('',#668,.T.);
#501=FACE_OUTER_BOUND('',#669,.T.);
#502=FACE_OUTER_BOUND('',#670,.T.);
#503=FACE_OUTER_BOUND('',#671,.T.);
#504=FACE_OUTER_BOUND('',#672,.T.);
#505=FACE_OUTER_BOUND('',#673,.T.);
#506=FACE_OUTER_BOUND('',#674,.T.);
#507=FACE_OUTER_BOUND('',#675,.T.);
#508=FACE_OUTER_BOUND('',#676,.T.);
#509=FACE_OUTER_BOUND('',#677,.T.);
#510=FACE_OUTER_BOUND('',#678,.T.);
#511=FACE_OUTER_BOUND('',#679,.T.);
#512=FACE_OUTER_BOUND('',#680,.T.);
#513=FACE_OUTER_BOUND('',#681,.T.);
#514=FACE_OUTER_BOUND('',#682,.T.);
#515=FACE_OUTER_BOUND('',#683,.T.);
#516=FACE_OUTER_BOUND('',#684,.T.);
#517=FACE_OUTER_BOUND('',#685,.T.);
#518=FACE_OUTER_BOUND('',#686,.T.);
#519=FACE_OUTER_BOUND('',#687,.T.);
#520=FACE_OUTER_BOUND('',#688,.T.);
#641=EDGE_LOOP('',(#2128,#2129,#2130,#2131));
#642=EDGE_LOOP('',(#2132,#2133,#2134,#2135,#2136));
#643=EDGE_LOOP('',(#2137,#2138,#2139,#2140,#2141));
#644=EDGE_LOOP('',(#2142,#2143,#2144,#2145,#2146));
#645=EDGE_LOOP('',(#2147,#2148,#2149,#2150,#2151));
#646=EDGE_LOOP('',(#2152,#2153,#2154,#2155,#2156));
#647=EDGE_LOOP('',(#2157,#2158,#2159,#2160,#2161));
#648=EDGE_LOOP('',(#2162,#2163,#2164,#2165,#2166));
#649=EDGE_LOOP('',(#2167,#2168,#2169,#2170,#2171));
#650=EDGE_LOOP('',(#2172,#2173,#2174,#2175,#2176));
#651=EDGE_LOOP('',(#2177,#2178,#2179,#2180,#2181));
#652=EDGE_LOOP('',(#2182,#2183,#2184,#2185,#2186));
#653=EDGE_LOOP('',(#2187,#2188,#2189,#2190,#2191));
#654=EDGE_LOOP('',(#2192,#2193,#2194,#2195,#2196));
#655=EDGE_LOOP('',(#2197,#2198,#2199,#2200,#2201));
#656=EDGE_LOOP('',(#2202,#2203,#2204,#2205,#2206));
#657=EDGE_LOOP('',(#2207,#2208,#2209,#2210,#2211));
#658=EDGE_LOOP('',(#2212,#2213,#2214,#2215,#2216));
#659=EDGE_LOOP('',(#2217,#2218,#2219,#2220,#2221));
#660=EDGE_LOOP('',(#2222,#2223,#2224,#2225,#2226));
#661=EDGE_LOOP('',(#2227,#2228,#2229,#2230,#2231,#2232));
#662=EDGE_LOOP('',(#2233,#2234,#2235,#2236));
#663=EDGE_LOOP('',(#2237,#2238,#2239,#2240));
#664=EDGE_LOOP('',(#2241,#2242,#2243,#2244));
#665=EDGE_LOOP('',(#2245,#2246,#2247,#2248));
#666=EDGE_LOOP('',(#2249,#2250,#2251,#2252));
#667=EDGE_LOOP('',(#2253,#2254,#2255,#2256));
#668=EDGE_LOOP('',(#2257,#2258,#2259,#2260));
#669=EDGE_LOOP('',(#2261,#2262,#2263,#2264));
#670=EDGE_LOOP('',(#2265,#2266,#2267,#2268));
#671=EDGE_LOOP('',(#2269,#2270,#2271,#2272));
#672=EDGE_LOOP('',(#2273,#2274,#2275,#2276));
#673=EDGE_LOOP('',(#2277,#2278,#2279,#2280));
#674=EDGE_LOOP('',(#2281,#2282,#2283,#2284));
#675=EDGE_LOOP('',(#2285,#2286,#2287,#2288));
#676=EDGE_LOOP('',(#2289,#2290,#2291,#2292));
#677=EDGE_LOOP('',(#2293,#2294,#2295,#2296));
#678=EDGE_LOOP('',(#2297,#2298,#2299,#2300));
#679=EDGE_LOOP('',(#2301,#2302,#2303,#2304));
#680=EDGE_LOOP('',(#2305,#2306,#2307,#2308));
#681=EDGE_LOOP('',(#2309,#2310,#2311,#2312));
#682=EDGE_LOOP('',(#2313,#2314,#2315,#2316));
#683=EDGE_LOOP('',(#2317,#2318,#2319,#2320));
#684=EDGE_LOOP('',(#2321,#2322,#2323,#2324,#2325));
#685=EDGE_LOOP('',(#2326,#2327,#2328,#2329,#2330,#2331,#2332,#2333,#2334,
#2335,#2336,#2337,#2338,#2339,#2340,#2341,#2342,#2343,#2344,#2345,#2346,
#2347,#2348,#2349,#2350,#2351,#2352,#2353,#2354,#2355,#2356,#2357,#2358,
#2359,#2360,#2361,#2362,#2363,#2364,#2365,#2366,#2367,#2368,#2369,#2370,
#2371,#2372,#2373,#2374,#2375,#2376,#2377,#2378,#2379,#2380,#2381,#2382,
#2383));
#686=EDGE_LOOP('',(#2384,#2385,#2386,#2387,#2388,#2389,#2390,#2391,#2392,
#2393,#2394,#2395,#2396,#2397,#2398,#2399,#2400,#2401,#2402,#2403,#2404,
#2405,#2406,#2407,#2408,#2409,#2410,#2411,#2412,#2413,#2414,#2415,#2416,
#2417,#2418,#2419,#2420,#2421,#2422,#2423,#2424,#2425,#2426,#2427,#2428,
#2429,#2430,#2431,#2432,#2433,#2434,#2435,#2436,#2437,#2438,#2439,#2440,
#2441));
#687=EDGE_LOOP('',(#2442,#2443,#2444,#2445,#2446));
#688=EDGE_LOOP('',(#2447,#2448,#2449,#2450,#2451));
#791=LINE('',#6488,#933);
#792=LINE('',#6654,#934);
#793=LINE('',#7082,#935);
#794=LINE('',#7529,#936);
#795=LINE('',#7976,#937);
#796=LINE('',#8421,#938);
#797=LINE('',#8870,#939);
#798=LINE('',#9311,#940);
#799=LINE('',#9758,#941);
#800=LINE('',#10209,#942);
#801=LINE('',#10646,#943);
#802=LINE('',#11121,#944);
#803=LINE('',#11574,#945);
#804=LINE('',#12023,#946);
#805=LINE('',#12470,#947);
#806=LINE('',#12923,#948);
#807=LINE('',#13400,#949);
#808=LINE('',#13855,#950);
#809=LINE('',#14326,#951);
#810=LINE('',#14763,#952);
#811=LINE('',#15181,#953);
#812=LINE('',#15634,#954);
#813=LINE('',#15652,#955);
#814=LINE('',#15838,#956);
#815=LINE('',#16024,#957);
#816=LINE('',#16372,#958);
#817=LINE('',#16396,#959);
#818=LINE('',#16420,#960);
#819=LINE('',#16607,#961);
#820=LINE('',#16955,#962);
#821=LINE('',#16979,#963);
#822=LINE('',#17005,#964);
#823=LINE('',#17191,#965);
#824=LINE('',#17539,#966);
#825=LINE('',#17565,#967);
#826=LINE('',#17589,#968);
#827=LINE('',#17775,#969);
#828=LINE('',#18123,#970);
#829=LINE('',#18147,#971);
#830=LINE('',#18171,#972);
#831=LINE('',#18358,#973);
#832=LINE('',#18706,#974);
#933=VECTOR('',#3694,1.17775);
#934=VECTOR('',#3699,1.17775);
#935=VECTOR('',#3702,1.17775);
#936=VECTOR('',#3705,1.17775);
#937=VECTOR('',#3708,1.17775);
#938=VECTOR('',#3711,1.17775);
#939=VECTOR('',#3714,1.17775);
#940=VECTOR('',#3717,1.17775);
#941=VECTOR('',#3720,1.17775);
#942=VECTOR('',#3723,1.17775);
#943=VECTOR('',#3726,1.17775);
#944=VECTOR('',#3729,1.17775);
#945=VECTOR('',#3732,1.17775);
#946=VECTOR('',#3735,1.17775);
#947=VECTOR('',#3738,1.17775);
#948=VECTOR('',#3741,1.17775);
#949=VECTOR('',#3744,1.17775);
#950=VECTOR('',#3747,1.17775);
#951=VECTOR('',#3750,1.17775);
#952=VECTOR('',#3753,1.17775);
#953=VECTOR('',#3756,1.17775);
#954=VECTOR('',#3759,1.4635);
#955=VECTOR('',#3764,1.4635);
#956=VECTOR('',#3767,1.4635);
#957=VECTOR('',#3770,1.4635);
#958=VECTOR('',#3773,1.4635);
#959=VECTOR('',#3776,1.4635);
#960=VECTOR('',#3779,1.4635);
#961=VECTOR('',#3782,1.4635);
#962=VECTOR('',#3785,1.4635);
#963=VECTOR('',#3788,1.4635);
#964=VECTOR('',#3791,1.4635);
#965=VECTOR('',#3794,1.4635);
#966=VECTOR('',#3797,1.4635);
#967=VECTOR('',#3800,1.4635);
#968=VECTOR('',#3803,1.4635);
#969=VECTOR('',#3806,1.4635);
#970=VECTOR('',#3809,1.4635);
#971=VECTOR('',#3812,1.4635);
#972=VECTOR('',#3815,1.4635);
#973=VECTOR('',#3818,1.4635);
#974=VECTOR('',#3821,1.4635);
#1078=CIRCLE('',#3353,1.17775);
#1079=CIRCLE('',#3375,1.4635);
#1080=CIRCLE('',#3397,1.4635);
#1081=CIRCLE('',#3399,1.17775);
#1163=VERTEX_POINT('',#6486);
#1164=VERTEX_POINT('',#6487);
#1165=VERTEX_POINT('',#6489);
#1166=VERTEX_POINT('',#6594);
#1167=VERTEX_POINT('',#6652);
#1168=VERTEX_POINT('',#6653);
#1169=VERTEX_POINT('',#6875);
#1170=VERTEX_POINT('',#7080);
#1171=VERTEX_POINT('',#7081);
#1172=VERTEX_POINT('',#7083);
#1173=VERTEX_POINT('',#7527);
#1174=VERTEX_POINT('',#7528);
#1175=VERTEX_POINT('',#7748);
#1176=VERTEX_POINT('',#7974);
#1177=VERTEX_POINT('',#7975);
#1178=VERTEX_POINT('',#7977);
#1179=VERTEX_POINT('',#8419);
#1180=VERTEX_POINT('',#8420);
#1181=VERTEX_POINT('',#8642);
#1182=VERTEX_POINT('',#8868);
#1183=VERTEX_POINT('',#8869);
#1184=VERTEX_POINT('',#8871);
#1185=VERTEX_POINT('',#9309);
#1186=VERTEX_POINT('',#9310);
#1187=VERTEX_POINT('',#9534);
#1188=VERTEX_POINT('',#9756);
#1189=VERTEX_POINT('',#9757);
#1190=VERTEX_POINT('',#9759);
#1191=VERTEX_POINT('',#10207);
#1192=VERTEX_POINT('',#10208);
#1193=VERTEX_POINT('',#10420);
#1194=VERTEX_POINT('',#10644);
#1195=VERTEX_POINT('',#10645);
#1196=VERTEX_POINT('',#10647);
#1197=VERTEX_POINT('',#11119);
#1198=VERTEX_POINT('',#11120);
#1199=VERTEX_POINT('',#11338);
#1200=VERTEX_POINT('',#11572);
#1201=VERTEX_POINT('',#11573);
#1202=VERTEX_POINT('',#11575);
#1203=VERTEX_POINT('',#12021);
#1204=VERTEX_POINT('',#12022);
#1205=VERTEX_POINT('',#12246);
#1206=VERTEX_POINT('',#12468);
#1207=VERTEX_POINT('',#12469);
#1208=VERTEX_POINT('',#12471);
#1209=VERTEX_POINT('',#12921);
#1210=VERTEX_POINT('',#12922);
#1211=VERTEX_POINT('',#13132);
#1212=VERTEX_POINT('',#13398);
#1213=VERTEX_POINT('',#13399);
#1214=VERTEX_POINT('',#13401);
#1215=VERTEX_POINT('',#13853);
#1216=VERTEX_POINT('',#13854);
#1217=VERTEX_POINT('',#14068);
#1218=VERTEX_POINT('',#14324);
#1219=VERTEX_POINT('',#14325);
#1220=VERTEX_POINT('',#14327);
#1221=VERTEX_POINT('',#14761);
#1222=VERTEX_POINT('',#14762);
#1223=VERTEX_POINT('',#14980);
#1224=VERTEX_POINT('',#15179);
#1225=VERTEX_POINT('',#15180);
#1226=VERTEX_POINT('',#15182);
#1227=VERTEX_POINT('',#15399);
#1228=VERTEX_POINT('',#15632);
#1229=VERTEX_POINT('',#15633);
#1230=VERTEX_POINT('',#15635);
#1231=VERTEX_POINT('',#15642);
#1232=VERTEX_POINT('',#15650);
#1233=VERTEX_POINT('',#15651);
#1234=VERTEX_POINT('',#15836);
#1235=VERTEX_POINT('',#15837);
#1236=VERTEX_POINT('',#16022);
#1237=VERTEX_POINT('',#16023);
#1238=VERTEX_POINT('',#16370);
#1239=VERTEX_POINT('',#16371);
#1240=VERTEX_POINT('',#16394);
#1241=VERTEX_POINT('',#16395);
#1242=VERTEX_POINT('',#16418);
#1243=VERTEX_POINT('',#16419);
#1244=VERTEX_POINT('',#16605);
#1245=VERTEX_POINT('',#16606);
#1246=VERTEX_POINT('',#16953);
#1247=VERTEX_POINT('',#16954);
#1248=VERTEX_POINT('',#16977);
#1249=VERTEX_POINT('',#16978);
#1250=VERTEX_POINT('',#17003);
#1251=VERTEX_POINT('',#17004);
#1252=VERTEX_POINT('',#17189);
#1253=VERTEX_POINT('',#17190);
#1254=VERTEX_POINT('',#17537);
#1255=VERTEX_POINT('',#17538);
#1256=VERTEX_POINT('',#17563);
#1257=VERTEX_POINT('',#17564);
#1258=VERTEX_POINT('',#17587);
#1259=VERTEX_POINT('',#17588);
#1260=VERTEX_POINT('',#17773);
#1261=VERTEX_POINT('',#17774);
#1262=VERTEX_POINT('',#18121);
#1263=VERTEX_POINT('',#18122);
#1264=VERTEX_POINT('',#18145);
#1265=VERTEX_POINT('',#18146);
#1266=VERTEX_POINT('',#18169);
#1267=VERTEX_POINT('',#18170);
#1268=VERTEX_POINT('',#18356);
#1269=VERTEX_POINT('',#18357);
#1270=VERTEX_POINT('',#18704);
#1271=VERTEX_POINT('',#18705);
#1272=VERTEX_POINT('',#18728);
#1273=VERTEX_POINT('',#18738);
#1274=VERTEX_POINT('',#18749);
#1275=VERTEX_POINT('',#18970);
#1276=VERTEX_POINT('',#18972);
#1277=VERTEX_POINT('',#19690);
#1278=VERTEX_POINT('',#20326);
#1540=EDGE_CURVE('',#1163,#1164,#791,.T.);
#1541=EDGE_CURVE('',#1165,#1163,#83,.F.);
#1542=EDGE_CURVE('',#1166,#1165,#1078,.T.);
#1543=EDGE_CURVE('',#1166,#1164,#84,.T.);
#1544=EDGE_CURVE('',#1167,#1168,#792,.T.);
#1545=EDGE_CURVE('',#1163,#1167,#85,.F.);
#1546=EDGE_CURVE('',#1164,#1169,#86,.T.);
#1547=EDGE_CURVE('',#1169,#1168,#87,.T.);
#1548=EDGE_CURVE('',#1170,#1171,#793,.T.);
#1549=EDGE_CURVE('',#1172,#1170,#88,.F.);
#1550=EDGE_CURVE('',#1167,#1172,#89,.F.);
#1551=EDGE_CURVE('',#1168,#1171,#90,.T.);
#1552=EDGE_CURVE('',#1173,#1174,#794,.T.);
#1553=EDGE_CURVE('',#1170,#1173,#91,.F.);
#1554=EDGE_CURVE('',#1171,#1175,#92,.T.);
#1555=EDGE_CURVE('',#1175,#1174,#93,.T.);
#1556=EDGE_CURVE('',#1176,#1177,#795,.T.);
#1557=EDGE_CURVE('',#1178,#1176,#94,.F.);
#1558=EDGE_CURVE('',#1173,#1178,#95,.F.);
#1559=EDGE_CURVE('',#1174,#1177,#96,.T.);
#1560=EDGE_CURVE('',#1179,#1180,#796,.T.);
#1561=EDGE_CURVE('',#1176,#1179,#97,.F.);
#1562=EDGE_CURVE('',#1177,#1181,#98,.T.);
#1563=EDGE_CURVE('',#1181,#1180,#99,.T.);
#1564=EDGE_CURVE('',#1182,#1183,#797,.T.);
#1565=EDGE_CURVE('',#1184,#1182,#100,.F.);
#1566=EDGE_CURVE('',#1179,#1184,#101,.F.);
#1567=EDGE_CURVE('',#1180,#1183,#102,.T.);
#1568=EDGE_CURVE('',#1185,#1186,#798,.T.);
#1569=EDGE_CURVE('',#1182,#1185,#103,.F.);
#1570=EDGE_CURVE('',#1183,#1187,#104,.T.);
#1571=EDGE_CURVE('',#1187,#1186,#105,.T.);
#1572=EDGE_CURVE('',#1188,#1189,#799,.T.);
#1573=EDGE_CURVE('',#1190,#1188,#106,.F.);
#1574=EDGE_CURVE('',#1185,#1190,#107,.F.);
#1575=EDGE_CURVE('',#1186,#1189,#108,.T.);
#1576=EDGE_CURVE('',#1191,#1192,#800,.T.);
#1577=EDGE_CURVE('',#1188,#1191,#109,.F.);
#1578=EDGE_CURVE('',#1189,#1193,#110,.T.);
#1579=EDGE_CURVE('',#1193,#1192,#111,.T.);
#1580=EDGE_CURVE('',#1194,#1195,#801,.T.);
#1581=EDGE_CURVE('',#1196,#1194,#112,.F.);
#1582=EDGE_CURVE('',#1191,#1196,#113,.F.);
#1583=EDGE_CURVE('',#1192,#1195,#114,.T.);
#1584=EDGE_CURVE('',#1197,#1198,#802,.T.);
#1585=EDGE_CURVE('',#1194,#1197,#115,.F.);
#1586=EDGE_CURVE('',#1195,#1199,#116,.T.);
#1587=EDGE_CURVE('',#1199,#1198,#117,.T.);
#1588=EDGE_CURVE('',#1200,#1201,#803,.T.);
#1589=EDGE_CURVE('',#1202,#1200,#118,.F.);
#1590=EDGE_CURVE('',#1197,#1202,#119,.F.);
#1591=EDGE_CURVE('',#1198,#1201,#120,.T.);
#1592=EDGE_CURVE('',#1203,#1204,#804,.T.);
#1593=EDGE_CURVE('',#1200,#1203,#121,.F.);
#1594=EDGE_CURVE('',#1201,#1205,#122,.T.);
#1595=EDGE_CURVE('',#1205,#1204,#123,.T.);
#1596=EDGE_CURVE('',#1206,#1207,#805,.T.);
#1597=EDGE_CURVE('',#1208,#1206,#124,.F.);
#1598=EDGE_CURVE('',#1203,#1208,#125,.F.);
#1599=EDGE_CURVE('',#1204,#1207,#126,.T.);
#1600=EDGE_CURVE('',#1209,#1210,#806,.T.);
#1601=EDGE_CURVE('',#1206,#1209,#127,.F.);
#1602=EDGE_CURVE('',#1207,#1211,#128,.T.);
#1603=EDGE_CURVE('',#1211,#1210,#129,.T.);
#1604=EDGE_CURVE('',#1212,#1213,#807,.T.);
#1605=EDGE_CURVE('',#1214,#1212,#130,.F.);
#1606=EDGE_CURVE('',#1209,#1214,#131,.F.);
#1607=EDGE_CURVE('',#1210,#1213,#132,.T.);
#1608=EDGE_CURVE('',#1215,#1216,#808,.T.);
#1609=EDGE_CURVE('',#1212,#1215,#133,.F.);
#1610=EDGE_CURVE('',#1213,#1217,#134,.T.);
#1611=EDGE_CURVE('',#1217,#1216,#135,.T.);
#1612=EDGE_CURVE('',#1218,#1219,#809,.T.);
#1613=EDGE_CURVE('',#1220,#1218,#136,.F.);
#1614=EDGE_CURVE('',#1215,#1220,#137,.F.);
#1615=EDGE_CURVE('',#1216,#1219,#138,.T.);
#1616=EDGE_CURVE('',#1221,#1222,#810,.T.);
#1617=EDGE_CURVE('',#1218,#1221,#139,.F.);
#1618=EDGE_CURVE('',#1219,#1223,#140,.T.);
#1619=EDGE_CURVE('',#1223,#1222,#141,.T.);
#1620=EDGE_CURVE('',#1224,#1225,#811,.T.);
#1621=EDGE_CURVE('',#1226,#1224,#142,.T.);
#1622=EDGE_CURVE('',#1221,#1226,#143,.F.);
#1623=EDGE_CURVE('',#1222,#1227,#144,.T.);
#1624=EDGE_CURVE('',#1227,#1225,#145,.F.);
#1625=EDGE_CURVE('',#1228,#1229,#812,.T.);
#1626=EDGE_CURVE('',#1228,#1230,#146,.T.);
#1627=EDGE_CURVE('',#1231,#1230,#1079,.F.);
#1628=EDGE_CURVE('',#1231,#1229,#147,.T.);
#1629=EDGE_CURVE('',#1232,#1233,#813,.T.);
#1630=EDGE_CURVE('',#1232,#1228,#148,.T.);
#1631=EDGE_CURVE('',#1229,#1233,#149,.T.);
#1632=EDGE_CURVE('',#1234,#1235,#814,.T.);
#1633=EDGE_CURVE('',#1234,#1232,#150,.T.);
#1634=EDGE_CURVE('',#1233,#1235,#151,.T.);
#1635=EDGE_CURVE('',#1236,#1237,#815,.T.);
#1636=EDGE_CURVE('',#1236,#1234,#152,.T.);
#1637=EDGE_CURVE('',#1235,#1237,#153,.T.);
#1638=EDGE_CURVE('',#1238,#1239,#816,.T.);
#1639=EDGE_CURVE('',#1238,#1236,#154,.T.);
#1640=EDGE_CURVE('',#1237,#1239,#155,.T.);
#1641=EDGE_CURVE('',#1240,#1241,#817,.T.);
#1642=EDGE_CURVE('',#1240,#1238,#156,.T.);
#1643=EDGE_CURVE('',#1239,#1241,#157,.T.);
#1644=EDGE_CURVE('',#1242,#1243,#818,.T.);
#1645=EDGE_CURVE('',#1242,#1240,#158,.T.);
#1646=EDGE_CURVE('',#1241,#1243,#159,.T.);
#1647=EDGE_CURVE('',#1244,#1245,#819,.T.);
#1648=EDGE_CURVE('',#1244,#1242,#160,.T.);
#1649=EDGE_CURVE('',#1243,#1245,#161,.T.);
#1650=EDGE_CURVE('',#1246,#1247,#820,.T.);
#1651=EDGE_CURVE('',#1246,#1244,#162,.T.);
#1652=EDGE_CURVE('',#1245,#1247,#163,.T.);
#1653=EDGE_CURVE('',#1248,#1249,#821,.T.);
#1654=EDGE_CURVE('',#1248,#1246,#164,.T.);
#1655=EDGE_CURVE('',#1247,#1249,#165,.T.);
#1656=EDGE_CURVE('',#1250,#1251,#822,.T.);
#1657=EDGE_CURVE('',#1250,#1248,#166,.T.);
#1658=EDGE_CURVE('',#1249,#1251,#167,.T.);
#1659=EDGE_CURVE('',#1252,#1253,#823,.T.);
#1660=EDGE_CURVE('',#1252,#1250,#168,.T.);
#1661=EDGE_CURVE('',#1251,#1253,#169,.T.);
#1662=EDGE_CURVE('',#1254,#1255,#824,.T.);
#1663=EDGE_CURVE('',#1254,#1252,#170,.T.);
#1664=EDGE_CURVE('',#1253,#1255,#171,.T.);
#1665=EDGE_CURVE('',#1256,#1257,#825,.T.);
#1666=EDGE_CURVE('',#1256,#1254,#172,.T.);
#1667=EDGE_CURVE('',#1255,#1257,#173,.T.);
#1668=EDGE_CURVE('',#1258,#1259,#826,.T.);
#1669=EDGE_CURVE('',#1258,#1256,#174,.T.);
#1670=EDGE_CURVE('',#1257,#1259,#175,.T.);
#1671=EDGE_CURVE('',#1260,#1261,#827,.T.);
#1672=EDGE_CURVE('',#1260,#1258,#176,.T.);
#1673=EDGE_CURVE('',#1259,#1261,#177,.T.);
#1674=EDGE_CURVE('',#1262,#1263,#828,.T.);
#1675=EDGE_CURVE('',#1262,#1260,#178,.T.);
#1676=EDGE_CURVE('',#1261,#1263,#179,.T.);
#1677=EDGE_CURVE('',#1264,#1265,#829,.T.);
#1678=EDGE_CURVE('',#1264,#1262,#180,.T.);
#1679=EDGE_CURVE('',#1263,#1265,#181,.T.);
#1680=EDGE_CURVE('',#1266,#1267,#830,.T.);
#1681=EDGE_CURVE('',#1266,#1264,#182,.T.);
#1682=EDGE_CURVE('',#1265,#1267,#183,.T.);
#1683=EDGE_CURVE('',#1268,#1269,#831,.T.);
#1684=EDGE_CURVE('',#1268,#1266,#184,.T.);
#1685=EDGE_CURVE('',#1267,#1269,#185,.T.);
#1686=EDGE_CURVE('',#1270,#1271,#832,.T.);
#1687=EDGE_CURVE('',#1270,#1268,#186,.T.);
#1688=EDGE_CURVE('',#1269,#1271,#187,.T.);
#1689=EDGE_CURVE('',#1271,#1272,#188,.T.);
#1690=EDGE_CURVE('',#1273,#1272,#1080,.T.);
#1691=EDGE_CURVE('',#1273,#1270,#189,.T.);
#1692=EDGE_CURVE('',#1225,#1274,#190,.F.);
#1693=EDGE_CURVE('',#1275,#1274,#1081,.T.);
#1694=EDGE_CURVE('',#1276,#1275,#191,.T.);
#1695=EDGE_CURVE('',#1224,#1276,#192,.T.);
#1696=EDGE_CURVE('',#1272,#1275,#193,.T.);
#1697=EDGE_CURVE('',#1277,#1231,#194,.T.);
#1698=EDGE_CURVE('',#1277,#1165,#195,.T.);
#1699=EDGE_CURVE('',#1278,#1273,#196,.T.);
#1700=EDGE_CURVE('',#1274,#1278,#197,.T.);
#1701=EDGE_CURVE('',#1230,#1166,#198,.T.);
#2128=ORIENTED_EDGE('',*,*,#1540,.F.);
#2129=ORIENTED_EDGE('',*,*,#1541,.F.);
#2130=ORIENTED_EDGE('',*,*,#1542,.F.);
#2131=ORIENTED_EDGE('',*,*,#1543,.T.);
#2132=ORIENTED_EDGE('',*,*,#1544,.F.);
#2133=ORIENTED_EDGE('',*,*,#1545,.F.);
#2134=ORIENTED_EDGE('',*,*,#1540,.T.);
#2135=ORIENTED_EDGE('',*,*,#1546,.T.);
#2136=ORIENTED_EDGE('',*,*,#1547,.T.);
#2137=ORIENTED_EDGE('',*,*,#1548,.F.);
#2138=ORIENTED_EDGE('',*,*,#1549,.F.);
#2139=ORIENTED_EDGE('',*,*,#1550,.F.);
#2140=ORIENTED_EDGE('',*,*,#1544,.T.);
#2141=ORIENTED_EDGE('',*,*,#1551,.T.);
#2142=ORIENTED_EDGE('',*,*,#1552,.F.);
#2143=ORIENTED_EDGE('',*,*,#1553,.F.);
#2144=ORIENTED_EDGE('',*,*,#1548,.T.);
#2145=ORIENTED_EDGE('',*,*,#1554,.T.);
#2146=ORIENTED_EDGE('',*,*,#1555,.T.);
#2147=ORIENTED_EDGE('',*,*,#1556,.F.);
#2148=ORIENTED_EDGE('',*,*,#1557,.F.);
#2149=ORIENTED_EDGE('',*,*,#1558,.F.);
#2150=ORIENTED_EDGE('',*,*,#1552,.T.);
#2151=ORIENTED_EDGE('',*,*,#1559,.T.);
#2152=ORIENTED_EDGE('',*,*,#1560,.F.);
#2153=ORIENTED_EDGE('',*,*,#1561,.F.);
#2154=ORIENTED_EDGE('',*,*,#1556,.T.);
#2155=ORIENTED_EDGE('',*,*,#1562,.T.);
#2156=ORIENTED_EDGE('',*,*,#1563,.T.);
#2157=ORIENTED_EDGE('',*,*,#1564,.F.);
#2158=ORIENTED_EDGE('',*,*,#1565,.F.);
#2159=ORIENTED_EDGE('',*,*,#1566,.F.);
#2160=ORIENTED_EDGE('',*,*,#1560,.T.);
#2161=ORIENTED_EDGE('',*,*,#1567,.T.);
#2162=ORIENTED_EDGE('',*,*,#1568,.F.);
#2163=ORIENTED_EDGE('',*,*,#1569,.F.);
#2164=ORIENTED_EDGE('',*,*,#1564,.T.);
#2165=ORIENTED_EDGE('',*,*,#1570,.T.);
#2166=ORIENTED_EDGE('',*,*,#1571,.T.);
#2167=ORIENTED_EDGE('',*,*,#1572,.F.);
#2168=ORIENTED_EDGE('',*,*,#1573,.F.);
#2169=ORIENTED_EDGE('',*,*,#1574,.F.);
#2170=ORIENTED_EDGE('',*,*,#1568,.T.);
#2171=ORIENTED_EDGE('',*,*,#1575,.T.);
#2172=ORIENTED_EDGE('',*,*,#1576,.F.);
#2173=ORIENTED_EDGE('',*,*,#1577,.F.);
#2174=ORIENTED_EDGE('',*,*,#1572,.T.);
#2175=ORIENTED_EDGE('',*,*,#1578,.T.);
#2176=ORIENTED_EDGE('',*,*,#1579,.T.);
#2177=ORIENTED_EDGE('',*,*,#1580,.F.);
#2178=ORIENTED_EDGE('',*,*,#1581,.F.);
#2179=ORIENTED_EDGE('',*,*,#1582,.F.);
#2180=ORIENTED_EDGE('',*,*,#1576,.T.);
#2181=ORIENTED_EDGE('',*,*,#1583,.T.);
#2182=ORIENTED_EDGE('',*,*,#1584,.F.);
#2183=ORIENTED_EDGE('',*,*,#1585,.F.);
#2184=ORIENTED_EDGE('',*,*,#1580,.T.);
#2185=ORIENTED_EDGE('',*,*,#1586,.T.);
#2186=ORIENTED_EDGE('',*,*,#1587,.T.);
#2187=ORIENTED_EDGE('',*,*,#1588,.F.);
#2188=ORIENTED_EDGE('',*,*,#1589,.F.);
#2189=ORIENTED_EDGE('',*,*,#1590,.F.);
#2190=ORIENTED_EDGE('',*,*,#1584,.T.);
#2191=ORIENTED_EDGE('',*,*,#1591,.T.);
#2192=ORIENTED_EDGE('',*,*,#1592,.F.);
#2193=ORIENTED_EDGE('',*,*,#1593,.F.);
#2194=ORIENTED_EDGE('',*,*,#1588,.T.);
#2195=ORIENTED_EDGE('',*,*,#1594,.T.);
#2196=ORIENTED_EDGE('',*,*,#1595,.T.);
#2197=ORIENTED_EDGE('',*,*,#1596,.F.);
#2198=ORIENTED_EDGE('',*,*,#1597,.F.);
#2199=ORIENTED_EDGE('',*,*,#1598,.F.);
#2200=ORIENTED_EDGE('',*,*,#1592,.T.);
#2201=ORIENTED_EDGE('',*,*,#1599,.T.);
#2202=ORIENTED_EDGE('',*,*,#1600,.F.);
#2203=ORIENTED_EDGE('',*,*,#1601,.F.);
#2204=ORIENTED_EDGE('',*,*,#1596,.T.);
#2205=ORIENTED_EDGE('',*,*,#1602,.T.);
#2206=ORIENTED_EDGE('',*,*,#1603,.T.);
#2207=ORIENTED_EDGE('',*,*,#1604,.F.);
#2208=ORIENTED_EDGE('',*,*,#1605,.F.);
#2209=ORIENTED_EDGE('',*,*,#1606,.F.);
#2210=ORIENTED_EDGE('',*,*,#1600,.T.);
#2211=ORIENTED_EDGE('',*,*,#1607,.T.);
#2212=ORIENTED_EDGE('',*,*,#1608,.F.);
#2213=ORIENTED_EDGE('',*,*,#1609,.F.);
#2214=ORIENTED_EDGE('',*,*,#1604,.T.);
#2215=ORIENTED_EDGE('',*,*,#1610,.T.);
#2216=ORIENTED_EDGE('',*,*,#1611,.T.);
#2217=ORIENTED_EDGE('',*,*,#1612,.F.);
#2218=ORIENTED_EDGE('',*,*,#1613,.F.);
#2219=ORIENTED_EDGE('',*,*,#1614,.F.);
#2220=ORIENTED_EDGE('',*,*,#1608,.T.);
#2221=ORIENTED_EDGE('',*,*,#1615,.T.);
#2222=ORIENTED_EDGE('',*,*,#1616,.F.);
#2223=ORIENTED_EDGE('',*,*,#1617,.F.);
#2224=ORIENTED_EDGE('',*,*,#1612,.T.);
#2225=ORIENTED_EDGE('',*,*,#1618,.T.);
#2226=ORIENTED_EDGE('',*,*,#1619,.T.);
#2227=ORIENTED_EDGE('',*,*,#1620,.F.);
#2228=ORIENTED_EDGE('',*,*,#1621,.F.);
#2229=ORIENTED_EDGE('',*,*,#1622,.F.);
#2230=ORIENTED_EDGE('',*,*,#1616,.T.);
#2231=ORIENTED_EDGE('',*,*,#1623,.T.);
#2232=ORIENTED_EDGE('',*,*,#1624,.T.);
#2233=ORIENTED_EDGE('',*,*,#1625,.F.);
#2234=ORIENTED_EDGE('',*,*,#1626,.T.);
#2235=ORIENTED_EDGE('',*,*,#1627,.F.);
#2236=ORIENTED_EDGE('',*,*,#1628,.T.);
#2237=ORIENTED_EDGE('',*,*,#1629,.F.);
#2238=ORIENTED_EDGE('',*,*,#1630,.T.);
#2239=ORIENTED_EDGE('',*,*,#1625,.T.);
#2240=ORIENTED_EDGE('',*,*,#1631,.T.);
#2241=ORIENTED_EDGE('',*,*,#1632,.F.);
#2242=ORIENTED_EDGE('',*,*,#1633,.T.);
#2243=ORIENTED_EDGE('',*,*,#1629,.T.);
#2244=ORIENTED_EDGE('',*,*,#1634,.T.);
#2245=ORIENTED_EDGE('',*,*,#1635,.F.);
#2246=ORIENTED_EDGE('',*,*,#1636,.T.);
#2247=ORIENTED_EDGE('',*,*,#1632,.T.);
#2248=ORIENTED_EDGE('',*,*,#1637,.T.);
#2249=ORIENTED_EDGE('',*,*,#1638,.F.);
#2250=ORIENTED_EDGE('',*,*,#1639,.T.);
#2251=ORIENTED_EDGE('',*,*,#1635,.T.);
#2252=ORIENTED_EDGE('',*,*,#1640,.T.);
#2253=ORIENTED_EDGE('',*,*,#1641,.F.);
#2254=ORIENTED_EDGE('',*,*,#1642,.T.);
#2255=ORIENTED_EDGE('',*,*,#1638,.T.);
#2256=ORIENTED_EDGE('',*,*,#1643,.T.);
#2257=ORIENTED_EDGE('',*,*,#1644,.F.);
#2258=ORIENTED_EDGE('',*,*,#1645,.T.);
#2259=ORIENTED_EDGE('',*,*,#1641,.T.);
#2260=ORIENTED_EDGE('',*,*,#1646,.T.);
#2261=ORIENTED_EDGE('',*,*,#1647,.F.);
#2262=ORIENTED_EDGE('',*,*,#1648,.T.);
#2263=ORIENTED_EDGE('',*,*,#1644,.T.);
#2264=ORIENTED_EDGE('',*,*,#1649,.T.);
#2265=ORIENTED_EDGE('',*,*,#1650,.F.);
#2266=ORIENTED_EDGE('',*,*,#1651,.T.);
#2267=ORIENTED_EDGE('',*,*,#1647,.T.);
#2268=ORIENTED_EDGE('',*,*,#1652,.T.);
#2269=ORIENTED_EDGE('',*,*,#1653,.F.);
#2270=ORIENTED_EDGE('',*,*,#1654,.T.);
#2271=ORIENTED_EDGE('',*,*,#1650,.T.);
#2272=ORIENTED_EDGE('',*,*,#1655,.T.);
#2273=ORIENTED_EDGE('',*,*,#1656,.F.);
#2274=ORIENTED_EDGE('',*,*,#1657,.T.);
#2275=ORIENTED_EDGE('',*,*,#1653,.T.);
#2276=ORIENTED_EDGE('',*,*,#1658,.T.);
#2277=ORIENTED_EDGE('',*,*,#1659,.F.);
#2278=ORIENTED_EDGE('',*,*,#1660,.T.);
#2279=ORIENTED_EDGE('',*,*,#1656,.T.);
#2280=ORIENTED_EDGE('',*,*,#1661,.T.);
#2281=ORIENTED_EDGE('',*,*,#1662,.F.);
#2282=ORIENTED_EDGE('',*,*,#1663,.T.);
#2283=ORIENTED_EDGE('',*,*,#1659,.T.);
#2284=ORIENTED_EDGE('',*,*,#1664,.T.);
#2285=ORIENTED_EDGE('',*,*,#1665,.F.);
#2286=ORIENTED_EDGE('',*,*,#1666,.T.);
#2287=ORIENTED_EDGE('',*,*,#1662,.T.);
#2288=ORIENTED_EDGE('',*,*,#1667,.T.);
#2289=ORIENTED_EDGE('',*,*,#1668,.F.);
#2290=ORIENTED_EDGE('',*,*,#1669,.T.);
#2291=ORIENTED_EDGE('',*,*,#1665,.T.);
#2292=ORIENTED_EDGE('',*,*,#1670,.T.);
#2293=ORIENTED_EDGE('',*,*,#1671,.F.);
#2294=ORIENTED_EDGE('',*,*,#1672,.T.);
#2295=ORIENTED_EDGE('',*,*,#1668,.T.);
#2296=ORIENTED_EDGE('',*,*,#1673,.T.);
#2297=ORIENTED_EDGE('',*,*,#1674,.F.);
#2298=ORIENTED_EDGE('',*,*,#1675,.T.);
#2299=ORIENTED_EDGE('',*,*,#1671,.T.);
#2300=ORIENTED_EDGE('',*,*,#1676,.T.);
#2301=ORIENTED_EDGE('',*,*,#1677,.F.);
#2302=ORIENTED_EDGE('',*,*,#1678,.T.);
#2303=ORIENTED_EDGE('',*,*,#1674,.T.);
#2304=ORIENTED_EDGE('',*,*,#1679,.T.);
#2305=ORIENTED_EDGE('',*,*,#1680,.F.);
#2306=ORIENTED_EDGE('',*,*,#1681,.T.);
#2307=ORIENTED_EDGE('',*,*,#1677,.T.);
#2308=ORIENTED_EDGE('',*,*,#1682,.T.);
#2309=ORIENTED_EDGE('',*,*,#1683,.F.);
#2310=ORIENTED_EDGE('',*,*,#1684,.T.);
#2311=ORIENTED_EDGE('',*,*,#1680,.T.);
#2312=ORIENTED_EDGE('',*,*,#1685,.T.);
#2313=ORIENTED_EDGE('',*,*,#1686,.F.);
#2314=ORIENTED_EDGE('',*,*,#1687,.T.);
#2315=ORIENTED_EDGE('',*,*,#1683,.T.);
#2316=ORIENTED_EDGE('',*,*,#1688,.T.);
#2317=ORIENTED_EDGE('',*,*,#1686,.T.);
#2318=ORIENTED_EDGE('',*,*,#1689,.T.);
#2319=ORIENTED_EDGE('',*,*,#1690,.F.);
#2320=ORIENTED_EDGE('',*,*,#1691,.T.);
#2321=ORIENTED_EDGE('',*,*,#1620,.T.);
#2322=ORIENTED_EDGE('',*,*,#1692,.T.);
#2323=ORIENTED_EDGE('',*,*,#1693,.F.);
#2324=ORIENTED_EDGE('',*,*,#1694,.F.);
#2325=ORIENTED_EDGE('',*,*,#1695,.F.);
#2326=ORIENTED_EDGE('',*,*,#1696,.F.);
#2327=ORIENTED_EDGE('',*,*,#1689,.F.);
#2328=ORIENTED_EDGE('',*,*,#1688,.F.);
#2329=ORIENTED_EDGE('',*,*,#1685,.F.);
#2330=ORIENTED_EDGE('',*,*,#1682,.F.);
#2331=ORIENTED_EDGE('',*,*,#1679,.F.);
#2332=ORIENTED_EDGE('',*,*,#1676,.F.);
#2333=ORIENTED_EDGE('',*,*,#1673,.F.);
#2334=ORIENTED_EDGE('',*,*,#1670,.F.);
#2335=ORIENTED_EDGE('',*,*,#1667,.F.);
#2336=ORIENTED_EDGE('',*,*,#1664,.F.);
#2337=ORIENTED_EDGE('',*,*,#1661,.F.);
#2338=ORIENTED_EDGE('',*,*,#1658,.F.);
#2339=ORIENTED_EDGE('',*,*,#1655,.F.);
#2340=ORIENTED_EDGE('',*,*,#1652,.F.);
#2341=ORIENTED_EDGE('',*,*,#1649,.F.);
#2342=ORIENTED_EDGE('',*,*,#1646,.F.);
#2343=ORIENTED_EDGE('',*,*,#1643,.F.);
#2344=ORIENTED_EDGE('',*,*,#1640,.F.);
#2345=ORIENTED_EDGE('',*,*,#1637,.F.);
#2346=ORIENTED_EDGE('',*,*,#1634,.F.);
#2347=ORIENTED_EDGE('',*,*,#1631,.F.);
#2348=ORIENTED_EDGE('',*,*,#1628,.F.);
#2349=ORIENTED_EDGE('',*,*,#1697,.F.);
#2350=ORIENTED_EDGE('',*,*,#1698,.T.);
#2351=ORIENTED_EDGE('',*,*,#1541,.T.);
#2352=ORIENTED_EDGE('',*,*,#1545,.T.);
#2353=ORIENTED_EDGE('',*,*,#1550,.T.);
#2354=ORIENTED_EDGE('',*,*,#1549,.T.);
#2355=ORIENTED_EDGE('',*,*,#1553,.T.);
#2356=ORIENTED_EDGE('',*,*,#1558,.T.);
#2357=ORIENTED_EDGE('',*,*,#1557,.T.);
#2358=ORIENTED_EDGE('',*,*,#1561,.T.);
#2359=ORIENTED_EDGE('',*,*,#1566,.T.);
#2360=ORIENTED_EDGE('',*,*,#1565,.T.);
#2361=ORIENTED_EDGE('',*,*,#1569,.T.);
#2362=ORIENTED_EDGE('',*,*,#1574,.T.);
#2363=ORIENTED_EDGE('',*,*,#1573,.T.);
#2364=ORIENTED_EDGE('',*,*,#1577,.T.);
#2365=ORIENTED_EDGE('',*,*,#1582,.T.);
#2366=ORIENTED_EDGE('',*,*,#1581,.T.);
#2367=ORIENTED_EDGE('',*,*,#1585,.T.);
#2368=ORIENTED_EDGE('',*,*,#1590,.T.);
#2369=ORIENTED_EDGE('',*,*,#1589,.T.);
#2370=ORIENTED_EDGE('',*,*,#1593,.T.);
#2371=ORIENTED_EDGE('',*,*,#1598,.T.);
#2372=ORIENTED_EDGE('',*,*,#1597,.T.);
#2373=ORIENTED_EDGE('',*,*,#1601,.T.);
#2374=ORIENTED_EDGE('',*,*,#1606,.T.);
#2375=ORIENTED_EDGE('',*,*,#1605,.T.);
#2376=ORIENTED_EDGE('',*,*,#1609,.T.);
#2377=ORIENTED_EDGE('',*,*,#1614,.T.);
#2378=ORIENTED_EDGE('',*,*,#1613,.T.);
#2379=ORIENTED_EDGE('',*,*,#1617,.T.);
#2380=ORIENTED_EDGE('',*,*,#1622,.T.);
#2381=ORIENTED_EDGE('',*,*,#1621,.T.);
#2382=ORIENTED_EDGE('',*,*,#1695,.T.);
#2383=ORIENTED_EDGE('',*,*,#1694,.T.);
#2384=ORIENTED_EDGE('',*,*,#1699,.F.);
#2385=ORIENTED_EDGE('',*,*,#1700,.F.);
#2386=ORIENTED_EDGE('',*,*,#1692,.F.);
#2387=ORIENTED_EDGE('',*,*,#1624,.F.);
#2388=ORIENTED_EDGE('',*,*,#1623,.F.);
#2389=ORIENTED_EDGE('',*,*,#1619,.F.);
#2390=ORIENTED_EDGE('',*,*,#1618,.F.);
#2391=ORIENTED_EDGE('',*,*,#1615,.F.);
#2392=ORIENTED_EDGE('',*,*,#1611,.F.);
#2393=ORIENTED_EDGE('',*,*,#1610,.F.);
#2394=ORIENTED_EDGE('',*,*,#1607,.F.);
#2395=ORIENTED_EDGE('',*,*,#1603,.F.);
#2396=ORIENTED_EDGE('',*,*,#1602,.F.);
#2397=ORIENTED_EDGE('',*,*,#1599,.F.);
#2398=ORIENTED_EDGE('',*,*,#1595,.F.);
#2399=ORIENTED_EDGE('',*,*,#1594,.F.);
#2400=ORIENTED_EDGE('',*,*,#1591,.F.);
#2401=ORIENTED_EDGE('',*,*,#1587,.F.);
#2402=ORIENTED_EDGE('',*,*,#1586,.F.);
#2403=ORIENTED_EDGE('',*,*,#1583,.F.);
#2404=ORIENTED_EDGE('',*,*,#1579,.F.);
#2405=ORIENTED_EDGE('',*,*,#1578,.F.);
#2406=ORIENTED_EDGE('',*,*,#1575,.F.);
#2407=ORIENTED_EDGE('',*,*,#1571,.F.);
#2408=ORIENTED_EDGE('',*,*,#1570,.F.);
#2409=ORIENTED_EDGE('',*,*,#1567,.F.);
#2410=ORIENTED_EDGE('',*,*,#1563,.F.);
#2411=ORIENTED_EDGE('',*,*,#1562,.F.);
#2412=ORIENTED_EDGE('',*,*,#1559,.F.);
#2413=ORIENTED_EDGE('',*,*,#1555,.F.);
#2414=ORIENTED_EDGE('',*,*,#1554,.F.);
#2415=ORIENTED_EDGE('',*,*,#1551,.F.);
#2416=ORIENTED_EDGE('',*,*,#1547,.F.);
#2417=ORIENTED_EDGE('',*,*,#1546,.F.);
#2418=ORIENTED_EDGE('',*,*,#1543,.F.);
#2419=ORIENTED_EDGE('',*,*,#1701,.F.);
#2420=ORIENTED_EDGE('',*,*,#1626,.F.);
#2421=ORIENTED_EDGE('',*,*,#1630,.F.);
#2422=ORIENTED_EDGE('',*,*,#1633,.F.);
#2423=ORIENTED_EDGE('',*,*,#1636,.F.);
#2424=ORIENTED_EDGE('',*,*,#1639,.F.);
#2425=ORIENTED_EDGE('',*,*,#1642,.F.);
#2426=ORIENTED_EDGE('',*,*,#1645,.F.);
#2427=ORIENTED_EDGE('',*,*,#1648,.F.);
#2428=ORIENTED_EDGE('',*,*,#1651,.F.);
#2429=ORIENTED_EDGE('',*,*,#1654,.F.);
#2430=ORIENTED_EDGE('',*,*,#1657,.F.);
#2431=ORIENTED_EDGE('',*,*,#1660,.F.);
#2432=ORIENTED_EDGE('',*,*,#1663,.F.);
#2433=ORIENTED_EDGE('',*,*,#1666,.F.);
#2434=ORIENTED_EDGE('',*,*,#1669,.F.);
#2435=ORIENTED_EDGE('',*,*,#1672,.F.);
#2436=ORIENTED_EDGE('',*,*,#1675,.F.);
#2437=ORIENTED_EDGE('',*,*,#1678,.F.);
#2438=ORIENTED_EDGE('',*,*,#1681,.F.);
#2439=ORIENTED_EDGE('',*,*,#1684,.F.);
#2440=ORIENTED_EDGE('',*,*,#1687,.F.);
#2441=ORIENTED_EDGE('',*,*,#1691,.F.);
#2442=ORIENTED_EDGE('',*,*,#1696,.T.);
#2443=ORIENTED_EDGE('',*,*,#1693,.T.);
#2444=ORIENTED_EDGE('',*,*,#1700,.T.);
#2445=ORIENTED_EDGE('',*,*,#1699,.T.);
#2446=ORIENTED_EDGE('',*,*,#1690,.T.);
#2447=ORIENTED_EDGE('',*,*,#1697,.T.);
#2448=ORIENTED_EDGE('',*,*,#1627,.T.);
#2449=ORIENTED_EDGE('',*,*,#1701,.T.);
#2450=ORIENTED_EDGE('',*,*,#1542,.T.);
#2451=ORIENTED_EDGE('',*,*,#1698,.F.);
#2910=CYLINDRICAL_SURFACE('',#3352,1.17775);
#2911=CYLINDRICAL_SURFACE('',#3354,1.17775);
#2912=CYLINDRICAL_SURFACE('',#3355,1.17775);
#2913=CYLINDRICAL_SURFACE('',#3356,1.17775);
#2914=CYLINDRICAL_SURFACE('',#3357,1.17775);
#2915=CYLINDRICAL_SURFACE('',#3358,1.17775);
#2916=CYLINDRICAL_SURFACE('',#3359,1.17775);
#2917=CYLINDRICAL_SURFACE('',#3360,1.17775);
#2918=CYLINDRICAL_SURFACE('',#3361,1.17775);
#2919=CYLINDRICAL_SURFACE('',#3362,1.17775);
#2920=CYLINDRICAL_SURFACE('',#3363,1.17775);
#2921=CYLINDRICAL_SURFACE('',#3364,1.17775);
#2922=CYLINDRICAL_SURFACE('',#3365,1.17775);
#2923=CYLINDRICAL_SURFACE('',#3366,1.17775);
#2924=CYLINDRICAL_SURFACE('',#3367,1.17775);
#2925=CYLINDRICAL_SURFACE('',#3368,1.17775);
#2926=CYLINDRICAL_SURFACE('',#3369,1.17775);
#2927=CYLINDRICAL_SURFACE('',#3370,1.17775);
#2928=CYLINDRICAL_SURFACE('',#3371,1.17775);
#2929=CYLINDRICAL_SURFACE('',#3372,1.17775);
#2930=CYLINDRICAL_SURFACE('',#3373,1.17775);
#2931=CYLINDRICAL_SURFACE('',#3374,1.4635);
#2932=CYLINDRICAL_SURFACE('',#3376,1.4635);
#2933=CYLINDRICAL_SURFACE('',#3377,1.4635);
#2934=CYLINDRICAL_SURFACE('',#3378,1.4635);
#2935=CYLINDRICAL_SURFACE('',#3379,1.4635);
#2936=CYLINDRICAL_SURFACE('',#3380,1.4635);
#2937=CYLINDRICAL_SURFACE('',#3381,1.4635);
#2938=CYLINDRICAL_SURFACE('',#3382,1.4635);
#2939=CYLINDRICAL_SURFACE('',#3383,1.4635);
#2940=CYLINDRICAL_SURFACE('',#3384,1.4635);
#2941=CYLINDRICAL_SURFACE('',#3385,1.4635);
#2942=CYLINDRICAL_SURFACE('',#3386,1.4635);
#2943=CYLINDRICAL_SURFACE('',#3387,1.4635);
#2944=CYLINDRICAL_SURFACE('',#3388,1.4635);
#2945=CYLINDRICAL_SURFACE('',#3389,1.4635);
#2946=CYLINDRICAL_SURFACE('',#3390,1.4635);
#2947=CYLINDRICAL_SURFACE('',#3391,1.4635);
#2948=CYLINDRICAL_SURFACE('',#3392,1.4635);
#2949=CYLINDRICAL_SURFACE('',#3393,1.4635);
#2950=CYLINDRICAL_SURFACE('',#3394,1.4635);
#2951=CYLINDRICAL_SURFACE('',#3395,1.4635);
#2952=CYLINDRICAL_SURFACE('',#3396,1.4635);
#2953=CYLINDRICAL_SURFACE('',#3398,1.17775);
#3052=ADVANCED_FACE('',(#473),#2910,.T.);
#3053=ADVANCED_FACE('',(#474),#2911,.T.);
#3054=ADVANCED_FACE('',(#475),#2912,.T.);
#3055=ADVANCED_FACE('',(#476),#2913,.T.);
#3056=ADVANCED_FACE('',(#477),#2914,.T.);
#3057=ADVANCED_FACE('',(#478),#2915,.T.);
#3058=ADVANCED_FACE('',(#479),#2916,.T.);
#3059=ADVANCED_FACE('',(#480),#2917,.T.);
#3060=ADVANCED_FACE('',(#481),#2918,.T.);
#3061=ADVANCED_FACE('',(#482),#2919,.T.);
#3062=ADVANCED_FACE('',(#483),#2920,.T.);
#3063=ADVANCED_FACE('',(#484),#2921,.T.);
#3064=ADVANCED_FACE('',(#485),#2922,.T.);
#3065=ADVANCED_FACE('',(#486),#2923,.T.);
#3066=ADVANCED_FACE('',(#487),#2924,.T.);
#3067=ADVANCED_FACE('',(#488),#2925,.T.);
#3068=ADVANCED_FACE('',(#489),#2926,.T.);
#3069=ADVANCED_FACE('',(#490),#2927,.T.);
#3070=ADVANCED_FACE('',(#491),#2928,.T.);
#3071=ADVANCED_FACE('',(#492),#2929,.T.);
#3072=ADVANCED_FACE('',(#493),#2930,.T.);
#3073=ADVANCED_FACE('',(#494),#2931,.T.);
#3074=ADVANCED_FACE('',(#495),#2932,.T.);
#3075=ADVANCED_FACE('',(#496),#2933,.T.);
#3076=ADVANCED_FACE('',(#497),#2934,.T.);
#3077=ADVANCED_FACE('',(#498),#2935,.T.);
#3078=ADVANCED_FACE('',(#499),#2936,.T.);
#3079=ADVANCED_FACE('',(#500),#2937,.T.);
#3080=ADVANCED_FACE('',(#501),#2938,.T.);
#3081=ADVANCED_FACE('',(#502),#2939,.T.);
#3082=ADVANCED_FACE('',(#503),#2940,.T.);
#3083=ADVANCED_FACE('',(#504),#2941,.T.);
#3084=ADVANCED_FACE('',(#505),#2942,.T.);
#3085=ADVANCED_FACE('',(#506),#2943,.T.);
#3086=ADVANCED_FACE('',(#507),#2944,.T.);
#3087=ADVANCED_FACE('',(#508),#2945,.T.);
#3088=ADVANCED_FACE('',(#509),#2946,.T.);
#3089=ADVANCED_FACE('',(#510),#2947,.T.);
#3090=ADVANCED_FACE('',(#511),#2948,.T.);
#3091=ADVANCED_FACE('',(#512),#2949,.T.);
#3092=ADVANCED_FACE('',(#513),#2950,.T.);
#3093=ADVANCED_FACE('',(#514),#2951,.T.);
#3094=ADVANCED_FACE('',(#515),#2952,.T.);
#3095=ADVANCED_FACE('',(#516),#2953,.T.);
#3096=ADVANCED_FACE('',(#517),#45,.F.);
#3097=ADVANCED_FACE('',(#518),#46,.F.);
#3098=ADVANCED_FACE('',(#519),#415,.F.);
#3099=ADVANCED_FACE('',(#520),#416,.T.);
#3172=CLOSED_SHELL('',(#3052,#3053,#3054,#3055,#3056,#3057,#3058,#3059,
#3060,#3061,#3062,#3063,#3064,#3065,#3066,#3067,#3068,#3069,#3070,#3071,
#3072,#3073,#3074,#3075,#3076,#3077,#3078,#3079,#3080,#3081,#3082,#3083,
#3084,#3085,#3086,#3087,#3088,#3089,#3090,#3091,#3092,#3093,#3094,#3095,
#3096,#3097,#3098,#3099));
#3351=AXIS2_PLACEMENT_3D('',#6484,#3690,#3691);
#3352=AXIS2_PLACEMENT_3D('',#6485,#3692,#3693);
#3353=AXIS2_PLACEMENT_3D('',#6595,#3695,#3696);
#3354=AXIS2_PLACEMENT_3D('',#6651,#3697,#3698);
#3355=AXIS2_PLACEMENT_3D('',#7079,#3700,#3701);
#3356=AXIS2_PLACEMENT_3D('',#7526,#3703,#3704);
#3357=AXIS2_PLACEMENT_3D('',#7973,#3706,#3707);
#3358=AXIS2_PLACEMENT_3D('',#8418,#3709,#3710);
#3359=AXIS2_PLACEMENT_3D('',#8867,#3712,#3713);
#3360=AXIS2_PLACEMENT_3D('',#9308,#3715,#3716);
#3361=AXIS2_PLACEMENT_3D('',#9755,#3718,#3719);
#3362=AXIS2_PLACEMENT_3D('',#10206,#3721,#3722);
#3363=AXIS2_PLACEMENT_3D('',#10643,#3724,#3725);
#3364=AXIS2_PLACEMENT_3D('',#11118,#3727,#3728);
#3365=AXIS2_PLACEMENT_3D('',#11571,#3730,#3731);
#3366=AXIS2_PLACEMENT_3D('',#12020,#3733,#3734);
#3367=AXIS2_PLACEMENT_3D('',#12467,#3736,#3737);
#3368=AXIS2_PLACEMENT_3D('',#12920,#3739,#3740);
#3369=AXIS2_PLACEMENT_3D('',#13397,#3742,#3743);
#3370=AXIS2_PLACEMENT_3D('',#13852,#3745,#3746);
#3371=AXIS2_PLACEMENT_3D('',#14323,#3748,#3749);
#3372=AXIS2_PLACEMENT_3D('',#14760,#3751,#3752);
#3373=AXIS2_PLACEMENT_3D('',#15178,#3754,#3755);
#3374=AXIS2_PLACEMENT_3D('',#15631,#3757,#3758);
#3375=AXIS2_PLACEMENT_3D('',#15643,#3760,#3761);
#3376=AXIS2_PLACEMENT_3D('',#15649,#3762,#3763);
#3377=AXIS2_PLACEMENT_3D('',#15835,#3765,#3766);
#3378=AXIS2_PLACEMENT_3D('',#16021,#3768,#3769);
#3379=AXIS2_PLACEMENT_3D('',#16369,#3771,#3772);
#3380=AXIS2_PLACEMENT_3D('',#16393,#3774,#3775);
#3381=AXIS2_PLACEMENT_3D('',#16417,#3777,#3778);
#3382=AXIS2_PLACEMENT_3D('',#16604,#3780,#3781);
#3383=AXIS2_PLACEMENT_3D('',#16952,#3783,#3784);
#3384=AXIS2_PLACEMENT_3D('',#16976,#3786,#3787);
#3385=AXIS2_PLACEMENT_3D('',#17002,#3789,#3790);
#3386=AXIS2_PLACEMENT_3D('',#17188,#3792,#3793);
#3387=AXIS2_PLACEMENT_3D('',#17536,#3795,#3796);
#3388=AXIS2_PLACEMENT_3D('',#17562,#3798,#3799);
#3389=AXIS2_PLACEMENT_3D('',#17586,#3801,#3802);
#3390=AXIS2_PLACEMENT_3D('',#17772,#3804,#3805);
#3391=AXIS2_PLACEMENT_3D('',#18120,#3807,#3808);
#3392=AXIS2_PLACEMENT_3D('',#18144,#3810,#3811);
#3393=AXIS2_PLACEMENT_3D('',#18168,#3813,#3814);
#3394=AXIS2_PLACEMENT_3D('',#18355,#3816,#3817);
#3395=AXIS2_PLACEMENT_3D('',#18703,#3819,#3820);
#3396=AXIS2_PLACEMENT_3D('',#18727,#3822,#3823);
#3397=AXIS2_PLACEMENT_3D('',#18739,#3824,#3825);
#3398=AXIS2_PLACEMENT_3D('',#18748,#3826,#3827);
#3399=AXIS2_PLACEMENT_3D('',#18971,#3828,#3829);
#3400=AXIS2_PLACEMENT_3D('',#20483,#3830,#3831);
#3401=AXIS2_PLACEMENT_3D('',#20484,#3832,#3833);
#3690=DIRECTION('axis',(0.,0.,1.));
#3691=DIRECTION('refdir',(1.,0.,0.));
#3692=DIRECTION('center_axis',(0.,0.,-1.));
#3693=DIRECTION('ref_axis',(-0.457355310655569,0.889284049005237,0.));
#3694=DIRECTION('',(0.,0.,1.));
#3695=DIRECTION('center_axis',(0.,0.,1.));
#3696=DIRECTION('ref_axis',(1.,-4.0036529262094E-14,0.));
#3697=DIRECTION('center_axis',(0.,0.,-1.));
#3698=DIRECTION('ref_axis',(-0.457355310655569,0.889284049005237,0.));
#3699=DIRECTION('',(0.,0.,1.));
#3700=DIRECTION('center_axis',(0.,0.,-1.));
#3701=DIRECTION('ref_axis',(-0.457355310655569,0.889284049005237,0.));
#3702=DIRECTION('',(0.,0.,1.));
#3703=DIRECTION('center_axis',(0.,0.,-1.));
#3704=DIRECTION('ref_axis',(-0.457355310655569,0.889284049005237,0.));
#3705=DIRECTION('',(0.,0.,1.));
#3706=DIRECTION('center_axis',(0.,0.,-1.));
#3707=DIRECTION('ref_axis',(-0.457355310655569,0.889284049005237,0.));
#3708=DIRECTION('',(0.,0.,1.));
#3709=DIRECTION('center_axis',(0.,0.,-1.));
#3710=DIRECTION('ref_axis',(-0.457355310655569,0.889284049005237,0.));
#3711=DIRECTION('',(0.,0.,1.));
#3712=DIRECTION('center_axis',(0.,0.,-1.));
#3713=DIRECTION('ref_axis',(-0.457355310655569,0.889284049005237,0.));
#3714=DIRECTION('',(0.,0.,1.));
#3715=DIRECTION('center_axis',(0.,0.,-1.));
#3716=DIRECTION('ref_axis',(-0.457355310655569,0.889284049005237,0.));
#3717=DIRECTION('',(0.,0.,1.));
#3718=DIRECTION('center_axis',(0.,0.,-1.));
#3719=DIRECTION('ref_axis',(-0.457355310655569,0.889284049005237,0.));
#3720=DIRECTION('',(0.,0.,1.));
#3721=DIRECTION('center_axis',(0.,0.,-1.));
#3722=DIRECTION('ref_axis',(-0.457355310655569,0.889284049005237,0.));
#3723=DIRECTION('',(0.,0.,1.));
#3724=DIRECTION('center_axis',(0.,0.,-1.));
#3725=DIRECTION('ref_axis',(-0.457355310655569,0.889284049005237,0.));
#3726=DIRECTION('',(0.,0.,1.));
#3727=DIRECTION('center_axis',(0.,0.,-1.));
#3728=DIRECTION('ref_axis',(-0.457355310655569,0.889284049005237,0.));
#3729=DIRECTION('',(0.,0.,1.));
#3730=DIRECTION('center_axis',(0.,0.,-1.));
#3731=DIRECTION('ref_axis',(-0.457355310655569,0.889284049005237,0.));
#3732=DIRECTION('',(0.,0.,1.));
#3733=DIRECTION('center_axis',(0.,0.,-1.));
#3734=DIRECTION('ref_axis',(-0.457355310655569,0.889284049005237,0.));
#3735=DIRECTION('',(0.,0.,1.));
#3736=DIRECTION('center_axis',(0.,0.,-1.));
#3737=DIRECTION('ref_axis',(-0.457355310655569,0.889284049005237,0.));
#3738=DIRECTION('',(0.,0.,1.));
#3739=DIRECTION('center_axis',(0.,0.,-1.));
#3740=DIRECTION('ref_axis',(-0.457355310655569,0.889284049005237,0.));
#3741=DIRECTION('',(0.,0.,1.));
#3742=DIRECTION('center_axis',(0.,0.,-1.));
#3743=DIRECTION('ref_axis',(-0.457355310655569,0.889284049005237,0.));
#3744=DIRECTION('',(0.,0.,1.));
#3745=DIRECTION('center_axis',(0.,0.,-1.));
#3746=DIRECTION('ref_axis',(-0.457355310655569,0.889284049005237,0.));
#3747=DIRECTION('',(0.,0.,1.));
#3748=DIRECTION('center_axis',(0.,0.,-1.));
#3749=DIRECTION('ref_axis',(-0.457355310655569,0.889284049005237,0.));
#3750=DIRECTION('',(0.,0.,1.));
#3751=DIRECTION('center_axis',(0.,0.,-1.));
#3752=DIRECTION('ref_axis',(-0.457355310655569,0.889284049005237,0.));
#3753=DIRECTION('',(0.,0.,1.));
#3754=DIRECTION('center_axis',(0.,0.,-1.));
#3755=DIRECTION('ref_axis',(-0.457355310655569,0.889284049005237,0.));
#3756=DIRECTION('',(0.,0.,1.));
#3757=DIRECTION('center_axis',(0.,0.,-1.));
#3758=DIRECTION('ref_axis',(1.,0.,0.));
#3759=DIRECTION('',(0.,0.,1.));
#3760=DIRECTION('center_axis',(0.,0.,-1.));
#3761=DIRECTION('ref_axis',(1.,0.,0.));
#3762=DIRECTION('center_axis',(0.,0.,-1.));
#3763=DIRECTION('ref_axis',(1.,0.,0.));
#3764=DIRECTION('',(0.,0.,1.));
#3765=DIRECTION('center_axis',(0.,0.,-1.));
#3766=DIRECTION('ref_axis',(1.,0.,0.));
#3767=DIRECTION('',(0.,0.,1.));
#3768=DIRECTION('center_axis',(0.,0.,-1.));
#3769=DIRECTION('ref_axis',(1.,0.,0.));
#3770=DIRECTION('',(0.,0.,1.));
#3771=DIRECTION('center_axis',(0.,0.,-1.));
#3772=DIRECTION('ref_axis',(1.,0.,0.));
#3773=DIRECTION('',(0.,0.,1.));
#3774=DIRECTION('center_axis',(0.,0.,-1.));
#3775=DIRECTION('ref_axis',(1.,0.,0.));
#3776=DIRECTION('',(0.,0.,1.));
#3777=DIRECTION('center_axis',(0.,0.,-1.));
#3778=DIRECTION('ref_axis',(1.,0.,0.));
#3779=DIRECTION('',(0.,0.,1.));
#3780=DIRECTION('center_axis',(0.,0.,-1.));
#3781=DIRECTION('ref_axis',(1.,0.,0.));
#3782=DIRECTION('',(0.,0.,1.));
#3783=DIRECTION('center_axis',(0.,0.,-1.));
#3784=DIRECTION('ref_axis',(1.,0.,0.));
#3785=DIRECTION('',(0.,0.,1.));
#3786=DIRECTION('center_axis',(0.,0.,-1.));
#3787=DIRECTION('ref_axis',(1.,0.,0.));
#3788=DIRECTION('',(0.,0.,1.));
#3789=DIRECTION('center_axis',(0.,0.,-1.));
#3790=DIRECTION('ref_axis',(1.,0.,0.));
#3791=DIRECTION('',(0.,0.,1.));
#3792=DIRECTION('center_axis',(0.,0.,-1.));
#3793=DIRECTION('ref_axis',(1.,0.,0.));
#3794=DIRECTION('',(0.,0.,1.));
#3795=DIRECTION('center_axis',(0.,0.,-1.));
#3796=DIRECTION('ref_axis',(1.,0.,0.));
#3797=DIRECTION('',(0.,0.,1.));
#3798=DIRECTION('center_axis',(0.,0.,-1.));
#3799=DIRECTION('ref_axis',(1.,0.,0.));
#3800=DIRECTION('',(0.,0.,1.));
#3801=DIRECTION('center_axis',(0.,0.,-1.));
#3802=DIRECTION('ref_axis',(1.,0.,0.));
#3803=DIRECTION('',(0.,0.,1.));
#3804=DIRECTION('center_axis',(0.,0.,-1.));
#3805=DIRECTION('ref_axis',(1.,0.,0.));
#3806=DIRECTION('',(0.,0.,1.));
#3807=DIRECTION('center_axis',(0.,0.,-1.));
#3808=DIRECTION('ref_axis',(1.,0.,0.));
#3809=DIRECTION('',(0.,0.,1.));
#3810=DIRECTION('center_axis',(0.,0.,-1.));
#3811=DIRECTION('ref_axis',(1.,0.,0.));
#3812=DIRECTION('',(0.,0.,1.));
#3813=DIRECTION('center_axis',(0.,0.,-1.));
#3814=DIRECTION('ref_axis',(1.,0.,0.));
#3815=DIRECTION('',(0.,0.,1.));
#3816=DIRECTION('center_axis',(0.,0.,-1.));
#3817=DIRECTION('ref_axis',(1.,0.,0.));
#3818=DIRECTION('',(0.,0.,1.));
#3819=DIRECTION('center_axis',(0.,0.,-1.));
#3820=DIRECTION('ref_axis',(1.,0.,0.));
#3821=DIRECTION('',(0.,0.,1.));
#3822=DIRECTION('center_axis',(0.,0.,-1.));
#3823=DIRECTION('ref_axis',(1.,0.,0.));
#3824=DIRECTION('center_axis',(0.,0.,-1.));
#3825=DIRECTION('ref_axis',(1.,0.,0.));
#3826=DIRECTION('center_axis',(0.,0.,-1.));
#3827=DIRECTION('ref_axis',(-0.457355310655569,0.889284049005237,0.));
#3828=DIRECTION('center_axis',(0.,0.,-1.));
#3829=DIRECTION('ref_axis',(1.,-4.0036529262094E-14,0.));
#3830=DIRECTION('center_axis',(0.,0.,1.));
#3831=DIRECTION('ref_axis',(1.,0.,0.));
#3832=DIRECTION('center_axis',(0.,0.,1.));
#3833=DIRECTION('ref_axis',(1.,0.,0.));
#6484=CARTESIAN_POINT('',(0.,0.,0.));
#6485=CARTESIAN_POINT('Origin',(3.53951905042299,8.32667268468867E-16,0.924367114736157));
#6486=CARTESIAN_POINT('',(4.07816931076926,-1.04735426648718,-0.262501355395651));
#6487=CARTESIAN_POINT('',(4.07816926754758,-1.04735428871592,-0.162850680997093));
#6488=CARTESIAN_POINT('',(4.07816926754759,-1.04735428871592,0.924367114736157));
#6489=CARTESIAN_POINT('',(2.86617836717395,0.966285354738297,1.30764946397119E-15));
#6490=CARTESIAN_POINT('Ctrl Pts',(4.07816931076926,-1.04735426648718,-0.262501355395651));
#6491=CARTESIAN_POINT('Ctrl Pts',(4.13816550929519,-1.01649845294839,-0.257760959449959));
#6492=CARTESIAN_POINT('Ctrl Pts',(4.19540688115252,-0.980540763988985,-0.252855425799963));
#6493=CARTESIAN_POINT('Ctrl Pts',(4.30612909358366,-0.896929430168507,-0.242678032345055));
#6494=CARTESIAN_POINT('Ctrl Pts',(4.35898806098992,-0.848908539803626,-0.237423776835087));
#6495=CARTESIAN_POINT('Ctrl Pts',(4.41381673949112,-0.789173500392151,-0.231741146856556));
#6496=CARTESIAN_POINT('Ctrl Pts',(4.4203588187141,-0.781864809957386,-0.231059038775153));
#6497=CARTESIAN_POINT('Ctrl Pts',(4.42936456010577,-0.771547233408173,-0.230115323768185));
#6498=CARTESIAN_POINT('Ctrl Pts',(4.43190557214461,-0.768606831483667,-0.229848510688452));
#6499=CARTESIAN_POINT('Ctrl Pts',(4.43628102834384,-0.7634927025417,-0.22938821683561));
#6500=CARTESIAN_POINT('Ctrl Pts',(4.43812221904588,-0.76132483058054,-0.22919425806598));
#6501=CARTESIAN_POINT('Ctrl Pts',(4.4419940328539,-0.756732429561088,-0.228785856907052));
#6502=CARTESIAN_POINT('Ctrl Pts',(4.44402276326807,-0.754306368515252,-0.228571560869313));
#6503=CARTESIAN_POINT('Ctrl Pts',(4.44906391192553,-0.748228319777068,-0.228038218896995));
#6504=CARTESIAN_POINT('Ctrl Pts',(4.45206417443405,-0.744566230880235,-0.227720036311731));
#6505=CARTESIAN_POINT('Ctrl Pts',(4.4635118607649,-0.730420164685874,-0.226502596978593));
#6506=CARTESIAN_POINT('Ctrl Pts',(4.47180174820231,-0.719809238841447,-0.225613787694774));
#6507=CARTESIAN_POINT('Ctrl Pts',(4.49281897725252,-0.691935104910647,-0.2233344621005));
#6508=CARTESIAN_POINT('Ctrl Pts',(4.50526041034554,-0.674461769680659,-0.221959206687815));
#6509=CARTESIAN_POINT('Ctrl Pts',(4.54393811714973,-0.616874402055789,-0.217562693758889));
#6510=CARTESIAN_POINT('Ctrl Pts',(4.56820618750021,-0.575495412961658,-0.214608207433024));
#6511=CARTESIAN_POINT('Ctrl Pts',(4.62526109382569,-0.46300640102283,-0.206815767260325));
#6512=CARTESIAN_POINT('Ctrl Pts',(4.65359724115015,-0.389921160068868,-0.201974641152135));
#6513=CARTESIAN_POINT('Ctrl Pts',(4.67862153917193,-0.299634523535007,-0.195871749338333));
#6514=CARTESIAN_POINT('Ctrl Pts',(4.68246619326538,-0.284617496968038,-0.194853457399708));
#6515=CARTESIAN_POINT('Ctrl Pts',(4.68762666705435,-0.262666457670646,-0.193358256177876));
#6516=CARTESIAN_POINT('Ctrl Pts',(4.68917841867376,-0.255789172372448,-0.192888861792896));
#6517=CARTESIAN_POINT('Ctrl Pts',(4.69181882450146,-0.243577362041553,-0.192053506347722));
#6518=CARTESIAN_POINT('Ctrl Pts',(4.69293241996632,-0.238248395356479,-0.191688349687422));
#6519=CARTESIAN_POINT('Ctrl Pts',(4.69517493593701,-0.227132770342401,-0.190925282428703));
#6520=CARTESIAN_POINT('Ctrl Pts',(4.69629742865534,-0.22134498536421,-0.190527179087801));
#6521=CARTESIAN_POINT('Ctrl Pts',(4.6991075394683,-0.206250014609,-0.189486738128586));
#6522=CARTESIAN_POINT('Ctrl Pts',(4.70072654364688,-0.196930650270888,-0.188842255840524));
#6523=CARTESIAN_POINT('Ctrl Pts',(4.70755352597748,-0.154616561061837,-0.185905682610639));
#6524=CARTESIAN_POINT('Ctrl Pts',(4.71146816972925,-0.121431845216441,-0.183573664947217));
#6525=CARTESIAN_POINT('Ctrl Pts',(4.7222007063528,0.0215960176556974,-0.173392427299512));
#6526=CARTESIAN_POINT('Ctrl Pts',(4.7150171499791,0.131911029667048,-0.165146131316402));
#6527=CARTESIAN_POINT('Ctrl Pts',(4.68764035004445,0.263657969696757,-0.155483063352771));
#6528=CARTESIAN_POINT('Ctrl Pts',(4.6818933217096,0.287540033878893,-0.153742465559107));
#6529=CARTESIAN_POINT('Ctrl Pts',(4.67381354591698,0.31702878431748,-0.151620868600707));
#6530=CARTESIAN_POINT('Ctrl Pts',(4.67217935970378,0.322818649137025,-0.151205659590905));
#6531=CARTESIAN_POINT('Ctrl Pts',(4.66952958748343,0.331938800090816,-0.150554031777303));
#6532=CARTESIAN_POINT('Ctrl Pts',(4.6685435046414,0.335277442496423,-0.150315999857958));
#6533=CARTESIAN_POINT('Ctrl Pts',(4.66675225279319,0.34124467336953,-0.149891537487618));
#6534=CARTESIAN_POINT('Ctrl Pts',(4.66595268757235,0.343874804090377,-0.149704797040631));
#6535=CARTESIAN_POINT('Ctrl Pts',(4.66400429706283,0.350204220881102,-0.149256203118779));
#6536=CARTESIAN_POINT('Ctrl Pts',(4.6628464201863,0.353900674827748,-0.148994873079714));
#6537=CARTESIAN_POINT('Ctrl Pts',(4.65924128714954,0.365213878672216,-0.148196873893526));
#6538=CARTESIAN_POINT('Ctrl Pts',(4.65673458250859,0.37281165228385,-0.147663480767335));
#6539=CARTESIAN_POINT('Ctrl Pts',(4.65070235991253,0.3904877728462,-0.146427187882288));
#6540=CARTESIAN_POINT('Ctrl Pts',(4.64711678380012,0.400545036969767,-0.145727318775054));
#6541=CARTESIAN_POINT('Ctrl Pts',(4.6339872215201,0.435847231618147,-0.143278675086443));
#6542=CARTESIAN_POINT('Ctrl Pts',(4.62371233511675,0.460812876058328,-0.141561441921139));
#6543=CARTESIAN_POINT('Ctrl Pts',(4.57996758790865,0.557517959585241,-0.134886761353886));
#6544=CARTESIAN_POINT('Ctrl Pts',(4.54016092197969,0.626159728430909,-0.130084903250573));
#6545=CARTESIAN_POINT('Ctrl Pts',(4.46659256838585,0.727859655020217,-0.122197192651481));
#6546=CARTESIAN_POINT('Ctrl Pts',(4.43722437578685,0.763786207839597,-0.119234669369417));
#6547=CARTESIAN_POINT('Ctrl Pts',(4.39853048789781,0.805797813695031,-0.115480076350559));
#6548=CARTESIAN_POINT('Ctrl Pts',(4.39113543028509,0.813609424325328,-0.11476870308578));
#6549=CARTESIAN_POINT('Ctrl Pts',(4.37924973285856,0.825825029854022,-0.113634342328986));
#6550=CARTESIAN_POINT('Ctrl Pts',(4.3748289102129,0.830296353430724,-0.11321433654788));
#6551=CARTESIAN_POINT('Ctrl Pts',(4.3665082443372,0.83857835839877,-0.112427231231687));
#6552=CARTESIAN_POINT('Ctrl Pts',(4.36261731559497,0.842397788573141,-0.11206052573141));
#6553=CARTESIAN_POINT('Ctrl Pts',(4.35387656196646,0.850859551665857,-0.111239670772204));
#6554=CARTESIAN_POINT('Ctrl Pts',(4.34901331199061,0.855487679951562,-0.110784933099378));
#6555=CARTESIAN_POINT('Ctrl Pts',(4.33455613023088,0.869012250190631,-0.109438706396591));
#6556=CARTESIAN_POINT('Ctrl Pts',(4.32485347967524,0.877790441808004,-0.108542344696331));
#6557=CARTESIAN_POINT('Ctrl Pts',(4.26077881466586,0.93384736061385,-0.102666467791259));
#6558=CARTESIAN_POINT('Ctrl Pts',(4.20232102972743,0.97620529648228,-0.0974916761104508));
#6559=CARTESIAN_POINT('Ctrl Pts',(4.07211685570001,1.05343834723275,-0.0864287426029128));
#6560=CARTESIAN_POINT('Ctrl Pts',(3.99994258612451,1.08692428653761,-0.0805489349057646));
#6561=CARTESIAN_POINT('Ctrl Pts',(3.91355719641518,1.11684187728582,-0.0741140552653006));
#6562=CARTESIAN_POINT('Ctrl Pts',(3.90210839820426,1.12061113066185,-0.0732731940006031));
#6563=CARTESIAN_POINT('Ctrl Pts',(3.88615710198964,1.12559265263226,-0.0721199958198652));
#6564=CARTESIAN_POINT('Ctrl Pts',(3.88170268793243,1.12695479877715,-0.0717999317519526));
#6565=CARTESIAN_POINT('Ctrl Pts',(3.87421306498854,1.12919660102562,-0.0712652072392914));
#6566=CARTESIAN_POINT('Ctrl Pts',(3.87118223068805,1.13009051981056,-0.0710497608330243));
#6567=CARTESIAN_POINT('Ctrl Pts',(3.86502742030902,1.13187893437307,-0.0706141865561824));
#6568=CARTESIAN_POINT('Ctrl Pts',(3.86190331726675,1.13277270715122,-0.0703940957941245));
#6569=CARTESIAN_POINT('Ctrl Pts',(3.85395803619936,1.13501023579287,-0.0698368025066016));
#6570=CARTESIAN_POINT('Ctrl Pts',(3.84913186046174,1.13633622716197,-0.0695005691621308));
#6571=CARTESIAN_POINT('Ctrl Pts',(3.83011999513144,1.14142961887213,-0.0681844603270428));
#6572=CARTESIAN_POINT('Ctrl Pts',(3.81587217898588,1.14496265396246,-0.0672165297757819));
#6573=CARTESIAN_POINT('Ctrl Pts',(3.77811043176378,1.15358042621109,-0.0646904738735653));
#6574=CARTESIAN_POINT('Ctrl Pts',(3.75449964641512,1.15821290470527,-0.0631508132919473));
#6575=CARTESIAN_POINT('Ctrl Pts',(3.67970544957271,1.1705213458426,-0.0583521744794719));
#6576=CARTESIAN_POINT('Ctrl Pts',(3.62814852508006,1.17554995615846,-0.0551573055353008));
#6577=CARTESIAN_POINT('Ctrl Pts',(3.50563494505662,1.17939105836018,-0.0475283777116149));
#6578=CARTESIAN_POINT('Ctrl Pts',(3.43479699254525,1.17522033949375,-0.0430809171857789));
#6579=CARTESIAN_POINT('Ctrl Pts',(3.35444620471573,1.16316466451054,-0.0377452881286854));
#6580=CARTESIAN_POINT('Ctrl Pts',(3.34414597583988,1.16147894757009,-0.0370559974738152));
#6581=CARTESIAN_POINT('Ctrl Pts',(3.32717257087031,1.15846894566891,-0.0359106524132708));
#6582=CARTESIAN_POINT('Ctrl Pts',(3.32048590746682,1.15722331663216,-0.0354570009017416));
#6583=CARTESIAN_POINT('Ctrl Pts',(3.30838947893792,1.15486133015112,-0.034631714068847));
#6584=CARTESIAN_POINT('Ctrl Pts',(3.30297602833448,1.15376469336405,-0.0342606960157208));
#6585=CARTESIAN_POINT('Ctrl Pts',(3.29133535025683,1.15132119951867,-0.0334591600867042));
#6586=CARTESIAN_POINT('Ctrl Pts',(3.28511096165394,1.14996181464974,-0.0330282645783143));
#6587=CARTESIAN_POINT('Ctrl Pts',(3.26797624459067,1.14607372973679,-0.0318355405930534));
#6588=CARTESIAN_POINT('Ctrl Pts',(3.25709071863468,1.14343985937194,-0.0310704672878365));
#6589=CARTESIAN_POINT('Ctrl Pts',(3.18929186352776,1.12600800713029,-0.0262576732137973));
#6590=CARTESIAN_POINT('Ctrl Pts',(3.13352468638961,1.10712229042616,-0.0220817387791934));
#6591=CARTESIAN_POINT('Ctrl Pts',(3.00443184308116,1.0523357870937,-0.0119100216368716));
#6592=CARTESIAN_POINT('Ctrl Pts',(2.93297576091339,1.01283206324342,-0.00585245073367892));
#6593=CARTESIAN_POINT('Ctrl Pts',(2.86617836717395,0.966285354738297,1.30764946397119E-15));
#6594=CARTESIAN_POINT('',(4.22418347496246,0.958295198918397,0.));
#6595=CARTESIAN_POINT('Origin',(3.53951905042299,8.32667268468867E-16,0.));
#6596=CARTESIAN_POINT('Ctrl Pts',(4.22418347496246,0.958295198918393,4.44089209850063E-16));
#6597=CARTESIAN_POINT('Ctrl Pts',(4.26382260582939,0.92997459086893,-0.00329165982698132));
#6598=CARTESIAN_POINT('Ctrl Pts',(4.30173542240052,0.89916685852182,-0.00658331965396309));
#6599=CARTESIAN_POINT('Ctrl Pts',(4.33761006999466,0.86610956984613,-0.00987497948094485));
#6600=CARTESIAN_POINT('Ctrl Pts',(4.37303430005125,0.833467325876437,-0.0131253114785776));
#6601=CARTESIAN_POINT('Ctrl Pts',(4.40647088077483,0.79863207783641,-0.0163756434762103));
#6602=CARTESIAN_POINT('Ctrl Pts',(4.43765337026355,0.76187256547571,-0.019625975473843));
#6603=CARTESIAN_POINT('Ctrl Pts',(4.4688290359802,0.725121097326283,-0.022875596190079));
#6604=CARTESIAN_POINT('Ctrl Pts',(4.49775125328327,0.686446597209151,-0.0261252169063152));
#6605=CARTESIAN_POINT('Ctrl Pts',(4.52419296687062,0.646151948668183,-0.0293748376225512));
#6606=CARTESIAN_POINT('Ctrl Pts',(4.5506380448392,0.60585217313124,-0.0326248718128573));
#6607=CARTESIAN_POINT('Ctrl Pts',(4.57460170861404,0.563932275665533,-0.0358749060031633));
#6608=CARTESIAN_POINT('Ctrl Pts',(4.59590072517422,0.520723362016513,-0.0391249401934693));
#6609=CARTESIAN_POINT('Ctrl Pts',(4.61767731820734,0.476545597973794,-0.0424478481646437));
#6610=CARTESIAN_POINT('Ctrl Pts',(4.63666802073486,0.431020796741864,-0.0457707561358183));
#6611=CARTESIAN_POINT('Ctrl Pts',(4.65272839029913,0.384525718401926,-0.0490936641069927));
#6612=CARTESIAN_POINT('Ctrl Pts',(4.66846915279708,0.338955908657327,-0.05235044502772));
#6613=CARTESIAN_POINT('Ctrl Pts',(4.68139509545731,0.292454626199629,-0.0556072259484471));
#6614=CARTESIAN_POINT('Ctrl Pts',(4.69142118679469,0.245390567712603,-0.0588640068691744));
#6615=CARTESIAN_POINT('Ctrl Pts',(4.70175263909914,0.196893096549577,-0.0622199783655723));
#6616=CARTESIAN_POINT('Ctrl Pts',(4.70900458391102,0.147798590244708,-0.0655759498619703));
#6617=CARTESIAN_POINT('Ctrl Pts',(4.71314140620248,0.098517148327605,-0.0689319213583682));
#6618=CARTESIAN_POINT('Ctrl Pts',(4.71727822849394,0.0492357064105011,-0.0722878928547662));
#6619=CARTESIAN_POINT('Ctrl Pts',(4.71829998113881,-0.000232073325149317,
-0.075643864351164));
#6620=CARTESIAN_POINT('Ctrl Pts',(4.71622928026619,-0.0494782526203934,
-0.078999835847562));
#6621=CARTESIAN_POINT('Ctrl Pts',(4.71419826096718,-0.0977807099542783,
-0.0822914956745437));
#6622=CARTESIAN_POINT('Ctrl Pts',(4.70918221066814,-0.146094497186642,-0.0855831555015257));
#6623=CARTESIAN_POINT('Ctrl Pts',(4.70117871293859,-0.194015182354719,-0.0888748153285074));
#6624=CARTESIAN_POINT('Ctrl Pts',(4.69354694837555,-0.23971012714772,-0.0920135896082097));
#6625=CARTESIAN_POINT('Ctrl Pts',(4.68319921317479,-0.285047032934924,-0.095152363887912));
#6626=CARTESIAN_POINT('Ctrl Pts',(4.67018650263742,-0.329675863543162,-0.0982911381676143));
#6627=CARTESIAN_POINT('Ctrl Pts',(4.65718861687458,-0.374253850605062,-0.101426336588094));
#6628=CARTESIAN_POINT('Ctrl Pts',(4.641531917044,-0.418124812744379,-0.104561535008573));
#6629=CARTESIAN_POINT('Ctrl Pts',(4.6233183718038,-0.460949122435977,-0.107696733429053));
#6630=CARTESIAN_POINT('Ctrl Pts',(4.60511713162024,-0.503744500058096,-0.11082981371198));
#6631=CARTESIAN_POINT('Ctrl Pts',(4.5843626867868,-0.545494100397139,-0.113962893994906));
#6632=CARTESIAN_POINT('Ctrl Pts',(4.56120581261628,-0.585876456651907,-0.117095974277833));
#6633=CARTESIAN_POINT('Ctrl Pts',(4.53805384812113,-0.62625025111813,-0.120228390291179));
#6634=CARTESIAN_POINT('Ctrl Pts',(4.51250074913838,-0.665256882154561,-0.123360806304525));
#6635=CARTESIAN_POINT('Ctrl Pts',(4.4847427284623,-0.702600356514171,-0.12649322231787));
#6636=CARTESIAN_POINT('Ctrl Pts',(4.45695818213,-0.739979516421182,-0.129628631678301));
#6637=CARTESIAN_POINT('Ctrl Pts',(4.42696485136167,-0.77569188988454,-0.132764041038732));
#6638=CARTESIAN_POINT('Ctrl Pts',(4.39500041587223,-0.8094730976809,-0.135899450399163));
#6639=CARTESIAN_POINT('Ctrl Pts',(4.36301801761838,-0.843273289196747,-0.139036621737203));
#6640=CARTESIAN_POINT('Ctrl Pts',(4.32906272850112,-0.87513976659434,-0.142173793075244));
#6641=CARTESIAN_POINT('Ctrl Pts',(4.29340766366195,-0.904846407590057,-0.145310964413285));
#6642=CARTESIAN_POINT('Ctrl Pts',(4.25768672285757,-0.934607934298585,-0.148453931959828));
#6643=CARTESIAN_POINT('Ctrl Pts',(4.22026020429182,-0.962201331231541,-0.15159689950637));
#6644=CARTESIAN_POINT('Ctrl Pts',(4.18143101926719,-0.987443206850178,-0.154739867052913));
#6645=CARTESIAN_POINT('Ctrl Pts',(4.16800681048762,-0.996169947009094,-0.155826468600317));
#6646=CARTESIAN_POINT('Ctrl Pts',(4.15441516069387,-1.00461602573018,-0.15691307014772));
#6647=CARTESIAN_POINT('Ctrl Pts',(4.14066920303589,-1.01277517569966,-0.157999671695124));
#6648=CARTESIAN_POINT('Ctrl Pts',(4.12021344700688,-1.02491704208196,-0.15961667479578));
#6649=CARTESIAN_POINT('Ctrl Pts',(4.09936714904988,-1.03645230111076,-0.161233677896437));
#6650=CARTESIAN_POINT('Ctrl Pts',(4.07816926754758,-1.04735428871592,-0.162850680997093));
#6651=CARTESIAN_POINT('Origin',(3.53951905042299,8.32667268468867E-16,0.924367114736157));
#6652=CARTESIAN_POINT('',(4.07816931162903,-1.047354266045,-0.76175719316035));
#6653=CARTESIAN_POINT('',(4.0781692670594,-1.04735428896699,-0.661995228290505));
#6654=CARTESIAN_POINT('',(4.07816926754759,-1.04735428871592,0.924367114736157));
#6655=CARTESIAN_POINT('Ctrl Pts',(4.07816931162903,-1.047354266045,-0.76175719316035));
#6656=CARTESIAN_POINT('Ctrl Pts',(4.11408449771752,-1.028883224302,-0.75925178827356));
#6657=CARTESIAN_POINT('Ctrl Pts',(4.14903578684085,-1.00857194726112,-0.756728985411424));
#6658=CARTESIAN_POINT('Ctrl Pts',(4.2007960181172,-0.974815447192962,-0.752791344928083));
#6659=CARTESIAN_POINT('Ctrl Pts',(4.21838604571316,-0.962648380607407,-0.751415312608433));
#6660=CARTESIAN_POINT('Ctrl Pts',(4.24838438327225,-0.940667235500158,-0.748993071487715));
#6661=CARTESIAN_POINT('Ctrl Pts',(4.26094451012015,-0.931069372113161,-0.747954718235958));
#6662=CARTESIAN_POINT('Ctrl Pts',(4.27894960649694,-0.916727631974777,-0.746428293310126));
#6663=CARTESIAN_POINT('Ctrl Pts',(4.28455047789923,-0.912181597427246,-0.745947959461167));
#6664=CARTESIAN_POINT('Ctrl Pts',(4.29433453304305,-0.904089992843911,-0.745098905772204));
#6665=CARTESIAN_POINT('Ctrl Pts',(4.29853541639712,-0.900566089975633,-0.744731059244522));
#6666=CARTESIAN_POINT('Ctrl Pts',(4.30723995822577,-0.893160132434266,-0.743961850541347));
#6667=CARTESIAN_POINT('Ctrl Pts',(4.3117391222387,-0.889273058682218,-0.743560290905421));
#6668=CARTESIAN_POINT('Ctrl Pts',(4.32339363388339,-0.879048949164388,-0.742509544390645));
#6669=CARTESIAN_POINT('Ctrl Pts',(4.33050149084711,-0.872658688850285,-0.741858179270333));
#6670=CARTESIAN_POINT('Ctrl Pts',(4.36008715374033,-0.845401507957279,-0.739101460142049));
#6671=CARTESIAN_POINT('Ctrl Pts',(4.38182137522774,-0.823748880257132,-0.736963353839677));
#6672=CARTESIAN_POINT('Ctrl Pts',(4.47365648348548,-0.72482038699092,-0.727406996775484));
#6673=CARTESIAN_POINT('Ctrl Pts',(4.5341517001094,-0.639278883383134,-0.719627547302095));
#6674=CARTESIAN_POINT('Ctrl Pts',(4.59269268464872,-0.527630994946312,-0.710508477288347));
#6675=CARTESIAN_POINT('Ctrl Pts',(4.60226786336298,-0.508069135975042,-0.708947669468941));
#6676=CARTESIAN_POINT('Ctrl Pts',(4.61694606614582,-0.475848566393389,-0.706447942174642));
#6677=CARTESIAN_POINT('Ctrl Pts',(4.6223810304526,-0.463347390777703,-0.705495008183453));
#6678=CARTESIAN_POINT('Ctrl Pts',(4.62942754962777,-0.44633773829989,-0.704223722673499));
#6679=CARTESIAN_POINT('Ctrl Pts',(4.6312302042334,-0.441910253211254,-0.703895105860567));
#6680=CARTESIAN_POINT('Ctrl Pts',(4.63419017831379,-0.434511621910368,-0.703349915704065));
#6681=CARTESIAN_POINT('Ctrl Pts',(4.63536246155079,-0.431546575476847,-0.70313247922492));
#6682=CARTESIAN_POINT('Ctrl Pts',(4.63755726769565,-0.425928654410585,-0.702722534290551));
#6683=CARTESIAN_POINT('Ctrl Pts',(4.63858224762229,-0.42327678206877,-0.702529877765054));
#6684=CARTESIAN_POINT('Ctrl Pts',(4.64098460495769,-0.416993737098885,-0.702075375912999));
#6685=CARTESIAN_POINT('Ctrl Pts',(4.64235365513237,-0.413359383977703,-0.701814015570827));
#6686=CARTESIAN_POINT('Ctrl Pts',(4.6471143769742,-0.40052929715995,-0.700896550309365));
#6687=CARTESIAN_POINT('Ctrl Pts',(4.65040932566734,-0.391297760024812,-0.700245786661472));
#6688=CARTESIAN_POINT('Ctrl Pts',(4.67668190005899,-0.314681260081685,-0.694913501140349));
#6689=CARTESIAN_POINT('Ctrl Pts',(4.69362443346622,-0.245371636196225,-0.690520723646131));
#6690=CARTESIAN_POINT('Ctrl Pts',(4.71294218216511,-0.116767203974033,-0.682476742640783));
#6691=CARTESIAN_POINT('Ctrl Pts',(4.71730924433082,-0.0580174760102126,
-0.678840815355901));
#6692=CARTESIAN_POINT('Ctrl Pts',(4.71725417857355,0.0220216548452417,-0.673739202646583));
#6693=CARTESIAN_POINT('Ctrl Pts',(4.71666656343383,0.0432277413949803,-0.672374017768371));
#6694=CARTESIAN_POINT('Ctrl Pts',(4.7146477537229,0.0800894300116951,-0.669969176964529));
#6695=CARTESIAN_POINT('Ctrl Pts',(4.71347515043739,0.0957539741828366,-0.668937221381266));
#6696=CARTESIAN_POINT('Ctrl Pts',(4.71130920694993,0.118552336391043,-0.667418537026304));
#6697=CARTESIAN_POINT('Ctrl Pts',(4.71056312962085,0.125708345514172,-0.666939436700112));
#6698=CARTESIAN_POINT('Ctrl Pts',(4.70913342086259,0.138301527783642,-0.666091858638477));
#6699=CARTESIAN_POINT('Ctrl Pts',(4.708477314275,0.143741656343089,-0.665724245326205));
#6700=CARTESIAN_POINT('Ctrl Pts',(4.70702935797867,0.155081181386098,-0.664954826762459));
#6701=CARTESIAN_POINT('Ctrl Pts',(4.70623070192685,0.160979536189289,-0.664552819428059));
#6702=CARTESIAN_POINT('Ctrl Pts',(4.70402842114411,0.176366043482055,-0.663499339699145));
#6703=CARTESIAN_POINT('Ctrl Pts',(4.7025535646726,0.185843388415899,-0.662845666701782));
#6704=CARTESIAN_POINT('Ctrl Pts',(4.69582292627179,0.225870030830573,-0.66006400337114));
#6705=CARTESIAN_POINT('Ctrl Pts',(4.68947834026259,0.256221093285343,-0.657902500612395));
#6706=CARTESIAN_POINT('Ctrl Pts',(4.66175928895829,0.366834741893492,-0.649826221414154));
#6707=CARTESIAN_POINT('Ctrl Pts',(4.63311311665378,0.445016349434409,-0.643705355196698));
#6708=CARTESIAN_POINT('Ctrl Pts',(4.57349100981242,0.566317723505985,-0.633811177738374));
#6709=CARTESIAN_POINT('Ctrl Pts',(4.54740564813502,0.611538782282844,-0.630028315018804));
#6710=CARTESIAN_POINT('Ctrl Pts',(4.51453737800882,0.660668387759828,-0.625917024807517));
#6711=CARTESIAN_POINT('Ctrl Pts',(4.5106178609278,0.666416209135279,-0.625436051349425));
#6712=CARTESIAN_POINT('Ctrl Pts',(4.5045583301707,0.675135284761337,-0.624706877598847));
#6713=CARTESIAN_POINT('Ctrl Pts',(4.50245509286179,0.678131730030445,-0.624456364723646));
#6714=CARTESIAN_POINT('Ctrl Pts',(4.49857887217485,0.683599716204206,-0.62399943936819));
#6715=CARTESIAN_POINT('Ctrl Pts',(4.49681028021669,0.686074205534111,-0.62379275103892));
#6716=CARTESIAN_POINT('Ctrl Pts',(4.49279566884896,0.691645418160335,-0.623327583656288));
#6717=CARTESIAN_POINT('Ctrl Pts',(4.49054413556597,0.694738068743461,-0.623069482746365));
#6718=CARTESIAN_POINT('Ctrl Pts',(4.48468548333397,0.702703515435972,-0.622404869374956));
#6719=CARTESIAN_POINT('Ctrl Pts',(4.48105568348254,0.707559600974885,-0.621999840755215));
#6720=CARTESIAN_POINT('Ctrl Pts',(4.45643277879081,0.739976041151459,-0.61929548392679));
#6721=CARTESIAN_POINT('Ctrl Pts',(4.4342677094121,0.766629421105363,-0.617068717688261));
#6722=CARTESIAN_POINT('Ctrl Pts',(4.39197017125308,0.813153627948617,-0.613095667419175));
#6723=CARTESIAN_POINT('Ctrl Pts',(4.37223764639561,0.83334962476219,-0.6113381980851));
#6724=CARTESIAN_POINT('Ctrl Pts',(4.31706497679318,0.885899642417509,-0.606614124979173));
#6725=CARTESIAN_POINT('Ctrl Pts',(4.28034418190566,0.916828160617236,-0.60366447820395));
#6726=CARTESIAN_POINT('Ctrl Pts',(4.19900455947919,0.977251953123329,-0.597328175616331));
#6727=CARTESIAN_POINT('Ctrl Pts',(4.15406105479072,1.00612104417369,-0.593936107167316));
#6728=CARTESIAN_POINT('Ctrl Pts',(4.09782796236123,1.0370648888041,-0.589717631800969));
#6729=CARTESIAN_POINT('Ctrl Pts',(4.08826535138482,1.04215637460957,-0.589001273482033));
#6730=CARTESIAN_POINT('Ctrl Pts',(4.07310138206807,1.04996365813097,-0.58786618172041));
#6731=CARTESIAN_POINT('Ctrl Pts',(4.0675462465069,1.05276828681743,-0.587450538969502));
#6732=CARTESIAN_POINT('Ctrl Pts',(4.05710439987679,1.05793663952144,-0.586669477544284));
#6733=CARTESIAN_POINT('Ctrl Pts',(4.05222304822086,1.06031086770052,-0.586304432982237));
#6734=CARTESIAN_POINT('Ctrl Pts',(4.04125803340685,1.06555069180061,-0.585484530986028));
#6735=CARTESIAN_POINT('Ctrl Pts',(4.03516592921754,1.06839807756334,-0.585029065845042));
#6736=CARTESIAN_POINT('Ctrl Pts',(4.01960214284205,1.07551066388787,-0.583865473250612));
#6737=CARTESIAN_POINT('Ctrl Pts',(4.01009796859312,1.07970293764442,-0.583154916002278));
#6738=CARTESIAN_POINT('Ctrl Pts',(3.93114963436176,1.11328650496325,-0.577251064435099));
#6739=CARTESIAN_POINT('Ctrl Pts',(3.85909799301456,1.13606636397634,-0.571836493757893));
#6740=CARTESIAN_POINT('Ctrl Pts',(3.72893207294945,1.16385091630774,-0.562100384833522));
#6741=CARTESIAN_POINT('Ctrl Pts',(3.6716772924882,1.17173405437578,-0.557837701210622));
#6742=CARTESIAN_POINT('Ctrl Pts',(3.59353599937772,1.17669059596362,-0.552183027628493));
#6743=CARTESIAN_POINT('Ctrl Pts',(3.57296562531858,1.17745488945251,-0.550710203259791));
#6744=CARTESIAN_POINT('Ctrl Pts',(3.5392954801517,1.17782271969558,-0.548335318281514));
#6745=CARTESIAN_POINT('Ctrl Pts',(3.5262041532421,1.17774749339292,-0.547420816853431));
#6746=CARTESIAN_POINT('Ctrl Pts',(3.50840960648368,1.17734847331151,-0.546192189089015));
#6747=CARTESIAN_POINT('Ctrl Pts',(3.50370364540243,1.17721471438579,-0.545868637771748));
#6748=CARTESIAN_POINT('Ctrl Pts',(3.49582678100196,1.17694355000632,-0.545329512527767));
#6749=CARTESIAN_POINT('Ctrl Pts',(3.49265544192516,1.17682154012441,-0.545113114684295));
#6750=CARTESIAN_POINT('Ctrl Pts',(3.48662904248441,1.17656528860321,-0.5447032060178));
#6751=CARTESIAN_POINT('Ctrl Pts',(3.48377392680237,1.17643347152374,-0.544509559187604));
#6752=CARTESIAN_POINT('Ctrl Pts',(3.4769863838525,1.17609533379558,-0.544050456644416));
#6753=CARTESIAN_POINT('Ctrl Pts',(3.47305442450417,1.17587968056627,-0.543785508299114));
#6754=CARTESIAN_POINT('Ctrl Pts',(3.45913654671919,1.17504630268861,-0.542851002320313));
#6755=CARTESIAN_POINT('Ctrl Pts',(3.44915716117522,1.17432104025507,-0.542187009214251));
#6756=CARTESIAN_POINT('Ctrl Pts',(3.37649840170159,1.16810873799805,-0.537388895013115));
#6757=CARTESIAN_POINT('Ctrl Pts',(3.3143306057952,1.15773313196141,-0.533477738502758));
#6758=CARTESIAN_POINT('Ctrl Pts',(3.19279366532602,1.12728221874041,-0.525719715587363));
#6759=CARTESIAN_POINT('Ctrl Pts',(3.13360704270085,1.10734754524679,-0.52188301482203));
#6760=CARTESIAN_POINT('Ctrl Pts',(3.04357354125242,1.06883042761197,-0.515665273788253));
#6761=CARTESIAN_POINT('Ctrl Pts',(3.01152217534904,1.05336572442389,-0.513371551354849));
#6762=CARTESIAN_POINT('Ctrl Pts',(2.97168790094352,1.03187057455983,-0.510389305659565));
#6763=CARTESIAN_POINT('Ctrl Pts',(2.96321137931696,1.02716043340691,-0.509746887872278));
#6764=CARTESIAN_POINT('Ctrl Pts',(2.94960534160534,1.01937854118037,-0.508702506422669));
#6765=CARTESIAN_POINT('Ctrl Pts',(2.94443924513565,1.01637139726705,-0.508302837680211));
#6766=CARTESIAN_POINT('Ctrl Pts',(2.93458453332311,1.01053415729336,-0.507534306565444));
#6767=CARTESIAN_POINT('Ctrl Pts',(2.92989231613606,1.00771042276113,-0.507165679822961));
#6768=CARTESIAN_POINT('Ctrl Pts',(2.91922001133851,1.001186106108,-0.506320966044665));
#6769=CARTESIAN_POINT('Ctrl Pts',(2.91325308112705,0.997464510117761,-0.505844126681568));
#6770=CARTESIAN_POINT('Ctrl Pts',(2.89447572171364,0.985518095710768,-0.504328829548049));
#6771=CARTESIAN_POINT('Ctrl Pts',(2.88179168990913,0.977098508108748,-0.503283294007638));
#6772=CARTESIAN_POINT('Ctrl Pts',(2.79849433201982,0.919449288834153,-0.496265998921689));
#6773=CARTESIAN_POINT('Ctrl Pts',(2.73331010182913,0.862859493913574,-0.490010157572538));
#6774=CARTESIAN_POINT('Ctrl Pts',(2.64128832777086,0.763364062141092,-0.480064157035253));
#6775=CARTESIAN_POINT('Ctrl Pts',(2.61001358585827,0.724957405587742,-0.476429821568471));
#6776=CARTESIAN_POINT('Ctrl Pts',(2.57220907780569,0.672047702865381,-0.471771685140373));
#6777=CARTESIAN_POINT('Ctrl Pts',(2.56342288198954,0.659221523585968,-0.470667668710592));
#6778=CARTESIAN_POINT('Ctrl Pts',(2.54904844629212,0.637319775002072,-0.468828985805786));
#6779=CARTESIAN_POINT('Ctrl Pts',(2.54332493433572,0.62833575115913,-0.468087556264866));
#6780=CARTESIAN_POINT('Ctrl Pts',(2.53543978477891,0.615580019273414,-0.467054028632626));
#6781=CARTESIAN_POINT('Ctrl Pts',(2.53317613291337,0.611872426003054,-0.466755868346626));
#6782=CARTESIAN_POINT('Ctrl Pts',(2.52933052133893,0.605494697835627,-0.46624692796133));
#6783=CARTESIAN_POINT('Ctrl Pts',(2.52773852007144,0.602830699880699,-0.466035514820911));
#6784=CARTESIAN_POINT('Ctrl Pts',(2.52466024614019,0.597633079228416,-0.465625351499246));
#6785=CARTESIAN_POINT('Ctrl Pts',(2.52317290790217,0.595100167266194,-0.465426527806647));
#6786=CARTESIAN_POINT('Ctrl Pts',(2.51911476997904,0.588129635191564,-0.464882190848579));
#6787=CARTESIAN_POINT('Ctrl Pts',(2.51656341656705,0.583680680597963,-0.464537893310958));
#6788=CARTESIAN_POINT('Ctrl Pts',(2.50663973876124,0.566111193398668,-0.463189898050406));
#6789=CARTESIAN_POINT('Ctrl Pts',(2.49948975314791,0.552865868291557,-0.462199131912969));
#6790=CARTESIAN_POINT('Ctrl Pts',(2.48079891243461,0.516594542644462,-0.459544318379849));
#6791=CARTESIAN_POINT('Ctrl Pts',(2.46975579057744,0.493320379541933,-0.457903096754138));
#6792=CARTESIAN_POINT('Ctrl Pts',(2.43866585011557,0.421831926798036,-0.452993197536466));
#6793=CARTESIAN_POINT('Ctrl Pts',(2.42105243085542,0.37262957223303,-0.449787385593403));
#6794=CARTESIAN_POINT('Ctrl Pts',(2.38680369428382,0.252303245680422,-0.442037562267477));
#6795=CARTESIAN_POINT('Ctrl Pts',(2.37340204448034,0.180495606953495,-0.437476198545167));
#6796=CARTESIAN_POINT('Ctrl Pts',(2.36576884580909,0.0975401421354294,-0.432009429681297));
#6797=CARTESIAN_POINT('Ctrl Pts',(2.3649518993186,0.0871528450724344,-0.431321692456492));
#6798=CARTESIAN_POINT('Ctrl Pts',(2.3638342430538,0.0700399756648277,-0.430182711244844));
#6799=CARTESIAN_POINT('Ctrl Pts',(2.36345318195266,0.0633200941985408,-0.429733950973512));
#6800=CARTESIAN_POINT('Ctrl Pts',(2.36286911964247,0.0511802383485442,-0.428920356891009));
#6801=CARTESIAN_POINT('Ctrl Pts',(2.362645917926,0.045761389049225,-0.428556158269894));
#6802=CARTESIAN_POINT('Ctrl Pts',(2.36224754351222,0.0341378042762881,-0.427772631466832));
#6803=CARTESIAN_POINT('Ctrl Pts',(2.36208398072578,0.0279328617127304,-0.427352955289438));
#6804=CARTESIAN_POINT('Ctrl Pts',(2.36177063975281,0.0109505707505099,-0.426200336928075));
#6805=CARTESIAN_POINT('Ctrl Pts',(2.36171975055371,0.000172225592996742,
-0.425464370900915));
#6806=CARTESIAN_POINT('Ctrl Pts',(2.36228815092201,-0.0629495674470405,
-0.421127166975548));
#6807=CARTESIAN_POINT('Ctrl Pts',(2.36624861359716,-0.115196890798785,-0.417423970045857));
#6808=CARTESIAN_POINT('Ctrl Pts',(2.3846456014432,-0.243627653030059,-0.408053258502117));
#6809=CARTESIAN_POINT('Ctrl Pts',(2.40314844599993,-0.318979470628389,-0.402308323745594));
#6810=CARTESIAN_POINT('Ctrl Pts',(2.44041472212273,-0.424570381034427,-0.394189749252246));
#6811=CARTESIAN_POINT('Ctrl Pts',(2.45335211089965,-0.456653266429886,-0.391716164687622));
#6812=CARTESIAN_POINT('Ctrl Pts',(2.4701938787623,-0.49363490295437,-0.388891676654412));
#6813=CARTESIAN_POINT('Ctrl Pts',(2.47274644084436,-0.499127181662356,-0.388472927190597));
#6814=CARTESIAN_POINT('Ctrl Pts',(2.47697873190624,-0.508052890830636,-0.387793874028403));
#6815=CARTESIAN_POINT('Ctrl Pts',(2.47863296944214,-0.511498184330585,-0.38753212263193));
#6816=CARTESIAN_POINT('Ctrl Pts',(2.48163303910204,-0.517669286275346,-0.387064010937824));
#6817=CARTESIAN_POINT('Ctrl Pts',(2.48297267462688,-0.520397981662914,-0.386857288022044));
#6818=CARTESIAN_POINT('Ctrl Pts',(2.48594857656599,-0.526400716910466,-0.386403109047352));
#6819=CARTESIAN_POINT('Ctrl Pts',(2.48758954705423,-0.529672331729539,-0.386155944910589));
#6820=CARTESIAN_POINT('Ctrl Pts',(2.49239283842223,-0.539138319672939,-0.385441737465978));
#6821=CARTESIAN_POINT('Ctrl Pts',(2.49559487486044,-0.545312527862871,-0.384977054239299));
#6822=CARTESIAN_POINT('Ctrl Pts',(2.52321642272114,-0.597437691035325,-0.381060800405111));
#6823=CARTESIAN_POINT('Ctrl Pts',(2.55060525970189,-0.641758361821393,-0.377774770905265));
#6824=CARTESIAN_POINT('Ctrl Pts',(2.62889195496161,-0.751462911630926,-0.369379228826727));
#6825=CARTESIAN_POINT('Ctrl Pts',(2.68390195297865,-0.813546090546265,-0.364345822705794));
#6826=CARTESIAN_POINT('Ctrl Pts',(2.76821455933966,-0.890604704517804,-0.357066201713279));
#6827=CARTESIAN_POINT('Ctrl Pts',(2.79230816550589,-0.9109132663389,-0.355029515449641));
#6828=CARTESIAN_POINT('Ctrl Pts',(2.82481215057754,-0.93615295519475,-0.352317847251739));
#6829=CARTESIAN_POINT('Ctrl Pts',(2.83251147328147,-0.941981202015655,-0.351678074832365));
#6830=CARTESIAN_POINT('Ctrl Pts',(2.84508415781752,-0.951257517986378,-0.350636948144735));
#6831=CARTESIAN_POINT('Ctrl Pts',(2.84991369861984,-0.95476444327421,-0.350237862977285));
#6832=CARTESIAN_POINT('Ctrl Pts',(2.85922709550427,-0.961419749032661,-0.349469748097654));
#6833=CARTESIAN_POINT('Ctrl Pts',(2.86370668430362,-0.964573855035549,-0.349100948816312));
#6834=CARTESIAN_POINT('Ctrl Pts',(2.87409956674137,-0.971783611343328,-0.348246716411219));
#6835=CARTESIAN_POINT('Ctrl Pts',(2.88002816673208,-0.975816707652761,-0.347760455291054));
#6836=CARTESIAN_POINT('Ctrl Pts',(2.89893811511055,-0.988429690411587,-0.346212484258325));
#6837=CARTESIAN_POINT('Ctrl Pts',(2.91205239458709,-0.996806271698867,-0.345143373329822));
#6838=CARTESIAN_POINT('Ctrl Pts',(2.94320612257778,-1.01584692007562,-0.342612705836933));
#6839=CARTESIAN_POINT('Ctrl Pts',(2.96137138418869,-1.02629394234843,-0.341143986729184));
#6840=CARTESIAN_POINT('Ctrl Pts',(3.03048086246985,-1.0636223408543,-0.335581141046875));
#6841=CARTESIAN_POINT('Ctrl Pts',(3.08309130671424,-1.08723720788527,-0.331390727282636));
#6842=CARTESIAN_POINT('Ctrl Pts',(3.20572098532464,-1.13180713383808,-0.32182359724022));
#6843=CARTESIAN_POINT('Ctrl Pts',(3.2763993843832,-1.15029492596286,-0.316444645571545));
#6844=CARTESIAN_POINT('Ctrl Pts',(3.3579025579419,-1.16370290727511,-0.310657113710584));
#6845=CARTESIAN_POINT('Ctrl Pts',(3.36748593749116,-1.16515819950296,-0.309983149321902));
#6846=CARTESIAN_POINT('Ctrl Pts',(3.38093760400852,-1.1670313215176,-0.30904729256321));
#6847=CARTESIAN_POINT('Ctrl Pts',(3.38479134147459,-1.16754850764564,-0.308780344875128));
#6848=CARTESIAN_POINT('Ctrl Pts',(3.39147208344645,-1.16841142953133,-0.308319666718604));
#6849=CARTESIAN_POINT('Ctrl Pts',(3.39429788585235,-1.16876601034484,-0.308125458803245));
#6850=CARTESIAN_POINT('Ctrl Pts',(3.40030619881635,-1.1694978044744,-0.307713944444898));
#6851=CARTESIAN_POINT('Ctrl Pts',(3.40348902512183,-1.16987228600488,-0.307496792866438));
#6852=CARTESIAN_POINT('Ctrl Pts',(3.41145269819462,-1.17077632709621,-0.306955480827591));
#6853=CARTESIAN_POINT('Ctrl Pts',(3.41623538933698,-1.17128960533117,-0.30663220510854));
#6854=CARTESIAN_POINT('Ctrl Pts',(3.43470570617148,-1.17315745165342,-0.305390284421834));
#6855=CARTESIAN_POINT('Ctrl Pts',(3.44841414207368,-1.17430157085485,-0.304482392145445));
#6856=CARTESIAN_POINT('Ctrl Pts',(3.4841273431563,-1.17665302959701,-0.302145807390136));
#6857=CARTESIAN_POINT('Ctrl Pts',(3.50615217395362,-1.17748348771582,-0.300732997229318));
#6858=CARTESIAN_POINT('Ctrl Pts',(3.63732332438298,-1.17874546582077,-0.292419217168538));
#6859=CARTESIAN_POINT('Ctrl Pts',(3.74607357239828,-1.16462181751565,-0.285887590347448));
#6860=CARTESIAN_POINT('Ctrl Pts',(3.87625889933871,-1.12887984453467,-0.277223401480889));
#6861=CARTESIAN_POINT('Ctrl Pts',(3.90095545211669,-1.12121675006157,-0.275543252923995));
#6862=CARTESIAN_POINT('Ctrl Pts',(3.93388533123544,-1.10979789439828,-0.273242994905945));
#6863=CARTESIAN_POINT('Ctrl Pts',(3.94235783155502,-1.10675066698364,-0.272645730522776));
#6864=CARTESIAN_POINT('Ctrl Pts',(3.95626348543776,-1.10156851971587,-0.271656069168298));
#6865=CARTESIAN_POINT('Ctrl Pts',(3.96171728815671,-1.09948977881939,-0.27126552021832));
#6866=CARTESIAN_POINT('Ctrl Pts',(3.97232662818089,-1.09535540648099,-0.270500969158009));
#6867=CARTESIAN_POINT('Ctrl Pts',(3.97748353676146,-1.09330369649639,-0.270127105007017));
#6868=CARTESIAN_POINT('Ctrl Pts',(3.98963103553707,-1.08837099851889,-0.269241040224813));
#6869=CARTESIAN_POINT('Ctrl Pts',(3.99660869424102,-1.08545901924974,-0.26872782021178));
#6870=CARTESIAN_POINT('Ctrl Pts',(4.01986012249731,-1.07549157406541,-0.267003046112239));
#6871=CARTESIAN_POINT('Ctrl Pts',(4.03600178336608,-1.06813599704391,-0.265781531605415));
#6872=CARTESIAN_POINT('Ctrl Pts',(4.060759723617,-1.05617163136073,-0.263869136273379));
#6873=CARTESIAN_POINT('Ctrl Pts',(4.06949331464938,-1.05181629783442,-0.263186859774962));
#6874=CARTESIAN_POINT('Ctrl Pts',(4.07816931076926,-1.04735426648718,-0.262501355395651));
#6875=CARTESIAN_POINT('',(2.36176935163321,-0.000842318577373219,-0.325632885263839));
#6876=CARTESIAN_POINT('Ctrl Pts',(4.07816926754758,-1.04735428871592,-0.162850680997093));
#6877=CARTESIAN_POINT('Ctrl Pts',(4.03648879475578,-1.0687903929655,-0.166030123892547));
#6878=CARTESIAN_POINT('Ctrl Pts',(3.99344742609404,-1.08777537239131,-0.169209566788002));
#6879=CARTESIAN_POINT('Ctrl Pts',(3.9493633730446,-1.10413889240205,-0.172389009683457));
#6880=CARTESIAN_POINT('Ctrl Pts',(3.90533328117549,-1.12048238261079,-0.175564560774969));
#6881=CARTESIAN_POINT('Ctrl Pts',(3.86026354815364,-1.13421057160714,-0.178740111866482));
#6882=CARTESIAN_POINT('Ctrl Pts',(3.81449436851147,-1.14520026062787,-0.181915662957994));
#6883=CARTESIAN_POINT('Ctrl Pts',(3.76876124798889,-1.15618129145297,-0.1850887122005));
#6884=CARTESIAN_POINT('Ctrl Pts',(3.72233031060124,-1.16442796521287,-0.188261761443006));
#6885=CARTESIAN_POINT('Ctrl Pts',(3.6755564187704,-1.16986704240829,-0.191434810685512));
#6886=CARTESIAN_POINT('Ctrl Pts',(3.62879897667555,-1.17530420675488,-0.194606744010136));
#6887=CARTESIAN_POINT('Ctrl Pts',(3.58169937055643,-1.17793566842164,-0.19777867733476));
#6888=CARTESIAN_POINT('Ctrl Pts',(3.53461946523157,-1.1777398085167,-0.200950610659384));
#6889=CARTESIAN_POINT('Ctrl Pts',(3.48750099629399,-1.17754378818098,-0.204125142145739));
#6890=CARTESIAN_POINT('Ctrl Pts',(3.44040281706057,-1.17451581787525,-0.207299673632094));
#6891=CARTESIAN_POINT('Ctrl Pts',(3.3936867592207,-1.16868644440786,-0.210474205118449));
#6892=CARTESIAN_POINT('Ctrl Pts',(3.34695251665996,-1.16285480179504,-0.213649972324846));
#6893=CARTESIAN_POINT('Ctrl Pts',(3.3006012400234,-1.15421967962168,-0.216825739531243));
#6894=CARTESIAN_POINT('Ctrl Pts',(3.25498596040136,-1.14286306405568,-0.220001506737639));
#6895=CARTESIAN_POINT('Ctrl Pts',(3.2092830980799,-1.13148464344857,-0.223183371511935));
#6896=CARTESIAN_POINT('Ctrl Pts',(3.16431958840069,-1.11737445457709,-0.22636523628623));
#6897=CARTESIAN_POINT('Ctrl Pts',(3.12043315625231,-1.10066437927606,-0.229547101060525));
#6898=CARTESIAN_POINT('Ctrl Pts',(3.08617027849336,-1.08761854165941,-0.232031236554579));
#6899=CARTESIAN_POINT('Ctrl Pts',(3.05256362255288,-1.07298905960761,-0.234515372048633));
#6900=CARTESIAN_POINT('Ctrl Pts',(3.01976355863634,-1.05685821719737,-0.236999507542687));
#6901=CARTESIAN_POINT('Ctrl Pts',(2.97630109333403,-1.03548368023501,-0.240291167369668));
#6902=CARTESIAN_POINT('Ctrl Pts',(2.93406351792174,-1.0113765558278,-0.24358282719665));
#6903=CARTESIAN_POINT('Ctrl Pts',(2.89341309480587,-0.984704095967967,-0.246874487023632));
#6904=CARTESIAN_POINT('Ctrl Pts',(2.85416982043374,-0.958954925843083,-0.250052203264414));
#6905=CARTESIAN_POINT('Ctrl Pts',(2.81640611387305,-0.930815467375344,-0.253229919505196));
#6906=CARTESIAN_POINT('Ctrl Pts',(2.78042461561076,-0.900483593152643,-0.256407635745978));
#6907=CARTESIAN_POINT('Ctrl Pts',(2.74447761515567,-0.870180800074408,-0.259582305303117));
#6908=CARTESIAN_POINT('Ctrl Pts',(2.71030986328289,-0.837690108820577,-0.262756974860256));
#6909=CARTESIAN_POINT('Ctrl Pts',(2.67819299342287,-0.803251197342788,-0.265931644417395));
#6910=CARTESIAN_POINT('Ctrl Pts',(2.64609291826073,-0.768830294815317,-0.269104653862066));
#6911=CARTESIAN_POINT('Ctrl Pts',(2.61604197842615,-0.732463596067216,-0.272277663306736));
#6912=CARTESIAN_POINT('Ctrl Pts',(2.58827484689098,-0.694427481992727,-0.275450672751407));
#6913=CARTESIAN_POINT('Ctrl Pts',(2.56051013444798,-0.656394681651432,-0.278623405761248));
#6914=CARTESIAN_POINT('Ctrl Pts',(2.53502916050988,-0.616693204514807,-0.281796138771089));
#6915=CARTESIAN_POINT('Ctrl Pts',(2.51202454191676,-0.575630174234756,-0.28496887178093));
#6916=CARTESIAN_POINT('Ctrl Pts',(2.48899611590444,-0.534524647932812,-0.288144888243807));
#6917=CARTESIAN_POINT('Ctrl Pts',(2.46844942873736,-0.492055243244083,-0.291320904706685));
#6918=CARTESIAN_POINT('Ctrl Pts',(2.45053121156843,-0.448553842171557,-0.294496921169562));
#6919=CARTESIAN_POINT('Ctrl Pts',(2.4326018017593,-0.405025267886123,-0.297674921535702));
#6920=CARTESIAN_POINT('Ctrl Pts',(2.41730430957338,-0.36046393975318,-0.300852921901843));
#6921=CARTESIAN_POINT('Ctrl Pts',(2.40473608172682,-0.315218458306463,-0.304030922267983));
#6922=CARTESIAN_POINT('Ctrl Pts',(2.39214524396919,-0.269891581429597,-0.307214639773129));
#6923=CARTESIAN_POINT('Ctrl Pts',(2.38229357788065,-0.223878639106408,-0.310398357278275));
#6924=CARTESIAN_POINT('Ctrl Pts',(2.37522729932057,-0.177538110880048,-0.313582074783422));
#6925=CARTESIAN_POINT('Ctrl Pts',(2.37343891898607,-0.165809944679764,-0.314387830985697));
#6926=CARTESIAN_POINT('Ctrl Pts',(2.37182869035538,-0.154060812079169,-0.315193587187973));
#6927=CARTESIAN_POINT('Ctrl Pts',(2.37039683387009,-0.142296539882158,-0.315999343390248));
#6928=CARTESIAN_POINT('Ctrl Pts',(2.3646904554523,-0.095412379593892,-0.319210524014779));
#6929=CARTESIAN_POINT('Ctrl Pts',(2.3618032037766,-0.0481751837724696,-0.322421704639309));
#6930=CARTESIAN_POINT('Ctrl Pts',(2.36176935163321,-0.000842318577373219,
-0.325632885263839));
#6931=CARTESIAN_POINT('Ctrl Pts',(2.3617693838383,-0.00088620519429726,
-0.326328626527825));
#6932=CARTESIAN_POINT('Ctrl Pts',(2.36168697442929,0.108634315111176,-0.333237160701623));
#6933=CARTESIAN_POINT('Ctrl Pts',(2.37688011695775,0.217634663538543,-0.339791136799143));
#6934=CARTESIAN_POINT('Ctrl Pts',(2.4112740138359,0.338245985790649,-0.347863569349079));
#6935=CARTESIAN_POINT('Ctrl Pts',(2.41593677931753,0.353426163559503,-0.348893890434319));
#6936=CARTESIAN_POINT('Ctrl Pts',(2.42482307569376,0.380400793188009,-0.350753733509043));
#6937=CARTESIAN_POINT('Ctrl Pts',(2.42893061655525,0.392231042178549,-0.351579547541527));
#6938=CARTESIAN_POINT('Ctrl Pts',(2.43547263533047,0.410145677589036,-0.352846697530529));
#6939=CARTESIAN_POINT('Ctrl Pts',(2.43777063119874,0.416279210781812,-0.353283537891786));
#6940=CARTESIAN_POINT('Ctrl Pts',(2.44186223727288,0.426928789990344,-0.354047405745229));
#6941=CARTESIAN_POINT('Ctrl Pts',(2.4436328733024,0.431453539511446,-0.354373662110115));
#6942=CARTESIAN_POINT('Ctrl Pts',(2.44768333197325,0.44161842628527,-0.355110521967119));
#6943=CARTESIAN_POINT('Ctrl Pts',(2.44997894358078,0.447252080696719,-0.35552164685082));
#6944=CARTESIAN_POINT('Ctrl Pts',(2.45628724947051,0.462396454681113,-0.356634375052862));
#6945=CARTESIAN_POINT('Ctrl Pts',(2.46038142670843,0.471872433114153,-0.357338703637262));
#6946=CARTESIAN_POINT('Ctrl Pts',(2.4805796305919,0.516983080198633,-0.360731520999217));
#6947=CARTESIAN_POINT('Ctrl Pts',(2.49832550390408,0.551851057964409,-0.363475290433457));
#6948=CARTESIAN_POINT('Ctrl Pts',(2.56016817984527,0.659722375024465,-0.372360792069148));
#6949=CARTESIAN_POINT('Ctrl Pts',(2.61046752690619,0.728849965862253,-0.378685905895085));
#6950=CARTESIAN_POINT('Ctrl Pts',(2.68673643930151,0.812804987824375,-0.386952545903791));
#6951=CARTESIAN_POINT('Ctrl Pts',(2.70644115942162,0.83298953900932,-0.388990140799229));
#6952=CARTESIAN_POINT('Ctrl Pts',(2.73478813095285,0.860013611376803,-0.391768860120055));
#6953=CARTESIAN_POINT('Ctrl Pts',(2.74282914441637,0.86746785395331,-0.392541027153686));
#6954=CARTESIAN_POINT('Ctrl Pts',(2.7569223959563,0.880171395036631,-0.393865226461982));
#6955=CARTESIAN_POINT('Ctrl Pts',(2.76292614743906,0.885473139109411,-0.394420460966358));
#6956=CARTESIAN_POINT('Ctrl Pts',(2.77192101918803,0.893254392263535,-0.395238654559867));
#6957=CARTESIAN_POINT('Ctrl Pts',(2.77487092324347,0.895780882552836,-0.395504839933977));
#6958=CARTESIAN_POINT('Ctrl Pts',(2.78012179328468,0.900233231331982,-0.395974785218987));
#6959=CARTESIAN_POINT('Ctrl Pts',(2.78241766033256,0.902164924318805,-0.396178959411012));
#6960=CARTESIAN_POINT('Ctrl Pts',(2.78742245995206,0.906343293668238,-0.396621220804574));
#6961=CARTESIAN_POINT('Ctrl Pts',(2.79013408968879,0.908586610518872,-0.396859069664233));
#6962=CARTESIAN_POINT('Ctrl Pts',(2.79759042463452,0.914699108094887,-0.397508392747629));
#6963=CARTESIAN_POINT('Ctrl Pts',(2.80235538891057,0.918543566875013,-0.397918164604192));
#6964=CARTESIAN_POINT('Ctrl Pts',(2.82725885899987,0.93831752361345,-0.40003435273515));
#6965=CARTESIAN_POINT('Ctrl Pts',(2.84788600843057,0.953623781698629,-0.401701615324763));
#6966=CARTESIAN_POINT('Ctrl Pts',(2.87836036939974,0.974727617884295,-0.404070550069948));
#6967=CARTESIAN_POINT('Ctrl Pts',(2.88781570976759,0.981074665709309,-0.404793012887576));
#6968=CARTESIAN_POINT('Ctrl Pts',(2.95939898335455,1.02763444647273,-0.410180820038382));
#6969=CARTESIAN_POINT('Ctrl Pts',(3.02510285903924,1.0620493044245,-0.414680448546493));
#6970=CARTESIAN_POINT('Ctrl Pts',(3.14374750320947,1.11058319039115,-0.422692628063581));
#6971=CARTESIAN_POINT('Ctrl Pts',(3.19524009606638,1.12760853877295,-0.426134584669825));
#6972=CARTESIAN_POINT('Ctrl Pts',(3.25826790389293,1.14372700071162,-0.430410126093525));
#6973=CARTESIAN_POINT('Ctrl Pts',(3.26885520119699,1.14627864297862,-0.431130221486981));
#6974=CARTESIAN_POINT('Ctrl Pts',(3.28556747898213,1.15006202817494,-0.432270585095368));
#6975=CARTESIAN_POINT('Ctrl Pts',(3.29166965160461,1.15139252310599,-0.432687732009335));
#6976=CARTESIAN_POINT('Ctrl Pts',(3.30310835136465,1.15379142891049,-0.433471246938598));
#6977=CARTESIAN_POINT('Ctrl Pts',(3.30844228287727,1.15487151054093,-0.433837236617798));
#6978=CARTESIAN_POINT('Ctrl Pts',(3.32039375465797,1.15720548307719,-0.434658794946688));
#6979=CARTESIAN_POINT('Ctrl Pts',(3.32701490686117,1.15843964496585,-0.435114969099434));
#6980=CARTESIAN_POINT('Ctrl Pts',(3.34387792244817,1.16143342473726,-0.436279548035995));
#6981=CARTESIAN_POINT('Ctrl Pts',(3.35413298064496,1.16311437280737,-0.436990372905088));
#6982=CARTESIAN_POINT('Ctrl Pts',(3.43846878062212,1.17579453943486,-0.4428588030807));
#6983=CARTESIAN_POINT('Ctrl Pts',(3.51340844765557,1.17983830107933,-0.448233681952999));
#6984=CARTESIAN_POINT('Ctrl Pts',(3.64542038779149,1.17437574872178,-0.45789229303986));
#6985=CARTESIAN_POINT('Ctrl Pts',(3.70238080571172,1.16783978823402,-0.46211810922811));
#6986=CARTESIAN_POINT('Ctrl Pts',(3.77902224233109,1.15332718177776,-0.467750668621716));
#6987=CARTESIAN_POINT('Ctrl Pts',(3.7992995701186,1.14892974135766,-0.469235134233333));
#6988=CARTESIAN_POINT('Ctrl Pts',(3.83224627818835,1.1408678044226,-0.471627283023445));
#6989=CARTESIAN_POINT('Ctrl Pts',(3.84498853188288,1.13752231144036,-0.472547521418659));
#6990=CARTESIAN_POINT('Ctrl Pts',(3.86222793237053,1.13268549227179,-0.473783423714395));
#6991=CARTESIAN_POINT('Ctrl Pts',(3.86677560466676,1.13137995231716,-0.474108578871976));
#6992=CARTESIAN_POINT('Ctrl Pts',(3.87437398894227,1.12914896900803,-0.474650258735744));
#6993=CARTESIAN_POINT('Ctrl Pts',(3.87742898614855,1.12823849431332,-0.474867611476438));
#6994=CARTESIAN_POINT('Ctrl Pts',(3.88321838829966,1.12648746580278,-0.475278633550124));
#6995=CARTESIAN_POINT('Ctrl Pts',(3.88595348981981,1.12564933487802,-0.475472442611575));
#6996=CARTESIAN_POINT('Ctrl Pts',(3.89244917617556,1.12363291101652,-0.475931903337706));
#6997=CARTESIAN_POINT('Ctrl Pts',(3.89620698414545,1.12244568306195,-0.476197047470731));
#6998=CARTESIAN_POINT('Ctrl Pts',(3.90948562860962,1.11817705779161,-0.477131867958273));
#6999=CARTESIAN_POINT('Ctrl Pts',(3.91897339704649,1.11499310160126,-0.477795984292783));
#7000=CARTESIAN_POINT('Ctrl Pts',(3.98514384102471,1.091844767732,-0.482408409744347));
#7001=CARTESIAN_POINT('Ctrl Pts',(4.04027356919942,1.06768592028281,-0.486153969788257));
#7002=CARTESIAN_POINT('Ctrl Pts',(4.15217776266215,1.00806321493159,-0.494010707439357));
#7003=CARTESIAN_POINT('Ctrl Pts',(4.20825882092962,0.97176574458282,-0.498106439889093));
#7004=CARTESIAN_POINT('Ctrl Pts',(4.28805197415633,0.909927378667701,-0.504525166683664));
#7005=CARTESIAN_POINT('Ctrl Pts',(4.31420696825961,0.887765542050408,-0.506737278164688));
#7006=CARTESIAN_POINT('Ctrl Pts',(4.34639021875562,0.857989388569559,-0.509626861940493));
#7007=CARTESIAN_POINT('Ctrl Pts',(4.35334363115579,0.851396744220246,-0.510261778919031));
#7008=CARTESIAN_POINT('Ctrl Pts',(4.36448437209197,0.840572841911628,-0.511296905029968));
#7009=CARTESIAN_POINT('Ctrl Pts',(4.36872151338084,0.836393303262204,-0.511694893988918));
#7010=CARTESIAN_POINT('Ctrl Pts',(4.37680070983434,0.828302206327701,-0.512462202262385));
#7011=CARTESIAN_POINT('Ctrl Pts',(4.38064749464227,0.824395572996321,-0.512831300815088));
#7012=CARTESIAN_POINT('Ctrl Pts',(4.38940075071394,0.81538108900083,-0.513679938728911));
#7013=CARTESIAN_POINT('Ctrl Pts',(4.39428866383154,0.810255594853679,-0.514160255500975));
#7014=CARTESIAN_POINT('Ctrl Pts',(4.40972840918327,0.793770192559621,-0.51569838948932));
#7015=CARTESIAN_POINT('Ctrl Pts',(4.42010190722888,0.78224627789502,-0.51676359295647));
#7016=CARTESIAN_POINT('Ctrl Pts',(4.48166067154539,0.711084131588965,-0.523284831203735));
#7017=CARTESIAN_POINT('Ctrl Pts',(4.52698958881951,0.646660128206376,-0.528972840683664));
#7018=CARTESIAN_POINT('Ctrl Pts',(4.58063723111642,0.55146263956364,-0.536986904800494));
#7019=CARTESIAN_POINT('Ctrl Pts',(4.59466180221519,0.524129670224106,-0.539244801603902));
#7020=CARTESIAN_POINT('Ctrl Pts',(4.62582731742985,0.457055876131071,-0.544648874078153));
#7021=CARTESIAN_POINT('Ctrl Pts',(4.64187994411099,0.41685364128635,-0.547777892581808));
#7022=CARTESIAN_POINT('Ctrl Pts',(4.65870084738575,0.366901133812908,-0.551467533879394));
#7023=CARTESIAN_POINT('Ctrl Pts',(4.66160840478246,0.357910368093936,-0.552123953663679));
#7024=CARTESIAN_POINT('Ctrl Pts',(4.66563373195058,0.344931761392496,-0.553059604024824));
#7025=CARTESIAN_POINT('Ctrl Pts',(4.66683907897295,0.340971773765715,-0.553343501177967));
#7026=CARTESIAN_POINT('Ctrl Pts',(4.66890202637153,0.334063738627193,-0.553835893272591));
#7027=CARTESIAN_POINT('Ctrl Pts',(4.6697690136202,0.331118573035162,-0.554044916310924));
#7028=CARTESIAN_POINT('Ctrl Pts',(4.67158485287182,0.324859908421564,-0.55448715960361));
#7029=CARTESIAN_POINT('Ctrl Pts',(4.6725306843868,0.321545609897299,-0.554720208152433));
#7030=CARTESIAN_POINT('Ctrl Pts',(4.67507453731076,0.312481065988549,-0.55535459459021));
#7031=CARTESIAN_POINT('Ctrl Pts',(4.67664344889033,0.306722654088504,-0.555754314351022));
#7032=CARTESIAN_POINT('Ctrl Pts',(4.6840146438666,0.278833834727577,-0.557675483197943));
#7033=CARTESIAN_POINT('Ctrl Pts',(4.68921546584654,0.256547829257607,-0.559166021673699));
#7034=CARTESIAN_POINT('Ctrl Pts',(4.69810206960813,0.212736119415637,-0.562034746814394));
#7035=CARTESIAN_POINT('Ctrl Pts',(4.70184502825559,0.191232006465518,-0.563414369590088));
#7036=CARTESIAN_POINT('Ctrl Pts',(4.70752387192921,0.152215855588442,-0.565885781010491));
#7037=CARTESIAN_POINT('Ctrl Pts',(4.7096684962859,0.134741342067537,-0.56698129657522));
#7038=CARTESIAN_POINT('Ctrl Pts',(4.71594649039535,0.0719800575475563,-0.570894290312237));
#7039=CARTESIAN_POINT('Ctrl Pts',(4.71784827121885,0.0265114797234634,-0.573690378143538));
#7040=CARTESIAN_POINT('Ctrl Pts',(4.71650227169159,-0.0571191282781658,
-0.578906926547529));
#7041=CARTESIAN_POINT('Ctrl Pts',(4.71403297465736,-0.0952302136696254,
-0.581312175056079));
#7042=CARTESIAN_POINT('Ctrl Pts',(4.70788339535222,-0.149275404393393,-0.584811784472708));
#7043=CARTESIAN_POINT('Ctrl Pts',(4.70571583456706,-0.165358431795092,-0.58586437571251));
#7044=CARTESIAN_POINT('Ctrl Pts',(4.70125253548774,-0.193992331123487,-0.587761823873281));
#7045=CARTESIAN_POINT('Ctrl Pts',(4.6990838141625,-0.20656053091543,-0.588602789459792));
#7046=CARTESIAN_POINT('Ctrl Pts',(4.69547962840132,-0.225597110364337,-0.589890082476426));
#7047=CARTESIAN_POINT('Ctrl Pts',(4.69419293172453,-0.232092953088178,-0.590331747844263));
#7048=CARTESIAN_POINT('Ctrl Pts',(4.6918603532172,-0.243369115781755,-0.591102773523019));
#7049=CARTESIAN_POINT('Ctrl Pts',(4.69083932284629,-0.248154455357563,-0.591431342633003));
#7050=CARTESIAN_POINT('Ctrl Pts',(4.68847809289501,-0.258892667519622,-0.592171783331215));
#7051=CARTESIAN_POINT('Ctrl Pts',(4.68712139893248,-0.264841729811598,-0.592584168749194));
#7052=CARTESIAN_POINT('Ctrl Pts',(4.68335143216703,-0.280799835578068,-0.593696368411557));
#7053=CARTESIAN_POINT('Ctrl Pts',(4.68085308396306,-0.290788028271361,-0.594398860754467));
#7054=CARTESIAN_POINT('Ctrl Pts',(4.66840246174506,-0.337930068216015,-0.597745607004141));
#7055=CARTESIAN_POINT('Ctrl Pts',(4.65676599167903,-0.374610709816397,-0.600442869794084));
#7056=CARTESIAN_POINT('Ctrl Pts',(4.61362254365121,-0.49058057471665,-0.609277032799512));
#7057=CARTESIAN_POINT('Ctrl Pts',(4.57529581940955,-0.567037343307796,-0.615598918979071));
#7058=CARTESIAN_POINT('Ctrl Pts',(4.51376099914961,-0.6623771644089,-0.623864569175167));
#7059=CARTESIAN_POINT('Ctrl Pts',(4.49761528903258,-0.685523662817829,-0.625902280730524));
#7060=CARTESIAN_POINT('Ctrl Pts',(4.47084046085439,-0.721111555270641,-0.629061290942799));
#7061=CARTESIAN_POINT('Ctrl Pts',(4.46075738582872,-0.733949208377229,-0.63020645131707));
#7062=CARTESIAN_POINT('Ctrl Pts',(4.44717374462461,-0.750522540988549,-0.631687978243776));
#7063=CARTESIAN_POINT('Ctrl Pts',(4.44391167162935,-0.754450208788329,-0.632039316911165));
#7064=CARTESIAN_POINT('Ctrl Pts',(4.43852762352065,-0.760847717138629,-0.632611804106465));
#7065=CARTESIAN_POINT('Ctrl Pts',(4.43642080713561,-0.763330140005019,-0.632833999941227));
#7066=CARTESIAN_POINT('Ctrl Pts',(4.43227345035486,-0.768176016964517,-0.633267794733483));
#7067=CARTESIAN_POINT('Ctrl Pts',(4.43023376428372,-0.770540142079035,-0.633479448804152));
#7068=CARTESIAN_POINT('Ctrl Pts',(4.42564335643877,-0.775818131432801,-0.63395209499033));
#7069=CARTESIAN_POINT('Ctrl Pts',(4.42308759398128,-0.778727608768272,-0.634212723749121));
#7070=CARTESIAN_POINT('Ctrl Pts',(4.41412724539791,-0.788827155643087,-0.635117946746003));
#7071=CARTESIAN_POINT('Ctrl Pts',(4.40764866721918,-0.795951480441159,-0.6357574148211));
#7072=CARTESIAN_POINT('Ctrl Pts',(4.35039150495479,-0.857384823221027,-0.641288075319325));
#7073=CARTESIAN_POINT('Ctrl Pts',(4.29465593472954,-0.906859588682673,-0.645863027935886));
#7074=CARTESIAN_POINT('Ctrl Pts',(4.18883333671004,-0.984227075975733,-0.653971699055674));
#7075=CARTESIAN_POINT('Ctrl Pts',(4.1406921550285,-1.01434818011597,-0.657483292085759));
#7076=CARTESIAN_POINT('Ctrl Pts',(4.08644946351141,-1.04306468112501,-0.661398375850873));
#7077=CARTESIAN_POINT('Ctrl Pts',(4.08231563063612,-1.0452218303879,-0.661696462973669));
#7078=CARTESIAN_POINT('Ctrl Pts',(4.0781692670594,-1.04735428896699,-0.661995228290505));
#7079=CARTESIAN_POINT('Origin',(3.53951905042299,8.32667268468867E-16,0.924367114736157));
#7080=CARTESIAN_POINT('',(4.07816926864924,-1.04735428814934,-1.26060176719249));
#7081=CARTESIAN_POINT('',(4.07816919733398,-1.04735432482649,-1.16244574507018));
#7082=CARTESIAN_POINT('',(4.07816926754759,-1.04735428871592,0.924367114736157));
#7083=CARTESIAN_POINT('',(2.36176946686129,0.00104026961872179,-0.924219816937961));
#7084=CARTESIAN_POINT('Ctrl Pts',(4.07816926864928,-1.04735428814932,-1.26060176719248));
#7085=CARTESIAN_POINT('Ctrl Pts',(4.08884795112987,-1.04186228347275,-1.25975288411232));
#7086=CARTESIAN_POINT('Ctrl Pts',(4.09944307827394,-1.03620673564027,-1.25891107276242));
#7087=CARTESIAN_POINT('Ctrl Pts',(4.11519672246416,-1.02748539330295,-1.25766203314466));
#7088=CARTESIAN_POINT('Ctrl Pts',(4.12042046061093,-1.02454115143288,-1.2572483069518));
#7089=CARTESIAN_POINT('Ctrl Pts',(4.12864847716065,-1.01982045416298,-1.2565976088512));
#7090=CARTESIAN_POINT('Ctrl Pts',(4.13166764964849,-1.01807036957726,-1.25635905167481));
#7091=CARTESIAN_POINT('Ctrl Pts',(4.13705697346545,-1.01491432481657,-1.25593365434014));
#7092=CARTESIAN_POINT('Ctrl Pts',(4.13942996186064,-1.01351347043171,-1.2557465043161));
#7093=CARTESIAN_POINT('Ctrl Pts',(4.14514400029037,-1.01011318281524,-1.25529620888823));
#7094=CARTESIAN_POINT('Ctrl Pts',(4.14848007859398,-1.00810549510168,-1.25503359514105));
#7095=CARTESIAN_POINT('Ctrl Pts',(4.15873503059597,-1.00186447308904,-1.25422702027125));
#7096=CARTESIAN_POINT('Ctrl Pts',(4.16562035291837,-0.997576072549032,-1.25368644513071));
#7097=CARTESIAN_POINT('Ctrl Pts',(4.18163001027191,-0.987373682438825,-1.25243043940545));
#7098=CARTESIAN_POINT('Ctrl Pts',(4.19071797727802,-0.981403713912158,-1.25171818050059));
#7099=CARTESIAN_POINT('Ctrl Pts',(4.22271767898707,-0.959742560384,-1.24920789715573));
#7100=CARTESIAN_POINT('Ctrl Pts',(4.24515696836875,-0.943367102041331,-1.24744316341442));
#7101=CARTESIAN_POINT('Ctrl Pts',(4.33212015627507,-0.875063270520032,-1.24049681309479));
#7102=CARTESIAN_POINT('Ctrl Pts',(4.39166649172802,-0.817188843989751,-1.23547825870419));
#7103=CARTESIAN_POINT('Ctrl Pts',(4.47095738287137,-0.721947483790242,-1.22765703468779));
#7104=CARTESIAN_POINT('Ctrl Pts',(4.49558851591988,-0.688996484404309,-1.22501989220541));
#7105=CARTESIAN_POINT('Ctrl Pts',(4.52428438311081,-0.646097988347847,-1.22162545445284));
#7106=CARTESIAN_POINT('Ctrl Pts',(4.53000672564423,-0.637290769255301,-1.22093059921813));
#7107=CARTESIAN_POINT('Ctrl Pts',(4.5388925251133,-0.62320587264089,-1.21982192172754));
#7108=CARTESIAN_POINT('Ctrl Pts',(4.54213381874223,-0.61797777106771,-1.21941094922122));
#7109=CARTESIAN_POINT('Ctrl Pts',(4.54787951211164,-0.608545957762582,-1.21867039410471));
#7110=CARTESIAN_POINT('Ctrl Pts',(4.55039896882165,-0.604351547319281,-1.21834136603355));
#7111=CARTESIAN_POINT('Ctrl Pts',(4.55624022542853,-0.594488254417214,-1.21756828356612));
#7112=CARTESIAN_POINT('Ctrl Pts',(4.55954084055412,-0.588807079593249,-1.21712348310464));
#7113=CARTESIAN_POINT('Ctrl Pts',(4.56897167690826,-0.572256989612077,-1.21582894457913));
#7114=CARTESIAN_POINT('Ctrl Pts',(4.57497675539408,-0.56131817429893,-1.21497483021721));
#7115=CARTESIAN_POINT('Ctrl Pts',(4.58817918015679,-0.536335687474715,-1.21302688024825));
#7116=CARTESIAN_POINT('Ctrl Pts',(4.595270236266,-0.522238863020427,-1.21192959816084));
#7117=CARTESIAN_POINT('Ctrl Pts',(4.61784886756158,-0.475012747859351,-1.20825892419414));
#7118=CARTESIAN_POINT('Ctrl Pts',(4.63207555035815,-0.441307335297537,-1.20564695497923));
#7119=CARTESIAN_POINT('Ctrl Pts',(4.6710422019801,-0.335494373439686,-1.19748686334835));
#7120=CARTESIAN_POINT('Ctrl Pts',(4.69037134943595,-0.261609072522471,-1.19183179675652));
#7121=CARTESIAN_POINT('Ctrl Pts',(4.70764347429664,-0.153838635619794,-1.18392967186133));
#7122=CARTESIAN_POINT('Ctrl Pts',(4.71149091838431,-0.121092414616739,-1.18157556512381));
#7123=CARTESIAN_POINT('Ctrl Pts',(4.71445082571294,-0.0816904289252436,
-1.178829954803));
#7124=CARTESIAN_POINT('Ctrl Pts',(4.71488717004093,-0.075151786817161,-1.1783771993553));
#7125=CARTESIAN_POINT('Ctrl Pts',(4.71547957795118,-0.0649998120297619,
-1.17767904085047));
#7126=CARTESIAN_POINT('Ctrl Pts',(4.71567360456513,-0.0613889527771861,
-1.17743165989542));
#7127=CARTESIAN_POINT('Ctrl Pts',(4.7160003789219,-0.0547358934510776,-1.17697765833948));
#7128=CARTESIAN_POINT('Ctrl Pts',(4.71613795973825,-0.0516940709573712,
-1.17677078665699));
#7129=CARTESIAN_POINT('Ctrl Pts',(4.71642409023076,-0.0447733882341851,
-1.17630168584423));
#7130=CARTESIAN_POINT('Ctrl Pts',(4.71656526284452,-0.0408943018009075,
-1.1760398637126));
#7131=CARTESIAN_POINT('Ctrl Pts',(4.71694023791755,-0.0289690156196302,
-1.1752381786659));
#7132=CARTESIAN_POINT('Ctrl Pts',(4.71711073820966,-0.0209208570094207,
-1.17470164276538));
#7133=CARTESIAN_POINT('Ctrl Pts',(4.71731637295538,-0.00210600396640012,
-1.17345654817815));
#7134=CARTESIAN_POINT('Ctrl Pts',(4.71728641972372,0.00866083266957495,
-1.17275108609864));
#7135=CARTESIAN_POINT('Ctrl Pts',(4.7166575927894,0.0467795522435654,-1.17027366716793));
#7136=CARTESIAN_POINT('Ctrl Pts',(4.7152534000642,0.0741108505661698,-1.16853406868859));
#7137=CARTESIAN_POINT('Ctrl Pts',(4.70594799466925,0.181822718668806,-1.16173907383884));
#7138=CARTESIAN_POINT('Ctrl Pts',(4.69074196946906,0.261347363644654,-1.15684181768749));
#7139=CARTESIAN_POINT('Ctrl Pts',(4.65501277556173,0.380341783272286,-1.14901710279447));
#7140=CARTESIAN_POINT('Ctrl Pts',(4.64021134439091,0.42126233038003,-1.14623314512473));
#7141=CARTESIAN_POINT('Ctrl Pts',(4.61905567945612,0.470963661633562,-1.14268171743881));
#7142=CARTESIAN_POINT('Ctrl Pts',(4.61479877438006,0.480603378558655,-1.14198478224458));
#7143=CARTESIAN_POINT('Ctrl Pts',(4.60782483745484,0.495839171159651,-1.14086962188246));
#7144=CARTESIAN_POINT('Ctrl Pts',(4.60519176510714,0.501473230529509,-1.14045424125655));
#7145=CARTESIAN_POINT('Ctrl Pts',(4.60017698667964,0.51198561790892,-1.139673418825));
#7146=CARTESIAN_POINT('Ctrl Pts',(4.59780592380346,0.516868864056127,-1.13930834903681));
#7147=CARTESIAN_POINT('Ctrl Pts',(4.59241986697501,0.527769103055894,-1.13848805697374));
#7148=CARTESIAN_POINT('Ctrl Pts',(4.58938690629979,0.533776954900184,-1.13803222430838));
#7149=CARTESIAN_POINT('Ctrl Pts',(4.58022320932044,0.551548625258632,-1.13667255906125));
#7150=CARTESIAN_POINT('Ctrl Pts',(4.57394520746903,0.563234882683309,-1.13576364649318));
#7151=CARTESIAN_POINT('Ctrl Pts',(4.5591461509936,0.589700438411027,-1.13367026644052));
#7152=CARTESIAN_POINT('Ctrl Pts',(4.55049884911401,0.604405349571571,-1.13248156382093));
#7153=CARTESIAN_POINT('Ctrl Pts',(4.51988697862427,0.653965498300141,-1.12838601100008));
#7154=CARTESIAN_POINT('Ctrl Pts',(4.49641641669209,0.687850989738129,-1.12543000807355));
#7155=CARTESIAN_POINT('Ctrl Pts',(4.43458296076068,0.767817114527967,-1.11808284254597));
#7156=CARTESIAN_POINT('Ctrl Pts',(4.39438497274184,0.812333959056298,-1.11365697335322));
#7157=CARTESIAN_POINT('Ctrl Pts',(4.32095919913548,0.882134712442782,-1.10627655920687));
#7158=CARTESIAN_POINT('Ctrl Pts',(4.28945415198576,0.909070111109058,-1.10329597032964));
#7159=CARTESIAN_POINT('Ctrl Pts',(4.25158784824816,0.938132657152573,-1.09997561112915));
#7160=CARTESIAN_POINT('Ctrl Pts',(4.24655277121828,0.94193321273168,-1.09953918000978));
#7161=CARTESIAN_POINT('Ctrl Pts',(4.23835632942023,0.948017259257392,-1.09883721114766));
#7162=CARTESIAN_POINT('Ctrl Pts',(4.23521381459628,0.950325766548631,-1.09857006738864));
#7163=CARTESIAN_POINT('Ctrl Pts',(4.22959599088233,0.954409847819512,-1.09809611642698));
#7164=CARTESIAN_POINT('Ctrl Pts',(4.22712520172596,0.956191467632653,-1.09788890691474));
#7165=CARTESIAN_POINT('Ctrl Pts',(4.22171725593542,0.960059190142491,-1.09743808436597));
#7166=CARTESIAN_POINT('Ctrl Pts',(4.21877742632116,0.962141413630804,-1.09719473082735));
#7167=CARTESIAN_POINT('Ctrl Pts',(4.21036072166443,0.968044994940203,-1.09650275833733));
#7168=CARTESIAN_POINT('Ctrl Pts',(4.20486072817006,0.971833379282359,-1.09605627763682));
#7169=CARTESIAN_POINT('Ctrl Pts',(4.16532450987109,0.99857287087287,-1.09288495886974));
#7170=CARTESIAN_POINT('Ctrl Pts',(4.13013703862062,1.01978009316341,-1.0902627021538));
#7171=CARTESIAN_POINT('Ctrl Pts',(4.02059690305597,1.07822255841859,-1.08246415829892));
#7172=CARTESIAN_POINT('Ctrl Pts',(3.94335074039314,1.10946850957014,-1.07742869781916));
#7173=CARTESIAN_POINT('Ctrl Pts',(3.82424205071352,1.14354343260029,-1.06960771180223));
#7174=CARTESIAN_POINT('Ctrl Pts',(3.7844741733988,1.15271644836675,-1.06699085748781));
#7175=CARTESIAN_POINT('Ctrl Pts',(3.73399183295129,1.16163043172554,-1.06361916061123));
#7176=CARTESIAN_POINT('Ctrl Pts',(3.72364648431919,1.16331509039633,-1.06292569422328));
#7177=CARTESIAN_POINT('Ctrl Pts',(3.70720086146154,1.16576826799626,-1.06181872387096));
#7178=CARTESIAN_POINT('Ctrl Pts',(3.701114520593,1.16662750954324,-1.06140805440622));
#7179=CARTESIAN_POINT('Ctrl Pts',(3.6901711465152,1.16808516599541,-1.06066776050874));
#7180=CARTESIAN_POINT('Ctrl Pts',(3.6853165484873,1.16870102994563,-1.06033868814949));
#7181=CARTESIAN_POINT('Ctrl Pts',(3.6739289004707,1.17007363331048,-1.05956512901717));
#7182=CARTESIAN_POINT('Ctrl Pts',(3.66739312512786,1.17080593316937,-1.05911989315564));
#7183=CARTESIAN_POINT('Ctrl Pts',(3.64840915902149,1.17277213627095,-1.05782280963187));
#7184=CARTESIAN_POINT('Ctrl Pts',(3.63594733911074,1.17386247218179,-1.05696655910112));
#7185=CARTESIAN_POINT('Ctrl Pts',(3.60768287382204,1.17588234578086,-1.05501297730987));
#7186=CARTESIAN_POINT('Ctrl Pts',(3.59187437200674,1.17669217596267,-1.05391217068112));
#7187=CARTESIAN_POINT('Ctrl Pts',(3.53933115594105,1.1783229462667,-1.05022550907506));
#7188=CARTESIAN_POINT('Ctrl Pts',(3.50257740621707,1.17774355232101,-1.04760070287487));
#7189=CARTESIAN_POINT('Ctrl Pts',(3.37890368063003,1.1699992292326,-1.03863167166116));
#7190=CARTESIAN_POINT('Ctrl Pts',(3.29277243021401,1.15490730394646,-1.03213444644967));
#7191=CARTESIAN_POINT('Ctrl Pts',(3.18712775935599,1.12402817327558,-1.02424957913164));
#7192=CARTESIAN_POINT('Ctrl Pts',(3.16534833255063,1.11696705293612,-1.02263048379369));
#7193=CARTESIAN_POINT('Ctrl Pts',(3.13816112675581,1.10726806026736,-1.02062881852968));
#7194=CARTESIAN_POINT('Ctrl Pts',(3.13255052480449,1.10521824229417,-1.02021680184776));
#7195=CARTESIAN_POINT('Ctrl Pts',(3.12372418742472,1.10191723695001,-1.01957058667346));
#7196=CARTESIAN_POINT('Ctrl Pts',(3.12049803361439,1.10069448687127,-1.0193347992979));
#7197=CARTESIAN_POINT('Ctrl Pts',(3.11440902885289,1.09835603157603,-1.01889062221534));
#7198=CARTESIAN_POINT('Ctrl Pts',(3.11154519187073,1.09724330900908,-1.01868207578175));
#7199=CARTESIAN_POINT('Ctrl Pts',(3.10497402927931,1.09466049142576,-1.01820434534152));
#7200=CARTESIAN_POINT('Ctrl Pts',(3.10126977782375,1.09318275833218,-1.01793561444452));
#7201=CARTESIAN_POINT('Ctrl Pts',(3.08937698475657,1.08836821324169,-1.01707445538923));
#7202=CARTESIAN_POINT('Ctrl Pts',(3.08121825743751,1.08495789848586,-1.01648616504898));
#7203=CARTESIAN_POINT('Ctrl Pts',(3.06177900535324,1.07657395207362,-1.01508866675573));
#7204=CARTESIAN_POINT('Ctrl Pts',(3.05053645061148,1.07151438070504,-1.01428384251026));
#7205=CARTESIAN_POINT('Ctrl Pts',(3.00885761720949,1.0519646915953,-1.01130546228494));
#7206=CARTESIAN_POINT('Ctrl Pts',(2.97896655476766,1.03634574503722,-1.00917987662706));
#7207=CARTESIAN_POINT('Ctrl Pts',(2.87534315230949,0.976402263300304,-1.00170891578259));
#7208=CARTESIAN_POINT('Ctrl Pts',(2.80584508500041,0.925317956202571,-0.996486589639262));
#7209=CARTESIAN_POINT('Ctrl Pts',(2.71968922318595,0.846130254695397,-0.989024600020789));
#7210=CARTESIAN_POINT('Ctrl Pts',(2.69769006547169,0.824245747744154,-0.987018124268657));
#7211=CARTESIAN_POINT('Ctrl Pts',(2.67005203494809,0.794489916749034,-0.984341848377458));
#7212=CARTESIAN_POINT('Ctrl Pts',(2.66360872696786,0.787380603729084,-0.983706120536616));
#7213=CARTESIAN_POINT('Ctrl Pts',(2.65330930448196,0.775733712432191,-0.982670069010851));
#7214=CARTESIAN_POINT('Ctrl Pts',(2.64939939348282,0.771244125119865,-0.982271975383961));
#7215=CARTESIAN_POINT('Ctrl Pts',(2.64195605353233,0.762565251221382,-0.98150473875416));
#7216=CARTESIAN_POINT('Ctrl Pts',(2.63841748898215,0.758380557494087,-0.981135818492017));
#7217=CARTESIAN_POINT('Ctrl Pts',(2.63030099649412,0.748645016636396,-0.98027978480689));
#7218=CARTESIAN_POINT('Ctrl Pts',(2.62574451257208,0.743076658578565,-0.979791829861827));
#7219=CARTESIAN_POINT('Ctrl Pts',(2.6120440622931,0.726017123307341,-0.978301688268817));
#7220=CARTESIAN_POINT('Ctrl Pts',(2.60306403609447,0.71439673105362,-0.977293140060038));
#7221=CARTESIAN_POINT('Ctrl Pts',(2.56154769446888,0.658545312257499,-0.972473957855018));
#7222=CARTESIAN_POINT('Ctrl Pts',(2.53191772962496,0.612248279629675,-0.968556722359695));
#7223=CARTESIAN_POINT('Ctrl Pts',(2.48286177121569,0.522331306975943,-0.961114368891997));
#7224=CARTESIAN_POINT('Ctrl Pts',(2.46264374027178,0.479263915643639,-0.957614792665407));
#7225=CARTESIAN_POINT('Ctrl Pts',(2.42508185818727,0.384780924418095,-0.950166755605304));
#7226=CARTESIAN_POINT('Ctrl Pts',(2.40857045909484,0.33314154948456,-0.946231809080753));
#7227=CARTESIAN_POINT('Ctrl Pts',(2.39413750361668,0.274294685758456,-0.942015416507684));
#7228=CARTESIAN_POINT('Ctrl Pts',(2.39265603166628,0.26803298901159,-0.941570121254137));
#7229=CARTESIAN_POINT('Ctrl Pts',(2.39035096761227,0.257921068263755,-0.940856757402183));
#7230=CARTESIAN_POINT('Ctrl Pts',(2.38949525802527,0.254078409262238,-0.940586999788746));
#7231=CARTESIAN_POINT('Ctrl Pts',(2.38801100115816,0.247252040633597,-0.940110226733926));
#7232=CARTESIAN_POINT('Ctrl Pts',(2.38737475537814,0.244270103091031,-0.939902789439959));
#7233=CARTESIAN_POINT('Ctrl Pts',(2.38601765345072,0.237786397172968,-0.93945356644503));
#7234=CARTESIAN_POINT('Ctrl Pts',(2.38530115700255,0.234283799817053,-0.939212025082583));
#7235=CARTESIAN_POINT('Ctrl Pts',(2.38385275711833,0.227035343721708,-0.938714410592869));
#7236=CARTESIAN_POINT('Ctrl Pts',(2.38312308943164,0.223289075332115,-0.938458460700184));
#7237=CARTESIAN_POINT('Ctrl Pts',(2.38129150428539,0.213635491159728,-0.937801938042549));
#7238=CARTESIAN_POINT('Ctrl Pts',(2.380216547132,0.207723087605955,-0.93740275386749));
#7239=CARTESIAN_POINT('Ctrl Pts',(2.36765734034256,0.135509677322557,-0.932559713736292));
#7240=CARTESIAN_POINT('Ctrl Pts',(2.3618289331582,0.0683427960735498,-0.928385095283674));
#7241=CARTESIAN_POINT('Ctrl Pts',(2.36176950948769,0.00103986859528879,
-0.924219717613382));
#7242=CARTESIAN_POINT('Ctrl Pts',(2.36176950984586,0.00104027417416537,
-0.924219742714656));
#7243=CARTESIAN_POINT('Ctrl Pts',(2.36169137254877,-0.087423102145968,-0.918744744905834));
#7244=CARTESIAN_POINT('Ctrl Pts',(2.37157967282482,-0.17560646492569,-0.913299058918513));
#7245=CARTESIAN_POINT('Ctrl Pts',(2.39344558752727,-0.271493055808622,-0.906875336705913));
#7246=CARTESIAN_POINT('Ctrl Pts',(2.39576560230082,-0.281106567316079,-0.906225880030156));
#7247=CARTESIAN_POINT('Ctrl Pts',(2.39980837696625,-0.2969794148988,-0.905143944706169));
#7248=CARTESIAN_POINT('Ctrl Pts',(2.40146234587091,-0.303255876299024,-0.904713615876211));
#7249=CARTESIAN_POINT('Ctrl Pts',(2.40480158054008,-0.315515388049364,-0.903867975787011));
#7250=CARTESIAN_POINT('Ctrl Pts',(2.40648249996904,-0.321499408072078,-0.903452814162152));
#7251=CARTESIAN_POINT('Ctrl Pts',(2.40972011665561,-0.332684388942151,-0.902672191964999));
#7252=CARTESIAN_POINT('Ctrl Pts',(2.41126556692301,-0.337888455955341,-0.902307101669647));
#7253=CARTESIAN_POINT('Ctrl Pts',(2.41480867964136,-0.349523957849553,-0.901486485428806));
#7254=CARTESIAN_POINT('Ctrl Pts',(2.41682562540537,-0.355949273660984,-0.901030346854788));
#7255=CARTESIAN_POINT('Ctrl Pts',(2.42210345141635,-0.372271431842001,-0.899863843113399));
#7256=CARTESIAN_POINT('Ctrl Pts',(2.425440717664,-0.382142769464095,-0.899151026909326));
#7257=CARTESIAN_POINT('Ctrl Pts',(2.45164623153488,-0.456393990929186,-0.893732255140715));
#7258=CARTESIAN_POINT('Ctrl Pts',(2.47994267163356,-0.518707723639068,-0.888847096663249));
#7259=CARTESIAN_POINT('Ctrl Pts',(2.54222202032079,-0.629223862472239,-0.879593136506329));
#7260=CARTESIAN_POINT('Ctrl Pts',(2.57473462638666,-0.678022877352781,-0.875265519245851));
#7261=CARTESIAN_POINT('Ctrl Pts',(2.62583047348316,-0.743552549334317,-0.869234744829148));
#7262=CARTESIAN_POINT('Ctrl Pts',(2.64152146788556,-0.762428819681802,-0.867469653372397));
#7263=CARTESIAN_POINT('Ctrl Pts',(2.66753834476747,-0.791808594105275,-0.864693078972203));
#7264=CARTESIAN_POINT('Ctrl Pts',(2.6774907588001,-0.802632216237684,-0.863663450222892));
#7265=CARTESIAN_POINT('Ctrl Pts',(2.69098264653742,-0.816764600931235,-0.862313199688891));
#7266=CARTESIAN_POINT('Ctrl Pts',(2.69434308600831,-0.820241448150295,-0.861980526507242));
#7267=CARTESIAN_POINT('Ctrl Pts',(2.70000965555534,-0.826032511704268,-0.861425756116281));
#7268=CARTESIAN_POINT('Ctrl Pts',(2.70230413634507,-0.828357967771663,-0.861202799993461));
#7269=CARTESIAN_POINT('Ctrl Pts',(2.7068073998265,-0.832884200240964,-0.860768537181673));
#7270=CARTESIAN_POINT('Ctrl Pts',(2.70901528694292,-0.835085793942235,-0.86055716984257));
#7271=CARTESIAN_POINT('Ctrl Pts',(2.713972488068,-0.839989760020111,-0.860085974574311));
#7272=CARTESIAN_POINT('Ctrl Pts',(2.71672640565149,-0.842687479616945,-0.859826502416486));
#7273=CARTESIAN_POINT('Ctrl Pts',(2.72633031888285,-0.852003445377359,-0.858929340455391));
#7274=CARTESIAN_POINT('Ctrl Pts',(2.73324753516953,-0.858552294193845,-0.858296658317883));
#7275=CARTESIAN_POINT('Ctrl Pts',(2.79581566704745,-0.916365238048771,-0.852684840706295));
#7276=CARTESIAN_POINT('Ctrl Pts',(2.85621489284541,-0.962246694790298,-0.848034235487393));
#7277=CARTESIAN_POINT('Ctrl Pts',(2.96814548089873,-1.03138227272268,-0.839896008093139));
#7278=CARTESIAN_POINT('Ctrl Pts',(3.01771085143064,-1.05732337115805,-0.836434060030371));
#7279=CARTESIAN_POINT('Ctrl Pts',(3.09725924760648,-1.09199659070477,-0.830896957977463));
#7280=CARTESIAN_POINT('Ctrl Pts',(3.12606448304018,-1.10322497634146,-0.828896451215516));
#7281=CARTESIAN_POINT('Ctrl Pts',(3.16380653281279,-1.11625113796333,-0.826263534660623));
#7282=CARTESIAN_POINT('Ctrl Pts',(3.1723703205623,-1.11909709212268,-0.825665389514593));
#7283=CARTESIAN_POINT('Ctrl Pts',(3.18663476751442,-1.12365615991865,-0.8246674655009));
#7284=CARTESIAN_POINT('Ctrl Pts',(3.19231732233661,-1.12542500445896,-0.824269500666078));
#7285=CARTESIAN_POINT('Ctrl Pts',(3.20325824027774,-1.12873990305329,-0.823502357645262));
#7286=CARTESIAN_POINT('Ctrl Pts',(3.20851447989547,-1.13029247265128,-0.823133401064346));
#7287=CARTESIAN_POINT('Ctrl Pts',(3.22058276062506,-1.13376575945037,-0.822285258784228));
#7288=CARTESIAN_POINT('Ctrl Pts',(3.22740160672693,-1.13566185627967,-0.821805297339097));
#7289=CARTESIAN_POINT('Ctrl Pts',(3.24919100749393,-1.14150971059971,-0.820269000508651));
#7290=CARTESIAN_POINT('Ctrl Pts',(3.26422205020613,-1.14522762542965,-0.819205299990023));
#7291=CARTESIAN_POINT('Ctrl Pts',(3.3561913221848,-1.16606097629717,-0.812670164013497));
#7292=CARTESIAN_POINT('Ctrl Pts',(3.43460161754377,-1.17571062278816,-0.806965241552146));
#7293=CARTESIAN_POINT('Ctrl Pts',(3.56029260173218,-1.17850159385758,-0.797745596129126));
#7294=CARTESIAN_POINT('Ctrl Pts',(3.60723329068936,-1.17673811478744,-0.794290943156639));
#7295=CARTESIAN_POINT('Ctrl Pts',(3.67508306737412,-1.17011475892615,-0.789363078053028));
#7296=CARTESIAN_POINT('Ctrl Pts',(3.69616308634227,-1.16747972427549,-0.787841711444709));
#7297=CARTESIAN_POINT('Ctrl Pts',(3.73039764636079,-1.16225629632423,-0.785397829837855));
#7298=CARTESIAN_POINT('Ctrl Pts',(3.74359911152947,-1.16001107900636,-0.784462014455471));
#7299=CARTESIAN_POINT('Ctrl Pts',(3.76142666009417,-1.15666530125683,-0.783209718614093));
#7300=CARTESIAN_POINT('Ctrl Pts',(3.76608798882877,-1.1557612748534,-0.782883350487185));
#7301=CARTESIAN_POINT('Ctrl Pts',(3.77386345352732,-1.15420443834303,-0.782340868071289));
#7302=CARTESIAN_POINT('Ctrl Pts',(3.77698059779126,-1.15356716277065,-0.782123907956946));
#7303=CARTESIAN_POINT('Ctrl Pts',(3.78288418319024,-1.15233527755197,-0.781714037158621));
#7304=CARTESIAN_POINT('Ctrl Pts',(3.78567110409258,-1.15174317738436,-0.781520983596849));
#7305=CARTESIAN_POINT('Ctrl Pts',(3.7922739125673,-1.15031530512018,-0.781064571896277));
#7306=CARTESIAN_POINT('Ctrl Pts',(3.79608787463899,-1.14947064384012,-0.780801708240299));
#7307=CARTESIAN_POINT('Ctrl Pts',(3.80947836718751,-1.14643514308341,-0.779881306358804));
#7308=CARTESIAN_POINT('Ctrl Pts',(3.81903193905991,-1.14414340470369,-0.779229121568934));
#7309=CARTESIAN_POINT('Ctrl Pts',(3.89633653720258,-1.12457323711456,-0.773980012266576));
#7310=CARTESIAN_POINT('Ctrl Pts',(3.96246415574902,-1.10140992798168,-0.769661003282745));
#7311=CARTESIAN_POINT('Ctrl Pts',(4.04370070732135,-1.06455025202621,-0.764142660288055));
#7312=CARTESIAN_POINT('Ctrl Pts',(4.06104457509595,-1.05616145202369,-0.762951796426201));
#7313=CARTESIAN_POINT('Ctrl Pts',(4.07816931162903,-1.047354266045,-0.76175719316035));
#7314=CARTESIAN_POINT('Ctrl Pts',(4.0781692670594,-1.04735428896699,-0.661995228290505));
#7315=CARTESIAN_POINT('Ctrl Pts',(4.06384449805672,-1.05472146166857,-0.663027396374779));
#7316=CARTESIAN_POINT('Ctrl Pts',(4.04937017112961,-1.06179393871798,-0.66406769041727));
#7317=CARTESIAN_POINT('Ctrl Pts',(4.02072968252284,-1.07506760891601,-0.666124908225273));
#7318=CARTESIAN_POINT('Ctrl Pts',(4.00657794537862,-1.08129088998704,-0.66714084293908));
#7319=CARTESIAN_POINT('Ctrl Pts',(3.98570657165901,-1.08998298186393,-0.668640397941914));
#7320=CARTESIAN_POINT('Ctrl Pts',(3.97908002581738,-1.09267211458824,-0.669116671298086));
#7321=CARTESIAN_POINT('Ctrl Pts',(3.96733728565307,-1.09731335625582,-0.669961166861675));
#7322=CARTESIAN_POINT('Ctrl Pts',(3.96223115113726,-1.09929046316112,-0.670328547794272));
#7323=CARTESIAN_POINT('Ctrl Pts',(3.95152332944664,-1.10335092082469,-0.671099402510311));
#7324=CARTESIAN_POINT('Ctrl Pts',(3.94591921285633,-1.10542737713696,-0.671503091308947));
#7325=CARTESIAN_POINT('Ctrl Pts',(3.93118353984429,-1.11076008967085,-0.672565346118283));
#7326=CARTESIAN_POINT('Ctrl Pts',(3.92202731489475,-1.11394634832691,-0.673226177654392));
#7327=CARTESIAN_POINT('Ctrl Pts',(3.88255610967042,-1.12713784375608,-0.676078982549639));
#7328=CARTESIAN_POINT('Ctrl Pts',(3.85188305553649,-1.13602048252598,-0.678306606130048));
#7329=CARTESIAN_POINT('Ctrl Pts',(3.72102999211968,-1.16821417866578,-0.687860298912885));
#7330=CARTESIAN_POINT('Ctrl Pts',(3.6183872022316,-1.17959531671325,-0.695527868963861));
#7331=CARTESIAN_POINT('Ctrl Pts',(3.49392431925198,-1.17706672365769,-0.704531277533278));
#7332=CARTESIAN_POINT('Ctrl Pts',(3.47226679019333,-1.17602814559389,-0.706084856838454));
#7333=CARTESIAN_POINT('Ctrl Pts',(3.43710060542435,-1.17336700816546,-0.708574448685394));
#7334=CARTESIAN_POINT('Ctrl Pts',(3.42357018593278,-1.17210732194144,-0.709524329552045));
#7335=CARTESIAN_POINT('Ctrl Pts',(3.40531674095537,-1.17008872043968,-0.710792343683378));
#7336=CARTESIAN_POINT('Ctrl Pts',(3.40057272145931,-1.16953486190257,-0.711120665498905));
#7337=CARTESIAN_POINT('Ctrl Pts',(3.3926673450815,-1.16856313742453,-0.711665577916761));
#7338=CARTESIAN_POINT('Ctrl Pts',(3.38950412782377,-1.16816127020335,-0.711883028231694));
#7339=CARTESIAN_POINT('Ctrl Pts',(3.38352194456256,-1.16737657079426,-0.712293101373884));
#7340=CARTESIAN_POINT('Ctrl Pts',(3.38070267321607,-1.16699636410948,-0.712485871540047));
#7341=CARTESIAN_POINT('Ctrl Pts',(3.37403250525875,-1.16607220646012,-0.712940852852626));
#7342=CARTESIAN_POINT('Ctrl Pts',(3.37018284094189,-1.16551938488063,-0.713202576963058));
#7343=CARTESIAN_POINT('Ctrl Pts',(3.35671972761983,-1.16351793490379,-0.714115070709402));
#7344=CARTESIAN_POINT('Ctrl Pts',(3.34712122419081,-1.16196930626575,-0.714760606893146));
#7345=CARTESIAN_POINT('Ctrl Pts',(3.26616547397237,-1.14787715250985,-0.720171052553844));
#7346=CARTESIAN_POINT('Ctrl Pts',(3.19607657484216,-1.12889076427616,-0.724636543500754));
#7347=CARTESIAN_POINT('Ctrl Pts',(3.07386342586199,-1.08333688949993,-0.732704191285957));
#7348=CARTESIAN_POINT('Ctrl Pts',(3.02112909993145,-1.05911528271416,-0.736288666416117));
#7349=CARTESIAN_POINT('Ctrl Pts',(2.95198291393492,-1.02094984151499,-0.741324442554763));
#7350=CARTESIAN_POINT('Ctrl Pts',(2.93384833753817,-1.01029708484264,-0.742678289251088));
#7351=CARTESIAN_POINT('Ctrl Pts',(2.90277187442234,-0.990904418547217,-0.745064937001914));
#7352=CARTESIAN_POINT('Ctrl Pts',(2.88970034193191,-0.982381871717211,-0.746090202802747));
#7353=CARTESIAN_POINT('Ctrl Pts',(2.87087042769946,-0.969564631657674,-0.747600847997373));
#7354=CARTESIAN_POINT('Ctrl Pts',(2.86497553909145,-0.965472735576419,-0.748078716623134));
#7355=CARTESIAN_POINT('Ctrl Pts',(2.85464807912376,-0.958163248733963,-0.74892488830745));
#7356=CARTESIAN_POINT('Ctrl Pts',(2.85019983029513,-0.954968098727821,-0.749292336592187));
#7357=CARTESIAN_POINT('Ctrl Pts',(2.84095722713426,-0.948230969574695,-0.750062179205172));
#7358=CARTESIAN_POINT('Ctrl Pts',(2.83616716465693,-0.944683394135114,-0.750464780728388));
#7359=CARTESIAN_POINT('Ctrl Pts',(2.82370884923174,-0.935309342610655,-0.751521552431347));
#7360=CARTESIAN_POINT('Ctrl Pts',(2.81608490217181,-0.929425001867218,-0.752177948352769));
#7361=CARTESIAN_POINT('Ctrl Pts',(2.78395797130701,-0.903993898601079,-0.754986295823248));
#7362=CARTESIAN_POINT('Ctrl Pts',(2.76017036639493,-0.88356823413951,-0.757172557513027));
#7363=CARTESIAN_POINT('Ctrl Pts',(2.67663884575618,-0.805842534028724,-0.765256783314842));
#7364=CARTESIAN_POINT('Ctrl Pts',(2.622167641112,-0.743241240029211,-0.771357615567682));
#7365=CARTESIAN_POINT('Ctrl Pts',(2.5448706598329,-0.63283282106341,-0.781223346798208));
#7366=CARTESIAN_POINT('Ctrl Pts',(2.51788128990069,-0.588268969840252,-0.784998270719495));
#7367=CARTESIAN_POINT('Ctrl Pts',(2.49072523848536,-0.535887082058305,-0.789102041887998));
#7368=CARTESIAN_POINT('Ctrl Pts',(2.48757916464597,-0.529684724369334,-0.78958284895361));
#7369=CARTESIAN_POINT('Ctrl Pts',(2.48286139513809,-0.520175987604878,-0.790311804809278));
#7370=CARTESIAN_POINT('Ctrl Pts',(2.48124993374357,-0.516889675028393,-0.790562264501288));
#7371=CARTESIAN_POINT('Ctrl Pts',(2.47832762263425,-0.5108591433676,-0.7910191040279));
#7372=CARTESIAN_POINT('Ctrl Pts',(2.4770120760809,-0.508117349335524,-0.791225759551085));
#7373=CARTESIAN_POINT('Ctrl Pts',(2.4740658509911,-0.501915503143293,-0.791690865530397));
#7374=CARTESIAN_POINT('Ctrl Pts',(2.47244139802913,-0.49845258276926,-0.791948937846555));
#7375=CARTESIAN_POINT('Ctrl Pts',(2.46828594927651,-0.489480804043665,-0.792613511583998));
#7376=CARTESIAN_POINT('Ctrl Pts',(2.46578052779981,-0.483960125807008,-0.793018528990502));
#7377=CARTESIAN_POINT('Ctrl Pts',(2.44923762748605,-0.446747043867711,-0.795723999814623));
#7378=CARTESIAN_POINT('Ctrl Pts',(2.43656104881631,-0.414464298927704,-0.797951814353656));
#7379=CARTESIAN_POINT('Ctrl Pts',(2.4161611494687,-0.354911134495222,-0.801929390635964));
#7380=CARTESIAN_POINT('Ctrl Pts',(2.40796255807533,-0.327833667094271,-0.803690262866974));
#7381=CARTESIAN_POINT('Ctrl Pts',(2.38846646301464,-0.253948059909044,-0.808427916813069));
#7382=CARTESIAN_POINT('Ctrl Pts',(2.37905102809295,-0.206701595100035,-0.811387699066481));
#7383=CARTESIAN_POINT('Ctrl Pts',(2.36538172610949,-0.106384593528173,-0.817719861059856));
#7384=CARTESIAN_POINT('Ctrl Pts',(2.36177966651481,-0.0533386013821922,
-0.821096818502703));
#7385=CARTESIAN_POINT('Ctrl Pts',(2.36176694100396,0.0104570720174762,-0.825289805850122));
#7386=CARTESIAN_POINT('Ctrl Pts',(2.36191040660988,0.0211482986329484,-0.825996773691546));
#7387=CARTESIAN_POINT('Ctrl Pts',(2.36236843029258,0.0380864760305374,-0.827124289206556));
#7388=CARTESIAN_POINT('Ctrl Pts',(2.36258722863895,0.044335611637442,-0.827541881960423));
#7389=CARTESIAN_POINT('Ctrl Pts',(2.3630887104801,0.0560011876736822,-0.828324563396148));
#7390=CARTESIAN_POINT('Ctrl Pts',(2.36335906826686,0.0614180140389397,-0.828689261279015));
#7391=CARTESIAN_POINT('Ctrl Pts',(2.36404586874551,0.0735015574446161,-0.82950572380842));
#7392=CARTESIAN_POINT('Ctrl Pts',(2.36448163076826,0.0801669447027157,-0.82995807455009));
#7393=CARTESIAN_POINT('Ctrl Pts',(2.36593395798388,0.0998129201257336,-0.831297402075247));
#7394=CARTESIAN_POINT('Ctrl Pts',(2.36710907778127,0.11278040919832,-0.832189235740729));
#7395=CARTESIAN_POINT('Ctrl Pts',(2.37541138509143,0.190109062418618,-0.837556130536567));
#7396=CARTESIAN_POINT('Ctrl Pts',(2.38762062974279,0.253802398273469,-0.842187646192627));
#7397=CARTESIAN_POINT('Ctrl Pts',(2.42266464211315,0.379555326406646,-0.851705799239318));
#7398=CARTESIAN_POINT('Ctrl Pts',(2.44561310265269,0.441356814852639,-0.856578300359325));
#7399=CARTESIAN_POINT('Ctrl Pts',(2.48649342933691,0.52834705120888,-0.863520453701498));
#7400=CARTESIAN_POINT('Ctrl Pts',(2.50043868614386,0.555271027494385,-0.865680197679378));
#7401=CARTESIAN_POINT('Ctrl Pts',(2.51857463403817,0.587204107457938,-0.868230899362441));
#7402=CARTESIAN_POINT('Ctrl Pts',(2.52178631641377,0.592753112095173,-0.868673714375721));
#7403=CARTESIAN_POINT('Ctrl Pts',(2.52686360051482,0.601362489549847,-0.86935976903767));
#7404=CARTESIAN_POINT('Ctrl Pts',(2.52869806961092,0.604440939776594,-0.869604883707214));
#7405=CARTESIAN_POINT('Ctrl Pts',(2.53211852103611,0.610121727728589,-0.870056769296397));
#7406=CARTESIAN_POINT('Ctrl Pts',(2.53370054920967,0.612726278385516,-0.870263773621644));
#7407=CARTESIAN_POINT('Ctrl Pts',(2.53734226971226,0.618669662859677,-0.870735763561398));
#7408=CARTESIAN_POINT('Ctrl Pts',(2.53940854878389,0.62200437069181,-0.87100032067971));
#7409=CARTESIAN_POINT('Ctrl Pts',(2.54587990940005,0.632332691975721,-0.87181908509676));
#7410=CARTESIAN_POINT('Ctrl Pts',(2.55034208928388,0.639290485563246,-0.872369756808881));
#7411=CARTESIAN_POINT('Ctrl Pts',(2.58460283914147,0.691494933514421,-0.876499249117139));
#7412=CARTESIAN_POINT('Ctrl Pts',(2.6174223945559,0.734690077843528,-0.879904942180072));
#7413=CARTESIAN_POINT('Ctrl Pts',(2.71491064449213,0.846124888822076,-0.88910799612077));
#7414=CARTESIAN_POINT('Ctrl Pts',(2.78493554889033,0.909125306547553,-0.894823258260179));
#7415=CARTESIAN_POINT('Ctrl Pts',(2.8775610485378,0.974311611141803,-0.902155332392961));
#7416=CARTESIAN_POINT('Ctrl Pts',(2.89370066749655,0.985083782634484,-0.903424134577679));
#7417=CARTESIAN_POINT('Ctrl Pts',(2.91688801648414,0.999745062323917,-0.905238981568036));
#7418=CARTESIAN_POINT('Ctrl Pts',(2.92372136057425,1.00396852238058,-0.905772853492476));
#7419=CARTESIAN_POINT('Ctrl Pts',(2.93493052200697,1.01073903744508,-0.906647302712863));
#7420=CARTESIAN_POINT('Ctrl Pts',(2.93928057915808,1.01332841012302,-0.906986345512928));
#7421=CARTESIAN_POINT('Ctrl Pts',(2.94846594288752,1.01871610198089,-0.907701669480715));
#7422=CARTESIAN_POINT('Ctrl Pts',(2.95330472474207,1.02150821576772,-0.908078161347059));
#7423=CARTESIAN_POINT('Ctrl Pts',(2.96497572562905,1.02813247862298,-0.908985548101728));
#7424=CARTESIAN_POINT('Ctrl Pts',(2.97182659520497,1.03193105235669,-0.909517613333797));
#7425=CARTESIAN_POINT('Ctrl Pts',(2.99587441125569,1.04495280433512,-0.911383616481748));
#7426=CARTESIAN_POINT('Ctrl Pts',(3.01326144961529,1.05381626288246,-0.912729933013163));
#7427=CARTESIAN_POINT('Ctrl Pts',(3.13103882273909,1.11021440999413,-0.92183642553937));
#7428=CARTESIAN_POINT('Ctrl Pts',(3.23748899173449,1.14376595067545,-0.930080065714455));
#7429=CARTESIAN_POINT('Ctrl Pts',(3.38604342108829,1.16837684160571,-0.941036663651135));
#7430=CARTESIAN_POINT('Ctrl Pts',(3.42536628638138,1.17287213541808,-0.943878359376383));
#7431=CARTESIAN_POINT('Ctrl Pts',(3.47106996531247,1.17577578450086,-0.947063210496579));
#7432=CARTESIAN_POINT('Ctrl Pts',(3.47729842939213,1.17612183518022,-0.947494697698407));
#7433=CARTESIAN_POINT('Ctrl Pts',(3.48740325408992,1.17660275629466,-0.94819029693238));
#7434=CARTESIAN_POINT('Ctrl Pts',(3.49127795050671,1.17676798890331,-0.948455969309928));
#7435=CARTESIAN_POINT('Ctrl Pts',(3.49819577274479,1.17702876686691,-0.948928330433654));
#7436=CARTESIAN_POINT('Ctrl Pts',(3.50123851863152,1.1771316548678,-0.949135410562213));
#7437=CARTESIAN_POINT('Ctrl Pts',(3.50789813417171,1.17733099431107,-0.949587140659578));
#7438=CARTESIAN_POINT('Ctrl Pts',(3.51151506676149,1.1774225793188,-0.94983152249864));
#7439=CARTESIAN_POINT('Ctrl Pts',(3.52188386560435,1.17763732288972,-0.950529499150087));
#7440=CARTESIAN_POINT('Ctrl Pts',(3.52863658062403,1.17771908414366,-0.950980896930664));
#7441=CARTESIAN_POINT('Ctrl Pts',(3.57886639929658,1.17789519262264,-0.954317570891468));
#7442=CARTESIAN_POINT('Ctrl Pts',(3.62232359078915,1.1756400930449,-0.957087661581744));
#7443=CARTESIAN_POINT('Ctrl Pts',(3.76508129985068,1.16027398363143,-0.966087390269286));
#7444=CARTESIAN_POINT('Ctrl Pts',(3.86282527951115,1.13692011861388,-0.972124422177075));
#7445=CARTESIAN_POINT('Ctrl Pts',(3.97941906442402,1.09278851738949,-0.980136753882568));
#7446=CARTESIAN_POINT('Ctrl Pts',(4.00211919111816,1.08337423817266,-0.981735261993988));
#7447=CARTESIAN_POINT('Ctrl Pts',(4.0325424193974,1.06962646314573,-0.983939374560743));
#7448=CARTESIAN_POINT('Ctrl Pts',(4.04053650888214,1.0659053955915,-0.984524447672939));
#7449=CARTESIAN_POINT('Ctrl Pts',(4.05318350688247,1.05984480038945,-0.985459871686834));
#7450=CARTESIAN_POINT('Ctrl Pts',(4.05786408793479,1.0575635183545,-0.985808229099558));
#7451=CARTESIAN_POINT('Ctrl Pts',(4.06744428067452,1.05281532310324,-0.986525782149849));
#7452=CARTESIAN_POINT('Ctrl Pts',(4.07234208507604,1.05034506962875,-0.986895086106371));
#7453=CARTESIAN_POINT('Ctrl Pts',(4.08366100012913,1.04453672662344,-0.987754374924724));
#7454=CARTESIAN_POINT('Ctrl Pts',(4.09006889919248,1.04117351804064,-0.988245222697718));
#7455=CARTESIAN_POINT('Ctrl Pts',(4.110491710607,1.03021328440735,-0.989823979759671));
#7456=CARTESIAN_POINT('Ctrl Pts',(4.12438301856667,1.02239096518677,-0.990919722137352));
#7457=CARTESIAN_POINT('Ctrl Pts',(4.15673407479203,1.00329871014212,-0.993524983590162));
#7458=CARTESIAN_POINT('Ctrl Pts',(4.17505011055746,0.99179779083554,-0.995042261847771));
#7459=CARTESIAN_POINT('Ctrl Pts',(4.27861351475689,0.922721771705734,-1.00386920464853));
#7460=CARTESIAN_POINT('Ctrl Pts',(4.35633757632152,0.854680234069028,-1.01153988794234));
#7461=CARTESIAN_POINT('Ctrl Pts',(4.4452055493561,0.753550022877049,-1.02127693373014));
#7462=CARTESIAN_POINT('Ctrl Pts',(4.46521679582857,0.728827657199198,-1.02354550196838));
#7463=CARTESIAN_POINT('Ctrl Pts',(4.4880811283507,0.698116882350186,-1.02620546000706));
#7464=CARTESIAN_POINT('Ctrl Pts',(4.49191446541519,0.69287818221052,-1.02665388379206));
#7465=CARTESIAN_POINT('Ctrl Pts',(4.49780721547107,0.684683742913695,-1.02734676236659));
#7466=CARTESIAN_POINT('Ctrl Pts',(4.49989664059119,0.681749895679036,-1.02759314994675));
#7467=CARTESIAN_POINT('Ctrl Pts',(4.50372797841694,0.676317589212855,-1.02804619575482));
#7468=CARTESIAN_POINT('Ctrl Pts',(4.50547365837579,0.673821960203314,-1.02825309748472));
#7469=CARTESIAN_POINT('Ctrl Pts',(4.50943187583426,0.668116286440486,-1.02872336065821));
#7470=CARTESIAN_POINT('Ctrl Pts',(4.51163817097607,0.664902006050303,-1.0289863061358));
#7471=CARTESIAN_POINT('Ctrl Pts',(4.51840122727407,0.654943503701617,-1.0297950818896));
#7472=CARTESIAN_POINT('Ctrl Pts',(4.5229041855042,0.648162783841992,-1.03033749881339));
#7473=CARTESIAN_POINT('Ctrl Pts',(4.56423244342651,0.584506916468017,-1.03535839404319));
#7474=CARTESIAN_POINT('Ctrl Pts',(4.59616106901539,0.524591459829858,-1.03956300181563));
#7475=CARTESIAN_POINT('Ctrl Pts',(4.656945925136,0.382148819435706,-1.04914823735399));
#7476=CARTESIAN_POINT('Ctrl Pts',(4.68213495463694,0.298508486263926,-1.05450828908948));
#7477=CARTESIAN_POINT('Ctrl Pts',(4.70061440431197,0.197945915105545,-1.06117487516569));
#7478=CARTESIAN_POINT('Ctrl Pts',(4.70306664402943,0.182980789793019,-1.06217176787215));
#7479=CARTESIAN_POINT('Ctrl Pts',(4.70623022961427,0.161025932881263,-1.06364321981611));
#7480=CARTESIAN_POINT('Ctrl Pts',(4.70716913059963,0.154070157414272,-1.06411070918958));
#7481=CARTESIAN_POINT('Ctrl Pts',(4.70872920702809,0.141677838557073,-1.0649460845104));
#7482=CARTESIAN_POINT('Ctrl Pts',(4.70937477926404,0.136244530979993,-1.06531320107108));
#7483=CARTESIAN_POINT('Ctrl Pts',(4.71064641320417,0.124865927367903,-1.06608390385087));
#7484=CARTESIAN_POINT('Ctrl Pts',(4.71126511297489,0.1189199827392,-1.06648770768215));
#7485=CARTESIAN_POINT('Ctrl Pts',(4.71276995507573,0.103303795312426,-1.06755117485564));
#7486=CARTESIAN_POINT('Ctrl Pts',(4.71358179594345,0.0936270216496876,-1.06821311621246));
#7487=CARTESIAN_POINT('Ctrl Pts',(4.71682358635542,0.0482584481335576,-1.07133113253047));
#7488=CARTESIAN_POINT('Ctrl Pts',(4.71774593736107,0.0124813294471392,-1.07383297825155));
#7489=CARTESIAN_POINT('Ctrl Pts',(4.71579391959372,-0.0862564181600668,
-1.08085981367337));
#7490=CARTESIAN_POINT('Ctrl Pts',(4.70949870385573,-0.14902627573032,-1.08546978685763));
#7491=CARTESIAN_POINT('Ctrl Pts',(4.69610124916665,-0.222603093001959,-1.09095850334604));
#7492=CARTESIAN_POINT('Ctrl Pts',(4.69381109208111,-0.234188822147068,-1.0918250568462));
#7493=CARTESIAN_POINT('Ctrl Pts',(4.67986476110268,-0.299558289735975,-1.09672251319418));
#7494=CARTESIAN_POINT('Ctrl Pts',(4.66462292232887,-0.35251414974623,-1.10072455182986));
#7495=CARTESIAN_POINT('Ctrl Pts',(4.64352304476232,-0.410258011082909,-1.10500267434292));
#7496=CARTESIAN_POINT('Ctrl Pts',(4.6412653916238,-0.416282907906336,-1.10544793027893));
#7497=CARTESIAN_POINT('Ctrl Pts',(4.63754708349992,-0.425963606964508,-1.10616121899824));
#7498=CARTESIAN_POINT('Ctrl Pts',(4.63611731159667,-0.42963101680436,-1.1064309406418));
#7499=CARTESIAN_POINT('Ctrl Pts',(4.63354759941266,-0.436126002630176,-1.10690764507312));
#7500=CARTESIAN_POINT('Ctrl Pts',(4.6324150383126,-0.43895639484777,-1.10711504962679));
#7501=CARTESIAN_POINT('Ctrl Pts',(4.62993067814571,-0.445095855863185,-1.10756419563971));
#7502=CARTESIAN_POINT('Ctrl Pts',(4.6285747987739,-0.448403185329899,-1.10780569288453));
#7503=CARTESIAN_POINT('Ctrl Pts',(4.62469250867243,-0.457751574411895,-1.10848714239649));
#7504=CARTESIAN_POINT('Ctrl Pts',(4.62213069776714,-0.46377792557394,-1.10892505686748));
#7505=CARTESIAN_POINT('Ctrl Pts',(4.60458118792502,-0.504123092750719,-1.11184957465907));
#7506=CARTESIAN_POINT('Ctrl Pts',(4.58801259693433,-0.537735397952453,-1.11425097635191));
#7507=CARTESIAN_POINT('Ctrl Pts',(4.54437384162106,-0.616548411627288,-1.11992937868765));
#7508=CARTESIAN_POINT('Ctrl Pts',(4.51582050306904,-0.660833584906177,-1.12316207461071));
#7509=CARTESIAN_POINT('Ctrl Pts',(4.44079596979284,-0.761662882574636,-1.13094811027053));
#7510=CARTESIAN_POINT('Ctrl Pts',(4.39184172443522,-0.816072549531273,-1.13551806672366));
#7511=CARTESIAN_POINT('Ctrl Pts',(4.33048488492769,-0.872684022937023,-1.14099635606994));
#7512=CARTESIAN_POINT('Ctrl Pts',(4.3227075763017,-0.879670436455903,-1.14168640103472));
#7513=CARTESIAN_POINT('Ctrl Pts',(4.30976164617698,-0.890992083576647,-1.14282862402646));
#7514=CARTESIAN_POINT('Ctrl Pts',(4.3046468478007,-0.895388183870356,-1.14327829969705));
#7515=CARTESIAN_POINT('Ctrl Pts',(4.29534731872871,-0.903243136425282,-1.1440931759109));
#7516=CARTESIAN_POINT('Ctrl Pts',(4.29117586424519,-0.906717468243931,-1.14445773693941));
#7517=CARTESIAN_POINT('Ctrl Pts',(4.28218373983157,-0.914102155161602,-1.14524163084726));
#7518=CARTESIAN_POINT('Ctrl Pts',(4.27735589570603,-0.918003473938131,-1.14566130903841));
#7519=CARTESIAN_POINT('Ctrl Pts',(4.26407308871906,-0.928564669859278,-1.14681287562956));
#7520=CARTESIAN_POINT('Ctrl Pts',(4.25555749051845,-0.935146961443839,-1.14754777160343));
#7521=CARTESIAN_POINT('Ctrl Pts',(4.20545732399026,-0.972787290712016,-1.15185322582288));
#7522=CARTESIAN_POINT('Ctrl Pts',(4.1619520991648,-1.00118161930328,-1.15552381851881));
#7523=CARTESIAN_POINT('Ctrl Pts',(4.10399612704973,-1.0337668160214,-1.16032415327027));
#7524=CARTESIAN_POINT('Ctrl Pts',(4.09114291367256,-1.04068199432085,-1.16138314355777));
#7525=CARTESIAN_POINT('Ctrl Pts',(4.07816919733399,-1.04735432482649,-1.16244574507018));
#7526=CARTESIAN_POINT('Origin',(3.53951905042299,8.32667268468867E-16,0.924367114736157));
#7527=CARTESIAN_POINT('',(4.07816941925732,-1.04735421069218,-1.7624800269618));
#7528=CARTESIAN_POINT('',(4.07816926735968,-1.04735428881255,-1.66387346933803));
#7529=CARTESIAN_POINT('',(4.07816926754759,-1.04735428871592,0.924367114736157));
#7530=CARTESIAN_POINT('Ctrl Pts',(4.07816941925732,-1.04735421069218,-1.7624800269618));
#7531=CARTESIAN_POINT('Ctrl Pts',(4.12402156783836,-1.02377262149066,-1.75884119833188));
#7532=CARTESIAN_POINT('Ctrl Pts',(4.16829267925419,-0.997196752434242,-1.75510908299161));
#7533=CARTESIAN_POINT('Ctrl Pts',(4.25805127955991,-0.93494805305265,-1.74711882129328));
#7534=CARTESIAN_POINT('Ctrl Pts',(4.30293455233965,-0.898673155174069,-1.74286238740916));
#7535=CARTESIAN_POINT('Ctrl Pts',(4.36006044211788,-0.845123661458328,-1.73720682626097));
#7536=CARTESIAN_POINT('Ctrl Pts',(4.37476471387704,-0.830594342664483,-1.73572758190825));
#7537=CARTESIAN_POINT('Ctrl Pts',(4.39817290656924,-0.806213989927964,-1.73334358094016));
#7538=CARTESIAN_POINT('Ctrl Pts',(4.40710749433009,-0.796591344546048,-1.7324262688827));
#7539=CARTESIAN_POINT('Ctrl Pts',(4.41902811922707,-0.783314157455995,-1.73119454737553));
#7540=CARTESIAN_POINT('Ctrl Pts',(4.42215548339693,-0.779788561383607,-1.73087065096255));
#7541=CARTESIAN_POINT('Ctrl Pts',(4.42735371647312,-0.773857056213299,-1.73033114347868));
#7542=CARTESIAN_POINT('Ctrl Pts',(4.42943614610039,-0.771461406217131,-1.73011470556488));
#7543=CARTESIAN_POINT('Ctrl Pts',(4.43337316642583,-0.766895059733491,-1.72970496766419));
#7544=CARTESIAN_POINT('Ctrl Pts',(4.43522958442939,-0.764725998675945,-1.72951153029195));
#7545=CARTESIAN_POINT('Ctrl Pts',(4.43962293930561,-0.759554803873737,-1.72905312696225));
#7546=CARTESIAN_POINT('Ctrl Pts',(4.44215279157775,-0.756546655069034,-1.72878866605188));
#7547=CARTESIAN_POINT('Ctrl Pts',(4.45104599166755,-0.745863986304985,-1.72785700877703));
#7548=CARTESIAN_POINT('Ctrl Pts',(4.45732711979027,-0.738121138150766,-1.72719533937084));
#7549=CARTESIAN_POINT('Ctrl Pts',(4.50346225542457,-0.679749961319573,-1.7222996377087));
#7550=CARTESIAN_POINT('Ctrl Pts',(4.53920515782283,-0.626000329528692,-1.71830009188633));
#7551=CARTESIAN_POINT('Ctrl Pts',(4.60005295353438,-0.515876746269686,-1.71051268168533));
#7552=CARTESIAN_POINT('Ctrl Pts',(4.62548652708865,-0.459929402292148,-1.7067343796029));
#7553=CARTESIAN_POINT('Ctrl Pts',(4.65848727668399,-0.369118359268179,-1.70059779161538));
#7554=CARTESIAN_POINT('Ctrl Pts',(4.66903463489072,-0.335458531143566,-1.69832372923198));
#7555=CARTESIAN_POINT('Ctrl Pts',(4.68052969360066,-0.292032938681058,-1.69536391229397));
#7556=CARTESIAN_POINT('Ctrl Pts',(4.68288834355618,-0.282657346423455,-1.69472342820524));
#7557=CARTESIAN_POINT('Ctrl Pts',(4.68651621840781,-0.267447550340622,-1.69368154173606));
#7558=CARTESIAN_POINT('Ctrl Pts',(4.6878570005195,-0.261630743028786,-1.69328241702915));
#7559=CARTESIAN_POINT('Ctrl Pts',(4.69034271350128,-0.250459454456107,-1.69251449611081));
#7560=CARTESIAN_POINT('Ctrl Pts',(4.6914946393424,-0.245106676009676,-1.69214593219876));
#7561=CARTESIAN_POINT('Ctrl Pts',(4.69404228381504,-0.232853449555932,-1.69130075239853));
#7562=CARTESIAN_POINT('Ctrl Pts',(4.69541352643238,-0.225948184367437,-1.69082337912172));
#7563=CARTESIAN_POINT('Ctrl Pts',(4.69956377094064,-0.20402126705809,-1.68930389967736));
#7564=CARTESIAN_POINT('Ctrl Pts',(4.70211236211434,-0.188958155811475,-1.68825465413436));
#7565=CARTESIAN_POINT('Ctrl Pts',(4.71689230484864,-0.0899282119012987,
-1.68131804608723));
#7566=CARTESIAN_POINT('Ctrl Pts',(4.72030932577333,-0.00491321944165487,
-1.67515549505037));
#7567=CARTESIAN_POINT('Ctrl Pts',(4.7130039623824,0.10277357668324,-1.66723486479033));
#7568=CARTESIAN_POINT('Ctrl Pts',(4.71076117480938,0.125782162099334,-1.66553769817192));
#7569=CARTESIAN_POINT('Ctrl Pts',(4.70221944697553,0.1928892962147,-1.66059222937456));
#7570=CARTESIAN_POINT('Ctrl Pts',(4.69409407948227,0.236718854694833,-1.65736698810654));
#7571=CARTESIAN_POINT('Ctrl Pts',(4.68122622746271,0.289295037690181,-1.65357697072449));
#7572=CARTESIAN_POINT('Ctrl Pts',(4.67883443609033,0.298575557605083,-1.65291107454052));
#7573=CARTESIAN_POINT('Ctrl Pts',(4.67524119513117,0.311845493205629,-1.6519643741052));
#7574=CARTESIAN_POINT('Ctrl Pts',(4.674131522781,0.315859051651586,-1.65167875891447));
#7575=CARTESIAN_POINT('Ctrl Pts',(4.67216533547617,0.322826444166616,-1.6511842930227));
#7576=CARTESIAN_POINT('Ctrl Pts',(4.67131850366377,0.3257829317743,-1.65097490277886));
#7577=CARTESIAN_POINT('Ctrl Pts',(4.66950011637425,0.332038674213376,-1.65053278261153));
#7578=CARTESIAN_POINT('Ctrl Pts',(4.66852568337388,0.335337015697624,-1.65030021836079));
#7579=CARTESIAN_POINT('Ctrl Pts',(4.66583356646529,0.344304755837359,-1.64966926988815));
#7580=CARTESIAN_POINT('Ctrl Pts',(4.66408750682879,0.349965633216039,-1.64927247032405));
#7581=CARTESIAN_POINT('Ctrl Pts',(4.6555581270602,0.37689549259379,-1.64739084734756));
#7582=CARTESIAN_POINT('Ctrl Pts',(4.6482132141992,0.397983465379435,-1.64593537569598));
#7583=CARTESIAN_POINT('Ctrl Pts',(4.63384364665159,0.435747100932546,-1.64334016055827));
#7584=CARTESIAN_POINT('Ctrl Pts',(4.62702620250074,0.452493211383162,-1.64219341864626));
#7585=CARTESIAN_POINT('Ctrl Pts',(4.61084911706903,0.489749855802069,-1.63963765582858));
#7586=CARTESIAN_POINT('Ctrl Pts',(4.60128071766576,0.510161986485313,-1.63823422661368));
#7587=CARTESIAN_POINT('Ctrl Pts',(4.55972093587499,0.592579193203745,-1.63250863585511));
#7588=CARTESIAN_POINT('Ctrl Pts',(4.52283891071328,0.651953610970371,-1.62823474923878));
#7589=CARTESIAN_POINT('Ctrl Pts',(4.46693956838103,0.726310918199653,-1.62232560530166));
#7590=CARTESIAN_POINT('Ctrl Pts',(4.45241171692637,0.744488578574955,-1.62083258294982));
#7591=CARTESIAN_POINT('Ctrl Pts',(4.42644659176075,0.775073373047359,-1.61822390401277));
#7592=CARTESIAN_POINT('Ctrl Pts',(4.41526329492532,0.78768722793614,-1.61711792090836));
#7593=CARTESIAN_POINT('Ctrl Pts',(4.39878757302733,0.805485822167764,-1.61551053875043));
#7594=CARTESIAN_POINT('Ctrl Pts',(4.39371059757371,0.810867806894958,-1.61501810984387));
#7595=CARTESIAN_POINT('Ctrl Pts',(4.38476409958284,0.820174518560993,-1.61415512696631));
#7596=CARTESIAN_POINT('Ctrl Pts',(4.38091707111418,0.824120624086463,-1.61378554052036));
#7597=CARTESIAN_POINT('Ctrl Pts',(4.37341422834849,0.831709400796884,-1.61306753254382));
#7598=CARTESIAN_POINT('Ctrl Pts',(4.36976188139756,0.835355334750929,-1.61271926654244));
#7599=CARTESIAN_POINT('Ctrl Pts',(4.35998035578412,0.844992169020553,-1.61178979408735));
#7600=CARTESIAN_POINT('Ctrl Pts',(4.35380963872326,0.85094027427078,-1.61120676282103));
#7601=CARTESIAN_POINT('Ctrl Pts',(4.33098266892604,0.872468079164142,-1.60906161114945));
#7602=CARTESIAN_POINT('Ctrl Pts',(4.31394070545571,0.887629530893936,-1.60748222245532));
#7603=CARTESIAN_POINT('Ctrl Pts',(4.21861436543652,0.967601300261546,-1.59875946098973));
#7604=CARTESIAN_POINT('Ctrl Pts',(4.13264048326198,1.02255700607095,-1.5912367982865));
#7605=CARTESIAN_POINT('Ctrl Pts',(4.01347828389879,1.0785930862681,-1.58163105591438));
#7606=CARTESIAN_POINT('Ctrl Pts',(3.98576720456792,1.09035004892502,-1.57945356177546));
#7607=CARTESIAN_POINT('Ctrl Pts',(3.9469219627294,1.10510146032129,-1.57650283524124));
#7608=CARTESIAN_POINT('Ctrl Pts',(3.93615015565345,1.10901314629823,-1.57569515093149));
#7609=CARTESIAN_POINT('Ctrl Pts',(3.91734150566344,1.11553422557838,-1.57430505373057));
#7610=CARTESIAN_POINT('Ctrl Pts',(3.90933064357695,1.11821545862779,-1.57371927910735));
#7611=CARTESIAN_POINT('Ctrl Pts',(3.89752491896508,1.12202608014478,-1.57286590499044));
#7612=CARTESIAN_POINT('Ctrl Pts',(3.89375231934396,1.12322282685655,-1.57259467676492));
#7613=CARTESIAN_POINT('Ctrl Pts',(3.88706100180845,1.12530838548232,-1.5721163017335));
#7614=CARTESIAN_POINT('Ctrl Pts',(3.8841447825356,1.12620489962643,-1.5719087221209));
#7615=CARTESIAN_POINT('Ctrl Pts',(3.87781775476554,1.12812309859558,-1.57146033365875));
#7616=CARTESIAN_POINT('Ctrl Pts',(3.87440577955913,1.12914065484973,-1.57121976095565));
#7617=CARTESIAN_POINT('Ctrl Pts',(3.86493792443298,1.13191757064232,-1.57055546566782));
#7618=CARTESIAN_POINT('Ctrl Pts',(3.85887234041032,1.13364382008187,-1.57013357843805));
#7619=CARTESIAN_POINT('Ctrl Pts',(3.82530460332513,1.14290630646632,-1.56781764691092));
#7620=CARTESIAN_POINT('Ctrl Pts',(3.79754718027202,1.14949118857355,-1.56597214837872));
#7621=CARTESIAN_POINT('Ctrl Pts',(3.66562919439549,1.17576561400528,-1.55740952463851));
#7622=CARTESIAN_POINT('Ctrl Pts',(3.5593615929637,1.18234417043931,-1.55107273857339));
#7623=CARTESIAN_POINT('Ctrl Pts',(3.43182088613601,1.17301955158421,-1.54293092883299));
#7624=CARTESIAN_POINT('Ctrl Pts',(3.41004967818746,1.17081653444504,-1.54152412013656));
#7625=CARTESIAN_POINT('Ctrl Pts',(3.37240117774762,1.16594400163605,-1.5390526761519));
#7626=CARTESIAN_POINT('Ctrl Pts',(3.35649358778646,1.16355293728631,-1.53799635541198));
#7627=CARTESIAN_POINT('Ctrl Pts',(3.33348154668428,1.15961043684511,-1.53644839662488));
#7628=CARTESIAN_POINT('Ctrl Pts',(3.32633417709084,1.1583177560671,-1.53596481569026));
#7629=CARTESIAN_POINT('Ctrl Pts',(3.31380615043783,1.15593204415302,-1.53511206084683));
#7630=CARTESIAN_POINT('Ctrl Pts',(3.30842027446222,1.15486733347588,-1.53474378558529));
#7631=CARTESIAN_POINT('Ctrl Pts',(3.29723925725165,1.15257566002025,-1.5339756800357));
#7632=CARTESIAN_POINT('Ctrl Pts',(3.29144554702594,1.15134255760537,-1.53357566561486));
#7633=CARTESIAN_POINT('Ctrl Pts',(3.27642675662717,1.14802741368854,-1.53253339315456));
#7634=CARTESIAN_POINT('Ctrl Pts',(3.26721716635233,1.14587790471841,-1.53188902120037));
#7635=CARTESIAN_POINT('Ctrl Pts',(3.2291991765614,1.13652034676396,-1.52920658546107));
#7636=CARTESIAN_POINT('Ctrl Pts',(3.20064485018686,1.12833546793783,-1.5271379560596));
#7637=CARTESIAN_POINT('Ctrl Pts',(3.09246082757994,1.09284839070095,-1.51908642499023));
#7638=CARTESIAN_POINT('Ctrl Pts',(3.01554006419951,1.05812149385582,-1.5128848914851));
#7639=CARTESIAN_POINT('Ctrl Pts',(2.897657373682,0.988874448589901,-1.50287557155424));
#7640=CARTESIAN_POINT('Ctrl Pts',(2.8541541765315,0.959236883287899,-1.4990600860629));
#7641=CARTESIAN_POINT('Ctrl Pts',(2.80729209670304,0.922489709671055,-1.49491802572919));
#7642=CARTESIAN_POINT('Ctrl Pts',(2.80184916997425,0.918143087732133,-1.49443645754283));
#7643=CARTESIAN_POINT('Ctrl Pts',(2.79360311053011,0.911437266156045,-1.49370655079394));
#7644=CARTESIAN_POINT('Ctrl Pts',(2.79077200578922,0.909112943255084,-1.49345589333044));
#7645=CARTESIAN_POINT('Ctrl Pts',(2.78560971517004,0.904834255483009,-1.49299880131462));
#7646=CARTESIAN_POINT('Ctrl Pts',(2.78327524734904,0.902884060352113,-1.49279208999418));
#7647=CARTESIAN_POINT('Ctrl Pts',(2.77802305366047,0.898461759202,-1.49232698616727));
#7648=CARTESIAN_POINT('Ctrl Pts',(2.77510979467302,0.89598447340852,-1.49206897092791));
#7649=CARTESIAN_POINT('Ctrl Pts',(2.76761311634263,0.889546505097599,-1.49140477643663));
#7650=CARTESIAN_POINT('Ctrl Pts',(2.76304802651306,0.885564514101435,-1.4910000775387));
#7651=CARTESIAN_POINT('Ctrl Pts',(2.73268080120068,0.858660725688144,-1.48830477319058));
#7652=CARTESIAN_POINT('Ctrl Pts',(2.70786355695607,0.834647136575428,-1.4860861621365));
#7653=CARTESIAN_POINT('Ctrl Pts',(2.6784630992231,0.803583093869982,-1.48338316824471));
#7654=CARTESIAN_POINT('Ctrl Pts',(2.6728545413076,0.797531048034353,-1.48286394456196));
#7655=CARTESIAN_POINT('Ctrl Pts',(2.65501060289876,0.777865591166287,-1.48119848872164));
#7656=CARTESIAN_POINT('Ctrl Pts',(2.64302862673834,0.76402553655045,-1.48005922381001));
#7657=CARTESIAN_POINT('Ctrl Pts',(2.60226028051457,0.714654945089442,-1.47608688593562));
#7658=CARTESIAN_POINT('Ctrl Pts',(2.5752248577766,0.677733251261796,-1.47327506229901));
#7659=CARTESIAN_POINT('Ctrl Pts',(2.52980832401545,0.607469216965361,-1.46805562199051));
#7660=CARTESIAN_POINT('Ctrl Pts',(2.51076539235449,0.574630464091372,-1.46566410296407));
#7661=CARTESIAN_POINT('Ctrl Pts',(2.48591578247145,0.52657060258171,-1.46218251098858));
#7662=CARTESIAN_POINT('Ctrl Pts',(2.47878702403522,0.512058566787382,-1.46113365207363));
#7663=CARTESIAN_POINT('Ctrl Pts',(2.46658769965374,0.485875661607356,-1.45924216773586));
#7664=CARTESIAN_POINT('Ctrl Pts',(2.46140321089575,0.474260538236342,-1.45840339004994));
#7665=CARTESIAN_POINT('Ctrl Pts',(2.45380809366998,0.45647628822524,-1.4571184532792));
#7666=CARTESIAN_POINT('Ctrl Pts',(2.45125959713045,0.450366786784851,-1.45667691925175));
#7667=CARTESIAN_POINT('Ctrl Pts',(2.44671774834194,0.439214949747966,-1.45587061022657));
#7668=CARTESIAN_POINT('Ctrl Pts',(2.44470744109183,0.434179682051117,-1.45550641231937));
#7669=CARTESIAN_POINT('Ctrl Pts',(2.44043520358832,0.423260552178374,-1.45471625919872));
#7670=CARTESIAN_POINT('Ctrl Pts',(2.43818561094402,0.417372075996157,-1.45428990838787));
#7671=CARTESIAN_POINT('Ctrl Pts',(2.43217166334469,0.401242902198157,-1.45312129086021));
#7672=CARTESIAN_POINT('Ctrl Pts',(2.42850224960028,0.39096771815302,-1.4523759398954));
#7673=CARTESIAN_POINT('Ctrl Pts',(2.4087606355546,0.333163278708378,-1.4481767701443));
#7674=CARTESIAN_POINT('Ctrl Pts',(2.39559781285615,0.284702182677126,-1.44463012504818));
#7675=CARTESIAN_POINT('Ctrl Pts',(2.36969404711082,0.157803112612822,-1.43528740164707));
#7676=CARTESIAN_POINT('Ctrl Pts',(2.3617224083408,0.0786523203925032,-1.42939606451052));
#7677=CARTESIAN_POINT('Ctrl Pts',(2.36178952604145,-0.0350283978066116,
-1.42115590347207));
#7678=CARTESIAN_POINT('Ctrl Pts',(2.3633110826812,-0.0693478293372115,-1.41870012363523));
#7679=CARTESIAN_POINT('Ctrl Pts',(2.36686244336644,-0.109581702054972,-1.41589288626285));
#7680=CARTESIAN_POINT('Ctrl Pts',(2.36744086055434,-0.11560444705143,-1.41547457393234));
#7681=CARTESIAN_POINT('Ctrl Pts',(2.36846034979838,-0.125424035540343,-1.41479595687285));
#7682=CARTESIAN_POINT('Ctrl Pts',(2.36887352829259,-0.129223571969174,-1.41453421033222));
#7683=CARTESIAN_POINT('Ctrl Pts',(2.36964875792967,-0.136043425957578,-1.41406597486874));
#7684=CARTESIAN_POINT('Ctrl Pts',(2.37000401958411,-0.139064403360385,-1.41385912422629));
#7685=CARTESIAN_POINT('Ctrl Pts',(2.37081311940635,-0.14572213348381,-1.41340450178702));
#7686=CARTESIAN_POINT('Ctrl Pts',(2.37127222982741,-0.149358161686565,-1.41315702336807));
#7687=CARTESIAN_POINT('Ctrl Pts',(2.37265428016482,-0.159907193152545,-1.41244121659493));
#7688=CARTESIAN_POINT('Ctrl Pts',(2.3736216803609,-0.166814360255853,-1.41197526313782));
#7689=CARTESIAN_POINT('Ctrl Pts',(2.38248084560995,-0.226221426809344,-1.40798810158194));
#7690=CARTESIAN_POINT('Ctrl Pts',(2.39385386137737,-0.278148061494531,-1.40463917024175));
#7691=CARTESIAN_POINT('Ctrl Pts',(2.4325892371466,-0.411232633154748,-1.39600968930499));
#7692=CARTESIAN_POINT('Ctrl Pts',(2.46535135532612,-0.490478444462737,-1.3908067015251));
#7693=CARTESIAN_POINT('Ctrl Pts',(2.51993512987423,-0.590201690231243,-1.38353327947164));
#7694=CARTESIAN_POINT('Ctrl Pts',(2.5343494264082,-0.614429193001555,-1.38170574176274));
#7695=CARTESIAN_POINT('Ctrl Pts',(2.55464441715308,-0.645912600656586,-1.37923546857936));
#7696=CARTESIAN_POINT('Ctrl Pts',(2.55976277795992,-0.653650341853781,-1.37862041904227));
#7697=CARTESIAN_POINT('Ctrl Pts',(2.56827614390267,-0.66619584683815,-1.37760972910029));
#7698=CARTESIAN_POINT('Ctrl Pts',(2.57161678364344,-0.671040155017402,-1.37721611655494));
#7699=CARTESIAN_POINT('Ctrl Pts',(2.57815249271537,-0.68036733234645,-1.37645163859999));
#7700=CARTESIAN_POINT('Ctrl Pts',(2.58134297108685,-0.68485324298345,-1.37608095323778));
#7701=CARTESIAN_POINT('Ctrl Pts',(2.58887202258151,-0.695283719576946,-1.37521188563698));
#7702=CARTESIAN_POINT('Ctrl Pts',(2.59323505916464,-0.701210257971917,-1.37471257891483));
#7703=CARTESIAN_POINT('Ctrl Pts',(2.60763724410199,-0.720394267844292,-1.37307799826549));
#7704=CARTESIAN_POINT('Ctrl Pts',(2.61790129612382,-0.733479562192908,-1.37193409363574));
#7705=CARTESIAN_POINT('Ctrl Pts',(2.6429217282258,-0.764022678330969,-1.36919276209822));
#7706=CARTESIAN_POINT('Ctrl Pts',(2.65791563419098,-0.781276332993568,-1.36758643508937));
#7707=CARTESIAN_POINT('Ctrl Pts',(2.71908167880184,-0.847656742967956,-1.36117275183795));
#7708=CARTESIAN_POINT('Ctrl Pts',(2.76892974071437,-0.893213128249696,-1.35623315699841));
#7709=CARTESIAN_POINT('Ctrl Pts',(2.82843086820848,-0.938885822236372,-1.3507288973519));
#7710=CARTESIAN_POINT('Ctrl Pts',(2.83451311610812,-0.943461511344577,-1.35017056792598));
#7711=CARTESIAN_POINT('Ctrl Pts',(2.88597945750959,-0.981404149145852,-1.34548407050552));
#7712=CARTESIAN_POINT('Ctrl Pts',(2.93366494064733,-1.01153863413426,-1.34138373138775));
#7713=CARTESIAN_POINT('Ctrl Pts',(2.98900271913295,-1.0411859849375,-1.3370150329672));
#7714=CARTESIAN_POINT('Ctrl Pts',(2.99470092534498,-1.04417896044123,-1.33656960734444));
#7715=CARTESIAN_POINT('Ctrl Pts',(3.00392407904516,-1.0489273525122,-1.33585607701315));
#7716=CARTESIAN_POINT('Ctrl Pts',(3.00743370054857,-1.05071201848643,-1.3355862820396));
#7717=CARTESIAN_POINT('Ctrl Pts',(3.01367704136102,-1.05384749415545,-1.33510946794191));
#7718=CARTESIAN_POINT('Ctrl Pts',(3.0164071275492,-1.05520532425152,-1.33490202669739));
#7719=CARTESIAN_POINT('Ctrl Pts',(3.02234940572972,-1.05813203318312,-1.33445282254889));
#7720=CARTESIAN_POINT('Ctrl Pts',(3.02556348326635,-1.05969689858941,-1.33421130378618));
#7721=CARTESIAN_POINT('Ctrl Pts',(3.03468490867483,-1.06408666346032,-1.33352983452817));
#7722=CARTESIAN_POINT('Ctrl Pts',(3.04060887289725,-1.06687702086005,-1.33309192167412));
#7723=CARTESIAN_POINT('Ctrl Pts',(3.08055007866884,-1.08528503352303,-1.33016858421557));
#7724=CARTESIAN_POINT('Ctrl Pts',(3.11527568093058,-1.09932447875169,-1.32776827851351));
#7725=CARTESIAN_POINT('Ctrl Pts',(3.20030478962864,-1.12907042679265,-1.32209015321045));
#7726=CARTESIAN_POINT('Ctrl Pts',(3.25110641094363,-1.14310321123864,-1.3188567341802));
#7727=CARTESIAN_POINT('Ctrl Pts',(3.37423656052095,-1.16838057105099,-1.31106954470835));
#7728=CARTESIAN_POINT('Ctrl Pts',(3.44699631956718,-1.17637958108633,-1.30649917109925));
#7729=CARTESIAN_POINT('Ctrl Pts',(3.53047489557254,-1.17776166705568,-1.30102045863125));
#7730=CARTESIAN_POINT('Ctrl Pts',(3.54092866205826,-1.17779554368283,-1.30033045772814));
#7731=CARTESIAN_POINT('Ctrl Pts',(3.55812558122246,-1.177622329282,-1.29918825891853));
#7732=CARTESIAN_POINT('Ctrl Pts',(3.56486910554612,-1.17749646493795,-1.29873856268896));
#7733=CARTESIAN_POINT('Ctrl Pts',(3.57703860877626,-1.17716474013002,-1.29792361613158));
#7734=CARTESIAN_POINT('Ctrl Pts',(3.58246498948656,-1.17697926374947,-1.29755900517698));
#7735=CARTESIAN_POINT('Ctrl Pts',(3.59409309806293,-1.1765012883705,-1.29677496667228));
#7736=CARTESIAN_POINT('Ctrl Pts',(3.60029416096478,-1.1761972587982,-1.29635519344792));
#7737=CARTESIAN_POINT('Ctrl Pts',(3.61724166762075,-1.17523196784924,-1.29520326709841));
#7738=CARTESIAN_POINT('Ctrl Pts',(3.62798168351054,-1.17447236352397,-1.29446810381238));
#7739=CARTESIAN_POINT('Ctrl Pts',(3.6904854325951,-1.16918951173482,-1.29015833817254));
#7740=CARTESIAN_POINT('Ctrl Pts',(3.74190759125941,-1.16139247237629,-1.28648346484916));
#7741=CARTESIAN_POINT('Ctrl Pts',(3.86495100312061,-1.13431523204402,-1.27738696469821));
#7742=CARTESIAN_POINT('Ctrl Pts',(3.93559803864069,-1.11161926810425,-1.27189983064239));
#7743=CARTESIAN_POINT('Ctrl Pts',(4.01785602921749,-1.07634940325568,-1.26539391958374));
#7744=CARTESIAN_POINT('Ctrl Pts',(4.03195083345737,-1.06997442715185,-1.26427535331562));
#7745=CARTESIAN_POINT('Ctrl Pts',(4.05674825621073,-1.05816489756866,-1.26230502090634));
#7746=CARTESIAN_POINT('Ctrl Pts',(4.06750046289602,-1.05284121326361,-1.26144986513958));
#7747=CARTESIAN_POINT('Ctrl Pts',(4.07816926864928,-1.04735428814932,-1.26060176719248));
#7748=CARTESIAN_POINT('',(2.36176947928705,0.00103427561139527,-1.32571981376975));
#7749=CARTESIAN_POINT('Ctrl Pts',(4.07816919733399,-1.04735432482649,-1.16244574507018));
#7750=CARTESIAN_POINT('Ctrl Pts',(4.02576993936297,-1.07430305395767,-1.16673746298016));
#7751=CARTESIAN_POINT('Ctrl Pts',(3.97140528621463,-1.09729006594874,-1.17109351575135));
#7752=CARTESIAN_POINT('Ctrl Pts',(3.89907451381304,-1.12165793381364,-1.17664363878772));
#7753=CARTESIAN_POINT('Ctrl Pts',(3.88249576664682,-1.12683790775929,-1.17789930736607));
#7754=CARTESIAN_POINT('Ctrl Pts',(3.84387492467964,-1.13797346763657,-1.18077851439586));
#7755=CARTESIAN_POINT('Ctrl Pts',(3.82176090442941,-1.14365895833256,-1.18239309715367));
#7756=CARTESIAN_POINT('Ctrl Pts',(3.793673930072,-1.1500156377344,-1.18438999917358));
#7757=CARTESIAN_POINT('Ctrl Pts',(3.78784384947714,-1.15128861186597,-1.18480160366909));
#7758=CARTESIAN_POINT('Ctrl Pts',(3.77862964379605,-1.15322724487107,-1.1854472995747));
#7759=CARTESIAN_POINT('Ctrl Pts',(3.7752519368968,-1.15392242424811,-1.18568297599713));
#7760=CARTESIAN_POINT('Ctrl Pts',(3.76885930787444,-1.15520887613308,-1.18612702649756));
#7761=CARTESIAN_POINT('Ctrl Pts',(3.765845148203,-1.15580318345222,-1.18633555663617));
#7762=CARTESIAN_POINT('Ctrl Pts',(3.75875951634206,-1.15717148922491,-1.18682383983025));
#7763=CARTESIAN_POINT('Ctrl Pts',(3.75468623909621,-1.15793580115188,-1.18710305112941));
#7764=CARTESIAN_POINT('Ctrl Pts',(3.74129006564816,-1.16037633702375,-1.1880166981226));
#7765=CARTESIAN_POINT('Ctrl Pts',(3.73195068943448,-1.16196164497823,-1.18864632247463));
#7766=CARTESIAN_POINT('Ctrl Pts',(3.67964637132004,-1.17019206334374,-1.1921366771471));
#7767=CARTESIAN_POINT('Ctrl Pts',(3.63635363864641,-1.17456759652873,-1.19489161152607));
#7768=CARTESIAN_POINT('Ctrl Pts',(3.53214613350913,-1.17929682718839,-1.20140941104788));
#7769=CARTESIAN_POINT('Ctrl Pts',(3.47125600694485,-1.1773426556639,-1.20512927121521));
#7770=CARTESIAN_POINT('Ctrl Pts',(3.35627386626345,-1.16469912933824,-1.21235313707226));
#7771=CARTESIAN_POINT('Ctrl Pts',(3.30225094683362,-1.15490499974966,-1.21583311105905));
#7772=CARTESIAN_POINT('Ctrl Pts',(3.23833792391426,-1.13864330090122,-1.22016387706283));
#7773=CARTESIAN_POINT('Ctrl Pts',(3.22760439318307,-1.13574991546692,-1.22089843078489));
#7774=CARTESIAN_POINT('Ctrl Pts',(3.21080718470864,-1.13096590859511,-1.22206013816313));
#7775=CARTESIAN_POINT('Ctrl Pts',(3.20471491851737,-1.12917738538525,-1.22248402212577));
#7776=CARTESIAN_POINT('Ctrl Pts',(3.19350052604868,-1.12578641165289,-1.22326912406143));
#7777=CARTESIAN_POINT('Ctrl Pts',(3.18837429237067,-1.12419803466002,-1.22362987959535));
#7778=CARTESIAN_POINT('Ctrl Pts',(3.17702541379756,-1.1205963588183,-1.22443280884789));
#7779=CARTESIAN_POINT('Ctrl Pts',(3.1708083605516,-1.11856616263138,-1.22487552068921));
#7780=CARTESIAN_POINT('Ctrl Pts',(3.1535420490446,-1.11276821304423,-1.22611319130398));
#7781=CARTESIAN_POINT('Ctrl Pts',(3.14253167525274,-1.10888788815956,-1.22691178483548));
#7782=CARTESIAN_POINT('Ctrl Pts',(3.11757796039311,-1.09967431559004,-1.22874370656214));
#7783=CARTESIAN_POINT('Ctrl Pts',(3.10367492285101,-1.09423843175196,-1.22978025392077));
#7784=CARTESIAN_POINT('Ctrl Pts',(3.05877932407595,-1.07569355690775,-1.2331803089629));
#7785=CARTESIAN_POINT('Ctrl Pts',(3.02824662366678,-1.06152129972799,-1.23557635164609));
#7786=CARTESIAN_POINT('Ctrl Pts',(2.9131747192986,-1.00199172343757,-1.24492209171011));
#7787=CARTESIAN_POINT('Ctrl Pts',(2.83369371688641,-0.947683414927965,-1.2520923931899));
#7788=CARTESIAN_POINT('Ctrl Pts',(2.74689536955338,-0.87133829678888,-1.26033802760937));
#7789=CARTESIAN_POINT('Ctrl Pts',(2.73243858553963,-0.857965011503711,-1.2617258781076));
#7790=CARTESIAN_POINT('Ctrl Pts',(2.71425643410172,-0.84027903678785,-1.2634830616131));
#7791=CARTESIAN_POINT('Ctrl Pts',(2.71021843622915,-0.836294051219419,-1.26387407605042));
#7792=CARTESIAN_POINT('Ctrl Pts',(2.70381824152164,-0.829885937273577,-1.2644948373947));
#7793=CARTESIAN_POINT('Ctrl Pts',(2.70143748236444,-0.827481599127388,-1.2647259754607));
#7794=CARTESIAN_POINT('Ctrl Pts',(2.6969002902336,-0.82285980225104,-1.26516684766887));
#7795=CARTESIAN_POINT('Ctrl Pts',(2.69474220501672,-0.820644082938962,-1.26537670272643));
#7796=CARTESIAN_POINT('Ctrl Pts',(2.69044817453351,-0.816200487295676,-1.26579462694863));
#7797=CARTESIAN_POINT('Ctrl Pts',(2.68831220304368,-0.813972660019503,-1.26600269974507));
#7798=CARTESIAN_POINT('Ctrl Pts',(2.68106270562862,-0.806351660297764,-1.26670964350527));
#7799=CARTESIAN_POINT('Ctrl Pts',(2.67599135001877,-0.80091835637258,-1.26720545364832));
#7800=CARTESIAN_POINT('Ctrl Pts',(2.63739458012216,-0.758774081422109,-1.27099222967911));
#7801=CARTESIAN_POINT('Ctrl Pts',(2.60616818009097,-0.720016726888708,-1.27413501527477));
#7802=CARTESIAN_POINT('Ctrl Pts',(2.54881866819172,-0.63880887967056,-1.28033320769855));
#7803=CARTESIAN_POINT('Ctrl Pts',(2.5227523346648,-0.596447477207469,-1.2833831006497));
#7804=CARTESIAN_POINT('Ctrl Pts',(2.47025513500272,-0.497633438810671,-1.29034240035067));
#7805=CARTESIAN_POINT('Ctrl Pts',(2.44547241356908,-0.440482454989256,-1.29426688321092));
#7806=CARTESIAN_POINT('Ctrl Pts',(2.42196509377384,-0.371853960864225,-1.29902829462145));
#7807=CARTESIAN_POINT('Ctrl Pts',(2.41874008757761,-0.362017568081936,-1.29971166474106));
#7808=CARTESIAN_POINT('Ctrl Pts',(2.41363805670928,-0.345734170114021,-1.30084510270445));
#7809=CARTESIAN_POINT('Ctrl Pts',(2.41168571945516,-0.33931121822877,-1.30129273502597));
#7810=CARTESIAN_POINT('Ctrl Pts',(2.40825472622772,-0.327666809348538,-1.30210542151025));
#7811=CARTESIAN_POINT('Ctrl Pts',(2.40675703548107,-0.322451120275434,-1.30246985168342));
#7812=CARTESIAN_POINT('Ctrl Pts',(2.40361755479659,-0.31122606167101,-1.30325515167251));
#7813=CARTESIAN_POINT('Ctrl Pts',(2.40198729933713,-0.305213666023405,-1.30367637871168));
#7814=CARTESIAN_POINT('Ctrl Pts',(2.39875087720502,-0.292891495436641,-1.30454100787296));
#7815=CARTESIAN_POINT('Ctrl Pts',(2.39714918565918,-0.286580777885108,-1.30498453668737));
#7816=CARTESIAN_POINT('Ctrl Pts',(2.39323485901956,-0.270603765024212,-1.30610936019814));
#7817=CARTESIAN_POINT('Ctrl Pts',(2.39099214593264,-0.260921030801323,-1.30679282937921));
#7818=CARTESIAN_POINT('Ctrl Pts',(2.3707780866703,-0.168332682349826,-1.31334643242981));
#7819=CARTESIAN_POINT('Ctrl Pts',(2.3616950574931,-0.0837599189378531,-1.31949818309692));
#7820=CARTESIAN_POINT('Ctrl Pts',(2.36176950434981,0.00103403308384097,
-1.32571983981107));
#7821=CARTESIAN_POINT('Ctrl Pts',(2.36176950455994,0.00103427238999479,
-1.32571985736988));
#7822=CARTESIAN_POINT('Ctrl Pts',(2.3618316127191,0.0717582489250692,-1.33090914618683));
#7823=CARTESIAN_POINT('Ctrl Pts',(2.36826403998405,0.142341883379032,-1.33611673408395));
#7824=CARTESIAN_POINT('Ctrl Pts',(2.38208108694226,0.217873682753449,-1.34148119336579));
#7825=CARTESIAN_POINT('Ctrl Pts',(2.38321426120892,0.223809783178999,-1.3419013035356));
#7826=CARTESIAN_POINT('Ctrl Pts',(2.38514025103522,0.233493727788146,-1.34258394379339));
#7827=CARTESIAN_POINT('Ctrl Pts',(2.38590573275984,0.2372468075739,-1.34284783772917));
#7828=CARTESIAN_POINT('Ctrl Pts',(2.38742299982363,0.244504808475719,-1.3433567962311));
#7829=CARTESIAN_POINT('Ctrl Pts',(2.3881725027798,0.248010159603775,-1.34360197964144));
#7830=CARTESIAN_POINT('Ctrl Pts',(2.38958880490685,0.254489253143669,-1.34405393722106));
#7831=CARTESIAN_POINT('Ctrl Pts',(2.39025114042218,0.257463824480693,-1.34426094528302));
#7832=CARTESIAN_POINT('Ctrl Pts',(2.39179232886378,0.264260889756969,-1.34473288535538));
#7833=CARTESIAN_POINT('Ctrl Pts',(2.3926787361519,0.268081591885901,-1.34499738933919));
#7834=CARTESIAN_POINT('Ctrl Pts',(2.39505853483023,0.278111439636333,-1.34568987077724));
#7835=CARTESIAN_POINT('Ctrl Pts',(2.39658339373676,0.284313090999179,-1.34611615072583));
#7836=CARTESIAN_POINT('Ctrl Pts',(2.41268497981492,0.347574961479989,-1.3504480310999));
#7837=CARTESIAN_POINT('Ctrl Pts',(2.43147386657798,0.403486333356421,-1.35414095607788));
#7838=CARTESIAN_POINT('Ctrl Pts',(2.47755504684468,0.512723754702348,-1.36150106191048));
#7839=CARTESIAN_POINT('Ctrl Pts',(2.50488077695117,0.565841544095042,-1.36515841169202));
#7840=CARTESIAN_POINT('Ctrl Pts',(2.56007294218793,0.655648196048438,-1.37178776666442));
#7841=CARTESIAN_POINT('Ctrl Pts',(2.58628298184903,0.693202345147572,-1.37471422240762));
#7842=CARTESIAN_POINT('Ctrl Pts',(2.6208166189692,0.73700844625919,-1.37838340892835));
#7843=CARTESIAN_POINT('Ctrl Pts',(2.62712451764267,0.744803204757438,-1.37904671598808));
#7844=CARTESIAN_POINT('Ctrl Pts',(2.6375206158764,0.757319532767677,-1.38012945697073));
#7845=CARTESIAN_POINT('Ctrl Pts',(2.64154828137164,0.762090904048538,-1.38054647071218));
#7846=CARTESIAN_POINT('Ctrl Pts',(2.64914594847734,0.770947621003043,-1.38132868766261));
#7847=CARTESIAN_POINT('Ctrl Pts',(2.65270662183671,0.775040779454269,-1.38169350517736));
#7848=CARTESIAN_POINT('Ctrl Pts',(2.66072333381586,0.784128786946163,-1.3825110434537));
#7849=CARTESIAN_POINT('Ctrl Pts',(2.66519390126566,0.789110509623414,-1.38296435684436));
#7850=CARTESIAN_POINT('Ctrl Pts',(2.67664225488379,0.801651121854137,-1.38411886726971));
#7851=CARTESIAN_POINT('Ctrl Pts',(2.68367694056488,0.80915706559828,-1.38482242984881));
#7852=CARTESIAN_POINT('Ctrl Pts',(2.73192855647619,0.859307883708574,-1.38961039835936));
#7853=CARTESIAN_POINT('Ctrl Pts',(2.77621110070649,0.898872316516266,-1.39382768074379));
#7854=CARTESIAN_POINT('Ctrl Pts',(2.88362765269659,0.981163177718446,-1.40365131255873));
#7855=CARTESIAN_POINT('Ctrl Pts',(2.94830986454206,1.02144312229219,-1.40929631897689));
#7856=CARTESIAN_POINT('Ctrl Pts',(3.03375213589413,1.06379934451007,-1.41617130460775));
#7857=CARTESIAN_POINT('Ctrl Pts',(3.0512926690889,1.07196282772527,-1.41755323438093));
#7858=CARTESIAN_POINT('Ctrl Pts',(3.08043278222723,1.084661075202,-1.4197926946376));
#7859=CARTESIAN_POINT('Ctrl Pts',(3.09191688692745,1.0894504044617,-1.4206612258589));
#7860=CARTESIAN_POINT('Ctrl Pts',(3.10766940087072,1.09572867422096,-1.42183154352114));
#7861=CARTESIAN_POINT('Ctrl Pts',(3.11187318018332,1.09737617008166,-1.42214183994511));
#7862=CARTESIAN_POINT('Ctrl Pts',(3.11906077122121,1.10014547130468,-1.42266882088822));
#7863=CARTESIAN_POINT('Ctrl Pts',(3.12203981937891,1.10127939912676,-1.42288620101202));
#7864=CARTESIAN_POINT('Ctrl Pts',(3.12768468402624,1.10340183084448,-1.42329609474297));
#7865=CARTESIAN_POINT('Ctrl Pts',(3.13034953167384,1.10439279743214,-1.42348875607539));
#7866=CARTESIAN_POINT('Ctrl Pts',(3.13666344259839,1.10671473669516,-1.42394330240407));
#7867=CARTESIAN_POINT('Ctrl Pts',(3.14031558131096,1.10803733713445,-1.42420470220452));
#7868=CARTESIAN_POINT('Ctrl Pts',(3.15320797390597,1.11263422369046,-1.42512233746239));
#7869=CARTESIAN_POINT('Ctrl Pts',(3.16248280395331,1.11581129577218,-1.42577323030606));
#7870=CARTESIAN_POINT('Ctrl Pts',(3.23929691575225,1.14105660205805,-1.43109631842507));
#7871=CARTESIAN_POINT('Ctrl Pts',(3.3086761641128,1.15709026437917,-1.43548099024168));
#7872=CARTESIAN_POINT('Ctrl Pts',(3.43746624218953,1.17479912980643,-1.44352234568844));
#7873=CARTESIAN_POINT('Ctrl Pts',(3.4963627932792,1.17843313375853,-1.4471639933981));
#7874=CARTESIAN_POINT('Ctrl Pts',(3.57651064851413,1.17736036807189,-1.45227287948557));
#7875=CARTESIAN_POINT('Ctrl Pts',(3.59772707650814,1.17650225660571,-1.45363929630321));
#7876=CARTESIAN_POINT('Ctrl Pts',(3.63459052712418,1.17401173194954,-1.45604610339223));
#7877=CARTESIAN_POINT('Ctrl Pts',(3.65024981481946,1.17263838944303,-1.45707877662303));
#7878=CARTESIAN_POINT('Ctrl Pts',(3.67303150385934,1.17018002019119,-1.45859831690869));
#7879=CARTESIAN_POINT('Ctrl Pts',(3.68017929364281,1.16934235663094,-1.4590775441531));
#7880=CARTESIAN_POINT('Ctrl Pts',(3.69275525302512,1.16775158160077,-1.45992526208627));
#7881=CARTESIAN_POINT('Ctrl Pts',(3.69818673352052,1.16702598716979,-1.46029288747278));
#7882=CARTESIAN_POINT('Ctrl Pts',(3.70950597616199,1.16543336305644,-1.46106224750131));
#7883=CARTESIAN_POINT('Ctrl Pts',(3.71539261237314,1.16455955906661,-1.46146418363111));
#7884=CARTESIAN_POINT('Ctrl Pts',(3.73074431239596,1.16216172277481,-1.46251728885668));
#7885=CARTESIAN_POINT('Ctrl Pts',(3.74019767451009,1.16056669395232,-1.46317065540774));
#7886=CARTESIAN_POINT('Ctrl Pts',(3.7800905088818,1.15333376009729,-1.46594918382699));
#7887=CARTESIAN_POINT('Ctrl Pts',(3.8103184753016,1.14661273075189,-1.46810775892774));
#7888=CARTESIAN_POINT('Ctrl Pts',(3.92056556168208,1.11749723599098,-1.47618312755397));
#7889=CARTESIAN_POINT('Ctrl Pts',(3.99840889809731,1.08784799929712,-1.48230636237904));
#7890=CARTESIAN_POINT('Ctrl Pts',(4.1189822626446,1.02666329477687,-1.49220390399194));
#7891=CARTESIAN_POINT('Ctrl Pts',(4.16387793549038,0.999996208824154,-1.49598770743971));
#7892=CARTESIAN_POINT('Ctrl Pts',(4.21259434248166,0.966495272226091,-1.50009989169716));
#7893=CARTESIAN_POINT('Ctrl Pts',(4.21829173769634,0.962502522009824,-1.50058087412274));
#7894=CARTESIAN_POINT('Ctrl Pts',(4.22693279799507,0.956331952767353,-1.5013100564271));
#7895=CARTESIAN_POINT('Ctrl Pts',(4.22990212372354,0.954190587488126,-1.50156056874576));
#7896=CARTESIAN_POINT('Ctrl Pts',(4.23532005820118,0.950244847781599,-1.50201748694578));
#7897=CARTESIAN_POINT('Ctrl Pts',(4.23777167179021,0.948444827262517,-1.502224168693));
#7898=CARTESIAN_POINT('Ctrl Pts',(4.24329089556351,0.944359510039678,-1.50268931573189));
#7899=CARTESIAN_POINT('Ctrl Pts',(4.24635436362051,0.942068752939169,-1.50294740299022));
#7900=CARTESIAN_POINT('Ctrl Pts',(4.25424385238277,0.936109112073236,-1.50361197863511));
#7901=CARTESIAN_POINT('Ctrl Pts',(4.25905287615919,0.93241776563965,-1.50401698352366));
#7902=CARTESIAN_POINT('Ctrl Pts',(4.29115064480108,0.907383698772624,-1.50672122581093));
#7903=CARTESIAN_POINT('Ctrl Pts',(4.31751758579733,0.884880791182493,-1.50894791567869));
#7904=CARTESIAN_POINT('Ctrl Pts',(4.36349461672023,0.841995159055702,-1.51292074942563));
#7905=CARTESIAN_POINT('Ctrl Pts',(4.38343501338009,0.822008242197079,-1.51467807736372));
#7906=CARTESIAN_POINT('Ctrl Pts',(4.43527920891394,0.766165946216926,-1.51940251074137));
#7907=CARTESIAN_POINT('Ctrl Pts',(4.46574048346297,0.729047517585867,-1.52235266101881));
#7908=CARTESIAN_POINT('Ctrl Pts',(4.52510298521389,0.646964528934716,-1.52868743618457));
#7909=CARTESIAN_POINT('Ctrl Pts',(4.55337853077468,0.601686516700835,-1.53207738809864));
#7910=CARTESIAN_POINT('Ctrl Pts',(4.58358801708743,0.545098479382363,-1.53629338947441));
#7911=CARTESIAN_POINT('Ctrl Pts',(4.58855632442101,0.535474690689785,-1.53700954969279));
#7912=CARTESIAN_POINT('Ctrl Pts',(4.59616862370413,0.520216734750667,-1.53814435401415));
#7913=CARTESIAN_POINT('Ctrl Pts',(4.59890197018941,0.514627631041915,-1.53855990943113));
#7914=CARTESIAN_POINT('Ctrl Pts',(4.60393648862499,0.50412303536163,-1.53934082251706));
#7915=CARTESIAN_POINT('Ctrl Pts',(4.60624822441958,0.499212765448509,-1.53970580633719));
#7916=CARTESIAN_POINT('Ctrl Pts',(4.61134783473277,0.488183705389914,-1.54052559207426));
#7917=CARTESIAN_POINT('Ctrl Pts',(4.61411739477131,0.482056706379556,-1.54098100166922));
#7918=CARTESIAN_POINT('Ctrl Pts',(4.62103141966154,0.466405343395531,-1.54214448823909));
#7919=CARTESIAN_POINT('Ctrl Pts',(4.62510255603357,0.456849416693217,-1.54285499495748));
#7920=CARTESIAN_POINT('Ctrl Pts',(4.657696268072,0.377447624340864,-1.54876135210881));
#7921=CARTESIAN_POINT('Ctrl Pts',(4.67956810737112,0.305075840223965,-1.55417873270455));
#7922=CARTESIAN_POINT('Ctrl Pts',(4.70570496835024,0.17447817038836,-1.56392160117353));
#7923=CARTESIAN_POINT('Ctrl Pts',(4.71285866530789,0.117075292893958,-1.56818821438827));
#7924=CARTESIAN_POINT('Ctrl Pts',(4.71680672146982,0.038866566434532,-1.57384334564509));
#7925=CARTESIAN_POINT('Ctrl Pts',(4.71730552758499,0.0183298876278521,-1.57531310782353));
#7926=CARTESIAN_POINT('Ctrl Pts',(4.7172424454715,-0.015280427074099,-1.57768356586059));
#7927=CARTESIAN_POINT('Ctrl Pts',(4.71700035115201,-0.0283497556969264,
-1.57859665273772));
#7928=CARTESIAN_POINT('Ctrl Pts',(4.71637531937082,-0.0461141263351836,
-1.57982363920567));
#7929=CARTESIAN_POINT('Ctrl Pts',(4.71618174531947,-0.0508143162551278,
-1.58014693564405));
#7930=CARTESIAN_POINT('Ctrl Pts',(4.71581049738897,-0.0586818204140145,
-1.58068569924795));
#7931=CARTESIAN_POINT('Ctrl Pts',(4.71564818095615,-0.0618497642636594,
-1.58090198879334));
#7932=CARTESIAN_POINT('Ctrl Pts',(4.71531540461906,-0.0678686395293367,
-1.58131164072307));
#7933=CARTESIAN_POINT('Ctrl Pts',(4.71514737138161,-0.0707196590406,-1.58150513920623));
#7934=CARTESIAN_POINT('Ctrl Pts',(4.71472313943746,-0.0774977326646866,
-1.58196392950753));
#7935=CARTESIAN_POINT('Ctrl Pts',(4.71445762330664,-0.0814242006804311,
-1.5822287140472));
#7936=CARTESIAN_POINT('Ctrl Pts',(4.71344767563238,-0.0953239980667431,
-1.58316279244578));
#7937=CARTESIAN_POINT('Ctrl Pts',(4.7125958736893,-0.105289432774669,-1.58382652127418));
#7938=CARTESIAN_POINT('Ctrl Pts',(4.70563587225787,-0.176077160377908,-1.58850649901327));
#7939=CARTESIAN_POINT('Ctrl Pts',(4.69492668981321,-0.236361462750202,-1.59231237929681));
#7940=CARTESIAN_POINT('Ctrl Pts',(4.66588685364125,-0.348381352898507,-1.59947994226449));
#7941=CARTESIAN_POINT('Ctrl Pts',(4.6485350061951,-0.400196614390326,-1.6028371824813));
#7942=CARTESIAN_POINT('Ctrl Pts',(4.61080228182311,-0.491311488272371,-1.60904849008933));
#7943=CARTESIAN_POINT('Ctrl Pts',(4.59168402756789,-0.531020647848604,-1.6118688383184));
#7944=CARTESIAN_POINT('Ctrl Pts',(4.56539714877969,-0.578598079656185,-1.61544518159952));
#7945=CARTESIAN_POINT('Ctrl Pts',(4.56028687385215,-0.587566719640654,-1.61612828721391));
#7946=CARTESIAN_POINT('Ctrl Pts',(4.55196436989243,-0.601736560116374,-1.61722248861349));
#7947=CARTESIAN_POINT('Ctrl Pts',(4.54882831401767,-0.606982059653343,-1.61763086245697));
#7948=CARTESIAN_POINT('Ctrl Pts',(4.542822908943,-0.61685171943176,-1.61840565615444));
#7949=CARTESIAN_POINT('Ctrl Pts',(4.53996204877292,-0.621480877932946,-1.61877176183307));
#7950=CARTESIAN_POINT('Ctrl Pts',(4.53340646425925,-0.631925901611348,-1.61960407368689));
#7951=CARTESIAN_POINT('Ctrl Pts',(4.5296926049546,-0.637729460607134,-1.62007096988646));
#7952=CARTESIAN_POINT('Ctrl Pts',(4.51823383336954,-0.655294396340474,-1.62149786795583));
#7953=CARTESIAN_POINT('Ctrl Pts',(4.51032894919217,-0.666949385558651,-1.6224637313036));
#7954=CARTESIAN_POINT('Ctrl Pts',(4.44531516409617,-0.759200527579021,-1.63026651294974));
#7955=CARTESIAN_POINT('Ctrl Pts',(4.37849165128539,-0.832447743524141,-1.63749260957849));
#7956=CARTESIAN_POINT('Ctrl Pts',(4.271917002868,-0.923250686143749,-1.64776100941429));
#7957=CARTESIAN_POINT('Ctrl Pts',(4.23911262651118,-0.948350069162419,-1.65077662203512));
#7958=CARTESIAN_POINT('Ctrl Pts',(4.19352502348027,-0.979574703247726,-1.6547226198031));
#7959=CARTESIAN_POINT('Ctrl Pts',(4.18185357360667,-0.987267344477696,-1.65571257675743));
#7960=CARTESIAN_POINT('Ctrl Pts',(4.16174350135364,-1.00001422710019,-1.65738065995565));
#7961=CARTESIAN_POINT('Ctrl Pts',(4.15337366153134,-1.00517374316936,-1.65806411209736));
#7962=CARTESIAN_POINT('Ctrl Pts',(4.14133160563545,-1.0123904416387,-1.65903105884131));
#7963=CARTESIAN_POINT('Ctrl Pts',(4.13771172393355,-1.01453353057352,-1.65931964380046));
#7964=CARTESIAN_POINT('Ctrl Pts',(4.13142065082237,-1.01821267497635,-1.65981748317565));
#7965=CARTESIAN_POINT('Ctrl Pts',(4.128754797754,-1.01975771191621,-1.66002729929873));
#7966=CARTESIAN_POINT('Ctrl Pts',(4.12311931540191,-1.02299436586058,-1.66046839975546));
#7967=CARTESIAN_POINT('Ctrl Pts',(4.12014836235405,-1.02468353394657,-1.66069953141028));
#7968=CARTESIAN_POINT('Ctrl Pts',(4.11209225081034,-1.029217636917,-1.66132258419626));
#7969=CARTESIAN_POINT('Ctrl Pts',(4.10699318220491,-1.03203785161569,-1.66171298662176));
#7970=CARTESIAN_POINT('Ctrl Pts',(4.09401964825911,-1.03908808278284,-1.66269684771795));
#7971=CARTESIAN_POINT('Ctrl Pts',(4.08611780186023,-1.04326638858741,-1.66328736455055));
#7972=CARTESIAN_POINT('Ctrl Pts',(4.07816926735968,-1.04735428881255,-1.66387346933803));
#7973=CARTESIAN_POINT('Origin',(3.53951905042299,8.32667268468867E-16,0.924367114736157));
#7974=CARTESIAN_POINT('',(4.07816947157496,-1.04735418378541,-2.2618380236781));
#7975=CARTESIAN_POINT('',(4.07816926754606,-1.0473542887167,-2.1620461556085));
#7976=CARTESIAN_POINT('',(4.07816926754759,-1.04735428871592,0.924367114736157));
#7977=CARTESIAN_POINT('',(2.36176911741392,-0.000397236870587705,-1.92540593443103));
#7978=CARTESIAN_POINT('Ctrl Pts',(4.07816947157471,-1.04735418378554,-2.26183802367812));
#7979=CARTESIAN_POINT('Ctrl Pts',(4.11215758083515,-1.02987422366249,-2.25946260336971));
#7980=CARTESIAN_POINT('Ctrl Pts',(4.14531453423107,-1.01072974373671,-2.25706537766911));
#7981=CARTESIAN_POINT('Ctrl Pts',(4.20217770663557,-0.974083814098255,-2.2527434404038));
#7982=CARTESIAN_POINT('Ctrl Pts',(4.22623386750672,-0.957276505535751,-2.25084314837658));
#7983=CARTESIAN_POINT('Ctrl Pts',(4.25716496907334,-0.93389959830894,-2.2482872055146));
#7984=CARTESIAN_POINT('Ctrl Pts',(4.26462500625597,-0.928119318065563,-2.24766173080797));
#7985=CARTESIAN_POINT('Ctrl Pts',(4.27664969228473,-0.918568732447784,-2.24663826132436));
#7986=CARTESIAN_POINT('Ctrl Pts',(4.28125689308624,-0.914852485376131,-2.24624239545728));
#7987=CARTESIAN_POINT('Ctrl Pts',(4.29008411770402,-0.907621782651955,-2.24547658656779));
#7988=CARTESIAN_POINT('Ctrl Pts',(4.29430796646247,-0.904112222590754,-2.24510684538091));
#7989=CARTESIAN_POINT('Ctrl Pts',(4.30406877140576,-0.895885980637119,-2.24424460835135));
#7990=CARTESIAN_POINT('Ctrl Pts',(4.309586835554,-0.891147332573264,-2.243751231464));
#7991=CARTESIAN_POINT('Ctrl Pts',(4.32720909635388,-0.875728286276171,-2.24215610848428));
#7992=CARTESIAN_POINT('Ctrl Pts',(4.33913727081319,-0.864850447594686,-2.24104630044757));
#7993=CARTESIAN_POINT('Ctrl Pts',(4.3667713270253,-0.838589231985334,-2.23840152057983));
#7994=CARTESIAN_POINT('Ctrl Pts',(4.38227705102541,-0.823004905773187,-2.23685846807011));
#7995=CARTESIAN_POINT('Ctrl Pts',(4.47088258983569,-0.728819380887682,-2.22768368720859));
#7996=CARTESIAN_POINT('Ctrl Pts',(4.53338307284256,-0.640971426619844,-2.21965793610917));
#7997=CARTESIAN_POINT('Ctrl Pts',(4.59571007065897,-0.521817399269699,-2.20997664042911));
#7998=CARTESIAN_POINT('Ctrl Pts',(4.60746466445453,-0.497318106622457,-2.2080468105851));
#7999=CARTESIAN_POINT('Ctrl Pts',(4.62085781807206,-0.466733578152843,-2.205729139911));
#8000=CARTESIAN_POINT('Ctrl Pts',(4.6233081351772,-0.461015170455292,-2.20529965444803));
#8001=CARTESIAN_POINT('Ctrl Pts',(4.62708194335128,-0.452011676322391,-2.2046297597358));
#8002=CARTESIAN_POINT('Ctrl Pts',(4.62843608217146,-0.44873968000058,-2.20438761100135));
#8003=CARTESIAN_POINT('Ctrl Pts',(4.63091947955316,-0.442661625021243,-2.20394026837235));
#8004=CARTESIAN_POINT('Ctrl Pts',(4.63205268204052,-0.439857334893244,-2.20373485236454));
#8005=CARTESIAN_POINT('Ctrl Pts',(4.63464831004131,-0.433362120813096,-2.20326129897013));
#8006=CARTESIAN_POINT('Ctrl Pts',(4.63610288887783,-0.42966813870244,-2.20299362569074));
#8007=CARTESIAN_POINT('Ctrl Pts',(4.64061729671911,-0.418031295518201,-2.20215535390965));
#8008=CARTESIAN_POINT('Ctrl Pts',(4.64360979867758,-0.410062363483671,-2.2015885365557));
#8009=CARTESIAN_POINT('Ctrl Pts',(4.66813750629124,-0.34253016373789,-2.19684023918535));
#8010=CARTESIAN_POINT('Ctrl Pts',(4.68492505219069,-0.281342976766287,-2.19289530235418));
#8011=CARTESIAN_POINT('Ctrl Pts',(4.71371485167868,-0.129284182677625,-2.18330913748751));
#8012=CARTESIAN_POINT('Ctrl Pts',(4.72020462868668,-0.0378102537561371,
-2.17770182371934));
#8013=CARTESIAN_POINT('Ctrl Pts',(4.71544570556673,0.0668640017647441,-2.17086642501106));
#8014=CARTESIAN_POINT('Ctrl Pts',(4.71460970412638,0.080226087733796,-2.16998668468026));
#8015=CARTESIAN_POINT('Ctrl Pts',(4.71300288566029,0.100386784409726,-2.16864710546221));
#8016=CARTESIAN_POINT('Ctrl Pts',(4.71240029154313,0.10719798969088,-2.1681924230823));
#8017=CARTESIAN_POINT('Ctrl Pts',(4.7112466021464,0.119060588088743,-2.16739667559879));
#8018=CARTESIAN_POINT('Ctrl Pts',(4.71072205864656,0.124114428083257,-2.16705643887368));
#8019=CARTESIAN_POINT('Ctrl Pts',(4.70955401554414,0.134700642993628,-2.1663411069894));
#8020=CARTESIAN_POINT('Ctrl Pts',(4.7089039420901,0.140232150874098,-2.16596581598723));
#8021=CARTESIAN_POINT('Ctrl Pts',(4.70725682905048,0.153438724543941,-2.16506607621159));
#8022=CARTESIAN_POINT('Ctrl Pts',(4.7062233315853,0.161108898539571,-2.16454050676996));
#8023=CARTESIAN_POINT('Ctrl Pts',(4.70240423910555,0.187485413052257,-2.1627224427146));
#8024=CARTESIAN_POINT('Ctrl Pts',(4.69924383924312,0.206133657309007,-2.16141840423657));
#8025=CARTESIAN_POINT('Ctrl Pts',(4.69046214842808,0.251317478911881,-2.15821132314327));
#8026=CARTESIAN_POINT('Ctrl Pts',(4.68437077120608,0.27774958959409,-2.15629477942774));
#8027=CARTESIAN_POINT('Ctrl Pts',(4.65162394725014,0.400340676491821,-2.14721891650269));
#8028=CARTESIAN_POINT('Ctrl Pts',(4.61373470193974,0.493059158604357,-2.13976386588413));
#8029=CARTESIAN_POINT('Ctrl Pts',(4.55193428615204,0.602307224508113,-2.1307411603056));
#8030=CARTESIAN_POINT('Ctrl Pts',(4.5385179544109,0.624307633798722,-2.12891358198425));
#8031=CARTESIAN_POINT('Ctrl Pts',(4.52102998027965,0.650975339720166,-2.12670056281189));
#8032=CARTESIAN_POINT('Ctrl Pts',(4.51763024335496,0.656072478203973,-2.12627768945603));
#8033=CARTESIAN_POINT('Ctrl Pts',(4.51221505622762,0.664055667867854,-2.12561584399497));
#8034=CARTESIAN_POINT('Ctrl Pts',(4.51022623855985,0.666959523099655,-2.12537519781994));
#8035=CARTESIAN_POINT('Ctrl Pts',(4.50665998089947,0.672116841662521,-2.12494804067539));
#8036=CARTESIAN_POINT('Ctrl Pts',(4.50508766668906,0.674373691490797,-2.12476120318403));
#8037=CARTESIAN_POINT('Ctrl Pts',(4.50129598067297,0.679775709909808,-2.1243141713941));
#8038=CARTESIAN_POINT('Ctrl Pts',(4.49906908066863,0.682915529074666,-2.12405448696543));
#8039=CARTESIAN_POINT('Ctrl Pts',(4.49223419721483,0.692452938799442,-2.12326593058064));
#8040=CARTESIAN_POINT('Ctrl Pts',(4.48757721896689,0.698815383849004,-2.12274022981454));
#8041=CARTESIAN_POINT('Ctrl Pts',(4.47658100425813,0.713526330734583,-2.12152430837908));
#8042=CARTESIAN_POINT('Ctrl Pts',(4.47019342475584,0.721838039770002,-2.12083698845388));
#8043=CARTESIAN_POINT('Ctrl Pts',(4.44740839806692,0.750681256627044,-2.11844635983074));
#8044=CARTESIAN_POINT('Ctrl Pts',(4.43043479654834,0.770749463485985,-2.11677300933939));
#8045=CARTESIAN_POINT('Ctrl Pts',(4.36050131592672,0.848032599723353,-2.1102126406485));
#8046=CARTESIAN_POINT('Ctrl Pts',(4.3025902750351,0.900496669303082,-2.10548104231662));
#8047=CARTESIAN_POINT('Ctrl Pts',(4.20175653762746,0.975084504588112,-2.09760778914742));
#8048=CARTESIAN_POINT('Ctrl Pts',(4.16192695028842,1.00097746188242,-2.09457846753382));
#8049=CARTESIAN_POINT('Ctrl Pts',(4.11127305683629,1.0297128581226,-2.09075148776885));
#8050=CARTESIAN_POINT('Ctrl Pts',(4.10182672876283,1.03490157809261,-2.0900389666824));
#8051=CARTESIAN_POINT('Ctrl Pts',(4.08677129796594,1.04290430817441,-2.08890449710871));
#8052=CARTESIAN_POINT('Ctrl Pts',(4.08120847701314,1.04580446595101,-2.08848556605197));
#8053=CARTESIAN_POINT('Ctrl Pts',(4.07079358406968,1.05112884525956,-2.08770154637793));
#8054=CARTESIAN_POINT('Ctrl Pts',(4.06594740098486,1.05356426926796,-2.08733685853089));
#8055=CARTESIAN_POINT('Ctrl Pts',(4.05511558356286,1.05891434936965,-2.0865219260801));
#8056=CARTESIAN_POINT('Ctrl Pts',(4.04912174727154,1.06181188188193,-2.0860711070971));
#8057=CARTESIAN_POINT('Ctrl Pts',(4.03143809584658,1.07017627064171,-2.08474123869227));
#8058=CARTESIAN_POINT('Ctrl Pts',(4.01968293775442,1.07550184372176,-2.08385743759266));
#8059=CARTESIAN_POINT('Ctrl Pts',(3.99273256546268,1.08718157750333,-2.08183095835449));
#8060=CARTESIAN_POINT('Ctrl Pts',(3.97748708335784,1.09341219513607,-2.08068441911204));
#8061=CARTESIAN_POINT('Ctrl Pts',(3.92569009147095,1.11332383607517,-2.07678754461713));
#8062=CARTESIAN_POINT('Ctrl Pts',(3.88859349658233,1.12550635338703,-2.07399316840746));
#8063=CARTESIAN_POINT('Ctrl Pts',(3.7814610450674,1.15488222956353,-2.06593461515874));
#8064=CARTESIAN_POINT('Ctrl Pts',(3.71035896181017,1.16751964654541,-2.06059098939022));
#8065=CARTESIAN_POINT('Ctrl Pts',(3.60548304147,1.17636940656165,-2.05296937992301));
#8066=CARTESIAN_POINT('Ctrl Pts',(3.57231008323076,1.1777611902697,-2.0505982642458));
#8067=CARTESIAN_POINT('Ctrl Pts',(3.53312072607992,1.17774789747898,-2.04787495365456));
#8068=CARTESIAN_POINT('Ctrl Pts',(3.52712183278505,1.17770003027821,-2.04746024793411));
#8069=CARTESIAN_POINT('Ctrl Pts',(3.51731756208877,1.17754687569113,-2.04678628912809));
#8070=CARTESIAN_POINT('Ctrl Pts',(3.51351195435492,1.1774689730574,-2.04652562603348));
#8071=CARTESIAN_POINT('Ctrl Pts',(3.50666647525204,1.17729563825144,-2.04605851795721));
#8072=CARTESIAN_POINT('Ctrl Pts',(3.5036265483414,1.17720688090659,-2.04585171945102));
#8073=CARTESIAN_POINT('Ctrl Pts',(3.49691052135481,1.17698475189216,-2.04539624495085));
#8074=CARTESIAN_POINT('Ctrl Pts',(3.49323468466054,1.17684593356359,-2.04514786960628));
#8075=CARTESIAN_POINT('Ctrl Pts',(3.48252650955096,1.17639128900629,-2.04442683417521));
#8076=CARTESIAN_POINT('Ctrl Pts',(3.47549612928041,1.17602962807248,-2.04395660247968));
#8077=CARTESIAN_POINT('Ctrl Pts',(3.41115089259976,1.17214080537759,-2.03967830741393));
#8078=CARTESIAN_POINT('Ctrl Pts',(3.3541541710711,1.16448880190623,-2.03607198645818));
#8079=CARTESIAN_POINT('Ctrl Pts',(3.2024120382917,1.1326869105901,-2.02644088861025));
#8080=CARTESIAN_POINT('Ctrl Pts',(3.10975637537805,1.10087381460123,-2.02049531625501));
#8081=CARTESIAN_POINT('Ctrl Pts',(3.00780374125507,1.05101224451846,-2.01310856129686));
#8082=CARTESIAN_POINT('Ctrl Pts',(2.99366295095826,1.04373798808611,-2.01206470887801));
#8083=CARTESIAN_POINT('Ctrl Pts',(2.97379801676143,1.03300502674894,-2.01056840659868));
#8084=CARTESIAN_POINT('Ctrl Pts',(2.9679489654152,1.02978022319167,-2.01012408261745));
#8085=CARTESIAN_POINT('Ctrl Pts',(2.95729270577498,1.02378626686852,-2.00930750860868));
#8086=CARTESIAN_POINT('Ctrl Pts',(2.9524769999611,1.02103254885945,-2.0089358110551));
#8087=CARTESIAN_POINT('Ctrl Pts',(2.94285131455196,1.01543777826472,-2.00818736994075));
#8088=CARTESIAN_POINT('Ctrl Pts',(2.938041738276,1.01259632118592,-2.00781061903259));
#8089=CARTESIAN_POINT('Ctrl Pts',(2.92626881634285,1.00552750842987,-2.0068814297528));
#8090=CARTESIAN_POINT('Ctrl Pts',(2.91932885318496,1.00126197035577,-2.00632762542175));
#8091=CARTESIAN_POINT('Ctrl Pts',(2.90451906600554,0.991946325149986,-2.00513248953443));
#8092=CARTESIAN_POINT('Ctrl Pts',(2.89666406024447,0.986873824292692,-2.00449036917237));
#8093=CARTESIAN_POINT('Ctrl Pts',(2.87464714894385,0.972281638756984,-2.00266682334521));
#8094=CARTESIAN_POINT('Ctrl Pts',(2.86063103430509,0.962547266700664,-2.00147770287939));
#8095=CARTESIAN_POINT('Ctrl Pts',(2.81349702912591,0.928270418454225,-1.99738015845952));
#8096=CARTESIAN_POINT('Ctrl Pts',(2.78146088420264,0.902297715308902,-1.99442252922296));
#8097=CARTESIAN_POINT('Ctrl Pts',(2.70616918336809,0.834411838518283,-1.98705391224051));
#8098=CARTESIAN_POINT('Ctrl Pts',(2.66463857002055,0.790758461605782,-1.98260760915353));
#8099=CARTESIAN_POINT('Ctrl Pts',(2.60063731001027,0.712241557537544,-1.97522936642346));
#8100=CARTESIAN_POINT('Ctrl Pts',(2.57633397546382,0.679015628986144,-1.97226989362256));
#8101=CARTESIAN_POINT('Ctrl Pts',(2.55037091061868,0.639312652357029,-1.96897017960545));
#8102=CARTESIAN_POINT('Ctrl Pts',(2.54696699242296,0.634015083744507,-1.96853455859723));
#8103=CARTESIAN_POINT('Ctrl Pts',(2.54152603994987,0.625396027070788,-1.96783363163928));
#8104=CARTESIAN_POINT('Ctrl Pts',(2.53946276683566,0.622091368194459,-1.96756672717929));
#8105=CARTESIAN_POINT('Ctrl Pts',(2.53581561511723,0.616184837461929,-1.96709303220929));
#8106=CARTESIAN_POINT('Ctrl Pts',(2.53422539493126,0.613587000271265,-1.96688584118828));
#8107=CARTESIAN_POINT('Ctrl Pts',(2.53077500214972,0.6079008999427,-1.96643486230176));
#8108=CARTESIAN_POINT('Ctrl Pts',(2.52891892131867,0.60481025041238,-1.96619133536824));
#8109=CARTESIAN_POINT('Ctrl Pts',(2.52365889129935,0.595959697982457,-1.96549837076114));
#8110=CARTESIAN_POINT('Ctrl Pts',(2.52028972365367,0.590179133082911,-1.96505108093439));
#8111=CARTESIAN_POINT('Ctrl Pts',(2.49641477132662,0.5484019851808,-1.96185407804208));
#8112=CARTESIAN_POINT('Ctrl Pts',(2.47776918723934,0.511370038509786,-1.95920885266609));
#8113=CARTESIAN_POINT('Ctrl Pts',(2.41980830418625,0.379342855806727,-1.95015498242245));
#8114=CARTESIAN_POINT('Ctrl Pts',(2.39099501075109,0.280260983889823,-1.94396970864142));
#8115=CARTESIAN_POINT('Ctrl Pts',(2.37173171027098,0.154769869163562,-1.93580584997123));
#8116=CARTESIAN_POINT('Ctrl Pts',(2.36879774570251,0.130738213834044,-1.93423048381664));
#8117=CARTESIAN_POINT('Ctrl Pts',(2.36581330168438,0.0979111982545516,-1.93205397431837));
#8118=CARTESIAN_POINT('Ctrl Pts',(2.36511758903647,0.0891795268502272,-1.93147270768654));
#8119=CARTESIAN_POINT('Ctrl Pts',(2.36416443601409,0.0752568612788502,-1.9305418081047));
#8120=CARTESIAN_POINT('Ctrl Pts',(2.36384383938036,0.0700704035632612,-1.93019413285541));
#8121=CARTESIAN_POINT('Ctrl Pts',(2.36326952695623,0.0596612204248427,-1.92949447181395));
#8122=CARTESIAN_POINT('Ctrl Pts',(2.36301624930578,0.0544385904398576,-1.92914248066085));
#8123=CARTESIAN_POINT('Ctrl Pts',(2.36257502195804,0.0438888252418186,-1.9284294689818));
#8124=CARTESIAN_POINT('Ctrl Pts',(2.36238844412332,0.0385617584877063,-1.92806841444257));
#8125=CARTESIAN_POINT('Ctrl Pts',(2.36208103489016,0.0276719919876058,-1.92732818045086));
#8126=CARTESIAN_POINT('Ctrl Pts',(2.36196344888742,0.0221093421832516,-1.92694890990719));
#8127=CARTESIAN_POINT('Ctrl Pts',(2.36180593426867,0.0108986051649463,-1.92618216766589));
#8128=CARTESIAN_POINT('Ctrl Pts',(2.36176721246393,0.005250664645738,-1.92579466996232));
#8129=CARTESIAN_POINT('Ctrl Pts',(2.36176911741392,-0.000397236870587705,
-1.92540593443103));
#8130=CARTESIAN_POINT('Ctrl Pts',(2.36176911714533,-0.000396439730100908,
-1.92540598929686));
#8131=CARTESIAN_POINT('Ctrl Pts',(2.36177360458169,-0.0137277924659618,
-1.9244884150583));
#8132=CARTESIAN_POINT('Ctrl Pts',(2.36200444424012,-0.0270577270212485,
-1.92356401270832));
#8133=CARTESIAN_POINT('Ctrl Pts',(2.36611628666943,-0.146914392811943,-1.91518818397968));
#8134=CARTESIAN_POINT('Ctrl Pts',(2.38421792108532,-0.252445856471833,-1.9072920268355));
#8135=CARTESIAN_POINT('Ctrl Pts',(2.42501706749847,-0.38187722484146,-1.89739960912129));
#8136=CARTESIAN_POINT('Ctrl Pts',(2.43481099395957,-0.409347312572779,-1.89529194144152));
#8137=CARTESIAN_POINT('Ctrl Pts',(2.45179991403706,-0.451930007109447,-1.89203809039909));
#8138=CARTESIAN_POINT('Ctrl Pts',(2.45831418179976,-0.467300496119891,-1.89086647598472));
#8139=CARTESIAN_POINT('Ctrl Pts',(2.46726361058637,-0.487226705758264,-1.88935603669819));
#8140=CARTESIAN_POINT('Ctrl Pts',(2.46940467226192,-0.491911385485655,-1.88900155139795));
#8141=CARTESIAN_POINT('Ctrl Pts',(2.47295453766577,-0.499545678890405,-1.88842506642008));
#8142=CARTESIAN_POINT('Ctrl Pts',(2.47434498083374,-0.502503678900463,-1.88820199553867));
#8143=CARTESIAN_POINT('Ctrl Pts',(2.47708545361274,-0.508271217330545,-1.88776768216505));
#8144=CARTESIAN_POINT('Ctrl Pts',(2.47843434718703,-0.511081237085492,-1.88755637793785));
#8145=CARTESIAN_POINT('Ctrl Pts',(2.4814747551645,-0.517351102284731,-1.88708550310272));
#8146=CARTESIAN_POINT('Ctrl Pts',(2.48317213206339,-0.520808105612696,-1.88682628661972));
#8147=CARTESIAN_POINT('Ctrl Pts',(2.48911617902321,-0.532765577293923,-1.88593088563877));
#8148=CARTESIAN_POINT('Ctrl Pts',(2.49344887670079,-0.541223205602549,-1.88529968282114));
#8149=CARTESIAN_POINT('Ctrl Pts',(2.53336507659208,-0.61687099516147,-1.87966485145346));
#8150=CARTESIAN_POINT('Ctrl Pts',(2.57527987022109,-0.680530520336309,-1.87499314778836));
#8151=CARTESIAN_POINT('Ctrl Pts',(2.66797915093551,-0.795381322042224,-1.86586289647907));
#8152=CARTESIAN_POINT('Ctrl Pts',(2.71788600011217,-0.84683577792764,-1.86142447049118));
#8153=CARTESIAN_POINT('Ctrl Pts',(2.78174873683519,-0.901686943084073,-1.85596479727039));
#8154=CARTESIAN_POINT('Ctrl Pts',(2.79148018452138,-0.909776361245537,-1.85513860171519));
#8155=CARTESIAN_POINT('Ctrl Pts',(2.80727902080868,-0.922484525026616,-1.8538050253309));
#8156=CARTESIAN_POINT('Ctrl Pts',(2.8132643597579,-0.927204011927492,-1.8533015366715));
#8157=CARTESIAN_POINT('Ctrl Pts',(2.82453300300452,-0.935913372547308,-1.85235653442545));
#8158=CARTESIAN_POINT('Ctrl Pts',(2.82980498081155,-0.939917456651158,-1.85191559017098));
#8159=CARTESIAN_POINT('Ctrl Pts',(2.83519496547793,-0.943939964730064,-1.85146586633317));
#8160=CARTESIAN_POINT('Ctrl Pts',(2.83527959262677,-0.944003103666063,-1.85145880557425));
#8161=CARTESIAN_POINT('Ctrl Pts',(2.8354527940327,-0.944132290158664,-1.85144435528945));
#8162=CARTESIAN_POINT('Ctrl Pts',(2.83554136909888,-0.944198336635476,-1.85143696572185));
#8163=CARTESIAN_POINT('Ctrl Pts',(2.8357229870537,-0.94433372128218,-1.85142181445682));
#8164=CARTESIAN_POINT('Ctrl Pts',(2.83581603089438,-0.94440305816482,-1.85141405271051));
#8165=CARTESIAN_POINT('Ctrl Pts',(2.84009552768198,-0.947591183775108,-1.85105707076736));
#8166=CARTESIAN_POINT('Ctrl Pts',(2.84430260203152,-0.950682073104077,-1.85070679058275));
#8167=CARTESIAN_POINT('Ctrl Pts',(2.85334745514616,-0.957235077514597,-1.84995504258621));
#8168=CARTESIAN_POINT('Ctrl Pts',(2.85819117774096,-0.960688700598437,-1.84955326459499));
#8169=CARTESIAN_POINT('Ctrl Pts',(2.87089783940785,-0.969604246685182,-1.84850121891595));
#8170=CARTESIAN_POINT('Ctrl Pts',(2.87880144704677,-0.975007158032249,-1.84784876253529));
#8171=CARTESIAN_POINT('Ctrl Pts',(2.91242640798183,-0.997396606049062,-1.84508033262812));
#8172=CARTESIAN_POINT('Ctrl Pts',(2.93874148677876,-1.01346494208846,-1.84293125248958));
#8173=CARTESIAN_POINT('Ctrl Pts',(3.03829916564307,-1.06901540417245,-1.83485851947973));
#8174=CARTESIAN_POINT('Ctrl Pts',(3.11502681593287,-1.10173421117534,-1.82872715827693));
#8175=CARTESIAN_POINT('Ctrl Pts',(3.2444557225463,-1.14138396422128,-1.81881798355753));
#8176=CARTESIAN_POINT('Ctrl Pts',(3.29533213345813,-1.1533402676166,-1.81503085952394));
#8177=CARTESIAN_POINT('Ctrl Pts',(3.35370407295029,-1.16302032485042,-1.81091549033579));
#8178=CARTESIAN_POINT('Ctrl Pts',(3.36057888706232,-1.16409789350249,-1.81043439770678));
#8179=CARTESIAN_POINT('Ctrl Pts',(3.37108528036573,-1.16564940452219,-1.80970505990988));
#8180=CARTESIAN_POINT('Ctrl Pts',(3.37471004518275,-1.16616742445791,-1.80945450122438));
#8181=CARTESIAN_POINT('Ctrl Pts',(3.38135057827423,-1.16708485146139,-1.80899750398719));
#8182=CARTESIAN_POINT('Ctrl Pts',(3.38436548948961,-1.16748948135267,-1.80879078943669));
#8183=CARTESIAN_POINT('Ctrl Pts',(3.39117569250037,-1.16837662875644,-1.80832557224422));
#8184=CARTESIAN_POINT('Ctrl Pts',(3.39497178976563,-1.16885233837873,-1.80806744772615));
#8185=CARTESIAN_POINT('Ctrl Pts',(3.4047897262201,-1.17003411545846,-1.80740278079862));
#8186=CARTESIAN_POINT('Ctrl Pts',(3.41081490970927,-1.17071220635879,-1.80699772225349));
#8187=CARTESIAN_POINT('Ctrl Pts',(3.45130532084887,-1.1749527326332,-1.80429309236003));
#8188=CARTESIAN_POINT('Ctrl Pts',(3.48591164305039,-1.17703964982149,-1.80206608865917));
#8189=CARTESIAN_POINT('Ctrl Pts',(3.54876402026999,-1.17805139772025,-1.79809409568572));
#8190=CARTESIAN_POINT('Ctrl Pts',(3.57697333670722,-1.17749219207441,-1.79633788044243));
#8191=CARTESIAN_POINT('Ctrl Pts',(3.65301400391627,-1.17324906472264,-1.79161586896054));
#8192=CARTESIAN_POINT('Ctrl Pts',(3.70068297840015,-1.16765601455771,-1.78866702832243));
#8193=CARTESIAN_POINT('Ctrl Pts',(3.80039134664677,-1.14973365439901,-1.78233193561143));
#8194=CARTESIAN_POINT('Ctrl Pts',(3.85219647212967,-1.13673812976287,-1.778940256606));
#8195=CARTESIAN_POINT('Ctrl Pts',(3.91324241519934,-1.1169347600789,-1.77472224660336));
#8196=CARTESIAN_POINT('Ctrl Pts',(3.92349967124746,-1.11345017028379,-1.77400592937972));
#8197=CARTESIAN_POINT('Ctrl Pts',(3.93957104330274,-1.10774193241084,-1.77287089204711));
#8198=CARTESIAN_POINT('Ctrl Pts',(3.94541826155139,-1.10561277748005,-1.77245526212335));
#8199=CARTESIAN_POINT('Ctrl Pts',(3.95633383295694,-1.10153981486296,-1.77167421786054));
#8200=CARTESIAN_POINT('Ctrl Pts',(3.96140617304079,-1.09960710289953,-1.77130917756624));
#8201=CARTESIAN_POINT('Ctrl Pts',(3.97273223910564,-1.095201633497,-1.77048927582917));
#8202=CARTESIAN_POINT('Ctrl Pts',(3.9789784692958,-1.09271025472641,-1.77003380660955));
#8203=CARTESIAN_POINT('Ctrl Pts',(3.9948183226715,-1.08623457137148,-1.76887018649871));
#8204=CARTESIAN_POINT('Ctrl Pts',(4.00438102869661,-1.08217664940954,-1.76815960546792));
#8205=CARTESIAN_POINT('Ctrl Pts',(4.03563143166245,-1.0684249463463,-1.76581014368275));
#8206=CARTESIAN_POINT('Ctrl Pts',(4.05706783446607,-1.05820667714026,-1.7641546497058));
#8207=CARTESIAN_POINT('Ctrl Pts',(4.07816941925732,-1.04735421069218,-1.7624800269618));
#8208=CARTESIAN_POINT('Ctrl Pts',(4.07816926735968,-1.04735428881255,-1.66387346933803));
#8209=CARTESIAN_POINT('Ctrl Pts',(4.06720879457529,-1.0529912171243,-1.66468166682041));
#8210=CARTESIAN_POINT('Ctrl Pts',(4.05615954688209,-1.0584562438635,-1.66548147668066));
#8211=CARTESIAN_POINT('Ctrl Pts',(3.95081656761454,-1.1085165965364,-1.67298556491338));
#8212=CARTESIAN_POINT('Ctrl Pts',(3.85107146589306,-1.14057620227135,-1.67921900281393));
#8213=CARTESIAN_POINT('Ctrl Pts',(3.70750636862628,-1.1664483987049,-1.68842713204318));
#8214=CARTESIAN_POINT('Ctrl Pts',(3.6662561153982,-1.1716478754437,-1.69109333101217));
#8215=CARTESIAN_POINT('Ctrl Pts',(3.61469131315169,-1.17539241730269,-1.69449615845441));
#8216=CARTESIAN_POINT('Ctrl Pts',(3.60455331739282,-1.17599691210483,-1.69516843657527));
#8217=CARTESIAN_POINT('Ctrl Pts',(3.58834038871373,-1.17675335051725,-1.69624933443881));
#8218=CARTESIAN_POINT('Ctrl Pts',(3.58226974978789,-1.17698952688365,-1.69665534808521));
#8219=CARTESIAN_POINT('Ctrl Pts',(3.57075183295034,-1.17734840277255,-1.69742825479403));
#8220=CARTESIAN_POINT('Ctrl Pts',(3.56530498397853,-1.17748028948946,-1.69779485387303));
#8221=CARTESIAN_POINT('Ctrl Pts',(3.55290674205266,-1.17769442537928,-1.69863188744016));
#8222=CARTESIAN_POINT('Ctrl Pts',(3.5459551962096,-1.17775292922565,-1.69910304251821));
#8223=CARTESIAN_POINT('Ctrl Pts',(3.52460097443909,-1.17774358461091,-1.70055623898748));
#8224=CARTESIAN_POINT('Ctrl Pts',(3.51020019158431,-1.17747308790573,-1.7015444624602));
#8225=CARTESIAN_POINT('Ctrl Pts',(3.39981744033141,-1.17337356395114,-1.70918556258179));
#8226=CARTESIAN_POINT('Ctrl Pts',(3.30464033561589,-1.15807896331459,-1.71620325589538));
#8227=CARTESIAN_POINT('Ctrl Pts',(3.17118047132161,-1.11949215940773,-1.72639536639203));
#8228=CARTESIAN_POINT('Ctrl Pts',(3.13064186749986,-1.10533067999223,-1.72953388205583));
#8229=CARTESIAN_POINT('Ctrl Pts',(3.07773670939239,-1.08353901177537,-1.73362270517513));
#8230=CARTESIAN_POINT('Ctrl Pts',(3.06460873182975,-1.07784968770978,-1.73463657268711));
#8231=CARTESIAN_POINT('Ctrl Pts',(3.04248008501204,-1.06777687330759,-1.73634061445457));
#8232=CARTESIAN_POINT('Ctrl Pts',(3.03342591750481,-1.06351536976818,-1.73703640312354));
#8233=CARTESIAN_POINT('Ctrl Pts',(3.02061712131598,-1.05728605250369,-1.73801755906626));
#8234=CARTESIAN_POINT('Ctrl Pts',(3.01681739688841,-1.05541271151954,-1.73830821718948));
#8235=CARTESIAN_POINT('Ctrl Pts',(3.01026757547089,-1.05213946808544,-1.73880844269938));
#8236=CARTESIAN_POINT('Ctrl Pts',(3.00751274636819,-1.05074919814524,-1.73901858715715));
#8237=CARTESIAN_POINT('Ctrl Pts',(3.0017307039087,-1.04780262552922,-1.73945909634588));
#8238=CARTESIAN_POINT('Ctrl Pts',(2.99870474602553,-1.04624401389536,-1.73968931698272));
#8239=CARTESIAN_POINT('Ctrl Pts',(2.99057264262707,-1.0420106189605,-1.74030728991804));
#8240=CARTESIAN_POINT('Ctrl Pts',(2.98547922572389,-1.03931138965471,-1.74069356553669));
#8241=CARTESIAN_POINT('Ctrl Pts',(2.96226964450017,-1.02679247971709,-1.74245109736812));
#8242=CARTESIAN_POINT('Ctrl Pts',(2.94439209618264,-1.01653514714861,-1.74379747133573));
#8243=CARTESIAN_POINT('Ctrl Pts',(2.85433860876496,-0.961675819485388,-1.7505892773089));
#8244=CARTESIAN_POINT('Ctrl Pts',(2.78686020957013,-0.909835205613063,-1.75572663758296));
#8245=CARTESIAN_POINT('Ctrl Pts',(2.68595027687882,-0.813335780464355,-1.7644227735283));
#8246=CARTESIAN_POINT('Ctrl Pts',(2.64906016171293,-0.772772056499071,-1.76788111736715));
#8247=CARTESIAN_POINT('Ctrl Pts',(2.60629376462096,-0.718602046806227,-1.7723880742219));
#8248=CARTESIAN_POINT('Ctrl Pts',(2.59766342985112,-0.707252640307025,-1.77332641156375));
#8249=CARTESIAN_POINT('Ctrl Pts',(2.58515126005506,-0.690163114121485,-1.77473223660069));
#8250=CARTESIAN_POINT('Ctrl Pts',(2.58111040059674,-0.684540619608032,-1.7751936418779));
#8251=CARTESIAN_POINT('Ctrl Pts',(2.57398056398201,-0.674433203603279,-1.77602130128997));
#8252=CARTESIAN_POINT('Ctrl Pts',(2.57087264862487,-0.669961835857362,-1.7763868265982));
#8253=CARTESIAN_POINT('Ctrl Pts',(2.56435408651734,-0.66044338135412,-1.77716372753591));
#8254=CARTESIAN_POINT('Ctrl Pts',(2.56095137473905,-0.655391080581236,-1.77757538558351));
#8255=CARTESIAN_POINT('Ctrl Pts',(2.55193958339063,-0.641783846262471,-1.77868233103703));
#8256=CARTESIAN_POINT('Ctrl Pts',(2.54640262378268,-0.633182012311385,-1.77938024608536));
#8257=CARTESIAN_POINT('Ctrl Pts',(2.52109413313629,-0.592715762147237,-1.78265585148403));
#8258=CARTESIAN_POINT('Ctrl Pts',(2.50274160539872,-0.559994001780803,-1.78528371881742));
#8259=CARTESIAN_POINT('Ctrl Pts',(2.44749598487698,-0.449437143368032,-1.79409891734746));
#8260=CARTESIAN_POINT('Ctrl Pts',(2.41757390006504,-0.368434922198221,-1.80048059439767));
#8261=CARTESIAN_POINT('Ctrl Pts',(2.38989355259196,-0.257409291542364,-1.80881582218067));
#8262=CARTESIAN_POINT('Ctrl Pts',(2.38403177980866,-0.229668696262755,-1.81086321079438));
#8263=CARTESIAN_POINT('Ctrl Pts',(2.3772887773929,-0.190885513886392,-1.81365562251017));
#8264=CARTESIAN_POINT('Ctrl Pts',(2.37555361561142,-0.180002702933001,-1.81443159796881));
#8265=CARTESIAN_POINT('Ctrl Pts',(2.37279471082329,-0.160986159582724,-1.81577256321965));
#8266=CARTESIAN_POINT('Ctrl Pts',(2.37170268528861,-0.152863255524331,-1.81634061688686));
#8267=CARTESIAN_POINT('Ctrl Pts',(2.37021508896511,-0.140849536249192,-1.81717313947139));
#8268=CARTESIAN_POINT('Ctrl Pts',(2.36975398577981,-0.136967298248811,-1.81744099632176));
#8269=CARTESIAN_POINT('Ctrl Pts',(2.36896797372442,-0.130055834766786,-1.81791568526622));
#8270=CARTESIAN_POINT('Ctrl Pts',(2.36863547807778,-0.127027572021349,-1.81812292519326));
#8271=CARTESIAN_POINT('Ctrl Pts',(2.36793635811066,-0.120424137179884,-1.81857319921629));
#8272=CARTESIAN_POINT('Ctrl Pts',(2.36757434493591,-0.11684855962326,-1.818815978365));
#8273=CARTESIAN_POINT('Ctrl Pts',(2.36660784008911,-0.106845813176737,-1.81949241455126));
#8274=CARTESIAN_POINT('Ctrl Pts',(2.36603980413247,-0.100415129805642,-1.81992412617205));
#8275=CARTESIAN_POINT('Ctrl Pts',(2.36304215872024,-0.0629686326593251,
-1.82242132650595));
#8276=CARTESIAN_POINT('Ctrl Pts',(2.36178914359087,-0.03186802865735,-1.82442884456396));
#8277=CARTESIAN_POINT('Ctrl Pts',(2.36173950065284,0.0459379929296807,-1.829365563715));
#8278=CARTESIAN_POINT('Ctrl Pts',(2.36448609594123,0.0925904886839736,-1.8322496682962));
#8279=CARTESIAN_POINT('Ctrl Pts',(2.37933491330058,0.217563020057073,-1.84003412765772));
#8280=CARTESIAN_POINT('Ctrl Pts',(2.39657341976869,0.295015600107938,-1.84493496905921));
#8281=CARTESIAN_POINT('Ctrl Pts',(2.42631095937341,0.3848405948513,-1.85110108312394));
#8282=CARTESIAN_POINT('Ctrl Pts',(2.43146339661839,0.399433560576364,-1.85211805133336));
#8283=CARTESIAN_POINT('Ctrl Pts',(2.43938833097985,0.420544319337278,-1.85361361703527));
#8284=CARTESIAN_POINT('Ctrl Pts',(2.44193459038297,0.427145729013813,-1.85408480430946));
#8285=CARTESIAN_POINT('Ctrl Pts',(2.44655813732052,0.438818336950527,-1.85492441579771));
#8286=CARTESIAN_POINT('Ctrl Pts',(2.44861164599582,0.443898776355467,-1.85529204286599));
#8287=CARTESIAN_POINT('Ctrl Pts',(2.45296908538613,0.454466336746174,-1.85606139942585));
#8288=CARTESIAN_POINT('Ctrl Pts',(2.45527929620904,0.459950683115552,-1.85646333035864));
#8289=CARTESIAN_POINT('Ctrl Pts',(2.46141928971215,0.474223438814875,-1.85751640628447));
#8290=CARTESIAN_POINT('Ctrl Pts',(2.46531492183368,0.482982861669442,-1.85816974850413));
#8291=CARTESIAN_POINT('Ctrl Pts',(2.48365618987188,0.522903792524002,-1.86118056379435));
#8292=CARTESIAN_POINT('Ctrl Pts',(2.49935241787434,0.553468804735726,-1.86358003416854));
#8293=CARTESIAN_POINT('Ctrl Pts',(2.54951603707422,0.641459860708164,-1.87077583092555));
#8294=CARTESIAN_POINT('Ctrl Pts',(2.58756688549411,0.696679239316374,-1.8756796502683));
#8295=CARTESIAN_POINT('Ctrl Pts',(2.66810567521235,0.794551446040531,-1.88498109428815));
#8296=CARTESIAN_POINT('Ctrl Pts',(2.70958277242547,0.837783072776255,-1.88936135877682));
#8297=CARTESIAN_POINT('Ctrl Pts',(2.76165858078287,0.884380661498793,-1.89426200187052));
#8298=CARTESIAN_POINT('Ctrl Pts',(2.7692337839229,0.890986357703456,-1.89496128567395));
#8299=CARTESIAN_POINT('Ctrl Pts',(2.77989802854111,0.900048063570196,-1.89592592050504));
#8300=CARTESIAN_POINT('Ctrl Pts',(2.78291599325332,0.902586521404342,-1.89619674463837));
#8301=CARTESIAN_POINT('Ctrl Pts',(2.78814309287441,0.906938476982544,-1.89666200656722));
#8302=CARTESIAN_POINT('Ctrl Pts',(2.79034615978033,0.908759160055227,-1.89685694706525));
#8303=CARTESIAN_POINT('Ctrl Pts',(2.79500652115651,0.912582162564231,-1.89726685852578));
#8304=CARTESIAN_POINT('Ctrl Pts',(2.79746531079257,0.914582613871321,-1.89748169014809));
#8305=CARTESIAN_POINT('Ctrl Pts',(2.80358423025661,0.919519996773278,-1.89801285172971));
#8306=CARTESIAN_POINT('Ctrl Pts',(2.80725394338851,0.922445065506297,-1.89832835402901));
#8307=CARTESIAN_POINT('Ctrl Pts',(2.82114560724921,0.9333827426984,-1.89951166135836));
#8308=CARTESIAN_POINT('Ctrl Pts',(2.83148282373114,0.94124836479831,-1.90036989352394));
#8309=CARTESIAN_POINT('Ctrl Pts',(2.85835249537242,0.961000356663441,-1.90255025239896));
#8310=CARTESIAN_POINT('Ctrl Pts',(2.87506733994145,0.972632296228121,-1.90385892182145));
#8311=CARTESIAN_POINT('Ctrl Pts',(2.94068114695399,1.01581187999253,-1.90885008290914));
#8312=CARTESIAN_POINT('Ctrl Pts',(2.99159240929114,1.04415412022685,-1.91242235981348));
#8313=CARTESIAN_POINT('Ctrl Pts',(3.1127200429867,1.10027657425597,-1.92068869226887));
#8314=CARTESIAN_POINT('Ctrl Pts',(3.18391629143164,1.12530458544485,-1.92539239021672));
#8315=CARTESIAN_POINT('Ctrl Pts',(3.26709294763647,1.1458564402194,-1.93101549974067));
#8316=CARTESIAN_POINT('Ctrl Pts',(3.27720944777208,1.14821453754936,-1.93170121208814));
#8317=CARTESIAN_POINT('Ctrl Pts',(3.29392371832376,1.15187812233307,-1.93283773257314));
#8318=CARTESIAN_POINT('Ctrl Pts',(3.30050396891324,1.15326148965532,-1.93328608181594));
#8319=CARTESIAN_POINT('Ctrl Pts',(3.31241612433426,1.15565945618393,-1.93409953407945));
#8320=CARTESIAN_POINT('Ctrl Pts',(3.31774391911414,1.15669369634066,-1.93446400765489));
#8321=CARTESIAN_POINT('Ctrl Pts',(3.32919416946672,1.15883442063661,-1.93524880364358));
#8322=CARTESIAN_POINT('Ctrl Pts',(3.33531860239896,1.15992928425166,-1.93566947905483));
#8323=CARTESIAN_POINT('Ctrl Pts',(3.35212676887428,1.16279683415892,-1.93682663542608));
#8324=CARTESIAN_POINT('Ctrl Pts',(3.3628265066516,1.16447072788871,-1.93756617319535));
#8325=CARTESIAN_POINT('Ctrl Pts',(3.42632872900924,1.17350982832436,-1.9419737816769));
#8326=CARTESIAN_POINT('Ctrl Pts',(3.4795514082622,1.17742930915096,-1.94574768365034));
#8327=CARTESIAN_POINT('Ctrl Pts',(3.58083465922324,1.17800283611901,-1.95306801407391));
#8328=CARTESIAN_POINT('Ctrl Pts',(3.62878890282123,1.1753417035512,-1.956592113777));
#8329=CARTESIAN_POINT('Ctrl Pts',(3.70448574153653,1.16648109437251,-1.96218382384049));
#8330=CARTESIAN_POINT('Ctrl Pts',(3.7324008335434,1.16219140627998,-1.96425158999461));
#8331=CARTESIAN_POINT('Ctrl Pts',(3.79416225415088,1.15041376234611,-1.96881017644143));
#8332=CARTESIAN_POINT('Ctrl Pts',(3.82788984446797,1.14242626292964,-1.97128857889477));
#8333=CARTESIAN_POINT('Ctrl Pts',(3.86705082734306,1.13130665409029,-1.97411808040797));
#8334=CARTESIAN_POINT('Ctrl Pts',(3.87286959595853,1.12960578439532,-1.97453722169651));
#8335=CARTESIAN_POINT('Ctrl Pts',(3.8823381901651,1.1267585062086,-1.97521688775381));
#8336=CARTESIAN_POINT('Ctrl Pts',(3.88599593431311,1.1256391357162,-1.97547886183994));
#8337=CARTESIAN_POINT('Ctrl Pts',(3.89255218328838,1.12359775726526,-1.9759473041977));
#8338=CARTESIAN_POINT('Ctrl Pts',(3.89545262032294,1.12268232705864,-1.97615413611128));
#8339=CARTESIAN_POINT('Ctrl Pts',(3.90183641550061,1.12064025962907,-1.97660847690624));
#8340=CARTESIAN_POINT('Ctrl Pts',(3.90531808366598,1.1195086121721,-1.97685569430468));
#8341=CARTESIAN_POINT('Ctrl Pts',(3.91540068528495,1.11617940280244,-1.97757009444221));
#8342=CARTESIAN_POINT('Ctrl Pts',(3.9219876327481,1.11393951899269,-1.9780349161775));
#8343=CARTESIAN_POINT('Ctrl Pts',(3.97779012277,1.09441060402506,-1.98195969015905));
#8344=CARTESIAN_POINT('Ctrl Pts',(4.02583351377513,1.07392542025525,-1.985253356461));
#8345=CARTESIAN_POINT('Ctrl Pts',(4.14646870018387,1.01272491907379,-1.99367970135734));
#8346=CARTESIAN_POINT('Ctrl Pts',(4.2163817871874,0.967396552818754,-1.99873618223097));
#8347=CARTESIAN_POINT('Ctrl Pts',(4.30497128156978,0.895619548860395,-2.00600754950781));
#8348=CARTESIAN_POINT('Ctrl Pts',(4.32822236192517,0.875213300926312,-2.00800807257359));
#8349=CARTESIAN_POINT('Ctrl Pts',(4.35759067701704,0.847316778492877,-2.01067746094749));
#8350=CARTESIAN_POINT('Ctrl Pts',(4.36445823927226,0.840632045031352,-2.01131247663924));
#8351=CARTESIAN_POINT('Ctrl Pts',(4.37545630246784,0.829662208990441,-2.01234761092071));
#8352=CARTESIAN_POINT('Ctrl Pts',(4.37963733664293,0.825428212108018,-2.01274550621023));
#8353=CARTESIAN_POINT('Ctrl Pts',(4.38760684162724,0.817234477347509,-2.0135125265572));
#8354=CARTESIAN_POINT('Ctrl Pts',(4.3914001206636,0.813279615494939,-2.01388143016663));
#8355=CARTESIAN_POINT('Ctrl Pts',(4.40011192760904,0.804068888200546,-2.0147376701685));
#8356=CARTESIAN_POINT('Ctrl Pts',(4.40501010284007,0.798794160870089,-2.01522585004929));
#8357=CARTESIAN_POINT('Ctrl Pts',(4.42045517338131,0.78185289537306,-2.01678718859949));
#8358=CARTESIAN_POINT('Ctrl Pts',(4.43081649732216,0.770020274066548,-2.01786793923086));
#8359=CARTESIAN_POINT('Ctrl Pts',(4.45461110920002,0.741722984126297,-2.02043118988564));
#8360=CARTESIAN_POINT('Ctrl Pts',(4.4678415396249,0.725095662998175,-2.02192111430522));
#8361=CARTESIAN_POINT('Ctrl Pts',(4.51609158939471,0.660971128903884,-2.0276076303749));
#8362=CARTESIAN_POINT('Ctrl Pts',(4.54797162038507,0.611227261504883,-2.03190544218035));
#8363=CARTESIAN_POINT('Ctrl Pts',(4.60968126242485,0.49687190629247,-2.04143738216179));
#8364=CARTESIAN_POINT('Ctrl Pts',(4.637666865582,0.431511327252492,-2.04666771687595));
#8365=CARTESIAN_POINT('Ctrl Pts',(4.66262090364172,0.354729207774051,-2.05232608778339));
#8366=CARTESIAN_POINT('Ctrl Pts',(4.66552604264068,0.345396659632726,-2.05300581402567));
#8367=CARTESIAN_POINT('Ctrl Pts',(4.66942671478405,0.332293425870884,-2.05394797824683));
#8368=CARTESIAN_POINT('Ctrl Pts',(4.67052012076835,0.328552630208662,-2.05421557213698));
#8369=CARTESIAN_POINT('Ctrl Pts',(4.67237993449763,0.322070460370457,-2.05467679946803));
#8370=CARTESIAN_POINT('Ctrl Pts',(4.6731550017904,0.319331636886459,-2.05487091597544));
#8371=CARTESIAN_POINT('Ctrl Pts',(4.67477587322674,0.313523751716991,-2.05528090818236));
#8372=CARTESIAN_POINT('Ctrl Pts',(4.6756191785517,0.310454015882972,-2.05549663488754));
#8373=CARTESIAN_POINT('Ctrl Pts',(4.67769202571387,0.302787031777399,-2.05603309642252));
#8374=CARTESIAN_POINT('Ctrl Pts',(4.6789061867004,0.298185619899464,-2.05635296694511));
#8375=CARTESIAN_POINT('Ctrl Pts',(4.68345081379723,0.280529322081057,-2.05757280381143));
#8376=CARTESIAN_POINT('Ctrl Pts',(4.68658522180455,0.267424412390622,-2.05846241871889));
#8377=CARTESIAN_POINT('Ctrl Pts',(4.69411974484175,0.233348095729801,-2.06074181690958));
#8378=CARTESIAN_POINT('Ctrl Pts',(4.69817385148982,0.21230464175019,-2.06211655363904));
#8379=CARTESIAN_POINT('Ctrl Pts',(4.7108651956415,0.135149674411638,-2.06707563848272));
#8380=CARTESIAN_POINT('Ctrl Pts',(4.7160176858494,0.0785424066773082,-2.07056128549592));
#8381=CARTESIAN_POINT('Ctrl Pts',(4.71845491176731,-0.0532176947246951,
-2.07872190182494));
#8382=CARTESIAN_POINT('Ctrl Pts',(4.71267412206468,-0.12816739160587,-2.08340830867854));
#8383=CARTESIAN_POINT('Ctrl Pts',(4.69802419193994,-0.212294530724692,-2.08901262073761));
#8384=CARTESIAN_POINT('Ctrl Pts',(4.69610527027622,-0.222511652566463,-2.08969885623174));
#8385=CARTESIAN_POINT('Ctrl Pts',(4.69272235996702,-0.239295707541782,-2.09083606503381));
#8386=CARTESIAN_POINT('Ctrl Pts',(4.69133687770206,-0.24587801528933,-2.09128457421128));
#8387=CARTESIAN_POINT('Ctrl Pts',(4.6887317508209,-0.257749275210423,-2.09209819738475));
#8388=CARTESIAN_POINT('Ctrl Pts',(4.68753177703586,-0.263042387226824,-2.09246268071727));
#8389=CARTESIAN_POINT('Ctrl Pts',(4.68487822756179,-0.274383132361227,-2.09324736488095));
#8390=CARTESIAN_POINT('Ctrl Pts',(4.68341324921156,-0.280427900532047,-2.09366791777175));
#8391=CARTESIAN_POINT('Ctrl Pts',(4.67926840384141,-0.296957199951835,-2.09482438870743));
#8392=CARTESIAN_POINT('Ctrl Pts',(4.67649186071571,-0.307416626627177,-2.09556335751577));
#8393=CARTESIAN_POINT('Ctrl Pts',(4.65923185453813,-0.369001073588747,-2.09995818628309));
#8394=CARTESIAN_POINT('Ctrl Pts',(4.64144805162262,-0.41912954585212,-2.10371914225961));
#8395=CARTESIAN_POINT('Ctrl Pts',(4.60123004028068,-0.512034954937896,-2.11103504815499));
#8396=CARTESIAN_POINT('Ctrl Pts',(4.57942904879124,-0.554974571886197,-2.11456849444449));
#8397=CARTESIAN_POINT('Ctrl Pts',(4.5407388631058,-0.620849508269609,-2.12017366499362));
#8398=CARTESIAN_POINT('Ctrl Pts',(4.52553862666622,-0.644717546849175,-2.12224545726128));
#8399=CARTESIAN_POINT('Ctrl Pts',(4.48984118418507,-0.696551057450518,-2.12680858755197));
#8400=CARTESIAN_POINT('Ctrl Pts',(4.46893729297749,-0.724208367484301,-2.12928757302993));
#8401=CARTESIAN_POINT('Ctrl Pts',(4.44297688949179,-0.755576433836276,-2.13211764926407));
#8402=CARTESIAN_POINT('Ctrl Pts',(4.43907558355216,-0.760216983443321,-2.13253681292097));
#8403=CARTESIAN_POINT('Ctrl Pts',(4.4326544468697,-0.767736190521684,-2.13321650785764));
#8404=CARTESIAN_POINT('Ctrl Pts',(4.43015617511438,-0.770632991626648,-2.13347848865331));
#8405=CARTESIAN_POINT('Ctrl Pts',(4.42564622457119,-0.775811152467679,-2.13394693802956));
#8406=CARTESIAN_POINT('Ctrl Pts',(4.42363978820822,-0.77809693143885,-2.13415377030272));
#8407=CARTESIAN_POINT('Ctrl Pts',(4.41919880658925,-0.783116843471275,-2.13460810598139));
#8408=CARTESIAN_POINT('Ctrl Pts',(4.4167603572444,-0.785847411686301,-2.13485531794817));
#8409=CARTESIAN_POINT('Ctrl Pts',(4.40965133867465,-0.793733745118623,-2.13556968649325));
#8410=CARTESIAN_POINT('Ctrl Pts',(4.40494767421071,-0.798859662330359,-2.13603448238837));
#8411=CARTESIAN_POINT('Ctrl Pts',(4.36460601686487,-0.842048311412802,-2.13995780804612));
#8412=CARTESIAN_POINT('Ctrl Pts',(4.32651706350101,-0.877752498900697,-2.14325018980034));
#8413=CARTESIAN_POINT('Ctrl Pts',(4.22196399805932,-0.963462137019431,-2.15167183700275));
#8414=CARTESIAN_POINT('Ctrl Pts',(4.15236205602334,-1.00916473672304,-2.15672494055412));
#8415=CARTESIAN_POINT('Ctrl Pts',(4.07841162190961,-1.04722962021999,-2.16202877425628));
#8416=CARTESIAN_POINT('Ctrl Pts',(4.07829045001313,-1.04729196504753,-2.1620374646626));
#8417=CARTESIAN_POINT('Ctrl Pts',(4.07816926754606,-1.0473542887167,-2.1620461556085));
#8418=CARTESIAN_POINT('Origin',(3.53951905042299,8.32667268468867E-16,0.924367114736157));
#8419=CARTESIAN_POINT('',(4.07816927004253,-1.04735428743277,-2.76055935511047));
#8420=CARTESIAN_POINT('',(4.07816899834492,-1.04735442716575,-2.6623694009368));
#8421=CARTESIAN_POINT('',(4.07816926754759,-1.04735428871592,0.924367114736157));
#8422=CARTESIAN_POINT('Ctrl Pts',(4.07816927004253,-1.04735428743277,-2.76055935511047));
#8423=CARTESIAN_POINT('Ctrl Pts',(4.08356421506408,-1.04457968827797,-2.7601335800222));
#8424=CARTESIAN_POINT('Ctrl Pts',(4.0889381821921,-1.04176316825741,-2.75970976090382));
#8425=CARTESIAN_POINT('Ctrl Pts',(4.10015524195956,-1.03577329741215,-2.75882611700734));
#8426=CARTESIAN_POINT('Ctrl Pts',(4.10599335599956,-1.03259194706589,-2.75836677970824));
#8427=CARTESIAN_POINT('Ctrl Pts',(4.11494742482899,-1.02761382852509,-2.75766352092749));
#8428=CARTESIAN_POINT('Ctrl Pts',(4.11808249898953,-1.02585200272776,-2.75741752642351));
#8429=CARTESIAN_POINT('Ctrl Pts',(4.12385874729127,-1.02257100686899,-2.75696479772187));
#8430=CARTESIAN_POINT('Ctrl Pts',(4.12650209395693,-1.02105594968994,-2.75675782341948));
#8431=CARTESIAN_POINT('Ctrl Pts',(4.13252236890555,-1.01757427095392,-2.75628687613839));
#8432=CARTESIAN_POINT('Ctrl Pts',(4.13589541246349,-1.01560108730532,-2.75602332361189));
#8433=CARTESIAN_POINT('Ctrl Pts',(4.14471215943939,-1.01038434089713,-2.75533507329739));
#8434=CARTESIAN_POINT('Ctrl Pts',(4.15013970282066,-1.00711351829356,-2.75491203938387));
#8435=CARTESIAN_POINT('Ctrl Pts',(4.19375999704026,-0.98034416718816,-2.75151522471897));
#8436=CARTESIAN_POINT('Ctrl Pts',(4.23061342733199,-0.954722710688114,-2.74866372483842));
#8437=CARTESIAN_POINT('Ctrl Pts',(4.31055689783586,-0.892082677190189,-2.74230689562782));
#8438=CARTESIAN_POINT('Ctrl Pts',(4.35261057231845,-0.853928168979994,-2.73883424796629));
#8439=CARTESIAN_POINT('Ctrl Pts',(4.420051454405,-0.783223335717929,-2.7327534570326));
#8440=CARTESIAN_POINT('Ctrl Pts',(4.44677977570563,-0.752099516605598,-2.73017741838101));
#8441=CARTESIAN_POINT('Ctrl Pts',(4.48222070750397,-0.706185417569803,-2.72645139478416));
#8442=CARTESIAN_POINT('Ctrl Pts',(4.49231862592652,-0.692500673860304,-2.72534969240171));
#8443=CARTESIAN_POINT('Ctrl Pts',(4.50974142335659,-0.667786448218728,-2.72337149374909));
#8444=CARTESIAN_POINT('Ctrl Pts',(4.51718338591302,-0.656842916937278,-2.72249938887661));
#8445=CARTESIAN_POINT('Ctrl Pts',(4.5281258286655,-0.640153816361877,-2.72117386781109));
#8446=CARTESIAN_POINT('Ctrl Pts',(4.53176424051348,-0.634499606134734,-2.72072554327277));
#8447=CARTESIAN_POINT('Ctrl Pts',(4.53825205750843,-0.624225044674489,-2.71991206467609));
#8448=CARTESIAN_POINT('Ctrl Pts',(4.54111833285158,-0.619615527238064,-2.71954753954138));
#8449=CARTESIAN_POINT('Ctrl Pts',(4.54720236993772,-0.609678704707029,-2.71876255256481));
#8450=CARTESIAN_POINT('Ctrl Pts',(4.55040996106446,-0.604345397614385,-2.71834173705289));
#8451=CARTESIAN_POINT('Ctrl Pts',(4.55894461604881,-0.589896639534398,-2.71720288834666));
#8452=CARTESIAN_POINT('Ctrl Pts',(4.56419151894789,-0.580734749131844,-2.71648202634855));
#8453=CARTESIAN_POINT('Ctrl Pts',(4.59050099387927,-0.533327585183812,-2.71275748255032));
#8454=CARTESIAN_POINT('Ctrl Pts',(4.60954575662783,-0.49400746775547,-2.7096845237133));
#8455=CARTESIAN_POINT('Ctrl Pts',(4.6574118127644,-0.379350148992415,-2.70077035411512));
#8456=CARTESIAN_POINT('Ctrl Pts',(4.68074320058933,-0.301987209894065,-2.69479568605557));
#8457=CARTESIAN_POINT('Ctrl Pts',(4.70116213171401,-0.196028177435771,-2.6869421640297));
#8458=CARTESIAN_POINT('Ctrl Pts',(4.705397652984,-0.169023596004742,-2.68497042260464));
#8459=CARTESIAN_POINT('Ctrl Pts',(4.70998618472882,-0.131215369309465,-2.68227054088473));
#8460=CARTESIAN_POINT('Ctrl Pts',(4.71113591491256,-0.120518574392876,-2.68151342639212));
#8461=CARTESIAN_POINT('Ctrl Pts',(4.71288899571229,-0.10179758877045,-2.68020177212215));
#8462=CARTESIAN_POINT('Ctrl Pts',(4.71355697154527,-0.0937803083836858,
-2.6796443398046));
#8463=CARTESIAN_POINT('Ctrl Pts',(4.71442533032341,-0.0818862326155545,
-2.67882430828708));
#8464=CARTESIAN_POINT('Ctrl Pts',(4.71468876739008,-0.0780144797335104,
-2.67855846221651));
#8465=CARTESIAN_POINT('Ctrl Pts',(4.71510644160466,-0.0713928088246926,
-2.6781057413469));
#8466=CARTESIAN_POINT('Ctrl Pts',(4.7152701752967,-0.0686435750611099,-2.6779183526165));
#8467=CARTESIAN_POINT('Ctrl Pts',(4.71561998527273,-0.0624010457293062,
-2.67749417834076));
#8468=CARTESIAN_POINT('Ctrl Pts',(4.71580014331346,-0.0589074763591207,
-2.67725772092763));
#8469=CARTESIAN_POINT('Ctrl Pts',(4.71624859182551,-0.0493867073535359,
-2.67661572089007));
#8470=CARTESIAN_POINT('Ctrl Pts',(4.71648614533107,-0.0433580650099662,
-2.67621181963123));
#8471=CARTESIAN_POINT('Ctrl Pts',(4.71745314714548,-0.0128629086343577,
-2.67418077172513));
#8472=CARTESIAN_POINT('Ctrl Pts',(4.71746612650918,0.0116221950734552,-2.67258914283153));
#8473=CARTESIAN_POINT('Ctrl Pts',(4.71334518372222,0.146033717860345,-2.66398032862887));
#8474=CARTESIAN_POINT('Ctrl Pts',(4.69459048873785,0.254966027464975,-2.65742573700325));
#8475=CARTESIAN_POINT('Ctrl Pts',(4.65421625150648,0.380837211625539,-2.64901391847737));
#8476=CARTESIAN_POINT('Ctrl Pts',(4.64684835740117,0.401756826019076,-2.64758864549921));
#8477=CARTESIAN_POINT('Ctrl Pts',(4.63306526629313,0.437625241520115,-2.64508773436085));
#8478=CARTESIAN_POINT('Ctrl Pts',(4.62692272971513,0.452672480738562,-2.64402069230371));
#8479=CARTESIAN_POINT('Ctrl Pts',(4.61757564872198,0.474280739349009,-2.64245988601519));
#8480=CARTESIAN_POINT('Ctrl Pts',(4.61461818840335,0.480947074396737,-2.64197437188364));
#8481=CARTESIAN_POINT('Ctrl Pts',(4.60932433117624,0.492586960732433,-2.64111939192732));
#8482=CARTESIAN_POINT('Ctrl Pts',(4.60701466146038,0.497572478422809,-2.64075083973942));
#8483=CARTESIAN_POINT('Ctrl Pts',(4.60245528306627,0.50723621060023,-2.64003177548476));
#8484=CARTESIAN_POINT('Ctrl Pts',(4.60020936055344,0.511916079567099,-2.63968139955495));
#8485=CARTESIAN_POINT('Ctrl Pts',(4.59410323254831,0.524426818613807,-2.63873885431123));
#8486=CARTESIAN_POINT('Ctrl Pts',(4.59018682912239,0.532229740768374,-2.63814476446553));
#8487=CARTESIAN_POINT('Ctrl Pts',(4.57521163717373,0.561256319106046,-2.63591088128483));
#8488=CARTESIAN_POINT('Ctrl Pts',(4.56359419959941,0.582183592275196,-2.63425190280769));
#8489=CARTESIAN_POINT('Ctrl Pts',(4.4998366670267,0.689214137826032,-2.6255052445153));
#8490=CARTESIAN_POINT('Ctrl Pts',(4.43745757934006,0.768717079948001,-2.61805178385223));
#8491=CARTESIAN_POINT('Ctrl Pts',(4.34455460439164,0.860172994016073,-2.60854445056867));
#8492=CARTESIAN_POINT('Ctrl Pts',(4.3225729302063,0.880231038859097,-2.60639259063669));
#8493=CARTESIAN_POINT('Ctrl Pts',(4.29116808863293,0.90677899388292,-2.60347296115957));
#8494=CARTESIAN_POINT('Ctrl Pts',(4.28237593907986,0.913995669937662,-2.60267143926328));
#8495=CARTESIAN_POINT('Ctrl Pts',(4.26691204521181,0.926317995377002,-2.60129086879716));
#8496=CARTESIAN_POINT('Ctrl Pts',(4.26028778320911,0.931481637672731,-2.60070851745956));
#8497=CARTESIAN_POINT('Ctrl Pts',(4.2504686251344,0.938968240099166,-2.59985916122319));
#8498=CARTESIAN_POINT('Ctrl Pts',(4.2473165538372,0.941346561579019,-2.59958857472766));
#8499=CARTESIAN_POINT('Ctrl Pts',(4.24170856380623,0.945533845344303,-2.59911089964739));
#8500=CARTESIAN_POINT('Ctrl Pts',(4.23925751352847,0.947349169739976,-2.59890338303929));
#8501=CARTESIAN_POINT('Ctrl Pts',(4.23392488638581,0.951266691936722,-2.5984546341473));
#8502=CARTESIAN_POINT('Ctrl Pts',(4.23104079774334,0.953365332931716,-2.59821364156447));
#8503=CARTESIAN_POINT('Ctrl Pts',(4.22300853917452,0.959154473199115,-2.59754706023847));
#8504=CARTESIAN_POINT('Ctrl Pts',(4.2178399709548,0.96281665848811,-2.59712332728447));
#8505=CARTESIAN_POINT('Ctrl Pts',(4.18889814295964,0.982974626727414,-2.59477783334878));
#8506=CARTESIAN_POINT('Ctrl Pts',(4.1645506575597,0.998633128590652,-2.59290608158786));
#8507=CARTESIAN_POINT('Ctrl Pts',(4.05645625592928,1.06264728489848,-2.58491329665853));
#8508=CARTESIAN_POINT('Ctrl Pts',(3.96751097215398,1.10148473096663,-2.57910429978621));
#8509=CARTESIAN_POINT('Ctrl Pts',(3.83593711864401,1.14055954851559,-2.57043258994896));
#8510=CARTESIAN_POINT('Ctrl Pts',(3.7964938881081,1.15008832062027,-2.56782827087683));
#8511=CARTESIAN_POINT('Ctrl Pts',(3.74672745131903,1.15942290482044,-2.56449511859617));
#8512=CARTESIAN_POINT('Ctrl Pts',(3.73679092794977,1.16115485168715,-2.56382737512894));
#8513=CARTESIAN_POINT('Ctrl Pts',(3.72085012638427,1.1637228342143,-2.56275200857603));
#8514=CARTESIAN_POINT('Ctrl Pts',(3.71485936497829,1.16464053070163,-2.56234694340977));
#8515=CARTESIAN_POINT('Ctrl Pts',(3.70346607023002,1.1662959172512,-2.56157470255183));
#8516=CARTESIAN_POINT('Ctrl Pts',(3.69806495991129,1.16704240915702,-2.56120781217038));
#8517=CARTESIAN_POINT('Ctrl Pts',(3.68573763194173,1.1686590252291,-2.56036851394296));
#8518=CARTESIAN_POINT('Ctrl Pts',(3.67880852551826,1.16950512154891,-2.55989537153765));
#8519=CARTESIAN_POINT('Ctrl Pts',(3.65741429672787,1.17192469246386,-2.55843003346276));
#8520=CARTESIAN_POINT('Ctrl Pts',(3.64292768985563,1.17329169193208,-2.55743150569861));
#8521=CARTESIAN_POINT('Ctrl Pts',(3.533990830082,1.18153818006976,-2.54987221544559));
#8522=CARTESIAN_POINT('Ctrl Pts',(3.43906116836297,1.17726987968544,-2.54295841446134));
#8523=CARTESIAN_POINT('Ctrl Pts',(3.30254460625993,1.15449184839412,-2.5328033230465));
#8524=CARTESIAN_POINT('Ctrl Pts',(3.25983209947081,1.14489475278669,-2.52960192552092));
#8525=CARTESIAN_POINT('Ctrl Pts',(3.2038296428696,1.1289894151128,-2.52544026421777));
#8526=CARTESIAN_POINT('Ctrl Pts',(3.18998236256407,1.12477936606106,-2.52441437887715));
#8527=CARTESIAN_POINT('Ctrl Pts',(3.16661424906073,1.11720139229929,-2.52269228422701));
#8528=CARTESIAN_POINT('Ctrl Pts',(3.15705296383702,1.11396438519246,-2.52199031327273));
#8529=CARTESIAN_POINT('Ctrl Pts',(3.14352500969638,1.10918972998623,-2.52100202047301));
#8530=CARTESIAN_POINT('Ctrl Pts',(3.1395235459356,1.10775301182045,-2.5207103062204));
#8531=CARTESIAN_POINT('Ctrl Pts',(3.13262880019684,1.10523523528111,-2.52020883558979));
#8532=CARTESIAN_POINT('Ctrl Pts',(3.12973185657808,1.10416441606982,-2.51999849447311));
#8533=CARTESIAN_POINT('Ctrl Pts',(3.12365672845941,1.10189161735747,-2.51955818469412));
#8534=CARTESIAN_POINT('Ctrl Pts',(3.12047950397054,1.10068727006229,-2.51932835608941));
#8535=CARTESIAN_POINT('Ctrl Pts',(3.11195296446409,1.09741295943522,-2.51871267117988));
#8536=CARTESIAN_POINT('Ctrl Pts',(3.10661340102892,1.09531760847428,-2.51832827245048));
#8537=CARTESIAN_POINT('Ctrl Pts',(3.08243820263907,1.0856263762999,-2.51659224013371));
#8538=CARTESIAN_POINT('Ctrl Pts',(3.06378442333429,1.07758257876514,-2.51526475272673));
#8539=CARTESIAN_POINT('Ctrl Pts',(2.96820091616922,1.03339915209238,-2.50847899445197));
#8540=CARTESIAN_POINT('Ctrl Pts',(2.89513471994717,0.989489723408842,-2.50333256587488));
#8541=CARTESIAN_POINT('Ctrl Pts',(2.78367003400686,0.904878534813775,-2.4946175995915));
#8542=CARTESIAN_POINT('Ctrl Pts',(2.74229610113198,0.868646879644988,-2.49114931914335));
#8543=CARTESIAN_POINT('Ctrl Pts',(2.69354509354465,0.819528540735376,-2.48663029228173));
#8544=CARTESIAN_POINT('Ctrl Pts',(2.68367149815664,0.80921190267889,-2.48569053034149));
#8545=CARTESIAN_POINT('Ctrl Pts',(2.6692893077337,0.793626653985059,-2.48428293920833));
#8546=CARTESIAN_POINT('Ctrl Pts',(2.66463548298678,0.788493380421825,-2.48382121432477));
#8547=CARTESIAN_POINT('Ctrl Pts',(2.65640473565994,0.77925210026199,-2.48299315132483));
#8548=CARTESIAN_POINT('Ctrl Pts',(2.65281047731249,0.775159747003033,-2.48262754415319));
#8549=CARTESIAN_POINT('Ctrl Pts',(2.64525776447829,0.766439106564089,-2.48185064793042));
#8550=CARTESIAN_POINT('Ctrl Pts',(2.64130657679308,0.761804765949063,-2.48143907760195));
#8551=CARTESIAN_POINT('Ctrl Pts',(2.63082066674637,0.749310872098327,-2.48033280208272));
#8552=CARTESIAN_POINT('Ctrl Pts',(2.62435214513884,0.74139669515883,-2.47963547541483));
#8553=CARTESIAN_POINT('Ctrl Pts',(2.5947125794674,0.704153978543222,-2.476368939241));
#8554=CARTESIAN_POINT('Ctrl Pts',(2.57284537383398,0.673820129410011,-2.47374990132801));
#8555=CARTESIAN_POINT('Ctrl Pts',(2.49950212062077,0.561144488798077,-2.46416186660919));
#8556=CARTESIAN_POINT('Ctrl Pts',(2.45680926275963,0.473554783146209,-2.45692639003369));
#8557=CARTESIAN_POINT('Ctrl Pts',(2.41845313384539,0.361606441853206,-2.44837183985799));
#8558=CARTESIAN_POINT('Ctrl Pts',(2.41210147768409,0.341288344614352,-2.44684725501282));
#8559=CARTESIAN_POINT('Ctrl Pts',(2.40265113297913,0.307906157670654,-2.4443988125825));
#8560=CARTESIAN_POINT('Ctrl Pts',(2.39921905502597,0.29494206605236,-2.44346159659141));
#8561=CARTESIAN_POINT('Ctrl Pts',(2.39487179095101,0.277309001589889,-2.44220774981465));
#8562=CARTESIAN_POINT('Ctrl Pts',(2.39376251237781,0.272689545910477,-2.44188120048683));
#8563=CARTESIAN_POINT('Ctrl Pts',(2.39195694067214,0.264964888459799,-2.44133850372109));
#8564=CARTESIAN_POINT('Ctrl Pts',(2.39124523623644,0.261863392333106,-2.44112150903588));
#8565=CARTESIAN_POINT('Ctrl Pts',(2.38992030687273,0.255980280846619,-2.44071165503247));
#8566=CARTESIAN_POINT('Ctrl Pts',(2.38930458983194,0.253199270222425,-2.44051865234454));
#8567=CARTESIAN_POINT('Ctrl Pts',(2.38786888939029,0.246601317977667,-2.44006244603685));
#8568=CARTESIAN_POINT('Ctrl Pts',(2.38705777695381,0.242782449253529,-2.43979973602712));
#8569=CARTESIAN_POINT('Ctrl Pts',(2.38427498531351,0.229352293812495,-2.43888031773015));
#8570=CARTESIAN_POINT('Ctrl Pts',(2.382404365146,0.219720151889708,-2.43822894889428));
#8571=CARTESIAN_POINT('Ctrl Pts',(2.36815362126143,0.141103268443537,-2.43296950297869));
#8572=CARTESIAN_POINT('Ctrl Pts',(2.36183187491525,0.0711529470005039,-2.42864081734748));
#8573=CARTESIAN_POINT('Ctrl Pts',(2.36169695181929,-0.0805315584501841,
-2.41925791481658));
#8574=CARTESIAN_POINT('Ctrl Pts',(2.37010009790866,-0.161887316300625,-2.41421634373057));
#8575=CARTESIAN_POINT('Ctrl Pts',(2.3900025117513,-0.256795913985343,-2.40789614574099));
#8576=CARTESIAN_POINT('Ctrl Pts',(2.39345986337707,-0.27181007742759,-2.40688361418846));
#8577=CARTESIAN_POINT('Ctrl Pts',(2.39893041520147,-0.29360266190163,-2.40539333010729));
#8578=CARTESIAN_POINT('Ctrl Pts',(2.40071180265195,-0.300438024658899,-2.40492291151059));
#8579=CARTESIAN_POINT('Ctrl Pts',(2.40398385702866,-0.312545842562442,-2.40408413437813));
#8580=CARTESIAN_POINT('Ctrl Pts',(2.40545004435078,-0.317824742393573,-2.40371656689995));
#8581=CARTESIAN_POINT('Ctrl Pts',(2.40858747259038,-0.32882263819139,-2.4029467891541));
#8582=CARTESIAN_POINT('Ctrl Pts',(2.41026538261947,-0.334539553161827,-2.40254437373673));
#8583=CARTESIAN_POINT('Ctrl Pts',(2.41476453461829,-0.349449291259322,-2.40148879772812));
#8584=CARTESIAN_POINT('Ctrl Pts',(2.41765506322126,-0.3586205692598,-2.40083342119573));
#8585=CARTESIAN_POINT('Ctrl Pts',(2.43148241528656,-0.400689023674756,-2.39779842541338));
#8586=CARTESIAN_POINT('Ctrl Pts',(2.44375508470654,-0.433125597620229,-2.395375976772));
#8587=CARTESIAN_POINT('Ctrl Pts',(2.48433056127798,-0.527552774009048,-2.38807179302228));
#8588=CARTESIAN_POINT('Ctrl Pts',(2.51659776826546,-0.587677489052723,-2.38307831972427));
#8589=CARTESIAN_POINT('Ctrl Pts',(2.56843384221588,-0.666930334565932,-2.3761297263357));
#8590=CARTESIAN_POINT('Ctrl Pts',(2.58374358041938,-0.688691422818852,-2.37418083962557));
#8591=CARTESIAN_POINT('Ctrl Pts',(2.60684701081892,-0.719274278288497,-2.37139698512298));
#8592=CARTESIAN_POINT('Ctrl Pts',(2.61405623191907,-0.728526736914997,-2.37054858735982));
#8593=CARTESIAN_POINT('Ctrl Pts',(2.63782749577928,-0.758112841823712,-2.36781895349618));
#8594=CARTESIAN_POINT('Ctrl Pts',(2.65493203316285,-0.77800307858689,-2.36595756536672));
#8595=CARTESIAN_POINT('Ctrl Pts',(2.67685714137634,-0.801840022995481,-2.36370986225827));
#8596=CARTESIAN_POINT('Ctrl Pts',(2.68106201494558,-0.806340197523177,-2.36328474478683));
#8597=CARTESIAN_POINT('Ctrl Pts',(2.68773013180696,-0.813365317289847,-2.36262016660146));
#8598=CARTESIAN_POINT('Ctrl Pts',(2.69016967348418,-0.8159124572917,-2.36237900973142));
#8599=CARTESIAN_POINT('Ctrl Pts',(2.69453135392328,-0.820425752264362,-2.36195141279864));
#8600=CARTESIAN_POINT('Ctrl Pts',(2.69644893347515,-0.822396133487094,-2.3617646421664));
#8601=CARTESIAN_POINT('Ctrl Pts',(2.70106050587343,-0.827101607451648,-2.36131836561036));
#8602=CARTESIAN_POINT('Ctrl Pts',(2.70376098991346,-0.829830262953716,-2.36105936447165));
#8603=CARTESIAN_POINT('Ctrl Pts',(2.71201107194797,-0.838085285069375,-2.36027497813601));
#8604=CARTESIAN_POINT('Ctrl Pts',(2.71760262960361,-0.843569679865628,-2.35975271542219));
#8605=CARTESIAN_POINT('Ctrl Pts',(2.73073995524549,-0.856200580080385,-2.358546021087));
#8606=CARTESIAN_POINT('Ctrl Pts',(2.73832653224468,-0.863303899720868,-2.35786442975006));
#8607=CARTESIAN_POINT('Ctrl Pts',(2.76517301860309,-0.887781523375701,-2.35550092673505));
#8608=CARTESIAN_POINT('Ctrl Pts',(2.78491299221078,-0.904620189321162,-2.35384824180508));
#8609=CARTESIAN_POINT('Ctrl Pts',(2.86563192122239,-0.968992784711524,-2.34734669568882));
#8610=CARTESIAN_POINT('Ctrl Pts',(2.9306690175001,-1.01112478070619,-2.34265324003624));
#8611=CARTESIAN_POINT('Ctrl Pts',(3.04248362075683,-1.06883348508297,-2.33476087469136));
#8612=CARTESIAN_POINT('Ctrl Pts',(3.08692875914478,-1.08839809462577,-2.33166698148866));
#8613=CARTESIAN_POINT('Ctrl Pts',(3.14261604257234,-1.10890956936754,-2.32776766192681));
#8614=CARTESIAN_POINT('Ctrl Pts',(3.15283291597908,-1.1125134836653,-2.32705148179739));
#8615=CARTESIAN_POINT('Ctrl Pts',(3.16905424463737,-1.11798497585398,-2.32591248050451));
#8616=CARTESIAN_POINT('Ctrl Pts',(3.17502659879194,-1.11994635080558,-2.325492718003));
#8617=CARTESIAN_POINT('Ctrl Pts',(3.18617977620866,-1.12351049263088,-2.32470793492378));
#8618=CARTESIAN_POINT('Ctrl Pts',(3.19135654397516,-1.12512547619105,-2.32434332179092));
#8619=CARTESIAN_POINT('Ctrl Pts',(3.20289765849856,-1.12863865244498,-2.32352957321124));
#8620=CARTESIAN_POINT('Ctrl Pts',(3.20926723983762,-1.13051886661665,-2.32307987142123));
#8621=CARTESIAN_POINT('Ctrl Pts',(3.22798301238288,-1.13587184345754,-2.32175659594079));
#8622=CARTESIAN_POINT('Ctrl Pts',(3.24037009594021,-1.13919683473104,-2.3208783417576));
#8623=CARTESIAN_POINT('Ctrl Pts',(3.32523751935868,-1.160497699507,-2.31484238902654));
#8624=CARTESIAN_POINT('Ctrl Pts',(3.39921806453577,-1.17174375096012,-2.30947146078027));
#8625=CARTESIAN_POINT('Ctrl Pts',(3.55574322131604,-1.18049793974909,-2.29799821274768));
#8626=CARTESIAN_POINT('Ctrl Pts',(3.63799406062758,-1.17649616270969,-2.2919071136245));
#8627=CARTESIAN_POINT('Ctrl Pts',(3.72835482879296,-1.16255004039011,-2.28550938483745));
#8628=CARTESIAN_POINT('Ctrl Pts',(3.73752898362188,-1.16102266447757,-2.28486348988142));
#8629=CARTESIAN_POINT('Ctrl Pts',(3.75069102938883,-1.15867080016363,-2.28394299616137));
#8630=CARTESIAN_POINT('Ctrl Pts',(3.75469396270291,-1.15793410270981,-2.28366387221191));
#8631=CARTESIAN_POINT('Ctrl Pts',(3.76171161989338,-1.15660492955911,-2.28317607173157));
#8632=CARTESIAN_POINT('Ctrl Pts',(3.76472796135646,-1.1560213874877,-2.28296690780228));
#8633=CARTESIAN_POINT('Ctrl Pts',(3.77112722427484,-1.15475738688068,-2.28252425789375));
#8634=CARTESIAN_POINT('Ctrl Pts',(3.77450946342174,-1.15407386042605,-2.28229094443978));
#8635=CARTESIAN_POINT('Ctrl Pts',(3.78374049293312,-1.15216607118534,-2.28165580593086));
#8636=CARTESIAN_POINT('Ctrl Pts',(3.78958314567294,-1.15091212547518,-2.28125560119713));
#8637=CARTESIAN_POINT('Ctrl Pts',(3.82109279913945,-1.14389826612583,-2.27910575677516));
#8638=CARTESIAN_POINT('Ctrl Pts',(3.846573064171,-1.1373236548044,-2.27739769368109));
#8639=CARTESIAN_POINT('Ctrl Pts',(3.94312692874197,-1.10892792673493,-2.27096787394003));
#8640=CARTESIAN_POINT('Ctrl Pts',(4.01221342001257,-1.08127513956293,-2.2664476753402));
#8641=CARTESIAN_POINT('Ctrl Pts',(4.07816947157471,-1.04735418378554,-2.26183802367812));
#8642=CARTESIAN_POINT('',(2.3617693920187,-0.000311670151205854,-2.32461248197894));
#8643=CARTESIAN_POINT('Ctrl Pts',(4.07816926754606,-1.0473542887167,-2.1620461556085));
#8644=CARTESIAN_POINT('Ctrl Pts',(4.05073123587279,-1.06146556116525,-2.16401395222577));
#8645=CARTESIAN_POINT('Ctrl Pts',(4.0227513290571,-1.07449213620125,-2.16600987267141));
#8646=CARTESIAN_POINT('Ctrl Pts',(3.98544740015946,-1.09010776812031,-2.16867491911241));
#8647=CARTESIAN_POINT('Ctrl Pts',(3.9765560990177,-1.09370272397537,-2.16931037608124));
#8648=CARTESIAN_POINT('Ctrl Pts',(3.96207729854973,-1.09935208867815,-2.17034605191304));
#8649=CARTESIAN_POINT('Ctrl Pts',(3.95651626700993,-1.10147347090154,-2.17074404308492));
#8650=CARTESIAN_POINT('Ctrl Pts',(3.94580518148661,-1.10546671915603,-2.17151112655334));
#8651=CARTESIAN_POINT('Ctrl Pts',(3.9406576631559,-1.10734497745289,-2.17187999651113));
#8652=CARTESIAN_POINT('Ctrl Pts',(3.92872118666874,-1.11160628245965,-2.17273597810724));
#8653=CARTESIAN_POINT('Ctrl Pts',(3.92192318277157,-1.11396315273396,-2.17322393158914));
#8654=CARTESIAN_POINT('Ctrl Pts',(3.90021537039549,-1.12126713977771,-2.17478379865724));
#8655=CARTESIAN_POINT('Ctrl Pts',(3.88522852241034,-1.12597813197835,-2.1758632840228));
#8656=CARTESIAN_POINT('Ctrl Pts',(3.84979136327779,-1.13634334630803,-2.17842299651224));
#8657=CARTESIAN_POINT('Ctrl Pts',(3.82927415636777,-1.14174734116409,-2.17991062022575));
#8658=CARTESIAN_POINT('Ctrl Pts',(3.75132958942065,-1.16004083512243,-2.18558355348006));
#8659=CARTESIAN_POINT('Ctrl Pts',(3.693114645676,-1.16917297213438,-2.18986954975729));
#8660=CARTESIAN_POINT('Ctrl Pts',(3.56352584634092,-1.17965434944569,-2.19940625143114));
#8661=CARTESIAN_POINT('Ctrl Pts',(3.49220386942015,-1.17895029048881,-2.2046537977874));
#8662=CARTESIAN_POINT('Ctrl Pts',(3.41162541470622,-1.1708263485179,-2.21032971493028));
#8663=CARTESIAN_POINT('Ctrl Pts',(3.401886185522,-1.16972147562266,-2.21101132249905));
#8664=CARTESIAN_POINT('Ctrl Pts',(3.38830852202504,-1.16800921234235,-2.21195436499361));
#8665=CARTESIAN_POINT('Ctrl Pts',(3.38445790451514,-1.16750425528745,-2.21222100019463));
#8666=CARTESIAN_POINT('Ctrl Pts',(3.37779285987008,-1.16659666723653,-2.21268103350148));
#8667=CARTESIAN_POINT('Ctrl Pts',(3.37497729212429,-1.16620287897618,-2.21287490887173));
#8668=CARTESIAN_POINT('Ctrl Pts',(3.36900778119692,-1.1653459276259,-2.21328494394368));
#8669=CARTESIAN_POINT('Ctrl Pts',(3.36585423437264,-1.16488014669123,-2.21350095173145));
#8670=CARTESIAN_POINT('Ctrl Pts',(3.35797752004533,-1.16368405343863,-2.21403905898488));
#8671=CARTESIAN_POINT('Ctrl Pts',(3.35325677320652,-1.16293777543066,-2.21436028270096));
#8672=CARTESIAN_POINT('Ctrl Pts',(3.33509476144177,-1.15995320822496,-2.21559164140253));
#8673=CARTESIAN_POINT('Ctrl Pts',(3.3216875660417,-1.15751035369551,-2.21649117263143));
#8674=CARTESIAN_POINT('Ctrl Pts',(3.28698142459966,-1.15056230603112,-2.21880218404987));
#8675=CARTESIAN_POINT('Ctrl Pts',(3.26575898043834,-1.14569822064141,-2.22019808965914));
#8676=CARTESIAN_POINT('Ctrl Pts',(3.14379313867637,-1.11416122386063,-2.22818307382671));
#8677=CARTESIAN_POINT('Ctrl Pts',(3.04681164316509,-1.07480035543966,-2.23442602583379));
#8678=CARTESIAN_POINT('Ctrl Pts',(2.92954936891031,-1.00795739017186,-2.24303561309381));
#8679=CARTESIAN_POINT('Ctrl Pts',(2.90343689296424,-0.991685608863961,-2.24502553812767));
#8680=CARTESIAN_POINT('Ctrl Pts',(2.87007837176057,-0.96903856849742,-2.24768277519579));
#8681=CARTESIAN_POINT('Ctrl Pts',(2.86222995372842,-0.963569426720093,-2.24831663448374));
#8682=CARTESIAN_POINT('Ctrl Pts',(2.84961214042061,-0.954546426283682,-2.24935034965688));
#8683=CARTESIAN_POINT('Ctrl Pts',(2.84480141064312,-0.951050904623204,-2.24974799373266));
#8684=CARTESIAN_POINT('Ctrl Pts',(2.83580388540701,-0.944408523379313,-2.250498486953));
#8685=CARTESIAN_POINT('Ctrl Pts',(2.83161119403172,-0.941269864515296,-2.25085101504504));
#8686=CARTESIAN_POINT('Ctrl Pts',(2.82736461161161,-0.938046441628834,-2.25121098673338));
#8687=CARTESIAN_POINT('Ctrl Pts',(2.82728959612224,-0.937989485973974,-2.25121734653013));
#8688=CARTESIAN_POINT('Ctrl Pts',(2.82714379967878,-0.937878762169231,-2.25122970892862));
#8689=CARTESIAN_POINT('Ctrl Pts',(2.82707301797973,-0.937824995005365,-2.25123571149178));
#8690=CARTESIAN_POINT('Ctrl Pts',(2.82170413031255,-0.933745724259574,-2.25169107689551));
#8691=CARTESIAN_POINT('Ctrl Pts',(2.81644032390447,-0.929675475216095,-2.25214217511832));
#8692=CARTESIAN_POINT('Ctrl Pts',(2.8052578576919,-0.920876188440969,-2.25311062189075));
#8693=CARTESIAN_POINT('Ctrl Pts',(2.79934979658597,-0.916134228491322,-2.25362846614165));
#8694=CARTESIAN_POINT('Ctrl Pts',(2.78378447258346,-0.903392255485656,-2.25500950386272));
#8695=CARTESIAN_POINT('Ctrl Pts',(2.7742087560986,-0.895294617426583,-2.25587652190288));
#8696=CARTESIAN_POINT('Ctrl Pts',(2.71438152075821,-0.843040923127297,-2.26140644628375));
#8697=CARTESIAN_POINT('Ctrl Pts',(2.66784692635009,-0.794830251945468,-2.26623266981025));
#8698=CARTESIAN_POINT('Ctrl Pts',(2.57427819926975,-0.67973528537226,-2.27709019012116));
#8699=CARTESIAN_POINT('Ctrl Pts',(2.52958757441272,-0.611367573177025,-2.2831299420389));
#8700=CARTESIAN_POINT('Ctrl Pts',(2.48802228786831,-0.530600958041598,-2.28948697036161));
#8701=CARTESIAN_POINT('Ctrl Pts',(2.48383500333495,-0.522220283805889,-2.29013766994944));
#8702=CARTESIAN_POINT('Ctrl Pts',(2.47796741466395,-0.510117483123086,-2.29106370037916));
#8703=CARTESIAN_POINT('Ctrl Pts',(2.47620589792119,-0.50643544794795,-2.29134363020673));
#8704=CARTESIAN_POINT('Ctrl Pts',(2.47315155044716,-0.499964862595573,-2.291832325748));
#8705=CARTESIAN_POINT('Ctrl Pts',(2.4718504413181,-0.497180300149088,-2.29204158487014));
#8706=CARTESIAN_POINT('Ctrl Pts',(2.46911472805537,-0.491265209968073,-2.29248385705357));
#8707=CARTESIAN_POINT('Ctrl Pts',(2.46768294128971,-0.488133461044548,-2.29271670158411));
#8708=CARTESIAN_POINT('Ctrl Pts',(2.46381687895138,-0.479578189661555,-2.29334932101888));
#8709=CARTESIAN_POINT('Ctrl Pts',(2.46140985699213,-0.474142354593266,-2.29374749673964));
#8710=CARTESIAN_POINT('Ctrl Pts',(2.44875489332431,-0.444968659549882,-2.29586555627874));
#8711=CARTESIAN_POINT('Ctrl Pts',(2.43924871055521,-0.420914440670272,-2.29754530190582));
#8712=CARTESIAN_POINT('Ctrl Pts',(2.39454646724692,-0.295906384200299,-2.30603247300616));
#8713=CARTESIAN_POINT('Ctrl Pts',(2.37242132185075,-0.190812240438875,-2.3124152820028));
#8714=CARTESIAN_POINT('Ctrl Pts',(2.36278079051669,-0.0562588296494679,
-2.3209841257008));
#8715=CARTESIAN_POINT('Ctrl Pts',(2.36177651634134,-0.0282893539699714,
-2.32278333724587));
#8716=CARTESIAN_POINT('Ctrl Pts',(2.36176909189499,-0.000312549685508988,
-2.32461190331719));
#8717=CARTESIAN_POINT('Ctrl Pts',(2.36176909165296,-0.000311636306741051,
-2.32461196301571));
#8718=CARTESIAN_POINT('Ctrl Pts',(2.36176714494032,0.00704546771741885,
-2.32509282406184));
#8719=CARTESIAN_POINT('Ctrl Pts',(2.36183413518344,0.014402326824858,-2.32557564586804));
#8720=CARTESIAN_POINT('Ctrl Pts',(2.36209751886435,0.0286567381129853,-2.3265152767732));
#8721=CARTESIAN_POINT('Ctrl Pts',(2.3622856101691,0.0355541200457753,-2.32697181785634));
#8722=CARTESIAN_POINT('Ctrl Pts',(2.36272874286164,0.0478407777693243,-2.32778862113952));
#8723=CARTESIAN_POINT('Ctrl Pts',(2.36296023165427,0.0532307462102336,-2.32814815608438));
#8724=CARTESIAN_POINT('Ctrl Pts',(2.36348635219762,0.0637882783698974,-2.32885486723026));
#8725=CARTESIAN_POINT('Ctrl Pts',(2.36377803381177,0.0689558710647757,-2.32920194478199));
#8726=CARTESIAN_POINT('Ctrl Pts',(2.36446929188937,0.079917838391069,-2.32994074744835));
#8727=CARTESIAN_POINT('Ctrl Pts',(2.36487768690705,0.0857114984080915,-2.33033273623927));
#8728=CARTESIAN_POINT('Ctrl Pts',(2.36602230913766,0.100399777229516,-2.33133047839124));
#8729=CARTESIAN_POINT('Ctrl Pts',(2.36681680914094,0.1092893533962,-2.33193801732483));
#8730=CARTESIAN_POINT('Ctrl Pts',(2.37026510927065,0.143484000467958,-2.33428971046191));
#8731=CARTESIAN_POINT('Ctrl Pts',(2.3736374575342,0.168707962199148,-2.33605579014994));
#8732=CARTESIAN_POINT('Ctrl Pts',(2.39405402143647,0.291090120934524,-2.34478381037125));
#8733=CARTESIAN_POINT('Ctrl Pts',(2.42244047808055,0.385944445135463,-2.35208776465424));
#8734=CARTESIAN_POINT('Ctrl Pts',(2.4800226550828,0.516220521963633,-2.36247573798136));
#8735=CARTESIAN_POINT('Ctrl Pts',(2.49996870468376,0.555294700243881,-2.36563471135706));
#8736=CARTESIAN_POINT('Ctrl Pts',(2.52545543365817,0.599012339321944,-2.36915238976667));
#8737=CARTESIAN_POINT('Ctrl Pts',(2.52891199031007,0.604825740975665,-2.36961977464174));
#8738=CARTESIAN_POINT('Ctrl Pts',(2.53429539853988,0.613704796668374,-2.3703326686158));
#8739=CARTESIAN_POINT('Ctrl Pts',(2.53618655810856,0.616791762681776,-2.37058033854345));
#8740=CARTESIAN_POINT('Ctrl Pts',(2.53969411591302,0.62245837562568,-2.37103457256516));
#8741=CARTESIAN_POINT('Ctrl Pts',(2.54130628236905,0.62504047800591,-2.3712413902536));
#8742=CARTESIAN_POINT('Ctrl Pts',(2.54499339671477,0.630895237902823,-2.37170999020497));
#8743=CARTESIAN_POINT('Ctrl Pts',(2.54707449718152,0.634163927470638,-2.37197136873037));
#8744=CARTESIAN_POINT('Ctrl Pts',(2.5525422508336,0.642659040999688,-2.37265021423398));
#8745=CARTESIAN_POINT('Ctrl Pts',(2.55595434474355,0.647869060667929,-2.37306608994603));
#8746=CARTESIAN_POINT('Ctrl Pts',(2.58117657951703,0.685723017493762,-2.37608623415576));
#8747=CARTESIAN_POINT('Ctrl Pts',(2.6045680189091,0.717289075709418,-2.37859711033031));
#8748=CARTESIAN_POINT('Ctrl Pts',(2.70003622473673,0.833493945439406,-2.38805530972885));
#8749=CARTESIAN_POINT('Ctrl Pts',(2.782369527941,0.908938386376902,-2.39472051930603));
#8750=CARTESIAN_POINT('Ctrl Pts',(2.88510326384161,0.979292735583572,-2.40278182644444));
#8751=CARTESIAN_POINT('Ctrl Pts',(2.89627659879153,0.986667831489673,-2.40365465971774));
#8752=CARTESIAN_POINT('Ctrl Pts',(2.91425338258447,0.998098482295169,-2.40505442507073));
#8753=CARTESIAN_POINT('Ctrl Pts',(2.92097640840086,1.00227876899897,-2.40557692470281));
#8754=CARTESIAN_POINT('Ctrl Pts',(2.93383567404664,1.01009582840448,-2.40657478804085));
#8755=CARTESIAN_POINT('Ctrl Pts',(2.93996382704281,1.0137452665026,-2.40704967468512));
#8756=CARTESIAN_POINT('Ctrl Pts',(2.95078359394454,1.02005623146141,-2.40788718810417));
#8757=CARTESIAN_POINT('Ctrl Pts',(2.95546109373587,1.02274163630893,-2.40824894964358));
#8758=CARTESIAN_POINT('Ctrl Pts',(2.96528111377719,1.02829008353822,-2.40900789227968));
#8759=CARTESIAN_POINT('Ctrl Pts',(2.97042696863603,1.03114688772593,-2.4094052816034));
#8760=CARTESIAN_POINT('Ctrl Pts',(2.98374589794393,1.03841103977904,-2.41043316627688));
#8761=CARTESIAN_POINT('Ctrl Pts',(2.99194994108768,1.04276044540044,-2.41106566776457));
#8762=CARTESIAN_POINT('Ctrl Pts',(3.0253289204826,1.05995391520183,-2.41363707451244));
#8763=CARTESIAN_POINT('Ctrl Pts',(3.05090914878522,1.0719859708675,-2.41560347251735));
#8764=CARTESIAN_POINT('Ctrl Pts',(3.18168690422588,1.12784569423022,-2.42564263867971));
#8765=CARTESIAN_POINT('Ctrl Pts',(3.2923946298944,1.15715238259871,-2.43417590664319));
#8766=CARTESIAN_POINT('Ctrl Pts',(3.4317982713568,1.17311044143113,-2.44426477971486));
#8767=CARTESIAN_POINT('Ctrl Pts',(3.45812012148976,1.17523033301461,-2.44613762042885));
#8768=CARTESIAN_POINT('Ctrl Pts',(3.49046756576221,1.1767432965422,-2.44838325310531));
#8769=CARTESIAN_POINT('Ctrl Pts',(3.49644417215425,1.17697722694499,-2.4487958201167));
#8770=CARTESIAN_POINT('Ctrl Pts',(3.50587215824342,1.17727433565949,-2.44944267781701));
#8771=CARTESIAN_POINT('Ctrl Pts',(3.50932237676741,1.17736788491519,-2.44967856286774));
#8772=CARTESIAN_POINT('Ctrl Pts',(3.51584363896025,1.17751601730299,-2.45012276810754));
#8773=CARTESIAN_POINT('Ctrl Pts',(3.51891446205776,1.1775737544982,-2.45033124613507));
#8774=CARTESIAN_POINT('Ctrl Pts',(3.52605185125736,1.17768002245485,-2.45081423666654));
#8775=CARTESIAN_POINT('Ctrl Pts',(3.53011848621199,1.1777195045357,-2.45108825140376));
#8776=CARTESIAN_POINT('Ctrl Pts',(3.54346813430815,1.17777996232603,-2.4519841446979));
#8777=CARTESIAN_POINT('Ctrl Pts',(3.55275147825245,1.17771225304544,-2.45260140044808));
#8778=CARTESIAN_POINT('Ctrl Pts',(3.64428176549376,1.17596220270868,-2.45863916813081));
#8779=CARTESIAN_POINT('Ctrl Pts',(3.72615182411669,1.16577640389569,-2.46366698742564));
#8780=CARTESIAN_POINT('Ctrl Pts',(3.8566515644846,1.13542693010188,-2.47196101923897));
#8781=CARTESIAN_POINT('Ctrl Pts',(3.90617352466559,1.12041565887996,-2.47517572290052));
#8782=CARTESIAN_POINT('Ctrl Pts',(3.97294596164391,1.09527289972979,-2.47973602958418));
#8783=CARTESIAN_POINT('Ctrl Pts',(3.99116843908936,1.08788527730156,-2.48100438058015));
#8784=CARTESIAN_POINT('Ctrl Pts',(4.02278286221714,1.07413716067061,-2.48325347544909));
#8785=CARTESIAN_POINT('Ctrl Pts',(4.03625577210155,1.06797338411652,-2.48422785320584));
#8786=CARTESIAN_POINT('Ctrl Pts',(4.05594479107972,1.05851260625127,-2.48567722236988));
#8787=CARTESIAN_POINT('Ctrl Pts',(4.06225371764276,1.05541126927136,-2.48614555682778));
#8788=CARTESIAN_POINT('Ctrl Pts',(4.07341047867017,1.04980226286008,-2.48698093689607));
#8789=CARTESIAN_POINT('Ctrl Pts',(4.07826939854137,1.04731700499614,-2.48734720081016));
#8790=CARTESIAN_POINT('Ctrl Pts',(4.08846220851999,1.04201384890239,-2.48812078749652));
#8791=CARTESIAN_POINT('Ctrl Pts',(4.09379205849155,1.03918856918159,-2.48852835943091));
#8792=CARTESIAN_POINT('Ctrl Pts',(4.10786329610926,1.03159055333359,-2.48961266336607));
#8793=CARTESIAN_POINT('Ctrl Pts',(4.11656609128106,1.02674775548998,-2.49029183840444));
#8794=CARTESIAN_POINT('Ctrl Pts',(4.15515103655396,1.00463108833202,-2.49334228693625));
#8795=CARTESIAN_POINT('Ctrl Pts',(4.18432395214428,0.986160526803372,-2.49575566049454));
#8796=CARTESIAN_POINT('Ctrl Pts',(4.29478593303441,0.909223897929501,-2.50532712296572));
#8797=CARTESIAN_POINT('Ctrl Pts',(4.36929693350183,0.841772125940284,-2.51279052793263));
#8798=CARTESIAN_POINT('Ctrl Pts',(4.4483440591119,0.749395963933119,-2.52158205437072));
#8799=CARTESIAN_POINT('Ctrl Pts',(4.46187202106959,0.732681593081876,-2.52312248253535));
#8800=CARTESIAN_POINT('Ctrl Pts',(4.48314152308866,0.704878774787815,-2.52559334453062));
#8801=CARTESIAN_POINT('Ctrl Pts',(4.49116278496185,0.694011310819136,-2.52653742320049));
#8802=CARTESIAN_POINT('Ctrl Pts',(4.50175800458639,0.679127340725465,-2.52779885391969));
#8803=CARTESIAN_POINT('Ctrl Pts',(4.50449675698573,0.675230166406004,-2.52812627574458));
#8804=CARTESIAN_POINT('Ctrl Pts',(4.50902690176018,0.668700028797116,-2.52866999942555));
#8805=CARTESIAN_POINT('Ctrl Pts',(4.5108313682993,0.666076260037713,-2.52888715539594));
#8806=CARTESIAN_POINT('Ctrl Pts',(4.51422817391446,0.661094005805544,-2.52929699090346));
#8807=CARTESIAN_POINT('Ctrl Pts',(4.51582263969086,0.658737020327767,-2.52948981583178));
#8808=CARTESIAN_POINT('Ctrl Pts',(4.51957889465443,0.65314081911715,-2.52994519919291));
#8809=CARTESIAN_POINT('Ctrl Pts',(4.52173320828097,0.649896589500528,-2.53020726807833));
#8810=CARTESIAN_POINT('Ctrl Pts',(4.52922797928574,0.638487650169794,-2.53112237803691));
#8811=CARTESIAN_POINT('Ctrl Pts',(4.53448321935766,0.630267055273255,-2.53177014428657));
#8812=CARTESIAN_POINT('Ctrl Pts',(4.57742867063534,0.561212830679454,-2.53712388786931));
#8813=CARTESIAN_POINT('Ctrl Pts',(4.6096096461867,0.497116894239392,-2.54153801287404));
#8814=CARTESIAN_POINT('Ctrl Pts',(4.65718428524163,0.375966075302231,-2.5495888659345));
#8815=CARTESIAN_POINT('Ctrl Pts',(4.67449578182659,0.319926912502816,-2.55320965941292));
#8816=CARTESIAN_POINT('Ctrl Pts',(4.69228824251175,0.242210470480923,-2.55829191314062));
#8817=CARTESIAN_POINT('Ctrl Pts',(4.69645315165062,0.221463603923614,-2.559653780897));
#8818=CARTESIAN_POINT('Ctrl Pts',(4.70272726024923,0.185168818388048,-2.5620532991407));
#8819=CARTESIAN_POINT('Ctrl Pts',(4.70508885038399,0.169669780928801,-2.56308329841438));
#8820=CARTESIAN_POINT('Ctrl Pts',(4.70808112462437,0.147001447260928,-2.56459962712176));
#8821=CARTESIAN_POINT('Ctrl Pts',(4.70895665440399,0.139865768943647,-2.56507836328552));
#8822=CARTESIAN_POINT('Ctrl Pts',(4.71038418714273,0.127278867426568,-2.56592552043681));
#8823=CARTESIAN_POINT('Ctrl Pts',(4.71096358752092,0.121830920761624,-2.56629307990902));
#8824=CARTESIAN_POINT('Ctrl Pts',(4.71209334488938,0.110453805093115,-2.56706260785041));
#8825=CARTESIAN_POINT('Ctrl Pts',(4.71263678741601,0.10452412166865,-2.5674647798512));
#8826=CARTESIAN_POINT('Ctrl Pts',(4.71393906526567,0.0890218998158714,-2.56851919093632));
#8827=CARTESIAN_POINT('Ctrl Pts',(4.71462582199949,0.0794439162948227,-2.56917363755248));
#8828=CARTESIAN_POINT('Ctrl Pts',(4.71704036438852,0.0388088294362735,-2.57196347131861));
#8829=CARTESIAN_POINT('Ctrl Pts',(4.71765442451819,0.00770065833032227,
-2.57413261346457));
#8830=CARTESIAN_POINT('Ctrl Pts',(4.7149742090219,-0.127211525198988,-2.58369058201898));
#8831=CARTESIAN_POINT('Ctrl Pts',(4.6991895760309,-0.230296077338879,-2.5914341498898));
#8832=CARTESIAN_POINT('Ctrl Pts',(4.66401479646512,-0.350823526437734,-2.6005160207918));
#8833=CARTESIAN_POINT('Ctrl Pts',(4.65734612672852,-0.371524659118201,-2.60207455748754));
#8834=CARTESIAN_POINT('Ctrl Pts',(4.64557562306867,-0.40486948655366,-2.60457103662758));
#8835=CARTESIAN_POINT('Ctrl Pts',(4.64082098287936,-0.417629664262643,-2.60552295342225));
#8836=CARTESIAN_POINT('Ctrl Pts',(4.63410025134089,-0.434752670455405,-2.60679307347657));
#8837=CARTESIAN_POINT('Ctrl Pts',(4.63232753935671,-0.439189592727695,-2.60712152010739));
#8838=CARTESIAN_POINT('Ctrl Pts',(4.62932726301842,-0.446568339363818,-2.60766647800685));
#8839=CARTESIAN_POINT('Ctrl Pts',(4.62811468607908,-0.449516145100719,-2.60788385130585));
#8840=CARTESIAN_POINT('Ctrl Pts',(4.6257978724115,-0.455084021856134,-2.60829374278524));
#8841=CARTESIAN_POINT('Ctrl Pts',(4.62469609298194,-0.457705071841693,-2.60848640862326));
#8842=CARTESIAN_POINT('Ctrl Pts',(4.6220665896892,-0.463897592790223,-2.60894097825564));
#8843=CARTESIAN_POINT('Ctrl Pts',(4.62053065523347,-0.467465573806555,-2.60920239673242));
#8844=CARTESIAN_POINT('Ctrl Pts',(4.6150560812966,-0.480011746047182,-2.61012010957465));
#8845=CARTESIAN_POINT('Ctrl Pts',(4.61102288771898,-0.488948589470601,-2.61077106036355));
#8846=CARTESIAN_POINT('Ctrl Pts',(4.57684652289852,-0.56222288362376,-2.6160938940057));
#8847=CARTESIAN_POINT('Ctrl Pts',(4.54104547186122,-0.623771193209739,-2.62047829871699));
#8848=CARTESIAN_POINT('Ctrl Pts',(4.46579723399229,-0.729778559808056,-2.62851950498376));
#8849=CARTESIAN_POINT('Ctrl Pts',(4.42812909766632,-0.775202906246022,-2.63216127658421));
#8850=CARTESIAN_POINT('Ctrl Pts',(4.37248221861363,-0.8328974688399,-2.63727032110493));
#8851=CARTESIAN_POINT('Ctrl Pts',(4.35733320394883,-0.847776953516559,-2.63863676512808));
#8852=CARTESIAN_POINT('Ctrl Pts',(4.33028321266681,-0.872945691321945,-2.64104361591959));
#8853=CARTESIAN_POINT('Ctrl Pts',(4.31856270978703,-0.88342123544306,-2.64207630525539));
#8854=CARTESIAN_POINT('Ctrl Pts',(4.30117573251054,-0.898346232910581,-2.64359586499526));
#8855=CARTESIAN_POINT('Ctrl Pts',(4.29567221033426,-0.902983527239545,-2.64407509531094));
#8856=CARTESIAN_POINT('Ctrl Pts',(4.2859039545646,-0.911062382650963,-2.64492281687599));
#8857=CARTESIAN_POINT('Ctrl Pts',(4.28165701469321,-0.914525194005671,-2.64529044280048));
#8858=CARTESIAN_POINT('Ctrl Pts',(4.27274771403405,-0.921686609048955,-2.64605980217086));
#8859=CARTESIAN_POINT('Ctrl Pts',(4.26808118581423,-0.925379755059735,-2.64646173709269));
#8860=CARTESIAN_POINT('Ctrl Pts',(4.25582465277012,-0.934929544448758,-2.64751483515616));
#8861=CARTESIAN_POINT('Ctrl Pts',(4.24819090344159,-0.940729060013479,-2.64816819569537));
#8862=CARTESIAN_POINT('Ctrl Pts',(4.21561129091714,-0.964858859684301,-2.65094665999334));
#8863=CARTESIAN_POINT('Ctrl Pts',(4.1900206592744,-0.982293585291936,-2.65310517502672));
#8864=CARTESIAN_POINT('Ctrl Pts',(4.13591074816408,-1.01611602628934,-2.65762425458699));
#8865=CARTESIAN_POINT('Ctrl Pts',(4.10734937419749,-1.03234708339974,-2.65998568832657));
#8866=CARTESIAN_POINT('Ctrl Pts',(4.07816899834492,-1.04735442716575,-2.6623694009368));
#8867=CARTESIAN_POINT('Origin',(3.53951905042299,8.32667268468867E-16,0.924367114736157));
#8868=CARTESIAN_POINT('',(4.07816931781854,-1.04735426286176,-3.26243320031815));
#8869=CARTESIAN_POINT('',(4.07816926753082,-1.04735428872454,-3.16389876579091));
#8870=CARTESIAN_POINT('',(4.07816926754759,-1.04735428871592,0.924367114736157));
#8871=CARTESIAN_POINT('',(2.36176898865594,-0.000625254868193132,-2.92357953805437));
#8872=CARTESIAN_POINT('Ctrl Pts',(4.07816931781854,-1.04735426286176,-3.26243320031815));
#8873=CARTESIAN_POINT('Ctrl Pts',(4.09898123165306,-1.03665077565644,-3.26077374776886));
#8874=CARTESIAN_POINT('Ctrl Pts',(4.11947420255453,-1.02532691942579,-3.25909590190709));
#8875=CARTESIAN_POINT('Ctrl Pts',(4.18089036335886,-0.988958206562127,-3.25393705625322));
#8876=CARTESIAN_POINT('Ctrl Pts',(4.22062680818187,-0.962022496624445,-3.25041459606803));
#8877=CARTESIAN_POINT('Ctrl Pts',(4.28095180582499,-0.91551542035171,-3.24482602715964));
#8878=CARTESIAN_POINT('Ctrl Pts',(4.30266984491695,-0.897492047178338,-3.2427597435237));
#8879=CARTESIAN_POINT('Ctrl Pts',(4.34956955752838,-0.855636381517705,-3.23820211300989));
#8880=CARTESIAN_POINT('Ctrl Pts',(4.37439114140176,-0.831435222165497,-3.23572322234103));
#8881=CARTESIAN_POINT('Ctrl Pts',(4.40226168444952,-0.801752435915756,-3.23289319515093));
#8882=CARTESIAN_POINT('Ctrl Pts',(4.40637765999414,-0.797300430167136,-3.2324739926128));
#8883=CARTESIAN_POINT('Ctrl Pts',(4.41303447604109,-0.789987657795277,-3.23179422630176));
#8884=CARTESIAN_POINT('Ctrl Pts',(4.4155960194558,-0.787146011634137,-3.23153221282202));
#8885=CARTESIAN_POINT('Ctrl Pts',(4.42016942300341,-0.782022529874782,-3.23106369850168));
#8886=CARTESIAN_POINT('Ctrl Pts',(4.42218632461181,-0.77974534283531,-3.23085683392516));
#8887=CARTESIAN_POINT('Ctrl Pts',(4.4266115195677,-0.774709894419688,-3.23040241652877));
#8888=CARTESIAN_POINT('Ctrl Pts',(4.42901578492135,-0.771948203931422,-3.2301551553211));
#8889=CARTESIAN_POINT('Ctrl Pts',(4.43595169874441,-0.763905747078712,-3.2294406123789));
#8890=CARTESIAN_POINT('Ctrl Pts',(4.44044957034633,-0.7585958656908,-3.22897569269589));
#8891=CARTESIAN_POINT('Ctrl Pts',(4.47828760051015,-0.713115599425455,-3.22504820078121));
#8892=CARTESIAN_POINT('Ctrl Pts',(4.50897454489097,-0.670803815023034,-3.22175216591452));
#8893=CARTESIAN_POINT('Ctrl Pts',(4.58101811686311,-0.556144329431365,-3.21331711446517));
#8894=CARTESIAN_POINT('Ctrl Pts',(4.61769001547176,-0.48121076433104,-3.20825435836269));
#8895=CARTESIAN_POINT('Ctrl Pts',(4.65670197413009,-0.374094002510949,-3.20098314537484));
#8896=CARTESIAN_POINT('Ctrl Pts',(4.66610330262087,-0.344748712049452,-3.19899026191916));
#8897=CARTESIAN_POINT('Ctrl Pts',(4.67690373392857,-0.305847614166114,-3.19632957539751));
#8898=CARTESIAN_POINT('Ctrl Pts',(4.67935177201027,-0.296594064800206,-3.19569533491674));
#8899=CARTESIAN_POINT('Ctrl Pts',(4.68313781807165,-0.28154317784173,-3.19466111171145));
#8900=CARTESIAN_POINT('Ctrl Pts',(4.68454519643704,-0.275763611550849,-3.19426334430423));
#8901=CARTESIAN_POINT('Ctrl Pts',(4.68716528611193,-0.264637922322687,-3.19349632801746));
#8902=CARTESIAN_POINT('Ctrl Pts',(4.68838457508171,-0.259293495348176,-3.19312729888676));
#8903=CARTESIAN_POINT('Ctrl Pts',(4.69112020017064,-0.246904394060618,-3.19227040691711));
#8904=CARTESIAN_POINT('Ctrl Pts',(4.69260926728713,-0.239853988261029,-3.19178169703675));
#8905=CARTESIAN_POINT('Ctrl Pts',(4.69714974273213,-0.217335695288724,-3.19021715824792));
#8906=CARTESIAN_POINT('Ctrl Pts',(4.69995519319665,-0.201820566466135,-3.18913369440768));
#8907=CARTESIAN_POINT('Ctrl Pts',(4.70581889874727,-0.165208956842626,-3.18656290822938));
#8908=CARTESIAN_POINT('Ctrl Pts',(4.70861743537951,-0.144077077533306,-3.18506810293955));
#8909=CARTESIAN_POINT('Ctrl Pts',(4.717031610013,-0.0638724316287148,-3.17935291486217));
#8910=CARTESIAN_POINT('Ctrl Pts',(4.7187535358822,-0.00448560868510401,
-3.17503018604703));
#8911=CARTESIAN_POINT('Ctrl Pts',(4.71271772414196,0.125161570364879,-3.16550907888864));
#8912=CARTESIAN_POINT('Ctrl Pts',(4.70312976001682,0.195121626808908,-3.16031579482553));
#8913=CARTESIAN_POINT('Ctrl Pts',(4.68514159142383,0.27338733275801,-3.15468723984344));
#8914=CARTESIAN_POINT('Ctrl Pts',(4.6828204263157,0.28293748383211,-3.15400375945776));
#8915=CARTESIAN_POINT('Ctrl Pts',(4.67941435630051,0.296224362767218,-3.15305853801882));
#8916=CARTESIAN_POINT('Ctrl Pts',(4.67843015055881,0.299986147212322,-3.15279156679651));
#8917=CARTESIAN_POINT('Ctrl Pts',(4.67669373836408,0.306491243403072,-3.15233109522539));
#8918=CARTESIAN_POINT('Ctrl Pts',(4.67595019803625,0.309236803032795,-3.15213711568797));
#8919=CARTESIAN_POINT('Ctrl Pts',(4.67435251456974,0.315052737656819,-3.15172702876877));
#8920=CARTESIAN_POINT('Ctrl Pts',(4.67349584063548,0.318122395669769,-3.1515110724618));
#8921=CARTESIAN_POINT('Ctrl Pts',(4.67132482986644,0.325781413123964,-3.15097337925169));
#8922=CARTESIAN_POINT('Ctrl Pts',(4.66999501323815,0.330366388979926,-3.15065251490368));
#8923=CARTESIAN_POINT('Ctrl Pts',(4.66477473877105,0.347964317304035,-3.14942445343302));
#8924=CARTESIAN_POINT('Ctrl Pts',(4.66068699494352,0.360918286318838,-3.14852778654404));
#8925=CARTESIAN_POINT('Ctrl Pts',(4.64949903311173,0.394346254053465,-3.1462259827269));
#8926=CARTESIAN_POINT('Ctrl Pts',(4.64205607681412,0.414700796148441,-3.14483626430258));
#8927=CARTESIAN_POINT('Ctrl Pts',(4.59616468852104,0.530214176758995,-3.13695652331111));
#8928=CARTESIAN_POINT('Ctrl Pts',(4.54597120322335,0.620228405255614,-3.13080422978946));
#8929=CARTESIAN_POINT('Ctrl Pts',(4.46554235428616,0.728431022590795,-3.12221841882979));
#8930=CARTESIAN_POINT('Ctrl Pts',(4.44529301680332,0.753461443599445,-3.12013877275636));
#8931=CARTESIAN_POINT('Ctrl Pts',(4.41762695646553,0.784930613853651,-3.11737826916035));
#8932=CARTESIAN_POINT('Ctrl Pts',(4.4111184186301,0.792151560787731,-3.11673429720841));
#8933=CARTESIAN_POINT('Ctrl Pts',(4.40046232468838,0.803683714867934,-3.11568812872689));
#8934=CARTESIAN_POINT('Ctrl Pts',(4.39636991474247,0.808045437540622,-3.11528824500119));
#8935=CARTESIAN_POINT('Ctrl Pts',(4.3884701358773,0.816337589057383,-3.11451980373157));
#8936=CARTESIAN_POINT('Ctrl Pts',(4.38466823967373,0.820273034408421,-3.11415148542705));
#8937=CARTESIAN_POINT('Ctrl Pts',(4.37584579462664,0.829278935926336,-3.1133001398748));
#8938=CARTESIAN_POINT('Ctrl Pts',(4.37080635692301,0.834330502148808,-3.11281630092054));
#8939=CARTESIAN_POINT('Ctrl Pts',(4.35476144899995,0.850124347571058,-3.11128325649028));
#8940=CARTESIAN_POINT('Ctrl Pts',(4.34359168879005,0.860696652868589,-3.11022684326068));
#8941=CARTESIAN_POINT('Ctrl Pts',(4.31695691172093,0.884935734864475,-3.10773149347546));
#8942=CARTESIAN_POINT('Ctrl Pts',(4.30133372362759,0.898420390301959,-3.10628565668475));
#8943=CARTESIAN_POINT('Ctrl Pts',(4.24195762342701,0.947006308644113,-3.10085503001304));
#8944=CARTESIAN_POINT('Ctrl Pts',(4.19607283038112,0.979375707133186,-3.09677880310597));
#8945=CARTESIAN_POINT('Ctrl Pts',(4.08355915014974,1.04727809421341,-3.0871456659951));
#8946=CARTESIAN_POINT('Ctrl Pts',(4.01546488997766,1.07992985167665,-3.08157798058244));
#8947=CARTESIAN_POINT('Ctrl Pts',(3.93575110257492,1.10913764914287,-3.07563112378125));
#8948=CARTESIAN_POINT('Ctrl Pts',(3.92674910943286,1.11231248295765,-3.07496757098236));
#8949=CARTESIAN_POINT('Ctrl Pts',(3.9140550111687,1.11661665964354,-3.07404402858618));
#8950=CARTESIAN_POINT('Ctrl Pts',(3.91039472619574,1.11783772733574,-3.07377913886759));
#8951=CARTESIAN_POINT('Ctrl Pts',(3.90376503254966,1.12001323850551,-3.0733019843398));
#8952=CARTESIAN_POINT('Ctrl Pts',(3.90079771314711,1.12097391521363,-3.07308936738531));
#8953=CARTESIAN_POINT('Ctrl Pts',(3.89471579394369,1.12291629237651,-3.07265556628039));
#8954=CARTESIAN_POINT('Ctrl Pts',(3.89160087318409,1.12389684448009,-3.07243444833196));
#8955=CARTESIAN_POINT('Ctrl Pts',(3.88357512311059,1.1263866452399,-3.07186734855767));
#8956=CARTESIAN_POINT('Ctrl Pts',(3.87865836036316,1.12787676037447,-3.07152244821973));
#8957=CARTESIAN_POINT('Ctrl Pts',(3.85784106680156,1.13403738478238,-3.07007215887183));
#8958=CARTESIAN_POINT('Ctrl Pts',(3.84185175910993,1.13840445255659,-3.06898279057254));
#8959=CARTESIAN_POINT('Ctrl Pts',(3.79779539720328,1.14944350812838,-3.06603464785777));
#8960=CARTESIAN_POINT('Ctrl Pts',(3.76956603617532,1.15542445294395,-3.06420426936595));
#8961=CARTESIAN_POINT('Ctrl Pts',(3.65236277013015,1.17578968781411,-3.05674162313343));
#8962=CARTESIAN_POINT('Ctrl Pts',(3.56210673468793,1.18097644135648,-3.05129224510835));
#8963=CARTESIAN_POINT('Ctrl Pts',(3.43874818711212,1.17390757964574,-3.04343456534833));
#8964=CARTESIAN_POINT('Ctrl Pts',(3.40545524523167,1.17057265804319,-3.04127573186305));
#8965=CARTESIAN_POINT('Ctrl Pts',(3.36258897377222,1.16442607196494,-3.03842366942584));
#8966=CARTESIAN_POINT('Ctrl Pts',(3.35284466320023,1.16290369014257,-3.03777049843266));
#8967=CARTESIAN_POINT('Ctrl Pts',(3.33719321170105,1.16025663519616,-3.03671303332578));
#8968=CARTESIAN_POINT('Ctrl Pts',(3.33127342281148,1.15920876499731,-3.03631114569044));
#8969=CARTESIAN_POINT('Ctrl Pts',(3.31998938642432,1.15712213755397,-3.03554128387523));
#8970=CARTESIAN_POINT('Ctrl Pts',(3.3146238230945,1.15609128082198,-3.0351735670076));
#8971=CARTESIAN_POINT('Ctrl Pts',(3.30232945122369,1.15364040328501,-3.03432712145705));
#8972=CARTESIAN_POINT('Ctrl Pts',(3.29540592976194,1.15219523805879,-3.03384761236167));
#8973=CARTESIAN_POINT('Ctrl Pts',(3.27380142659997,1.14748220578995,-3.0323422102748));
#8974=CARTESIAN_POINT('Ctrl Pts',(3.25917025366127,1.14399553500785,-3.03130947404064));
#8975=CARTESIAN_POINT('Ctrl Pts',(3.22520160006125,1.13520989456155,-3.0288797077516));
#8976=CARTESIAN_POINT('Ctrl Pts',(3.20592516664892,1.12969553558251,-3.02747626244873));
#8977=CARTESIAN_POINT('Ctrl Pts',(3.13584961030794,1.1076993002196,-3.02228289252604));
#8978=CARTESIAN_POINT('Ctrl Pts',(3.08605149873003,1.08826137209012,-3.01841009580805));
#8979=CARTESIAN_POINT('Ctrl Pts',(2.96575488118993,1.03161149525829,-3.00867214789956));
#8980=CARTESIAN_POINT('Ctrl Pts',(2.89737749811574,0.990496727423987,-3.00277772670497));
#8981=CARTESIAN_POINT('Ctrl Pts',(2.82609590149246,0.937129602496751,-2.99654461758004));
#8982=CARTESIAN_POINT('Ctrl Pts',(2.81859441315035,0.931371119807035,-2.99588768084404));
#8983=CARTESIAN_POINT('Ctrl Pts',(2.80823067980064,0.923215198836997,-2.99497962198354));
#8984=CARTESIAN_POINT('Ctrl Pts',(2.80530948450529,0.920893749918574,-2.9947236181095));
#8985=CARTESIAN_POINT('Ctrl Pts',(2.7999920613324,0.916626653290633,-2.99425759677987));
#8986=CARTESIAN_POINT('Ctrl Pts',(2.79759235621169,0.914685394228212,-2.99404727900163));
#8987=CARTESIAN_POINT('Ctrl Pts',(2.79267853624424,0.910678261920784,-2.99361664491302));
#8988=CARTESIAN_POINT('Ctrl Pts',(2.79016531906168,0.908611378037216,-2.99339640243066));
#8989=CARTESIAN_POINT('Ctrl Pts',(2.78382471910707,0.903352631117224,-2.99284068094873));
#8990=CARTESIAN_POINT('Ctrl Pts',(2.78000892335124,0.900146803362335,-2.99250617943619));
#8991=CARTESIAN_POINT('Ctrl Pts',(2.77156590826644,0.892961521124877,-2.99176559787924));
#8992=CARTESIAN_POINT('Ctrl Pts',(2.76694900595163,0.888970098961088,-2.99136032179021));
#8993=CARTESIAN_POINT('Ctrl Pts',(2.75336838547996,0.877043613453188,-2.99016656850655));
#8994=CARTESIAN_POINT('Ctrl Pts',(2.74449412509974,0.869007341765758,-2.98938437205073));
#8995=CARTESIAN_POINT('Ctrl Pts',(2.71221159401029,0.838864687616953,-2.98652411146555));
#8996=CARTESIAN_POINT('Ctrl Pts',(2.68958869158389,0.815935216623709,-2.98449006959003));
#8997=CARTESIAN_POINT('Ctrl Pts',(2.64741628714215,0.76953118962899,-2.98057109969574));
#8998=CARTESIAN_POINT('Ctrl Pts',(2.62778452086387,0.74616742064803,-2.97868545287518));
#8999=CARTESIAN_POINT('Ctrl Pts',(2.56081044010637,0.659866347285038,-2.971928474251));
#9000=CARTESIAN_POINT('Ctrl Pts',(2.51890383847443,0.592989679325828,-2.96705225778148));
#9001=CARTESIAN_POINT('Ctrl Pts',(2.47711476945722,0.508558740284475,-2.96091314815011));
#9002=CARTESIAN_POINT('Ctrl Pts',(2.47052042962176,0.494547026085853,-2.959895532211));
#9003=CARTESIAN_POINT('Ctrl Pts',(2.46131737641683,0.473947580961091,-2.95839914599736));
#9004=CARTESIAN_POINT('Ctrl Pts',(2.45848862975219,0.467459501193249,-2.95792779670517));
#9005=CARTESIAN_POINT('Ctrl Pts',(2.4535735037439,0.45590280947347,-2.95708795222146));
#9006=CARTESIAN_POINT('Ctrl Pts',(2.4514636859194,0.45084434573589,-2.95672025509591));
#9007=CARTESIAN_POINT('Ctrl Pts',(2.44713671866986,0.440262788288645,-2.95595080791469));
#9008=CARTESIAN_POINT('Ctrl Pts',(2.44492597767211,0.434737258954002,-2.95554885673257));
#9009=CARTESIAN_POINT('Ctrl Pts',(2.43926421024867,0.420269229374129,-2.95449585176128));
#9010=CARTESIAN_POINT('Ctrl Pts',(2.43588036676449,0.411301088013082,-2.95384260188764));
#9011=CARTESIAN_POINT('Ctrl Pts',(2.42088304839541,0.370035825769206,-2.9508336237206));
#9012=CARTESIAN_POINT('Ctrl Pts',(2.41057640581616,0.337284906602885,-2.94843596440213));
#9013=CARTESIAN_POINT('Ctrl Pts',(2.37514083636209,0.204715705984923,-2.93868725117212));
#9014=CARTESIAN_POINT('Ctrl Pts',(2.3617147452602,0.102251104413654,-2.93100628751565));
#9015=CARTESIAN_POINT('Ctrl Pts',(2.36176921551447,-0.000623596785416757,
-2.92357926301356));
#9016=CARTESIAN_POINT('Ctrl Pts',(2.36176921637844,-0.000625226391580778,
-2.9235791453644));
#9017=CARTESIAN_POINT('Ctrl Pts',(2.36177995253325,-0.0208491080398596,
-2.92211908578818));
#9018=CARTESIAN_POINT('Ctrl Pts',(2.36231160441552,-0.0410707918882081,
-2.92067213902583));
#9019=CARTESIAN_POINT('Ctrl Pts',(2.36393814619697,-0.0722942803543454,
-2.91846711246166));
#9020=CARTESIAN_POINT('Ctrl Pts',(2.36466742904508,-0.0833103485689905,
-2.91769478376438));
#9021=CARTESIAN_POINT('Ctrl Pts',(2.36588675799784,-0.0984877076839081,
-2.91663990991943));
#9022=CARTESIAN_POINT('Ctrl Pts',(2.36624423883107,-0.102658677967047,-2.91635097498123));
#9023=CARTESIAN_POINT('Ctrl Pts',(2.36690394968759,-0.109901850026181,-2.91585098981703));
#9024=CARTESIAN_POINT('Ctrl Pts',(2.36719603042186,-0.112974901773122,-2.91563941588688));
#9025=CARTESIAN_POINT('Ctrl Pts',(2.36778565625838,-0.118929848571435,-2.91523054885575));
#9026=CARTESIAN_POINT('Ctrl Pts',(2.36808176065682,-0.121811874484103,-2.91503317878497));
#9027=CARTESIAN_POINT('Ctrl Pts',(2.36874028834502,-0.127996847255564,-2.91461074374743));
#9028=CARTESIAN_POINT('Ctrl Pts',(2.36910605785658,-0.131299391329682,-2.91438586583273));
#9029=CARTESIAN_POINT('Ctrl Pts',(2.37010253801986,-0.139961438132476,-2.91379774505669));
#9030=CARTESIAN_POINT('Ctrl Pts',(2.37075612493424,-0.145318307266515,-2.91343574125296));
#9031=CARTESIAN_POINT('Ctrl Pts',(2.37364228282265,-0.167693218127024,-2.9119301331203));
#9032=CARTESIAN_POINT('Ctrl Pts',(2.37621003124648,-0.184666870926862,-2.91080354726058));
#9033=CARTESIAN_POINT('Ctrl Pts',(2.38355629806838,-0.226954902118574,-2.90802219860602));
#9034=CARTESIAN_POINT('Ctrl Pts',(2.38879601553485,-0.25218064174336,-2.90638596880244));
#9035=CARTESIAN_POINT('Ctrl Pts',(2.40573826379939,-0.322137397521182,-2.90186293844977));
#9036=CARTESIAN_POINT('Ctrl Pts',(2.41925278262559,-0.3663811617874,-2.89901814094692));
#9037=CARTESIAN_POINT('Ctrl Pts',(2.46094290425218,-0.478735797902303,-2.89159887795137));
#9038=CARTESIAN_POINT('Ctrl Pts',(2.49296361809847,-0.545191890575193,-2.88700593960339));
#9039=CARTESIAN_POINT('Ctrl Pts',(2.53773130295301,-0.61942519771123,-2.88133325212123));
#9040=CARTESIAN_POINT('Ctrl Pts',(2.54467449665439,-0.630516104614747,-2.88047081024581));
#9041=CARTESIAN_POINT('Ctrl Pts',(2.55544671078219,-0.647102386879967,-2.87915704588438));
#9042=CARTESIAN_POINT('Ctrl Pts',(2.55914034169745,-0.652684803809364,-2.87871067758816));
#9043=CARTESIAN_POINT('Ctrl Pts',(2.56591382321415,-0.662734762261757,-2.87789928167066));
#9044=CARTESIAN_POINT('Ctrl Pts',(2.56897736423906,-0.667213112322162,-2.87753486806232));
#9045=CARTESIAN_POINT('Ctrl Pts',(2.57563359381759,-0.676800485599777,-2.87674847577718));
#9046=CARTESIAN_POINT('Ctrl Pts',(2.57923618273684,-0.68190239931979,-2.87632613176537));
#9047=CARTESIAN_POINT('Ctrl Pts',(2.58909409001416,-0.695629919435375,-2.87517908045506));
#9048=CARTESIAN_POINT('Ctrl Pts',(2.59542603320923,-0.704199511570753,-2.87445147492619));
#9049=CARTESIAN_POINT('Ctrl Pts',(2.62928880728463,-0.748751358861594,-2.87060648219384));
#9050=CARTESIAN_POINT('Ctrl Pts',(2.65875935563354,-0.783204399808276,-2.86741420673774));
#9051=CARTESIAN_POINT('Ctrl Pts',(2.76508018517716,-0.893892150996087,-2.85638692434851));
#9052=CARTESIAN_POINT('Ctrl Pts',(2.85040651993699,-0.961207661226993,-2.8482589597979));
#9053=CARTESIAN_POINT('Ctrl Pts',(2.95210904712649,-1.02085220409374,-2.83992351738191));
#9054=CARTESIAN_POINT('Ctrl Pts',(2.96056311954913,-1.02567040445183,-2.83924029034334));
#9055=CARTESIAN_POINT('Ctrl Pts',(2.97369773304519,-1.03294201375371,-2.83819467877136));
#9056=CARTESIAN_POINT('Ctrl Pts',(2.97833649597358,-1.03546951189299,-2.8378284118626));
#9057=CARTESIAN_POINT('Ctrl Pts',(2.98698223012976,-1.04010510128481,-2.83715155103884));
#9058=CARTESIAN_POINT('Ctrl Pts',(2.99098463496274,-1.04222145259095,-2.83684049007336));
#9059=CARTESIAN_POINT('Ctrl Pts',(2.99775568870063,-1.045751971641,-2.83631821348526));
#9060=CARTESIAN_POINT('Ctrl Pts',(3.00051788250106,-1.04717833629616,-2.8361062587771));
#9061=CARTESIAN_POINT('Ctrl Pts',(3.00582895168737,-1.04989432818294,-2.83570087696403));
#9062=CARTESIAN_POINT('Ctrl Pts',(3.00837691587402,-1.05118564259061,-2.83550734240186));
#9063=CARTESIAN_POINT('Ctrl Pts',(3.0144471776645,-1.05423435985338,-2.8350484510906));
#9064=CARTESIAN_POINT('Ctrl Pts',(3.01797366531702,-1.05598341342791,-2.83478360193138));
#9065=CARTESIAN_POINT('Ctrl Pts',(3.03049394491246,-1.06211515308135,-2.83384921154611));
#9066=CARTESIAN_POINT('Ctrl Pts',(3.03953504296172,-1.06640103384721,-2.8331852396339));
#9067=CARTESIAN_POINT('Ctrl Pts',(3.10446791240979,-1.09617469918957,-2.82848527632254));
#9068=CARTESIAN_POINT('Ctrl Pts',(3.16223100034578,-1.11737377807566,-2.82466175740634));
#9069=CARTESIAN_POINT('Ctrl Pts',(3.28255192659474,-1.15112901954021,-2.81692226045837));
#9070=CARTESIAN_POINT('Ctrl Pts',(3.34499733525782,-1.16331031487389,-2.81301786135179));
#9071=CARTESIAN_POINT('Ctrl Pts',(3.43177991591932,-1.17305338855851,-2.80747544948084));
#9072=CARTESIAN_POINT('Ctrl Pts',(3.45551501799545,-1.17499156879255,-2.80594867875171));
#9073=CARTESIAN_POINT('Ctrl Pts',(3.49642316028897,-1.17708626329455,-2.80328652079047));
#9074=CARTESIAN_POINT('Ctrl Pts',(3.51357121823404,-1.17758905744754,-2.80216136987946));
#9075=CARTESIAN_POINT('Ctrl Pts',(3.53817314099144,-1.17777279299101,-2.80053111148832));
#9076=CARTESIAN_POINT('Ctrl Pts',(3.54562303807762,-1.17775774268812,-2.80003533961058));
#9077=CARTESIAN_POINT('Ctrl Pts',(3.55859111690027,-1.17760850107451,-2.79916846485678));
#9078=CARTESIAN_POINT('Ctrl Pts',(3.56410948687455,-1.17750619284652,-2.79879835572167));
#9079=CARTESIAN_POINT('Ctrl Pts',(3.57547557982453,-1.17721553695408,-2.79803343347121));
#9080=CARTESIAN_POINT('Ctrl Pts',(3.581323016198,-1.17702239518642,-2.79763848250897));
#9081=CARTESIAN_POINT('Ctrl Pts',(3.59628177395603,-1.17641669502769,-2.79662435825079));
#9082=CARTESIAN_POINT('Ctrl Pts',(3.60539004330609,-1.17594185711139,-2.79600328115178));
#9083=CARTESIAN_POINT('Ctrl Pts',(3.64131579082277,-1.17365026633381,-2.79353885603012));
#9084=CARTESIAN_POINT('Ctrl Pts',(3.66807143424096,-1.17102160798452,-2.79167083174068));
#9085=CARTESIAN_POINT('Ctrl Pts',(3.71514288197416,-1.16476440979611,-2.78832427819953));
#9086=CARTESIAN_POINT('Ctrl Pts',(3.73549795867999,-1.1615128274658,-2.78685710071484));
#9087=CARTESIAN_POINT('Ctrl Pts',(3.83437104187927,-1.14304559977494,-2.77963608550316));
#9088=CARTESIAN_POINT('Ctrl Pts',(3.9112827884676,-1.12039316030081,-2.77370749788644));
#9089=CARTESIAN_POINT('Ctrl Pts',(4.01685826394394,-1.07722098807654,-2.76540715412209));
#9090=CARTESIAN_POINT('Ctrl Pts',(4.04784516790297,-1.06294985473338,-2.76295256712908));
#9091=CARTESIAN_POINT('Ctrl Pts',(4.07816927004253,-1.04735428743277,-2.76055935511047));
#9092=CARTESIAN_POINT('Ctrl Pts',(4.07816899834492,-1.04735442716575,-2.6623694009368));
#9093=CARTESIAN_POINT('Ctrl Pts',(4.0335762669856,-1.07028828012076,-2.66601213181191));
#9094=CARTESIAN_POINT('Ctrl Pts',(3.98753809253346,-1.0903643388365,-2.66970861591428));
#9095=CARTESIAN_POINT('Ctrl Pts',(3.89128984941738,-1.12519885517188,-2.67720140153078));
#9096=CARTESIAN_POINT('Ctrl Pts',(3.84111741288379,-1.13967314890724,-2.68098522172963));
#9097=CARTESIAN_POINT('Ctrl Pts',(3.78334776792184,-1.152254753361,-2.68509742216502));
#9098=CARTESIAN_POINT('Ctrl Pts',(3.77653707951909,-1.15367496282613,-2.68557840510683));
#9099=CARTESIAN_POINT('Ctrl Pts',(3.76612376885243,-1.15575030428102,-2.686307588158));
#9100=CARTESIAN_POINT('Ctrl Pts',(3.76253015568023,-1.15644909620269,-2.68655810071));
#9101=CARTESIAN_POINT('Ctrl Pts',(3.75594503727697,-1.15769776081088,-2.68701501927083));
#9102=CARTESIAN_POINT('Ctrl Pts',(3.75295464911626,-1.15825280436929,-2.68722170114632));
#9103=CARTESIAN_POINT('Ctrl Pts',(3.74619844681159,-1.15947976322849,-2.68768684842611));
#9104=CARTESIAN_POINT('Ctrl Pts',(3.74243148748152,-1.16014492118331,-2.68794493579724));
#9105=CARTESIAN_POINT('Ctrl Pts',(3.73268641675675,-1.16181675872849,-2.68860951174878));
#9106=CARTESIAN_POINT('Ctrl Pts',(3.72670356511524,-1.16279567145485,-2.68901451683044));
#9107=CARTESIAN_POINT('Ctrl Pts',(3.6864822382747,-1.16905819113362,-2.6917187615668));
#9108=CARTESIAN_POINT('Ctrl Pts',(3.65202899538887,-1.17287563292434,-2.69394545358489));
#9109=CARTESIAN_POINT('Ctrl Pts',(3.58929340211189,-1.17703614795284,-2.69791828714987));
#9110=CARTESIAN_POINT('Ctrl Pts',(3.56107348878191,-1.17789095713726,-2.69967561287454));
#9111=CARTESIAN_POINT('Ctrl Pts',(3.48487642248419,-1.17745942740425,-2.70440004502096));
#9112=CARTESIAN_POINT('Ctrl Pts',(3.43696596257267,-1.17425691029762,-2.70735019626798));
#9113=CARTESIAN_POINT('Ctrl Pts',(3.33649323509623,-1.16134375120642,-2.71368497026683));
#9114=CARTESIAN_POINT('Ctrl Pts',(3.28413075753254,-1.15096243469239,-2.7170749199365));
#9115=CARTESIAN_POINT('Ctrl Pts',(3.22219955533574,-1.13424895742127,-2.72129091886645));
#9116=CARTESIAN_POINT('Ctrl Pts',(3.21178298297185,-1.13128308424335,-2.72200707908536));
#9117=CARTESIAN_POINT('Ctrl Pts',(3.19544928162242,-1.12638792875238,-2.72314188347338));
#9118=CARTESIAN_POINT('Ctrl Pts',(3.189503838138,-1.12455463206792,-2.72355743895784));
#9119=CARTESIAN_POINT('Ctrl Pts',(3.17839984088432,-1.1210340913855,-2.72433835221193));
#9120=CARTESIAN_POINT('Ctrl Pts',(3.17323786273431,-1.1193581229451,-2.72470333613297));
#9121=CARTESIAN_POINT('Ctrl Pts',(3.16170697771525,-1.11552602427491,-2.7255231221525));
#9122=CARTESIAN_POINT('Ctrl Pts',(3.1553446233849,-1.11335092378222,-2.72597853192961));
#9123=CARTESIAN_POINT('Ctrl Pts',(3.13920211123965,-1.1076774338607,-2.72714201907597));
#9124=CARTESIAN_POINT('Ctrl Pts',(3.12944913969143,-1.10410398315409,-2.72785252619133));
#9125=CARTESIAN_POINT('Ctrl Pts',(3.04922531641467,-1.07350073234107,-2.73376105817357));
#9126=CARTESIAN_POINT('Ctrl Pts',(2.98146806609331,-1.03988796688262,-2.73918081187918));
#9127=CARTESIAN_POINT('Ctrl Pts',(2.86829878120403,-0.969485798722418,-2.74893061046611));
#9128=CARTESIAN_POINT('Ctrl Pts',(2.8215111047524,-0.935363141093665,-2.75320181318344));
#9129=CARTESIAN_POINT('Ctrl Pts',(2.76180456356438,-0.884689017107384,-2.75885673514513));
#9130=CARTESIAN_POINT('Ctrl Pts',(2.74653778073392,-0.871031162163133,-2.7603222094531));
#9131=CARTESIAN_POINT('Ctrl Pts',(2.72214329356571,-0.848034233290433,-2.76268655246011));
#9132=CARTESIAN_POINT('Ctrl Pts',(2.71280125319164,-0.838929620280964,-2.76359773775796));
#9133=CARTESIAN_POINT('Ctrl Pts',(2.70030074536453,-0.826335157333877,-2.76482260626028));
#9134=CARTESIAN_POINT('Ctrl Pts',(2.69700949265504,-0.822979223762437,-2.76514564572327));
#9135=CARTESIAN_POINT('Ctrl Pts',(2.6915314441139,-0.817326213328243,-2.76568410084221));
#9136=CARTESIAN_POINT('Ctrl Pts',(2.68933370360339,-0.815039874042446,-2.76590033690781));
#9137=CARTESIAN_POINT('Ctrl Pts',(2.68517389987865,-0.810677239313141,-2.76630997969622));
#9138=CARTESIAN_POINT('Ctrl Pts',(2.68321011946522,-0.808602645187202,-2.76650352192994));
#9139=CARTESIAN_POINT('Ctrl Pts',(2.67855715943709,-0.803651163410908,-2.76696253162854));
#9140=CARTESIAN_POINT('Ctrl Pts',(2.67587480087992,-0.800767869932894,-2.76722749067123));
#9141=CARTESIAN_POINT('Ctrl Pts',(2.66642093822593,-0.790503059292525,-2.768162799715));
#9142=CARTESIAN_POINT('Ctrl Pts',(2.65972896781401,-0.783048419406329,-2.76882756556243));
#9143=CARTESIAN_POINT('Ctrl Pts',(2.61337929261124,-0.730071959822742,-2.77345875290756));
#9144=CARTESIAN_POINT('Ctrl Pts',(2.57717310846499,-0.681639268235826,-2.77722018773758));
#9145=CARTESIAN_POINT('Ctrl Pts',(2.50919862475178,-0.574425642562403,-2.78508434954684));
#9146=CARTESIAN_POINT('Ctrl Pts',(2.47839070263651,-0.515297023926705,-2.78917202812655));
#9147=CARTESIAN_POINT('Ctrl Pts',(2.43954676301574,-0.422289475615677,-2.79558046347222));
#9148=CARTESIAN_POINT('Ctrl Pts',(2.42773646914373,-0.390136619642021,-2.79779068394603));
#9149=CARTESIAN_POINT('Ctrl Pts',(2.41443695070717,-0.348392093178328,-2.80067799789226));
#9150=CARTESIAN_POINT('Ctrl Pts',(2.41164124116129,-0.339232103672854,-2.80131257946533));
#9151=CARTESIAN_POINT('Ctrl Pts',(2.40729053770484,-0.324328611294449,-2.80234718099593));
#9152=CARTESIAN_POINT('Ctrl Pts',(2.40566677569756,-0.31860550845748,-2.80274498196999));
#9153=CARTESIAN_POINT('Ctrl Pts',(2.40263058552118,-0.307586924253439,-2.80351194039831));
#9154=CARTESIAN_POINT('Ctrl Pts',(2.40121162223718,-0.302293391912137,-2.80388087728166));
#9155=CARTESIAN_POINT('Ctrl Pts',(2.39804435933927,-0.290139133727082,-2.80472916029831));
#9156=CARTESIAN_POINT('Ctrl Pts',(2.3963208896416,-0.283272216609131,-2.80520928361004));
#9157=CARTESIAN_POINT('Ctrl Pts',(2.39102206727324,-0.26132351785221,-2.80674687234254));
#9158=CARTESIAN_POINT('Ctrl Pts',(2.38768260469289,-0.246187050675711,-2.80781172133476));
#9159=CARTESIAN_POINT('Ctrl Pts',(2.36935963841847,-0.154577960164166,-2.8142863291644));
#9160=CARTESIAN_POINT('Ctrl Pts',(2.3617001877326,-0.0768513395504396,-2.81992377176816));
#9161=CARTESIAN_POINT('Ctrl Pts',(2.36183524319387,0.0748995426607242,-2.83105050793921));
#9162=CARTESIAN_POINT('Ctrl Pts',(2.36884709221586,0.14858707453323,-2.83650379562567));
#9163=CARTESIAN_POINT('Ctrl Pts',(2.38452687808435,0.230610412638048,-2.84235479586892));
#9164=CARTESIAN_POINT('Ctrl Pts',(2.38645413805029,0.240061249095705,-2.84302540859916));
#9165=CARTESIAN_POINT('Ctrl Pts',(2.38931827618977,0.253275066697978,-2.84395707350117));
#9166=CARTESIAN_POINT('Ctrl Pts',(2.39015790003458,0.257058412619488,-2.84422313681158));
#9167=CARTESIAN_POINT('Ctrl Pts',(2.3917078613311,0.263883099285725,-2.84470175377106));
#9168=CARTESIAN_POINT('Ctrl Pts',(2.39241164933604,0.2669258830746,-2.84491466651426));
#9169=CARTESIAN_POINT('Ctrl Pts',(2.39387441982059,0.273137436772038,-2.84534828083118));
#9170=CARTESIAN_POINT('Ctrl Pts',(2.39463446173581,0.276305914225063,-2.84556892121881));
#9171=CARTESIAN_POINT('Ctrl Pts',(2.39661924858808,0.284431319942791,-2.84613344178053));
#9172=CARTESIAN_POINT('Ctrl Pts',(2.39786311222177,0.289383575791147,-2.8464762589737));
#9173=CARTESIAN_POINT('Ctrl Pts',(2.40321135187452,0.310105461421779,-2.84790609600727));
#9174=CARTESIAN_POINT('Ctrl Pts',(2.40761078629632,0.325797988927075,-2.84897765068756));
#9175=CARTESIAN_POINT('Ctrl Pts',(2.42049043011143,0.3683227135144,-2.85186331623996));
#9176=CARTESIAN_POINT('Ctrl Pts',(2.42960900065448,0.394951357489642,-2.8536504727228));
#9177=CARTESIAN_POINT('Ctrl Pts',(2.47001081814081,0.500441992274455,-2.86074316543338));
#9178=CARTESIAN_POINT('Ctrl Pts',(2.50881643998352,0.576144737026474,-2.86588065053091));
#9179=CARTESIAN_POINT('Ctrl Pts',(2.57675976314412,0.679484183467396,-2.8737022703326));
#9180=CARTESIAN_POINT('Ctrl Pts',(2.59969254572535,0.710865572105115,-2.87619844151437));
#9181=CARTESIAN_POINT('Ctrl Pts',(2.63064319301569,0.749097337641925,-2.8794346587919));
#9182=CARTESIAN_POINT('Ctrl Pts',(2.63725987636683,0.757053840289884,-2.88011944859016));
#9183=CARTESIAN_POINT('Ctrl Pts',(2.64795330045068,0.769573255148537,-2.88121571921039));
#9184=CARTESIAN_POINT('Ctrl Pts',(2.65196233903132,0.774193492121676,-2.88162445988091));
#9185=CARTESIAN_POINT('Ctrl Pts',(2.65924507690931,0.78245560395874,-2.88236305960074));
#9186=CARTESIAN_POINT('Ctrl Pts',(2.66250586409672,0.786108714098411,-2.88269238206574));
#9187=CARTESIAN_POINT('Ctrl Pts',(2.67022557207439,0.794649407414818,-2.88346888193945));
#9188=CARTESIAN_POINT('Ctrl Pts',(2.67470304495316,0.799519922078523,-2.8839168274462));
#9189=CARTESIAN_POINT('Ctrl Pts',(2.68789710546321,0.813631674369067,-2.88522997529913));
#9190=CARTESIAN_POINT('Ctrl Pts',(2.69672222941865,0.822769673289093,-2.88609975058559));
#9191=CARTESIAN_POINT('Ctrl Pts',(2.75544243813209,0.881635529218473,-2.89183407931891));
#9192=CARTESIAN_POINT('Ctrl Pts',(2.80955700845613,0.926935598762338,-2.89688685172822));
#9193=CARTESIAN_POINT('Ctrl Pts',(2.92891917880187,1.00989025676959,-2.90750836594389));
#9194=CARTESIAN_POINT('Ctrl Pts',(2.99439671839709,1.04668667507222,-2.91306538149354));
#9195=CARTESIAN_POINT('Ctrl Pts',(3.07927804988984,1.08424763401174,-2.919668682244));
#9196=CARTESIAN_POINT('Ctrl Pts',(3.09579125817803,1.09110972947562,-2.9209262365287));
#9197=CARTESIAN_POINT('Ctrl Pts',(3.11756094675155,1.09958011736903,-2.92254340301155));
#9198=CARTESIAN_POINT('Ctrl Pts',(3.12268045111398,1.10153105304701,-2.92292080691102));
#9199=CARTESIAN_POINT('Ctrl Pts',(3.13094325152188,1.10461397690072,-2.92352506638373));
#9200=CARTESIAN_POINT('Ctrl Pts',(3.13407800040985,1.10576841023846,-2.92375319036565));
#9201=CARTESIAN_POINT('Ctrl Pts',(3.14014190090279,1.10797230814809,-2.92419225802817));
#9202=CARTESIAN_POINT('Ctrl Pts',(3.14307033957583,1.10902351782215,-2.92440329559957));
#9203=CARTESIAN_POINT('Ctrl Pts',(3.15014043093986,1.11152985715307,-2.92491045940089));
#9204=CARTESIAN_POINT('Ctrl Pts',(3.15428617306356,1.11297347874417,-2.9252059207994));
#9205=CARTESIAN_POINT('Ctrl Pts',(3.16879417479833,1.11793464719039,-2.92623348568788));
#9206=CARTESIAN_POINT('Ctrl Pts',(3.17919767980351,1.12133105717032,-2.92695897524762));
#9207=CARTESIAN_POINT('Ctrl Pts',(3.20503835131956,1.12937041381321,-2.92873651172546));
#9208=CARTESIAN_POINT('Ctrl Pts',(3.22052671523768,1.13384249926455,-2.92978056944618));
#9209=CARTESIAN_POINT('Ctrl Pts',(3.28711731929589,1.15159711617302,-2.9341977534465));
#9210=CARTESIAN_POINT('Ctrl Pts',(3.33899277892716,1.16175411399418,-2.93746206694308));
#9211=CARTESIAN_POINT('Ctrl Pts',(3.47218680818687,1.17864177879736,-2.94576709366524));
#9212=CARTESIAN_POINT('Ctrl Pts',(3.55383019208463,1.18047584862365,-2.95080150113667));
#9213=CARTESIAN_POINT('Ctrl Pts',(3.65036408158042,1.17262351110741,-2.95711383275943));
#9214=CARTESIAN_POINT('Ctrl Pts',(3.66569638951891,1.17107291109217,-2.95812658599492));
#9215=CARTESIAN_POINT('Ctrl Pts',(3.68800579075667,1.16837350421285,-2.9596170929776));
#9216=CARTESIAN_POINT('Ctrl Pts',(3.69501036944245,1.16746194947664,-2.96008750865481));
#9217=CARTESIAN_POINT('Ctrl Pts',(3.70743185487514,1.16573168505209,-2.96092623525085));
#9218=CARTESIAN_POINT('Ctrl Pts',(3.71285209198115,1.16493807835835,-2.96129375483313));
#9219=CARTESIAN_POINT('Ctrl Pts',(3.7241541323763,1.16320266088734,-2.9620633854663));
#9220=CARTESIAN_POINT('Ctrl Pts',(3.73003470803057,1.16225398504054,-2.96246570129351));
#9221=CARTESIAN_POINT('Ctrl Pts',(3.74538514863154,1.15965796779391,-2.96352090887798));
#9222=CARTESIAN_POINT('Ctrl Pts',(3.7548423262836,1.15793926008036,-2.96417601432317));
#9223=CARTESIAN_POINT('Ctrl Pts',(3.79827410539926,1.14949569767008,-2.96720840084931));
#9224=CARTESIAN_POINT('Ctrl Pts',(3.83195960865803,1.1413906570153,-2.96962842398467));
#9225=CARTESIAN_POINT('Ctrl Pts',(3.9305775594233,1.11301005192873,-2.97692129466239));
#9226=CARTESIAN_POINT('Ctrl Pts',(3.99416128827089,1.08858471369999,-2.98190543918507));
#9227=CARTESIAN_POINT('Ctrl Pts',(4.07809681896068,1.04769911045244,-2.98875613486848));
#9228=CARTESIAN_POINT('Ctrl Pts',(4.10055312323137,1.03584760849696,-2.99061629496205));
#9229=CARTESIAN_POINT('Ctrl Pts',(4.13649242886478,1.01536849010507,-2.99362343919519));
#9230=CARTESIAN_POINT('Ctrl Pts',(4.15021358238763,1.00717556059032,-2.99477893875998));
#9231=CARTESIAN_POINT('Ctrl Pts',(4.18385514791999,0.986147759027043,-2.99762386402038));
#9232=CARTESIAN_POINT('Ctrl Pts',(4.20356425842518,0.972985382392181,-2.99930126104937));
#9233=CARTESIAN_POINT('Ctrl Pts',(4.22778394907507,0.955731644877706,-3.0013638055988));
#9234=CARTESIAN_POINT('Ctrl Pts',(4.2326766615559,0.952189097687222,-3.0017805295991));
#9235=CARTESIAN_POINT('Ctrl Pts',(4.24033242442056,0.946555692800768,-3.00243241348149));
#9236=CARTESIAN_POINT('Ctrl Pts',(4.24311378988524,0.944490078365305,-3.00266920817979));
#9237=CARTESIAN_POINT('Ctrl Pts',(4.24834109212685,0.94057205414652,-3.0031141079217));
#9238=CARTESIAN_POINT('Ctrl Pts',(4.25078888783022,0.938722373484953,-3.00332237844579));
#9239=CARTESIAN_POINT('Ctrl Pts',(4.25650196318259,0.934370102917066,-3.00380837484998));
#9240=CARTESIAN_POINT('Ctrl Pts',(4.25976139332397,0.931859943971826,-3.00408557452722));
#9241=CARTESIAN_POINT('Ctrl Pts',(4.2703463713036,0.92361950331609,-3.00498579089503));
#9242=CARTESIAN_POINT('Ctrl Pts',(4.27761742887499,0.917819348700225,-3.00560418907907));
#9243=CARTESIAN_POINT('Ctrl Pts',(4.31722890209964,0.885445889293677,-3.00897802170675));
#9244=CARTESIAN_POINT('Ctrl Pts',(4.34820714564328,0.857246388547044,-3.01163524727034));
#9245=CARTESIAN_POINT('Ctrl Pts',(4.42941672544203,0.774991806784186,-3.01886716324334));
#9246=CARTESIAN_POINT('Ctrl Pts',(4.47617196535344,0.717782524193531,-3.02335472003506));
#9247=CARTESIAN_POINT('Ctrl Pts',(4.54221317293923,0.619436069024034,-3.03080749755189));
#9248=CARTESIAN_POINT('Ctrl Pts',(4.56501481159752,0.580908164784793,-3.03366873407391));
#9249=CARTESIAN_POINT('Ctrl Pts',(4.59044763483391,0.531748927645906,-3.03730711659445));
#9250=CARTESIAN_POINT('Ctrl Pts',(4.5951988950759,0.522252683228913,-3.03800929981587));
#9251=CARTESIAN_POINT('Ctrl Pts',(4.60253594345096,0.5070789334289,-3.03913092362594));
#9252=CARTESIAN_POINT('Ctrl Pts',(4.60520621607486,0.501442740531811,-3.03954746167587));
#9253=CARTESIAN_POINT('Ctrl Pts',(4.6101156057203,0.490864052200142,-3.04032925083983));
#9254=CARTESIAN_POINT('Ctrl Pts',(4.61236558545537,0.485926756351989,-3.04069412011171));
#9255=CARTESIAN_POINT('Ctrl Pts',(4.61731886118822,0.474855309311859,-3.04151238006665));
#9256=CARTESIAN_POINT('Ctrl Pts',(4.6200040459766,0.468713311139167,-3.04196636822741));
#9257=CARTESIAN_POINT('Ctrl Pts',(4.62779530919577,0.450469066727201,-3.04331523884543));
#9258=CARTESIAN_POINT('Ctrl Pts',(4.63275137798849,0.438304288431218,-3.04421508189992));
#9259=CARTESIAN_POINT('Ctrl Pts',(4.66604231991797,0.352511327546618,-3.05056683363867));
#9260=CARTESIAN_POINT('Ctrl Pts',(4.68711461112448,0.276295233872228,-3.05625822540346));
#9261=CARTESIAN_POINT('Ctrl Pts',(4.71336463499763,0.122823006347651,-3.06766803820147));
#9262=CARTESIAN_POINT('Ctrl Pts',(4.71887708067265,0.0459944917971725,-3.07335114027535));
#9263=CARTESIAN_POINT('Ctrl Pts',(4.71661769191039,-0.040292448793193,-3.07939638705071));
#9264=CARTESIAN_POINT('Ctrl Pts',(4.7162557612288,-0.0497536006386948,-3.08005447272371));
#9265=CARTESIAN_POINT('Ctrl Pts',(4.71558647540485,-0.0630496367147106,
-3.08097167532275));
#9266=CARTESIAN_POINT('Ctrl Pts',(4.71537437936358,-0.0668886480235825,
-3.08123560754887));
#9267=CARTESIAN_POINT('Ctrl Pts',(4.71495642520805,-0.0738359208558632,
-3.08171153084766));
#9268=CARTESIAN_POINT('Ctrl Pts',(4.71475702857496,-0.0769445305130917,
-3.08192386863788));
#9269=CARTESIAN_POINT('Ctrl Pts',(4.7143230205281,-0.083314994928684,-3.08235769795794));
#9270=CARTESIAN_POINT('Ctrl Pts',(4.71408715356602,-0.0865767191283937,
-3.08257911951936));
#9271=CARTESIAN_POINT('Ctrl Pts',(4.71344409921951,-0.0949824625354806,
-3.08314802887223));
#9272=CARTESIAN_POINT('Ctrl Pts',(4.71301668094232,-0.100124931904641,-3.08349442159543));
#9273=CARTESIAN_POINT('Ctrl Pts',(4.71105559052224,-0.121978733833372,-3.08496006975015));
#9274=CARTESIAN_POINT('Ctrl Pts',(4.70919855654215,-0.138660015302232,-3.08606287801184));
#9275=CARTESIAN_POINT('Ctrl Pts',(4.70311045986344,-0.184428137373731,-3.08905871835853));
#9276=CARTESIAN_POINT('Ctrl Pts',(4.69814614018654,-0.213406222610518,-3.09092222271414));
#9277=CARTESIAN_POINT('Ctrl Pts',(4.67176970809976,-0.338942110519832,-3.09896414320742));
#9278=CARTESIAN_POINT('Ctrl Pts',(4.63933208403852,-0.432764229062663,-3.10492954575326));
#9279=CARTESIAN_POINT('Ctrl Pts',(4.58417377415846,-0.544474066613465,-3.11292500272328));
#9280=CARTESIAN_POINT('Ctrl Pts',(4.57204550526483,-0.567137079342937,-3.11459516879936));
#9281=CARTESIAN_POINT('Ctrl Pts',(4.55469807558289,-0.597149102400174,-3.11688292310302));
#9282=CARTESIAN_POINT('Ctrl Pts',(4.55012130311004,-0.604862449771233,-3.11747786294999));
#9283=CARTESIAN_POINT('Ctrl Pts',(4.54243145243252,-0.617491391945533,-3.11846390342629));
#9284=CARTESIAN_POINT('Ctrl Pts',(4.53936919452817,-0.622437621377973,-3.11885316566017));
#9285=CARTESIAN_POINT('Ctrl Pts',(4.53332257392306,-0.632044496402879,-3.11961534360429));
#9286=CARTESIAN_POINT('Ctrl Pts',(4.53034175313901,-0.636707200164753,-3.11998812283273));
#9287=CARTESIAN_POINT('Ctrl Pts',(4.52322112801467,-0.647674431118855,-3.12087181936196));
#9288=CARTESIAN_POINT('Ctrl Pts',(4.51905344718641,-0.653960478284892,-3.12138375493938));
#9289=CARTESIAN_POINT('Ctrl Pts',(4.50490111068044,-0.674867392270231,-3.1231049975264));
#9290=CARTESIAN_POINT('Ctrl Pts',(4.49464761806124,-0.689302458850134,-3.12432425689994));
#9291=CARTESIAN_POINT('Ctrl Pts',(4.43174018789539,-0.773765068565763,-3.131648665262));
#9292=CARTESIAN_POINT('Ctrl Pts',(4.37173890373178,-0.837959298383006,-3.1380419329809));
#9293=CARTESIAN_POINT('Ctrl Pts',(4.25928925017479,-0.934170902709694,-3.14890258317132));
#9294=CARTESIAN_POINT('Ctrl Pts',(4.21042926884041,-0.969858418313633,-3.15332771524153));
#9295=CARTESIAN_POINT('Ctrl Pts',(4.15052345754858,-1.00691062518918,-3.15826714305432));
#9296=CARTESIAN_POINT('Ctrl Pts',(4.14193749774653,-1.01207085895719,-3.15896405732997));
#9297=CARTESIAN_POINT('Ctrl Pts',(4.12988556169194,-1.01910644785608,-3.15992597233075));
#9298=CARTESIAN_POINT('Ctrl Pts',(4.12647472527301,-1.02107473113599,-3.1601964072787));
#9299=CARTESIAN_POINT('Ctrl Pts',(4.1205727225867,-1.02444123919993,-3.16066118221608));
#9300=CARTESIAN_POINT('Ctrl Pts',(4.11808625028956,-1.02584756089346,-3.16085602253505));
#9301=CARTESIAN_POINT('Ctrl Pts',(4.11282860208563,-1.02879603309051,-3.16126593870442));
#9302=CARTESIAN_POINT('Ctrl Pts',(4.11005626905409,-1.03033606280896,-3.16148087406596));
#9303=CARTESIAN_POINT('Ctrl Pts',(4.1031595129035,-1.03413083585424,-3.16201265489975));
#9304=CARTESIAN_POINT('Ctrl Pts',(4.09902769247929,-1.0363721522411,-3.16232866844552));
#9305=CARTESIAN_POINT('Ctrl Pts',(4.08933494865176,-1.04155514270696,-3.16306426060349));
#9306=CARTESIAN_POINT('Ctrl Pts',(4.08376370001831,-1.04447709396206,-3.16348268836972));
#9307=CARTESIAN_POINT('Ctrl Pts',(4.07816926753082,-1.04735428872454,-3.16389876579091));
#9308=CARTESIAN_POINT('Origin',(3.53951905042299,8.32667268468867E-16,0.924367114736157));
#9309=CARTESIAN_POINT('',(4.07816926790565,-1.04735428853177,-3.76191690485895));
#9310=CARTESIAN_POINT('',(4.07816923053759,-1.04735430775001,-3.66210420774532));
#9311=CARTESIAN_POINT('',(4.07816926754759,-1.04735428871592,0.924367114736157));
#9312=CARTESIAN_POINT('Ctrl Pts',(4.07816926790565,-1.04735428853177,-3.76191690485895));
#9313=CARTESIAN_POINT('Ctrl Pts',(4.07913040768384,-1.04685997810002,-3.76184957489129));
#9314=CARTESIAN_POINT('Ctrl Pts',(4.08009089746488,-1.0463643289823,-3.761782224073));
#9315=CARTESIAN_POINT('Ctrl Pts',(4.11564773853268,-1.02795362310974,-3.75928643561599));
#9316=CARTESIAN_POINT('Ctrl Pts',(4.14933213202587,-1.00833553976734,-3.75683339652415));
#9317=CARTESIAN_POINT('Ctrl Pts',(4.19576812665263,-0.978111870791754,-3.75327013250654));
#9318=CARTESIAN_POINT('Ctrl Pts',(4.20936541715728,-0.96885060086797,-3.75220341416066));
#9319=CARTESIAN_POINT('Ctrl Pts',(4.23326615670184,-0.951827855217013,-3.75028257824101));
#9320=CARTESIAN_POINT('Ctrl Pts',(4.24364462199304,-0.944176080840029,-3.74943248778705));
#9321=CARTESIAN_POINT('Ctrl Pts',(4.25918621132288,-0.932318900452617,-3.74813376356517));
#9322=CARTESIAN_POINT('Ctrl Pts',(4.26444296706617,-0.928237397783566,-3.74768991086955));
#9323=CARTESIAN_POINT('Ctrl Pts',(4.2739203505149,-0.920749264722594,-3.74688117308109));
#9324=CARTESIAN_POINT('Ctrl Pts',(4.27815260316191,-0.917357591755194,-3.74651688280406));
#9325=CARTESIAN_POINT('Ctrl Pts',(4.28723076988238,-0.909978914539727,-3.74572858673261));
#9326=CARTESIAN_POINT('Ctrl Pts',(4.29206852757928,-0.905982186427791,-3.74530420012196));
#9327=CARTESIAN_POINT('Ctrl Pts',(4.30513347654585,-0.895011693009504,-3.74414616680766));
#9328=CARTESIAN_POINT('Ctrl Pts',(4.31329701650725,-0.88796341473122,-3.74340952778165));
#9329=CARTESIAN_POINT('Ctrl Pts',(4.35696903772125,-0.84919807072921,-3.73939614747191));
#9330=CARTESIAN_POINT('Ctrl Pts',(4.39062172332617,-0.815466138952654,-3.73603627742989));
#9331=CARTESIAN_POINT('Ctrl Pts',(4.47369508999095,-0.72143867311156,-3.72700399104586));
#9332=CARTESIAN_POINT('Ctrl Pts',(4.5193364470668,-0.658114769689083,-3.72123031367233));
#9333=CARTESIAN_POINT('Ctrl Pts',(4.57154702260122,-0.568068013996911,-3.71366271554842));
#9334=CARTESIAN_POINT('Ctrl Pts',(4.58394252942266,-0.544942914614651,-3.71177235849283));
#9335=CARTESIAN_POINT('Ctrl Pts',(4.60019133093315,-0.512034166401618,-3.70917251056938));
#9336=CARTESIAN_POINT('Ctrl Pts',(4.60470128900284,-0.502584808570494,-3.70843612169731));
#9337=CARTESIAN_POINT('Ctrl Pts',(4.61238262758632,-0.485922685028345,-3.70715679460331));
#9338=CARTESIAN_POINT('Ctrl Pts',(4.6156087080141,-0.478736010989915,-3.70661114642421));
#9339=CARTESIAN_POINT('Ctrl Pts',(4.62030305592095,-0.467991241391654,-3.70580503026968));
#9340=CARTESIAN_POINT('Ctrl Pts',(4.62182630327857,-0.464457619199869,-3.7055414685735));
#9341=CARTESIAN_POINT('Ctrl Pts',(4.62440861127644,-0.458385501473841,-3.70509129008527));
#9342=CARTESIAN_POINT('Ctrl Pts',(4.62547612573965,-0.455850697419985,-3.70490417570074));
#9343=CARTESIAN_POINT('Ctrl Pts',(4.62788982772629,-0.450062782041408,-3.70447878315827));
#9344=CARTESIAN_POINT('Ctrl Pts',(4.62923031620903,-0.446807357482324,-3.70424084560102));
#9345=CARTESIAN_POINT('Ctrl Pts',(4.63286515675581,-0.4378663528556,-3.70359084847328));
#9346=CARTESIAN_POINT('Ctrl Pts',(4.63512978205513,-0.432168693839955,-3.70318049874956));
#9347=CARTESIAN_POINT('Ctrl Pts',(4.64669944591711,-0.402384591266964,-3.70105418308748));
#9348=CARTESIAN_POINT('Ctrl Pts',(4.65525578379767,-0.378012644262554,-3.69937784663078));
#9349=CARTESIAN_POINT('Ctrl Pts',(4.69291802244623,-0.258273751545842,-3.69135780128932));
#9350=CARTESIAN_POINT('Ctrl Pts',(4.71063673094573,-0.159752786772782,-3.68538053575237));
#9351=CARTESIAN_POINT('Ctrl Pts',(4.71711618857534,-0.0330932096947441,
-3.67737082054352));
#9352=CARTESIAN_POINT('Ctrl Pts',(4.71756586535087,-0.00597737547596642,
-3.67563990514936));
#9353=CARTESIAN_POINT('Ctrl Pts',(4.71674028366827,0.0400350078241747,-3.67265703435896));
#9354=CARTESIAN_POINT('Ctrl Pts',(4.71594578446671,0.0589296926818208,-3.67141909724141));
#9355=CARTESIAN_POINT('Ctrl Pts',(4.71418562626999,0.0855183635478312,-3.66965486510587));
#9356=CARTESIAN_POINT('Ctrl Pts',(4.71359833520841,0.0932350963669577,-3.66914020458147));
#9357=CARTESIAN_POINT('Ctrl Pts',(4.71245768337484,0.106494343779003,-3.66825110682771));
#9358=CARTESIAN_POINT('Ctrl Pts',(4.71194097070631,0.112039818611494,-3.66787781374963));
#9359=CARTESIAN_POINT('Ctrl Pts',(4.71087767805621,0.122637047736332,-3.66716161340163));
#9360=CARTESIAN_POINT('Ctrl Pts',(4.71033769923394,0.127689350427545,-3.66681891907835));
#9361=CARTESIAN_POINT('Ctrl Pts',(4.70899435805145,0.139532533501534,-3.66601261776856));
#9362=CARTESIAN_POINT('Ctrl Pts',(4.70816451799257,0.146320165290306,-3.66554819793542));
#9363=CARTESIAN_POINT('Ctrl Pts',(4.70553512146864,0.166375644178311,-3.66416894962612));
#9364=CARTESIAN_POINT('Ctrl Pts',(4.70356841932231,0.179620082701609,-3.66324898203622));
#9365=CARTESIAN_POINT('Ctrl Pts',(4.68641257396649,0.282990345069766,-3.65599471603356));
#9366=CARTESIAN_POINT('Ctrl Pts',(4.66100707201946,0.371088524346489,-3.64933334001237));
#9367=CARTESIAN_POINT('Ctrl Pts',(4.60795979972711,0.497625507950008,-3.63926398568833));
#9368=CARTESIAN_POINT('Ctrl Pts',(4.58778065409507,0.538836604957881,-3.63590395664767));
#9369=CARTESIAN_POINT('Ctrl Pts',(4.55793853455741,0.591724706893877,-3.6315594540595));
#9370=CARTESIAN_POINT('Ctrl Pts',(4.55038271832034,0.604542027586616,-3.63050408280422));
#9371=CARTESIAN_POINT('Ctrl Pts',(4.53718488130465,0.625990543464053,-3.62873786458802));
#9372=CARTESIAN_POINT('Ctrl Pts',(4.5316688386142,0.634696846124991,-3.62802088628616));
#9373=CARTESIAN_POINT('Ctrl Pts',(4.52369733746608,0.646920813731741,-3.62701536518473));
#9374=CARTESIAN_POINT('Ctrl Pts',(4.52133604766966,0.650498904908845,-3.6267211791538));
#9375=CARTESIAN_POINT('Ctrl Pts',(4.51723689446967,0.656637231386399,-3.62621684548329));
#9376=CARTESIAN_POINT('Ctrl Pts',(4.51550839725881,0.659203634695818,-3.62600609476067));
#9377=CARTESIAN_POINT('Ctrl Pts',(4.51186927544589,0.664561165290996,-3.62556640418511));
#9378=CARTESIAN_POINT('Ctrl Pts',(4.50995672343349,0.667350901733266,-3.62533759457949));
#9379=CARTESIAN_POINT('Ctrl Pts',(4.50480830310536,0.674791688798884,-3.62472758490312));
#9380=CARTESIAN_POINT('Ctrl Pts',(4.50155079635148,0.679427764842924,-3.62434779627613));
#9381=CARTESIAN_POINT('Ctrl Pts',(4.48686800385198,0.700006951953834,-3.62266234343192));
#9382=CARTESIAN_POINT('Ctrl Pts',(4.47507823580574,0.715687705074197,-3.62137914501653));
#9383=CARTESIAN_POINT('Ctrl Pts',(4.40984906847535,0.798076061005048,-3.61459937138855));
#9384=CARTESIAN_POINT('Ctrl Pts',(4.34965543213657,0.859116851982129,-3.60942454688346));
#9385=CARTESIAN_POINT('Ctrl Pts',(4.24056146039214,0.947989794624799,-3.60066308310607));
#9386=CARTESIAN_POINT('Ctrl Pts',(4.19534830471168,0.979812238336118,-3.59717724242399));
#9387=CARTESIAN_POINT('Ctrl Pts',(4.13581582552705,1.01574120085896,-3.59263698308964));
#9388=CARTESIAN_POINT('Ctrl Pts',(4.1234249907903,1.02291439283484,-3.59169481078906));
#9389=CARTESIAN_POINT('Ctrl Pts',(4.10484187890954,1.03322469474088,-3.59028430386699));
#9390=CARTESIAN_POINT('Ctrl Pts',(4.09874736112685,1.03653599227891,-3.58982211125941));
#9391=CARTESIAN_POINT('Ctrl Pts',(4.08781470247116,1.04235148348792,-3.58899353036805));
#9392=CARTESIAN_POINT('Ctrl Pts',(4.08298772559053,1.04487632502354,-3.58862787659347));
#9393=CARTESIAN_POINT('Ctrl Pts',(4.07273129502628,1.05015084779492,-3.58785121994767));
#9394=CARTESIAN_POINT('Ctrl Pts',(4.06729771237416,1.05289210392618,-3.58743993811942));
#9395=CARTESIAN_POINT('Ctrl Pts',(4.05269929998366,1.06011564312644,-3.58633526259548));
#9396=CARTESIAN_POINT('Ctrl Pts',(4.0434972399904,1.06452107467316,-3.58563926063488));
#9397=CARTESIAN_POINT('Ctrl Pts',(4.00054209790992,1.08440379918564,-3.58239097210093));
#9398=CARTESIAN_POINT('Ctrl Pts',(3.96612961488669,1.09839735843773,-3.57978954652323));
#9399=CARTESIAN_POINT('Ctrl Pts',(3.85766511125709,1.13663709834693,-3.57158960543992));
#9400=CARTESIAN_POINT('Ctrl Pts',(3.7818313782277,1.15518101492718,-3.5658414895152));
#9401=CARTESIAN_POINT('Ctrl Pts',(3.67078668784452,1.17091391571905,-3.55763800950096));
#9402=CARTESIAN_POINT('Ctrl Pts',(3.6366435066062,1.17423922092827,-3.55514695149548));
#9403=CARTESIAN_POINT('Ctrl Pts',(3.58385015865952,1.17706200483605,-3.55138375943416));
#9404=CARTESIAN_POINT('Ctrl Pts',(3.56527631492614,1.17761490684344,-3.55007671581533));
#9405=CARTESIAN_POINT('Ctrl Pts',(3.54134826138731,1.17776072071589,-3.54842092535495));
#9406=CARTESIAN_POINT('Ctrl Pts',(3.53600028981212,1.17775688592068,-3.54805265727843));
#9407=CARTESIAN_POINT('Ctrl Pts',(3.5273405797559,1.17769168976857,-3.54745945674535));
#9408=CARTESIAN_POINT('Ctrl Pts',(3.52402882385823,1.17765278620937,-3.54723333600872));
#9409=CARTESIAN_POINT('Ctrl Pts',(3.5176265450913,1.17755056598212,-3.5467976839724));
#9410=CARTESIAN_POINT('Ctrl Pts',(3.51453605982117,1.17748905203869,-3.54658806176255));
#9411=CARTESIAN_POINT('Ctrl Pts',(3.50769720608287,1.17732599259622,-3.546125621358));
#9412=CARTESIAN_POINT('Ctrl Pts',(3.50394897312646,1.17721871085199,-3.54587311516853));
#9413=CARTESIAN_POINT('Ctrl Pts',(3.49063347920839,1.17677394084557,-3.54497925854029));
#9414=CARTESIAN_POINT('Ctrl Pts',(3.48106958058478,1.17633769845862,-3.54434304876719));
#9415=CARTESIAN_POINT('Ctrl Pts',(3.39259245570817,1.17122018450565,-3.53850234645005));
#9416=CARTESIAN_POINT('Ctrl Pts',(3.31432125711008,1.15872075229503,-3.53365785630778));
#9417=CARTESIAN_POINT('Ctrl Pts',(3.18602824906264,1.12472979671431,-3.5254455112722));
#9418=CARTESIAN_POINT('Ctrl Pts',(3.1351744660868,1.1074645372386,-3.52211528317582));
#9419=CARTESIAN_POINT('Ctrl Pts',(3.06712775260272,1.07904848134746,-3.51740583289004));
#9420=CARTESIAN_POINT('Ctrl Pts',(3.04878017546468,1.07082886143696,-3.51610987910902));
#9421=CARTESIAN_POINT('Ctrl Pts',(3.01706022422097,1.0556320377273,-3.51381624026388));
#9422=CARTESIAN_POINT('Ctrl Pts',(3.00359455778155,1.04885991859225,-3.51282528670459));
#9423=CARTESIAN_POINT('Ctrl Pts',(2.98400129684174,1.03853030539245,-3.51135588899236));
#9424=CARTESIAN_POINT('Ctrl Pts',(2.97776956796749,1.03517278029445,-3.51088437414969));
#9425=CARTESIAN_POINT('Ctrl Pts',(2.96678149065349,1.0291241958636,-3.51004536696797));
#9426=CARTESIAN_POINT('Ctrl Pts',(2.96201285313594,1.02645580190351,-3.50967868035459));
#9427=CARTESIAN_POINT('Ctrl Pts',(2.95203986826865,1.02078370831495,-3.50890629107291));
#9428=CARTESIAN_POINT('Ctrl Pts',(2.9468396070646,1.01777317892497,-3.50850035329362));
#9429=CARTESIAN_POINT('Ctrl Pts',(2.93317727489808,1.00972358128782,-3.50742527847184));
#9430=CARTESIAN_POINT('Ctrl Pts',(2.92475513269853,1.00461802422746,-3.50675377269525));
#9431=CARTESIAN_POINT('Ctrl Pts',(2.88813167708821,0.981783658794715,-3.50379425848971));
#9432=CARTESIAN_POINT('Ctrl Pts',(2.86062821320882,0.962970152776744,-3.50146721340666));
#9433=CARTESIAN_POINT('Ctrl Pts',(2.7690877260293,0.89448035155823,-3.49334886704103));
#9434=CARTESIAN_POINT('Ctrl Pts',(2.70940209091129,0.839382163000545,-3.4873737131628));
#9435=CARTESIAN_POINT('Ctrl Pts',(2.6218978513112,0.740070382245344,-3.47768724635673));
#9436=CARTESIAN_POINT('Ctrl Pts',(2.59049722167838,0.699350887025435,-3.47396340714033));
#9437=CARTESIAN_POINT('Ctrl Pts',(2.55798154453704,0.650943460101822,-3.46990768228305));
#9438=CARTESIAN_POINT('Ctrl Pts',(2.55416124778644,0.645145929466778,-3.46942769117538));
#9439=CARTESIAN_POINT('Ctrl Pts',(2.54840654187993,0.636242438506985,-3.46869967140879));
#9440=CARTESIAN_POINT('Ctrl Pts',(2.54643504621833,0.633160806316008,-3.46844934168098));
#9441=CARTESIAN_POINT('Ctrl Pts',(2.54285043239605,0.627499787201232,-3.46799256367277));
#9442=CARTESIAN_POINT('Ctrl Pts',(2.54123294303013,0.62492332755839,-3.4677858411787));
#9443=CARTESIAN_POINT('Ctrl Pts',(2.53760180503328,0.619089299956832,-3.46732035927917));
#9444=CARTESIAN_POINT('Ctrl Pts',(2.53559404947504,0.615828159016731,-3.46706197999346));
#9445=CARTESIAN_POINT('Ctrl Pts',(2.53044216367006,0.607367939266451,-3.46639621163821));
#9446=CARTESIAN_POINT('Ctrl Pts',(2.52732224682173,0.602154142763915,-3.46599031462872));
#9447=CARTESIAN_POINT('Ctrl Pts',(2.50652066783282,0.56677338603445,-3.46326382727266));
#9448=CARTESIAN_POINT('Ctrl Pts',(2.49014784556306,0.535852891814161,-3.46101715709204));
#9449=CARTESIAN_POINT('Ctrl Pts',(2.43618139178108,0.421942460225974,-3.45305531087221));
#9450=CARTESIAN_POINT('Ctrl Pts',(2.40686622677984,0.335392811262,-3.44756195870265));
#9451=CARTESIAN_POINT('Ctrl Pts',(2.37951902092388,0.207530633690691,-3.43929402626011));
#9452=CARTESIAN_POINT('Ctrl Pts',(2.37318769978433,0.16834399623778,-3.43674449872643));
#9453=CARTESIAN_POINT('Ctrl Pts',(2.36774883917496,0.118954059385286,-3.43347314585464));
#9454=CARTESIAN_POINT('Ctrl Pts',(2.36677909526317,0.108979280658975,-3.43280960311076));
#9455=CARTESIAN_POINT('Ctrl Pts',(2.36542855198598,0.0929684089631018,-3.4317393974354));
#9456=CARTESIAN_POINT('Ctrl Pts',(2.36496673391375,0.086939502322136,-3.43133524838191));
#9457=CARTESIAN_POINT('Ctrl Pts',(2.36417659427538,0.0754647974873236,-3.43056370832573));
#9458=CARTESIAN_POINT('Ctrl Pts',(2.3638396469709,0.0700197362499726,-3.4301965946374));
#9459=CARTESIAN_POINT('Ctrl Pts',(2.36315641229044,0.0575768549608456,-3.42935530891398));
#9460=CARTESIAN_POINT('Ctrl Pts',(2.36283471799604,0.0505779474917043,-3.4288803895385));
#9461=CARTESIAN_POINT('Ctrl Pts',(2.3620321106912,0.0289006941063898,-3.42740393499206));
#9462=CARTESIAN_POINT('Ctrl Pts',(2.36176330164812,0.0142163969199187,-3.42639592784049));
#9463=CARTESIAN_POINT('Ctrl Pts',(2.36179229001102,-0.0586529238535955,
-3.42135267703571));
#9464=CARTESIAN_POINT('Ctrl Pts',(2.36612702697649,-0.116746921123347,-3.41719611126923));
#9465=CARTESIAN_POINT('Ctrl Pts',(2.38376036848421,-0.234600825214178,-3.40852461121926));
#9466=CARTESIAN_POINT('Ctrl Pts',(2.39745873432777,-0.294132094370935,-3.40401486542645));
#9467=CARTESIAN_POINT('Ctrl Pts',(2.42064731600968,-0.36809501408863,-3.39837923807716));
#9468=CARTESIAN_POINT('Ctrl Pts',(2.42591994151369,-0.383751171894167,-3.39718482853545));
#9469=CARTESIAN_POINT('Ctrl Pts',(2.43943908531861,-0.421265578299721,-3.39432650354487));
#9470=CARTESIAN_POINT('Ctrl Pts',(2.4480104194524,-0.443000792461012,-3.39267345285986));
#9471=CARTESIAN_POINT('Ctrl Pts',(2.45959453870256,-0.469993900498081,-3.39063627515722));
#9472=CARTESIAN_POINT('Ctrl Pts',(2.46200818721363,-0.47550137857206,-3.39022146981295));
#9473=CARTESIAN_POINT('Ctrl Pts',(2.4658765214276,-0.484147441832999,-3.38957188265893));
#9474=CARTESIAN_POINT('Ctrl Pts',(2.46730299348854,-0.487298423485471,-3.38933548490488));
#9475=CARTESIAN_POINT('Ctrl Pts',(2.47002183568154,-0.493234422993762,-3.38889084801167));
#9476=CARTESIAN_POINT('Ctrl Pts',(2.47131120454452,-0.496020651389935,-3.38868244698977));
#9477=CARTESIAN_POINT('Ctrl Pts',(2.47435902725332,-0.5025397626296,-3.38819549758624));
#9478=CARTESIAN_POINT('Ctrl Pts',(2.47612622151347,-0.506268486763313,-3.38791748155108));
#9479=CARTESIAN_POINT('Ctrl Pts',(2.48196940626618,-0.518431834238853,-3.38701197611357));
#9480=CARTESIAN_POINT('Ctrl Pts',(2.48612655957959,-0.526827381966958,-3.38638918009597));
#9481=CARTESIAN_POINT('Ctrl Pts',(2.50968661975854,-0.573013765869746,-3.38297038948569));
#9482=CARTESIAN_POINT('Ctrl Pts',(2.53102505680056,-0.609787072918135,-3.38027549290668));
#9483=CARTESIAN_POINT('Ctrl Pts',(2.56704905547136,-0.664784173335619,-3.37616427310001));
#9484=CARTESIAN_POINT('Ctrl Pts',(2.58036531360688,-0.683856740537999,-3.37472244524226));
#9485=CARTESIAN_POINT('Ctrl Pts',(2.64628668496426,-0.772557393307044,-3.36788228339454));
#9486=CARTESIAN_POINT('Ctrl Pts',(2.70595046368155,-0.836582497546907,-3.36251284843542));
#9487=CARTESIAN_POINT('Ctrl Pts',(2.7836309232053,-0.903303875352328,-3.35583607373008));
#9488=CARTESIAN_POINT('Ctrl Pts',(2.79531682443236,-0.912955510894286,-3.35483972156162));
#9489=CARTESIAN_POINT('Ctrl Pts',(2.81268160761175,-0.926742492323955,-3.35336887146596));
#9490=CARTESIAN_POINT('Ctrl Pts',(2.8182167185411,-0.9310570647421,-3.35290143382411));
#9491=CARTESIAN_POINT('Ctrl Pts',(2.82813577062354,-0.938647344216288,-3.35206606437501));
#9492=CARTESIAN_POINT('Ctrl Pts',(2.832504640965,-0.941942477372226,-3.35169890121372));
#9493=CARTESIAN_POINT('Ctrl Pts',(2.84169561916302,-0.948774621884138,-3.35092801074458));
#9494=CARTESIAN_POINT('Ctrl Pts',(2.8465220089522,-0.952305582565559,-3.3505240651533));
#9495=CARTESIAN_POINT('Ctrl Pts',(2.85926084867646,-0.961477125330561,-3.34946001733772));
#9496=CARTESIAN_POINT('Ctrl Pts',(2.86721644276734,-0.967056708526007,-3.34879763326682));
#9497=CARTESIAN_POINT('Ctrl Pts',(2.90483268352598,-0.992750003713544,-3.34567482152017));
#9498=CARTESIAN_POINT('Ctrl Pts',(2.93532951997544,-1.01159967163841,-3.3431684547107));
#9499=CARTESIAN_POINT('Ctrl Pts',(3.02184423668056,-1.05976438929647,-3.33612255142302));
#9500=CARTESIAN_POINT('Ctrl Pts',(3.07943182754454,-1.08600460148177,-3.33149741801535));
#9501=CARTESIAN_POINT('Ctrl Pts',(3.19701596866615,-1.12854518700131,-3.32232037541134));
#9502=CARTESIAN_POINT('Ctrl Pts',(3.2567666069878,-1.14497823832997,-3.31778426873837));
#9503=CARTESIAN_POINT('Ctrl Pts',(3.32737802061638,-1.15852995725997,-3.31274229332292));
#9504=CARTESIAN_POINT('Ctrl Pts',(3.33724330873386,-1.16029307475342,-3.31204507588797));
#9505=CARTESIAN_POINT('Ctrl Pts',(3.35101636673719,-1.16257357457425,-3.31108278865973));
#9506=CARTESIAN_POINT('Ctrl Pts',(3.35490570985758,-1.16319752993834,-3.31081227988626));
#9507=CARTESIAN_POINT('Ctrl Pts',(3.3616214755311,-1.16424038692886,-3.31034739291194));
#9508=CARTESIAN_POINT('Ctrl Pts',(3.3644463961517,-1.16466853305111,-3.31015251403851));
#9509=CARTESIAN_POINT('Ctrl Pts',(3.37041048954383,-1.16555026355276,-3.30974253246608));
#9510=CARTESIAN_POINT('Ctrl Pts',(3.37354998763642,-1.1660014549157,-3.30952757021895));
#9511=CARTESIAN_POINT('Ctrl Pts',(3.38134684249088,-1.16708984723169,-3.30899574628352));
#9512=CARTESIAN_POINT('Ctrl Pts',(3.38600632683078,-1.16771186704414,-3.30867971650503));
#9513=CARTESIAN_POINT('Ctrl Pts',(3.40360735039072,-1.16995434831707,-3.30749226675355));
#9514=CARTESIAN_POINT('Ctrl Pts',(3.41657234475879,-1.17138777082818,-3.30663050537581));
#9515=CARTESIAN_POINT('Ctrl Pts',(3.44994668827043,-1.17451741672958,-3.30443914066392));
#9516=CARTESIAN_POINT('Ctrl Pts',(3.47038187695158,-1.17589732585908,-3.30312316525829));
#9517=CARTESIAN_POINT('Ctrl Pts',(3.54862425781716,-1.1791337709615,-3.29814819724476));
#9518=CARTESIAN_POINT('Ctrl Pts',(3.60650567346308,-1.17726502977485,-3.29459727124975));
#9519=CARTESIAN_POINT('Ctrl Pts',(3.73906491257438,-1.1631733033116,-3.28634308521419));
#9520=CARTESIAN_POINT('Ctrl Pts',(3.81316022767033,-1.14800217019918,-3.28162975201806));
#9521=CARTESIAN_POINT('Ctrl Pts',(3.89522057104641,-1.12279980931841,-3.27599581681253));
#9522=CARTESIAN_POINT('Ctrl Pts',(3.90511022897173,-1.11961871302437,-3.27531004044194));
#9523=CARTESIAN_POINT('Ctrl Pts',(3.92133036282158,-1.11416354680174,-3.27417339913102));
#9524=CARTESIAN_POINT('Ctrl Pts',(3.92768587238572,-1.11196528834139,-3.2737249934423));
#9525=CARTESIAN_POINT('Ctrl Pts',(3.93913662693685,-1.10789454342505,-3.2729114281665));
#9526=CARTESIAN_POINT('Ctrl Pts',(3.94423844982924,-1.10604101771551,-3.2725468981214));
#9527=CARTESIAN_POINT('Ctrl Pts',(3.95516102595931,-1.10198708357626,-3.27176196807344));
#9528=CARTESIAN_POINT('Ctrl Pts',(3.96097749592488,-1.09977568637731,-3.27134121487764));
#9529=CARTESIAN_POINT('Ctrl Pts',(3.97687033641353,-1.09358870298832,-3.27018380951579));
#9530=CARTESIAN_POINT('Ctrl Pts',(3.98690960173241,-1.08952011439486,-3.26944409900032));
#9531=CARTESIAN_POINT('Ctrl Pts',(4.02446599860444,-1.07369312990808,-3.26664355615269));
#9532=CARTESIAN_POINT('Ctrl Pts',(4.05157800284191,-1.06103007383657,-3.26455347747179));
#9533=CARTESIAN_POINT('Ctrl Pts',(4.07816931781854,-1.04735426286176,-3.26243320031815));
#9534=CARTESIAN_POINT('',(2.36176924975877,-0.000685226520117502,-3.32646548062114));
#9535=CARTESIAN_POINT('Ctrl Pts',(4.07816926753082,-1.04735428872454,-3.16389876579091));
#9536=CARTESIAN_POINT('Ctrl Pts',(4.07216381045497,-1.05044287182632,-3.16434541254173));
#9537=CARTESIAN_POINT('Ctrl Pts',(4.0661316377366,-1.05347988029879,-3.16478935096556));
#9538=CARTESIAN_POINT('Ctrl Pts',(4.04170150629564,-1.06551739402014,-3.16656977557909));
#9539=CARTESIAN_POINT('Ctrl Pts',(4.02309548108024,-1.07408960108841,-3.16788600383687));
#9540=CARTESIAN_POINT('Ctrl Pts',(3.95114101430919,-1.10499152359238,-3.17286095269525));
#9541=CARTESIAN_POINT('Ctrl Pts',(3.89639619841826,-1.12386761349931,-3.17641164228168));
#9542=CARTESIAN_POINT('Ctrl Pts',(3.76751947088795,-1.15793201295094,-3.1846656140504));
#9543=CARTESIAN_POINT('Ctrl Pts',(3.69288120625955,-1.17015750197088,-3.18937897703656));
#9544=CARTESIAN_POINT('Ctrl Pts',(3.60722745895398,-1.17584800632533,-3.19501288167123));
#9545=CARTESIAN_POINT('Ctrl Pts',(3.59685443481875,-1.17639942412098,-3.19569859243701));
#9546=CARTESIAN_POINT('Ctrl Pts',(3.57975700251857,-1.17708163819283,-3.19683511084415));
#9547=CARTESIAN_POINT('Ctrl Pts',(3.57303621558054,-1.17729217794565,-3.19728345960666));
#9548=CARTESIAN_POINT('Ctrl Pts',(3.56088824968675,-1.17756862858315,-3.19809691136177));
#9549=CARTESIAN_POINT('Ctrl Pts',(3.55546168038015,-1.17765459646126,-3.19846138491279));
#9550=CARTESIAN_POINT('Ctrl Pts',(3.5438134945486,-1.17775860337308,-3.19924618125349));
#9551=CARTESIAN_POINT('Ctrl Pts',(3.53759196465681,-1.17776485507355,-3.19966685704404));
#9552=CARTESIAN_POINT('Ctrl Pts',(3.52054132154316,-1.17764688725659,-3.2008240155209));
#9553=CARTESIAN_POINT('Ctrl Pts',(3.50971373881204,-1.17742259833855,-3.20156355503496));
#9554=CARTESIAN_POINT('Ctrl Pts',(3.44560902489901,-1.17520990930784,-3.2059712027159));
#9555=CARTESIAN_POINT('Ctrl Pts',(3.39252115708324,-1.16975534760865,-3.20974514440144));
#9556=CARTESIAN_POINT('Ctrl Pts',(3.25762230127863,-1.14656638231187,-3.21963791839877));
#9557=CARTESIAN_POINT('Ctrl Pts',(3.17699969890276,-1.12368098674895,-3.22585635791559));
#9558=CARTESIAN_POINT('Ctrl Pts',(3.07352000319832,-1.08199965306938,-3.23389516112285));
#9559=CARTESIAN_POINT('Ctrl Pts',(3.0479379212352,-1.07061974606113,-3.23588521397672));
#9560=CARTESIAN_POINT('Ctrl Pts',(3.01714297967116,-1.05558405785667,-3.23826446056107));
#9561=CARTESIAN_POINT('Ctrl Pts',(3.01152440666644,-1.05278493672653,-3.23869786683944));
#9562=CARTESIAN_POINT('Ctrl Pts',(3.0027605067172,-1.04833103321215,-3.23937250824708));
#9563=CARTESIAN_POINT('Ctrl Pts',(2.99959993404511,-1.04670675838434,-3.23961552229055));
#9564=CARTESIAN_POINT('Ctrl Pts',(2.99379147890894,-1.04368837987008,-3.24006153687712));
#9565=CARTESIAN_POINT('Ctrl Pts',(2.99114156514094,-1.04229849397095,-3.24026477985168));
#9566=CARTESIAN_POINT('Ctrl Pts',(2.9851167029621,-1.03910910259628,-3.24072636597063));
#9567=CARTESIAN_POINT('Ctrl Pts',(2.98174519955562,-1.03730324509577,-3.24098431053808));
#9568=CARTESIAN_POINT('Ctrl Pts',(2.97462662472816,-1.03344562462295,-3.24152830139936));
#9569=CARTESIAN_POINT('Ctrl Pts',(2.97088178778538,-1.03138982763521,-3.24181410286266));
#9570=CARTESIAN_POINT('Ctrl Pts',(2.96091433669886,-1.02584722273583,-3.24257403280044));
#9571=CARTESIAN_POINT('Ctrl Pts',(2.95471196568868,-1.02232412596306,-3.24304609818235));
#9572=CARTESIAN_POINT('Ctrl Pts',(2.93559406328807,-1.01123376733574,-3.24449986382827));
#9573=CARTESIAN_POINT('Ctrl Pts',(2.92279004256329,-1.00347620650165,-3.24547164622372));
#9574=CARTESIAN_POINT('Ctrl Pts',(2.87097312393294,-0.970715356158586,-3.24941137615357));
#9575=CARTESIAN_POINT('Ctrl Pts',(2.83330164012755,-0.943662859352533,-3.25229324189072));
#9576=CARTESIAN_POINT('Ctrl Pts',(2.72694049566269,-0.857337321892232,-3.26077696244841));
#9577=CARTESIAN_POINT('Ctrl Pts',(2.66339886031281,-0.792289386717381,-3.2663405929274));
#9578=CARTESIAN_POINT('Ctrl Pts',(2.5988142427707,-0.708796378478885,-3.27322579319779));
#9579=CARTESIAN_POINT('Ctrl Pts',(2.58990756260922,-0.696818362934043,-3.27420731383331));
#9580=CARTESIAN_POINT('Ctrl Pts',(2.57717627467303,-0.678999335343267,-3.27566028473674));
#9581=CARTESIAN_POINT('Ctrl Pts',(2.57317189606556,-0.673288117522481,-3.27612492073691));
#9582=CARTESIAN_POINT('Ctrl Pts',(2.56612069163644,-0.663038890473538,-3.27695705544193));
#9583=CARTESIAN_POINT('Ctrl Pts',(2.563054255402,-0.658514568962686,-3.27732380621339));
#9584=CARTESIAN_POINT('Ctrl Pts',(2.55668771755714,-0.648978918308727,-3.27809566859469));
#9585=CARTESIAN_POINT('Ctrl Pts',(2.55339420794947,-0.64396339805248,-3.27850101078419));
#9586=CARTESIAN_POINT('Ctrl Pts',(2.54481625845102,-0.630680341864174,-3.27957297180535));
#9587=CARTESIAN_POINT('Ctrl Pts',(2.53959665666902,-0.622371701106363,-3.28024193531335));
#9588=CARTESIAN_POINT('Ctrl Pts',(2.51519668230655,-0.58243208119117,-3.2834510873421));
#9589=CARTESIAN_POINT('Ctrl Pts',(2.49741168586041,-0.549977425545492,-3.28604039349646));
#9590=CARTESIAN_POINT('Ctrl Pts',(2.4403237665403,-0.433056350756097,-3.29531007800162));
#9591=CARTESIAN_POINT('Ctrl Pts',(2.40953591555949,-0.344822560384054,-3.30223383750231));
#9592=CARTESIAN_POINT('Ctrl Pts',(2.38405244258881,-0.229394596659508,-3.31081303448707));
#9593=CARTESIAN_POINT('Ctrl Pts',(2.37942619461876,-0.204718573781859,-3.31261802054143));
#9594=CARTESIAN_POINT('Ctrl Pts',(2.37343136057271,-0.165935454035137,-3.31539256510061));
#9595=CARTESIAN_POINT('Ctrl Pts',(2.37152275457443,-0.151920282863744,-3.31638258817523));
#9596=CARTESIAN_POINT('Ctrl Pts',(2.3692807833377,-0.132900467540097,-3.31770615523241));
#9597=CARTESIAN_POINT('Ctrl Pts',(2.36872630502981,-0.127923749240768,-3.31805063293189));
#9598=CARTESIAN_POINT('Ctrl Pts',(2.36789925913393,-0.120044264887885,-3.31859295730121));
#9599=CARTESIAN_POINT('Ctrl Pts',(2.36760570750693,-0.117143834827476,-3.318791927765));
#9600=CARTESIAN_POINT('Ctrl Pts',(2.36704181257365,-0.111357926906338,-3.31918749063668));
#9601=CARTESIAN_POINT('Ctrl Pts',(2.36677134744997,-0.108472515060543,-3.31938408141543));
#9602=CARTESIAN_POINT('Ctrl Pts',(2.36623498913183,-0.102513849152593,-3.31978871643012));
#9603=CARTESIAN_POINT('Ctrl Pts',(2.36597051258046,-0.099440472716324,-3.31999668348267));
#9604=CARTESIAN_POINT('Ctrl Pts',(2.36537601758768,-0.0921991383807463,
-3.32048502538132));
#9605=CARTESIAN_POINT('Ctrl Pts',(2.36505610945279,-0.0880303597128459,
-3.32076486606148));
#9606=CARTESIAN_POINT('Ctrl Pts',(2.36403603387288,-0.0737405169386048,
-3.32171995080133));
#9607=CARTESIAN_POINT('Ctrl Pts',(2.36344441969837,-0.0636118322215455,
-3.32238977303471));
#9608=CARTESIAN_POINT('Ctrl Pts',(2.36218445924856,-0.0358914046913295,
-3.32420652091499));
#9609=CARTESIAN_POINT('Ctrl Pts',(2.36177949234592,-0.0182899231070387,
-3.3253420215642));
#9610=CARTESIAN_POINT('Ctrl Pts',(2.36176924975877,-0.000685226520117502,
-3.32646548062114));
#9611=CARTESIAN_POINT('Ctrl Pts',(2.36176925070335,-0.000686848120440911,
-3.32646537713726));
#9612=CARTESIAN_POINT('Ctrl Pts',(2.36170726434664,0.105602180019166,-3.33324830865505));
#9613=CARTESIAN_POINT('Ctrl Pts',(2.37603299620722,0.211421176431465,-3.33959912714655));
#9614=CARTESIAN_POINT('Ctrl Pts',(2.41354804809705,0.347088586105826,-3.34854667360927));
#9615=CARTESIAN_POINT('Ctrl Pts',(2.42417784471382,0.379861592893897,-3.35076944568466));
#9616=CARTESIAN_POINT('Ctrl Pts',(2.43958484639731,0.421107908988138,-3.35367101025298));
#9617=CARTESIAN_POINT('Ctrl Pts',(2.44305192570047,0.430054600776447,-3.35430675582835));
#9618=CARTESIAN_POINT('Ctrl Pts',(2.44884654203039,0.444481696883111,-3.35534278585602));
#9619=CARTESIAN_POINT('Ctrl Pts',(2.45110705102283,0.449988685178161,-3.35574083974396));
#9620=CARTESIAN_POINT('Ctrl Pts',(2.45552818028636,0.460531082118157,-3.3565079645948));
#9621=CARTESIAN_POINT('Ctrl Pts',(2.45768238753637,0.465569025204975,-3.35687681263688));
#9622=CARTESIAN_POINT('Ctrl Pts',(2.46269720757444,0.477074195585782,-3.35772443494346));
#9623=CARTESIAN_POINT('Ctrl Pts',(2.4655810480382,0.483531004785404,-3.3582039823009));
#9624=CARTESIAN_POINT('Ctrl Pts',(2.47495167208151,0.504014056184857,-3.35973781742062));
#9625=CARTESIAN_POINT('Ctrl Pts',(2.48165621733334,0.517938277138569,-3.36079943799464));
#9626=CARTESIAN_POINT('Ctrl Pts',(2.52476112601509,0.603129462187264,-3.36741575042592));
#9627=CARTESIAN_POINT('Ctrl Pts',(2.56806658265669,0.670652369217492,-3.37321192652271));
#9628=CARTESIAN_POINT('Ctrl Pts',(2.64656377591275,0.76931775989478,-3.3824597156805));
#9629=CARTESIAN_POINT('Ctrl Pts',(2.67734899298471,0.803667839564259,-3.38585092263168));
#9630=CARTESIAN_POINT('Ctrl Pts',(2.72500878935058,0.850947092530639,-3.39070236240518));
#9631=CARTESIAN_POINT('Ctrl Pts',(2.74034426517797,0.86536563873708,-3.39220938888766));
#9632=CARTESIAN_POINT('Ctrl Pts',(2.7627972435383,0.885369836249182,-3.39433118696085));
#9633=CARTESIAN_POINT('Ctrl Pts',(2.76960473775599,0.891295952340837,-3.39496384952596));
#9634=CARTESIAN_POINT('Ctrl Pts',(2.78029962481323,0.900392176131148,-3.39594052828667));
#9635=CARTESIAN_POINT('Ctrl Pts',(2.78414012996974,0.903616564563787,-3.39628785884223));
#9636=CARTESIAN_POINT('Ctrl Pts',(2.79126113383715,0.909518047600413,-3.39692546873384));
#9637=CARTESIAN_POINT('Ctrl Pts',(2.79453568242073,0.912202154913365,-3.39721620712816));
#9638=CARTESIAN_POINT('Ctrl Pts',(2.80022265302385,0.916812646518107,-3.39771679463652));
#9639=CARTESIAN_POINT('Ctrl Pts',(2.80262829048344,0.918747299719223,-3.39792721768062));
#9640=CARTESIAN_POINT('Ctrl Pts',(2.80729077894539,0.922466855551421,-3.39833244482174));
#9641=CARTESIAN_POINT('Ctrl Pts',(2.80954659580869,0.924252972458334,-3.39852733901311));
#9642=CARTESIAN_POINT('Ctrl Pts',(2.81496816533031,0.92851344704474,-3.39899302334752));
#9643=CARTESIAN_POINT('Ctrl Pts',(2.81814010523731,0.930979927304475,-3.39926327017837));
#9644=CARTESIAN_POINT('Ctrl Pts',(2.82790120678969,0.938490257021382,-3.40008838864706));
#9645=CARTESIAN_POINT('Ctrl Pts',(2.83453126823213,0.943480871155306,-3.40063980073496));
#9646=CARTESIAN_POINT('Ctrl Pts',(2.90763503479563,0.997306983977838,-3.4066284380068));
#9647=CARTESIAN_POINT('Ctrl Pts',(2.97902060174175,1.03910742673274,-3.41166912353977));
#9648=CARTESIAN_POINT('Ctrl Pts',(3.10123846769282,1.09438135336674,-3.4199728001698));
#9649=CARTESIAN_POINT('Ctrl Pts',(3.14962369045581,1.11253828342649,-3.42318352732863));
#9650=CARTESIAN_POINT('Ctrl Pts',(3.21784750161664,1.13314095429153,-3.42773869212644));
#9651=CARTESIAN_POINT('Ctrl Pts',(3.23679244996208,1.13834860553179,-3.42900608058295));
#9652=CARTESIAN_POINT('Ctrl Pts',(3.27022835051705,1.14664589351153,-3.43125362133875));
#9653=CARTESIAN_POINT('Ctrl Pts',(3.28466411201686,1.14994052659722,-3.43222742007851));
#9654=CARTESIAN_POINT('Ctrl Pts',(3.30603801579209,1.15439640764161,-3.43367609065437));
#9655=CARTESIAN_POINT('Ctrl Pts',(3.31293096609522,1.15576913610115,-3.43414431497071));
#9656=CARTESIAN_POINT('Ctrl Pts',(3.32519731393573,1.158098026627,-3.43497957147724));
#9657=CARTESIAN_POINT('Ctrl Pts',(3.33056589324368,1.15907869551772,-3.43534582281302));
#9658=CARTESIAN_POINT('Ctrl Pts',(3.34188347381798,1.16106487403492,-3.43611945808568));
#9659=CARTESIAN_POINT('Ctrl Pts',(3.34783375762494,1.16206205042879,-3.43652709169396));
#9660=CARTESIAN_POINT('Ctrl Pts',(3.36363011478829,1.16458465337228,-3.43761173710072));
#9661=CARTESIAN_POINT('Ctrl Pts',(3.37348815336498,1.16603090147432,-3.43829119468062));
#9662=CARTESIAN_POINT('Ctrl Pts',(3.41761556187732,1.17193379821133,-3.44134485153878));
#9663=CARTESIAN_POINT('Ctrl Pts',(3.45204972888783,1.17500552514447,-3.44376126031426));
#9664=CARTESIAN_POINT('Ctrl Pts',(3.58652512176652,1.1810577911401,-3.45333293945063));
#9665=CARTESIAN_POINT('Ctrl Pts',(3.68664598253958,1.17279846589486,-3.46079293544927));
#9666=CARTESIAN_POINT('Ctrl Pts',(3.8055198273816,1.14751935047887,-3.46958092230525));
#9667=CARTESIAN_POINT('Ctrl Pts',(3.82641911900404,1.14247342892441,-3.4711211205662));
#9668=CARTESIAN_POINT('Ctrl Pts',(3.8602048948648,1.13333049433681,-3.47359165703966));
#9669=CARTESIAN_POINT('Ctrl Pts',(3.87317909609806,1.12957887422423,-3.47453563592933));
#9670=CARTESIAN_POINT('Ctrl Pts',(3.8906386238749,1.12420318145022,-3.47579695597588));
#9671=CARTESIAN_POINT('Ctrl Pts',(3.89518223264772,1.12277399810062,-3.4761243647073));
#9672=CARTESIAN_POINT('Ctrl Pts',(3.90274883539869,1.12034339618434,-3.4766680726243));
#9673=CARTESIAN_POINT('Ctrl Pts',(3.90577661956073,1.11935722441194,-3.47688522582315));
#9674=CARTESIAN_POINT('Ctrl Pts',(3.91150255241309,1.1174665249375,-3.47729506064139));
#9675=CARTESIAN_POINT('Ctrl Pts',(3.91420147754474,1.11656448060691,-3.4774878876229));
#9676=CARTESIAN_POINT('Ctrl Pts',(3.92058621018787,1.11440479566742,-3.47794328146209));
#9677=CARTESIAN_POINT('Ctrl Pts',(3.92426913014604,1.11313862841971,-3.47820535871792));
#9678=CARTESIAN_POINT('Ctrl Pts',(3.93715667858821,1.1086363581155,-3.47912052663344));
#9679=CARTESIAN_POINT('Ctrl Pts',(3.94632761619663,1.10530405944322,-3.47976834159575));
#9680=CARTESIAN_POINT('Ctrl Pts',(4.02239051631051,1.07659128237761,-3.4851209376526));
#9681=CARTESIAN_POINT('Ctrl Pts',(4.08689285267823,1.0452743320777,-3.48953402068664));
#9682=CARTESIAN_POINT('Ctrl Pts',(4.19831752385726,0.978014352344575,-3.49758451897788));
#9683=CARTESIAN_POINT('Ctrl Pts',(4.24614239186915,0.944039352222448,-3.50120603232571));
#9684=CARTESIAN_POINT('Ctrl Pts',(4.30752885282754,0.893142638380204,-3.50628920565357));
#9685=CARTESIAN_POINT('Ctrl Pts',(4.3234507657923,0.879200668164769,-3.50765123085441));
#9686=CARTESIAN_POINT('Ctrl Pts',(4.35050071100402,0.854195306666699,-3.51005100141468));
#9687=CARTESIAN_POINT('Ctrl Pts',(4.36179946879558,0.843324226921271,-3.51108109328746));
#9688=CARTESIAN_POINT('Ctrl Pts',(4.37795770085741,0.827144110758473,-3.51259753322676));
#9689=CARTESIAN_POINT('Ctrl Pts',(4.38299117517655,0.822010657738938,-3.51307628641409));
#9690=CARTESIAN_POINT('Ctrl Pts',(4.39177702375597,0.812884632511011,-3.51392346300255));
#9691=CARTESIAN_POINT('Ctrl Pts',(4.3955491619606,0.808911321032259,-3.51429102475715));
#9692=CARTESIAN_POINT('Ctrl Pts',(4.40336283157961,0.800565075090087,-3.51506054685705));
#9693=CARTESIAN_POINT('Ctrl Pts',(4.40739918751501,0.796187530104291,-3.51546271066298));
#9694=CARTESIAN_POINT('Ctrl Pts',(4.41785731088173,0.784671370521888,-3.51651707636438));
#9695=CARTESIAN_POINT('Ctrl Pts',(4.42422516864763,0.777484620048002,-3.51717148544111));
#9696=CARTESIAN_POINT('Ctrl Pts',(4.45084271923568,0.746693659173968,-3.51996092598244));
#9697=CARTESIAN_POINT('Ctrl Pts',(4.4702394930117,0.722372063160032,-3.52212970052603));
#9698=CARTESIAN_POINT('Ctrl Pts',(4.55013336105227,0.613626512228272,-3.53168765057077));
#9699=CARTESIAN_POINT('Ctrl Pts',(4.60027455324008,0.52217904213109,-3.53943164409005));
#9700=CARTESIAN_POINT('Ctrl Pts',(4.64562364763627,0.405093156114715,-3.54851395530527));
#9701=CARTESIAN_POINT('Ctrl Pts',(4.65291428079418,0.384602419888728,-3.55007251834525));
#9702=CARTESIAN_POINT('Ctrl Pts',(4.66384095467244,0.350971085714961,-3.55256903472033));
#9703=CARTESIAN_POINT('Ctrl Pts',(4.66782348788451,0.337949084417064,-3.55352096288756));
#9704=CARTESIAN_POINT('Ctrl Pts',(4.67289737548775,0.320267797861634,-3.55479109554313));
#9705=CARTESIAN_POINT('Ctrl Pts',(4.67418731869843,0.315667250467204,-3.55511954365551));
#9706=CARTESIAN_POINT('Ctrl Pts',(4.67629108917916,0.307984665029283,-3.55566450333985));
#9707=CARTESIAN_POINT('Ctrl Pts',(4.67712045267563,0.304906989583668,-3.5558818769536));
#9708=CARTESIAN_POINT('Ctrl Pts',(4.67866595069244,0.299077725075181,-3.55629176851676));
#9709=CARTESIAN_POINT('Ctrl Pts',(4.6793846314702,0.296326852665477,-3.55648443412707));
#9710=CARTESIAN_POINT('Ctrl Pts',(4.6810616094954,0.289811554436046,-3.55693900259209));
#9711=CARTESIAN_POINT('Ctrl Pts',(4.68201126613269,0.286044907946762,-3.55720042013527));
#9712=CARTESIAN_POINT('Ctrl Pts',(4.68529202025881,0.272755351458151,-3.5581181287895));
#9713=CARTESIAN_POINT('Ctrl Pts',(4.68752290779695,0.263207786684577,-3.55876907637804));
#9714=CARTESIAN_POINT('Ctrl Pts',(4.70493527424386,0.184250308769002,-3.56409204425701));
#9715=CARTESIAN_POINT('Ctrl Pts',(4.71392850734407,0.113615126710396,-3.56847656896941));
#9716=CARTESIAN_POINT('Ctrl Pts',(4.71862980099597,-0.0162999310916891,
-3.57651781406767));
#9717=CARTESIAN_POINT('Ctrl Pts',(4.71633782467676,-0.0752646307378745,
-3.58015950101522));
#9718=CARTESIAN_POINT('Ctrl Pts',(4.70723106756163,-0.154901470779693,-3.58526843745962));
#9719=CARTESIAN_POINT('Ctrl Pts',(4.70424912552254,-0.175924961958891,-3.58663486306575));
#9720=CARTESIAN_POINT('Ctrl Pts',(4.69807348634403,-0.212352899720643,-3.58904168435294));
#9721=CARTESIAN_POINT('Ctrl Pts',(4.69513632732219,-0.227795536579788,-3.59007436286857));
#9722=CARTESIAN_POINT('Ctrl Pts',(4.69040518364349,-0.250215833784624,-3.59159390961371));
#9723=CARTESIAN_POINT('Ctrl Pts',(4.68885477090343,-0.257243567266619,-3.59207313794342));
#9724=CARTESIAN_POINT('Ctrl Pts',(4.68601056251381,-0.269596555743125,-3.59292085723932));
#9725=CARTESIAN_POINT('Ctrl Pts',(4.68474381325762,-0.27492786513071,-3.59328848289595));
#9726=CARTESIAN_POINT('Ctrl Pts',(4.68202382649776,-0.286030269814525,-3.59405784293975));
#9727=CARTESIAN_POINT('Ctrl Pts',(4.68056396190131,-0.29179956537404,-3.59445977881113));
#9728=CARTESIAN_POINT('Ctrl Pts',(4.67663834910841,-0.306833294800882,-3.59551288213372));
#9729=CARTESIAN_POINT('Ctrl Pts',(4.67410313672481,-0.316078964705457,-3.59616624702305));
#9730=CARTESIAN_POINT('Ctrl Pts',(4.66290524382952,-0.355044833938312,-3.59894475683703));
#9731=CARTESIAN_POINT('Ctrl Pts',(4.65318613497871,-0.384445955186067,-3.6011033144089));
#9732=CARTESIAN_POINT('Ctrl Pts',(4.61315909462352,-0.491216437982374,-3.60917867050923));
#9733=CARTESIAN_POINT('Ctrl Pts',(4.57585118577394,-0.565693277627063,-3.61530191180339));
#9734=CARTESIAN_POINT('Ctrl Pts',(4.50288073557931,-0.679521450349702,-3.62519946191976));
#9735=CARTESIAN_POINT('Ctrl Pts',(4.47184481147958,-0.721515843933072,-3.62898326707604));
#9736=CARTESIAN_POINT('Ctrl Pts',(4.433626253769,-0.766626225089008,-3.63309545334704));
#9737=CARTESIAN_POINT('Ctrl Pts',(4.42908215366013,-0.771894391271796,-3.63357643603305));
#9738=CARTESIAN_POINT('Ctrl Pts',(4.42207594827429,-0.779872929591528,-3.63430561877818));
#9739=CARTESIAN_POINT('Ctrl Pts',(4.41964753900396,-0.782612489523834,-3.63455613127705));
#9740=CARTESIAN_POINT('Ctrl Pts',(4.41517824336473,-0.787607320299338,-3.63501304978695));
#9741=CARTESIAN_POINT('Ctrl Pts',(4.41314138754797,-0.789866017559552,-3.63521973166424));
#9742=CARTESIAN_POINT('Ctrl Pts',(4.40852305839145,-0.794947626180182,-3.63568487900524));
#9743=CARTESIAN_POINT('Ctrl Pts',(4.40593656766778,-0.797765868584669,-3.63594296643533));
#9744=CARTESIAN_POINT('Ctrl Pts',(4.39921561262334,-0.805017784434225,-3.6366075426417));
#9745=CARTESIAN_POINT('Ctrl Pts',(4.39506050377296,-0.80943229348126,-3.63701254791732));
#9746=CARTESIAN_POINT('Ctrl Pts',(4.36693300716531,-0.838857188146637,-3.63971679768988));
#9747=CARTESIAN_POINT('Ctrl Pts',(4.34189873955786,-0.86283403825283,-3.64194349424006));
#9748=CARTESIAN_POINT('Ctrl Pts',(4.29461691407231,-0.904278078606839,-3.64591638524916));
#9749=CARTESIAN_POINT('Ctrl Pts',(4.27273000453715,-0.922113574868906,-3.64767376245757));
#9750=CARTESIAN_POINT('Ctrl Pts',(4.21196687787682,-0.968096383986053,-3.65239835475215));
#9751=CARTESIAN_POINT('Ctrl Pts',(4.17197858776579,-0.994681622510907,-3.65534861435949));
#9752=CARTESIAN_POINT('Ctrl Pts',(4.11328239948327,-1.02873028431044,-3.65959207142446));
#9753=CARTESIAN_POINT('Ctrl Pts',(4.09583950175425,-1.03826655711673,-3.66084262547221));
#9754=CARTESIAN_POINT('Ctrl Pts',(4.07816923053759,-1.04735430775001,-3.66210420774532));
#9755=CARTESIAN_POINT('Origin',(3.53951905042299,8.32667268468867E-16,0.924367114736157));
#9756=CARTESIAN_POINT('',(4.07816926766421,-1.04735428865594,-4.2605248066102));
#9757=CARTESIAN_POINT('',(4.07816926526045,-1.04735428989218,-4.16229603312229));
#9758=CARTESIAN_POINT('',(4.07816926754759,-1.04735428871592,0.924367114736157));
#9759=CARTESIAN_POINT('',(2.36176953086107,0.00104804198854717,-3.92438851548543));
#9760=CARTESIAN_POINT('Ctrl Pts',(4.07816926766421,-1.04735428865594,-4.2605248066102));
#9761=CARTESIAN_POINT('Ctrl Pts',(4.08061053188268,-1.04609875600966,-4.2603336670524));
#9762=CARTESIAN_POINT('Ctrl Pts',(4.08304747073253,-1.04483465478307,-4.26014296728099));
#9763=CARTESIAN_POINT('Ctrl Pts',(4.09058011353672,-1.04089379733266,-4.25955387279466));
#9764=CARTESIAN_POINT('Ctrl Pts',(4.09566069109069,-1.03818816767703,-4.25915706029222));
#9765=CARTESIAN_POINT('Ctrl Pts',(4.10371247460442,-1.03382417148908,-4.25852925003506));
#9766=CARTESIAN_POINT('Ctrl Pts',(4.10669660193925,-1.03219003252469,-4.25829680768267));
#9767=CARTESIAN_POINT('Ctrl Pts',(4.11237478811221,-1.02904853904742,-4.25785502607278));
#9768=CARTESIAN_POINT('Ctrl Pts',(4.11506998269182,-1.02754353508609,-4.25764555868759));
#9769=CARTESIAN_POINT('Ctrl Pts',(4.12145446755203,-1.02394542027381,-4.25714984676672));
#9770=CARTESIAN_POINT('Ctrl Pts',(4.12513841664614,-1.02184294913762,-4.25686419382229));
#9771=CARTESIAN_POINT('Ctrl Pts',(4.1374993928772,-1.01469959644986,-4.25590673186276));
#9772=CARTESIAN_POINT('Ctrl Pts',(4.14612361904362,-1.00956756822577,-4.25524039136865));
#9773=CARTESIAN_POINT('Ctrl Pts',(4.16692687595816,-0.996825304375324,-4.25363450212652));
#9774=CARTESIAN_POINT('Ctrl Pts',(4.17903459791511,-0.989101193390206,-4.2527010839145));
#9775=CARTESIAN_POINT('Ctrl Pts',(4.22696655719119,-0.957274805137691,-4.24899812589751));
#9776=CARTESIAN_POINT('Ctrl Pts',(4.26159696136062,-0.931430723446777,-4.246304311219));
#9777=CARTESIAN_POINT('Ctrl Pts',(4.36809309949528,-0.842437036899015,-4.23769869052084));
#9778=CARTESIAN_POINT('Ctrl Pts',(4.43370864790271,-0.77243639778176,-4.23185193496188));
#9779=CARTESIAN_POINT('Ctrl Pts',(4.49867305956475,-0.683613570832528,-4.22466819902152));
#9780=CARTESIAN_POINT('Ctrl Pts',(4.50698906377458,-0.671792878114884,-4.22371727338928));
#9781=CARTESIAN_POINT('Ctrl Pts',(4.51898549233882,-0.654055822919525,-4.22229618232871));
#9782=CARTESIAN_POINT('Ctrl Pts',(4.52283453696928,-0.648254719046718,-4.22183229678599));
#9783=CARTESIAN_POINT('Ctrl Pts',(4.52960481301824,-0.637851825501089,-4.22100183696605));
#9784=CARTESIAN_POINT('Ctrl Pts',(4.53254598068112,-0.633263201731448,-4.22063601010524));
#9785=CARTESIAN_POINT('Ctrl Pts',(4.53869575680349,-0.623520513039784,-4.21986019915829));
#9786=CARTESIAN_POINT('Ctrl Pts',(4.54189656441925,-0.618361737018811,-4.2194499444115));
#9787=CARTESIAN_POINT('Ctrl Pts',(4.55033347188491,-0.604526234410318,-4.21835096284075));
#9788=CARTESIAN_POINT('Ctrl Pts',(4.55549760825921,-0.595806446434642,-4.21765967454887));
#9789=CARTESIAN_POINT('Ctrl Pts',(4.58109743404105,-0.551279658458068,-4.2141354960387));
#9790=CARTESIAN_POINT('Ctrl Pts',(4.59975315332767,-0.514487835870052,-4.21124090284159));
#9791=CARTESIAN_POINT('Ctrl Pts',(4.65758864327877,-0.383857388771443,-4.20102029895914));
#9792=CARTESIAN_POINT('Ctrl Pts',(4.68652801991301,-0.285994970160333,-4.19341781970315));
#9793=CARTESIAN_POINT('Ctrl Pts',(4.70631058953558,-0.162058183566401,-4.18441574865013));
#9794=CARTESIAN_POINT('Ctrl Pts',(4.70935693446314,-0.138364963283824,-4.1827247103124));
#9795=CARTESIAN_POINT('Ctrl Pts',(4.71226330031275,-0.108636171484832,-4.18065279521174));
#9796=CARTESIAN_POINT('Ctrl Pts',(4.71280030919271,-0.102674169125688,-4.18023978299348));
#9797=CARTESIAN_POINT('Ctrl Pts',(4.71357820507985,-0.0932326402845001,
-4.17958995557705));
#9798=CARTESIAN_POINT('Ctrl Pts',(4.71384912428019,-0.0897557924563585,
-4.17935156195845));
#9799=CARTESIAN_POINT('Ctrl Pts',(4.71430650257029,-0.0835290420166838,
-4.17892629997626));
#9800=CARTESIAN_POINT('Ctrl Pts',(4.71449875208627,-0.0807796971831158,
-4.17873912305569));
#9801=CARTESIAN_POINT('Ctrl Pts',(4.71493955105354,-0.0741410596285472,
-4.17828856083999));
#9802=CARTESIAN_POINT('Ctrl Pts',(4.71517844973885,-0.0702511773201224,
-4.17802570897476));
#9803=CARTESIAN_POINT('Ctrl Pts',(4.71585610857507,-0.0582432892694729,
-4.17721765704315));
#9804=CARTESIAN_POINT('Ctrl Pts',(4.71623013770644,-0.0501216641725522,
-4.17667586089719));
#9805=CARTESIAN_POINT('Ctrl Pts',(4.71690889531294,-0.0310987080354761,
-4.17541655246524));
#9806=CARTESIAN_POINT('Ctrl Pts',(4.71714638286752,-0.0201955690324883,
-4.17470223480156));
#9807=CARTESIAN_POINT('Ctrl Pts',(4.71745243816693,0.0186025334968413,-4.17218195649293));
#9808=CARTESIAN_POINT('Ctrl Pts',(4.71668149644096,0.0464963480844941,-4.1704095728507));
#9809=CARTESIAN_POINT('Ctrl Pts',(4.70965218591332,0.157640511496342,-4.16341498001619));
#9810=CARTESIAN_POINT('Ctrl Pts',(4.6955434647511,0.240146314751699,-4.15835744008072));
#9811=CARTESIAN_POINT('Ctrl Pts',(4.66184794563702,0.359307605937843,-4.15053677189155));
#9812=CARTESIAN_POINT('Ctrl Pts',(4.64887736267885,0.397552145251989,-4.14794645042967));
#9813=CARTESIAN_POINT('Ctrl Pts',(4.63010914142649,0.444766894451285,-4.14460448463226));
#9814=CARTESIAN_POINT('Ctrl Pts',(4.62611865738864,0.454428893920434,-4.14391283952734));
#9815=CARTESIAN_POINT('Ctrl Pts',(4.61958077249236,0.469680153178574,-4.14280810627163));
#9816=CARTESIAN_POINT('Ctrl Pts',(4.61711728888309,0.475304958764741,-4.1423978326367));
#9817=CARTESIAN_POINT('Ctrl Pts',(4.61261146766434,0.485377874547179,-4.14165787604038));
#9818=CARTESIAN_POINT('Ctrl Pts',(4.61058516105375,0.489833035289314,-4.14132874190786));
#9819=CARTESIAN_POINT('Ctrl Pts',(4.60576755941568,0.500252479086613,-4.14055454423502));
#9820=CARTESIAN_POINT('Ctrl Pts',(4.60295391815795,0.506206188033336,-4.14010872758931));
#9821=CARTESIAN_POINT('Ctrl Pts',(4.5946332940985,0.523437194382726,-4.13880825412039));
#9822=CARTESIAN_POINT('Ctrl Pts',(4.58899594478057,0.534650157361515,-4.1379491589722));
#9823=CARTESIAN_POINT('Ctrl Pts',(4.5758153398171,0.559855057269436,-4.13598807522075));
#9824=CARTESIAN_POINT('Ctrl Pts',(4.56816596785051,0.573788429698947,-4.13488257260118));
#9825=CARTESIAN_POINT('Ctrl Pts',(4.5417921325487,0.619605290264273,-4.13117457130428));
#9826=CARTESIAN_POINT('Ctrl Pts',(4.52185000024186,0.650759174847572,-4.1285326195553));
#9827=CARTESIAN_POINT('Ctrl Pts',(4.45689326441853,0.742430159928311,-4.12039866623981));
#9828=CARTESIAN_POINT('Ctrl Pts',(4.40750685952794,0.79960891318014,-4.11480499022491));
#9829=CARTESIAN_POINT('Ctrl Pts',(4.32905812099177,0.87453929033869,-4.10694970727554));
#9830=CARTESIAN_POINT('Ctrl Pts',(4.30416374763319,0.89638710557455,-4.10458452546581));
#9831=CARTESIAN_POINT('Ctrl Pts',(4.27371548301067,0.920916136791995,-4.10186754626579));
#9832=CARTESIAN_POINT('Ctrl Pts',(4.26902277500115,0.924637903284017,-4.10145351954349));
#9833=CARTESIAN_POINT('Ctrl Pts',(4.26130386123392,0.930664394469423,-4.10078043807841));
#9834=CARTESIAN_POINT('Ctrl Pts',(4.25829458963188,0.932990489505517,-4.10051997928127));
#9835=CARTESIAN_POINT('Ctrl Pts',(4.25285895846267,0.937150194238444,-4.10005308296787));
#9836=CARTESIAN_POINT('Ctrl Pts',(4.25043672856546,0.93898901297233,-4.09984629347443));
#9837=CARTESIAN_POINT('Ctrl Pts',(4.24506685150815,0.943032826812734,-4.09939065465233));
#9838=CARTESIAN_POINT('Ctrl Pts',(4.24211597575685,0.945233396309607,-4.09914210736358));
#9839=CARTESIAN_POINT('Ctrl Pts',(4.2334820615523,0.951609231768336,-4.09842006761506));
#9840=CARTESIAN_POINT('Ctrl Pts',(4.22777166141942,0.955747424930096,-4.09794901388681));
#9841=CARTESIAN_POINT('Ctrl Pts',(4.17440171399425,0.993696965989265,-4.09360291461117));
#9842=CARTESIAN_POINT('Ctrl Pts',(4.124317875001,1.02397359821846,-4.08993682324242));
#9843=CARTESIAN_POINT('Ctrl Pts',(3.98289042213369,1.09569211070334,-4.08009061752558));
#9844=CARTESIAN_POINT('Ctrl Pts',(3.88819542218631,1.12939903378864,-4.07398770888766));
#9845=CARTESIAN_POINT('Ctrl Pts',(3.776789809715,1.15368589955443,-4.06653731535964));
#9846=CARTESIAN_POINT('Ctrl Pts',(3.76314746784564,1.15640774488468,-4.06562140119996));
#9847=CARTESIAN_POINT('Ctrl Pts',(3.74271296501456,1.1601096155009,-4.06424268845803));
#9848=CARTESIAN_POINT('Ctrl Pts',(3.73595493440078,1.16127302003279,-4.06378562719153));
#9849=CARTESIAN_POINT('Ctrl Pts',(3.72381890119517,1.16325328882587,-4.06296269762399));
#9850=CARTESIAN_POINT('Ctrl Pts',(3.71844462952846,1.16409204292713,-4.06259752475349));
#9851=CARTESIAN_POINT('Ctrl Pts',(3.70699846376436,1.16579729199978,-4.06181809217536));
#9852=CARTESIAN_POINT('Ctrl Pts',(3.70092524502847,1.16665364089561,-4.06140352734916));
#9853=CARTESIAN_POINT('Ctrl Pts',(3.68451695183003,1.16883670494143,-4.06028062581848));
#9854=CARTESIAN_POINT('Ctrl Pts',(3.67417070814974,1.17007373836235,-4.05956952871269));
#9855=CARTESIAN_POINT('Ctrl Pts',(3.61847336120699,1.17598461349988,-4.05572402320733));
#9856=CARTESIAN_POINT('Ctrl Pts',(3.57290172212529,1.17815883924604,-4.05251340373268));
#9857=CARTESIAN_POINT('Ctrl Pts',(3.47384477911607,1.17713305972653,-4.04539803565048));
#9858=CARTESIAN_POINT('Ctrl Pts',(3.4204692722681,1.17293722866013,-4.04147650344936));
#9859=CARTESIAN_POINT('Ctrl Pts',(3.30773673850691,1.15630001922453,-4.03311378444394));
#9860=CARTESIAN_POINT('Ctrl Pts',(3.24866864476852,1.1428736919329,-4.02868339999732));
#9861=CARTESIAN_POINT('Ctrl Pts',(3.18132310991926,1.12200312644769,-4.0237393033503));
#9862=CARTESIAN_POINT('Ctrl Pts',(3.17179546633534,1.11891676626416,-4.02304254796327));
#9863=CARTESIAN_POINT('Ctrl Pts',(3.15857750680626,1.1144478946439,-4.02208079078059));
#9864=CARTESIAN_POINT('Ctrl Pts',(3.15485333033057,1.11316793630992,-4.02181035757952));
#9865=CARTESIAN_POINT('Ctrl Pts',(3.14843852575694,1.11092720164919,-4.02134556514466));
#9866=CARTESIAN_POINT('Ctrl Pts',(3.14574487404639,1.10997528017534,-4.02115070569896));
#9867=CARTESIAN_POINT('Ctrl Pts',(3.14006778549723,1.10794576182489,-4.02074072307446));
#9868=CARTESIAN_POINT('Ctrl Pts',(3.13708518946234,1.10686589620766,-4.02052574057102));
#9869=CARTESIAN_POINT('Ctrl Pts',(3.12987506350698,1.10422243353542,-4.02000695764937));
#9870=CARTESIAN_POINT('Ctrl Pts',(3.12565202410281,1.10264657298445,-4.01970386605013));
#9871=CARTESIAN_POINT('Ctrl Pts',(3.11012318943527,1.0967500818957,-4.01859180379022));
#9872=CARTESIAN_POINT('Ctrl Pts',(3.09887468398434,1.09227932231176,-4.01779108428916));
#9873=CARTESIAN_POINT('Ctrl Pts',(3.07047745353267,1.08048262726898,-4.01577707660513));
#9874=CARTESIAN_POINT('Ctrl Pts',(3.05342965181525,1.07292120034171,-4.01457497722258));
#9875=CARTESIAN_POINT('Ctrl Pts',(2.97629148858613,1.03649088568396,-4.00913638265606));
#9876=CARTESIAN_POINT('Ctrl Pts',(2.91853692779347,1.00295617033013,-4.00506060738765));
#9877=CARTESIAN_POINT('Ctrl Pts',(2.80701036876662,0.924853681040899,-3.99661694422729));
#9878=CARTESIAN_POINT('Ctrl Pts',(2.75374048136893,0.880041723597862,-3.99225762688552));
#9879=CARTESIAN_POINT('Ctrl Pts',(2.69736398445248,0.82339484354784,-3.98701313005524));
#9880=CARTESIAN_POINT('Ctrl Pts',(2.69009288619344,0.815891784284244,-3.98632349404621));
#9881=CARTESIAN_POINT('Ctrl Pts',(2.67829502354259,0.803388888367515,-3.98518177511804));
#9882=CARTESIAN_POINT('Ctrl Pts',(2.67370957558064,0.798445039140589,-3.98473219019675));
#9883=CARTESIAN_POINT('Ctrl Pts',(2.66550904555044,0.789449841766682,-3.98391736286575));
#9884=CARTESIAN_POINT('Ctrl Pts',(2.66187902113842,0.785412323938286,-3.98355275898036));
#9885=CARTESIAN_POINT('Ctrl Pts',(2.6541573973039,0.776703525461425,-3.98276864421313));
#9886=CARTESIAN_POINT('Ctrl Pts',(2.6500745810392,0.772024712435805,-3.98234878701259));
#9887=CARTESIAN_POINT('Ctrl Pts',(2.63959839958359,0.75982584105821,-3.98125759556522));
#9888=CARTESIAN_POINT('Ctrl Pts',(2.63326233934121,0.752257435910597,-3.98058397388087));
#9889=CARTESIAN_POINT('Ctrl Pts',(2.59972377305831,0.711156977530592,-3.9769428939996));
#9890=CARTESIAN_POINT('Ctrl Pts',(2.57428886130969,0.676231681490388,-3.97390713292723));
#9891=CARTESIAN_POINT('Ctrl Pts',(2.51893595613765,0.590720136221662,-3.96660612569285));
#9892=CARTESIAN_POINT('Ctrl Pts',(2.49077131701302,0.539135696131241,-3.96229869425451));
#9893=CARTESIAN_POINT('Ctrl Pts',(2.45498938701325,0.460086113927367,-3.95593211292864));
#9894=CARTESIAN_POINT('Ctrl Pts',(2.44432650274012,0.434093534690042,-3.95387480918752));
#9895=CARTESIAN_POINT('Ctrl Pts',(2.42242302430421,0.374738861009808,-3.94928575615794));
#9896=CARTESIAN_POINT('Ctrl Pts',(2.4117268983113,0.341200999528359,-3.94676744994914));
#9897=CARTESIAN_POINT('Ctrl Pts',(2.4009604870144,0.301357724900448,-3.94389859401908));
#9898=CARTESIAN_POINT('Ctrl Pts',(2.39941882629276,0.295471764326554,-3.94347789072222));
#9899=CARTESIAN_POINT('Ctrl Pts',(2.39698060395358,0.285859486389673,-3.94279618734842));
#9900=CARTESIAN_POINT('Ctrl Pts',(2.39605651733753,0.282140362398127,-3.94253372421479));
#9901=CARTESIAN_POINT('Ctrl Pts',(2.39443140962181,0.275460727757623,-3.94206473919431));
#9902=CARTESIAN_POINT('Ctrl Pts',(2.39372369319832,0.272501959004331,-3.94185785017745));
#9903=CARTESIAN_POINT('Ctrl Pts',(2.39219069751879,0.26598135243111,-3.94140377386248));
#9904=CARTESIAN_POINT('Ctrl Pts',(2.39137053436685,0.262418397229183,-3.94115687522502));
#9905=CARTESIAN_POINT('Ctrl Pts',(2.38970274045107,0.255015641548476,-3.94064630343271));
#9906=CARTESIAN_POINT('Ctrl Pts',(2.38885771991015,0.251175292656659,-3.94038277413045));
#9907=CARTESIAN_POINT('Ctrl Pts',(2.38671054185215,0.241178766979878,-3.9397001135755));
#9908=CARTESIAN_POINT('Ctrl Pts',(2.38543843811288,0.235016168386021,-3.93928252983237));
#9909=CARTESIAN_POINT('Ctrl Pts',(2.36935683554983,0.153829124494053,-3.93382045884806));
#9910=CARTESIAN_POINT('Ctrl Pts',(2.36183758556985,0.0775370159629636,-3.92912004385086));
#9911=CARTESIAN_POINT('Ctrl Pts',(2.36176951678359,0.00104809931671655,
-3.92438854089391));
#9912=CARTESIAN_POINT('Ctrl Pts',(2.36176951673139,0.00104804065385484,
-3.9243885372651));
#9913=CARTESIAN_POINT('Ctrl Pts',(2.36170039876251,-0.0766241902070196,
-3.91958383605501));
#9914=CARTESIAN_POINT('Ctrl Pts',(2.3693146407461,-0.154105831735525,-3.91476439767892));
#9915=CARTESIAN_POINT('Ctrl Pts',(2.38650654758807,-0.240338486056077,-3.90902709243526));
#9916=CARTESIAN_POINT('Ctrl Pts',(2.38864487921786,-0.250377816775807,-3.90835358176155));
#9917=CARTESIAN_POINT('Ctrl Pts',(2.39238328244189,-0.266868414827862,-3.90723738745212));
#9918=CARTESIAN_POINT('Ctrl Pts',(2.39390725830348,-0.273336495541825,-3.90679706293527));
#9919=CARTESIAN_POINT('Ctrl Pts',(2.39698832868437,-0.285934627436938,-3.90593430283839));
#9920=CARTESIAN_POINT('Ctrl Pts',(2.39854022868984,-0.292065723787995,-3.90551204336876));
#9921=CARTESIAN_POINT('Ctrl Pts',(2.40137619339858,-0.302902105357035,-3.90476136262689));
#9922=CARTESIAN_POINT('Ctrl Pts',(2.40264025681513,-0.307612509248537,-3.90443358675066));
#9923=CARTESIAN_POINT('Ctrl Pts',(2.40562100562091,-0.318450594679178,-3.9036759577904));
#9924=CARTESIAN_POINT('Ctrl Pts',(2.4073581581274,-0.324572439478732,-3.90324545733122));
#9925=CARTESIAN_POINT('Ctrl Pts',(2.4122829544837,-0.341407041688736,-3.90205439266956));
#9926=CARTESIAN_POINT('Ctrl Pts',(2.41557354704853,-0.352088731177394,-3.90129054517984));
#9927=CARTESIAN_POINT('Ctrl Pts',(2.43634133737977,-0.41624365759082,-3.89665232042659));
#9928=CARTESIAN_POINT('Ctrl Pts',(2.4574768928721,-0.468447343896776,-3.89265983053281));
#9929=CARTESIAN_POINT('Ctrl Pts',(2.50249411084264,-0.560163981593247,-3.8852571726978));
#9930=CARTESIAN_POINT('Ctrl Pts',(2.52512414925314,-0.600172528765996,-3.88188198609267));
#9931=CARTESIAN_POINT('Ctrl Pts',(2.57284611689614,-0.674097993457289,-3.87542768333664));
#9932=CARTESIAN_POINT('Ctrl Pts',(2.59753970553716,-0.708194906783507,-3.87235238995357));
#9933=CARTESIAN_POINT('Ctrl Pts',(2.63188899261136,-0.750639562423619,-3.86845176226482));
#9934=CARTESIAN_POINT('Ctrl Pts',(2.63992692770269,-0.760253979608165,-3.86756314440714));
#9935=CARTESIAN_POINT('Ctrl Pts',(2.65527860910518,-0.778032115592743,-3.86591309394098));
#9936=CARTESIAN_POINT('Ctrl Pts',(2.66255583779512,-0.786225588577091,-3.86514977972861));
#9937=CARTESIAN_POINT('Ctrl Pts',(2.6722640627135,-0.796853597043191,-3.86415720818341));
#9938=CARTESIAN_POINT('Ctrl Pts',(2.6745925738031,-0.799380422330187,-3.86392103715912));
#9939=CARTESIAN_POINT('Ctrl Pts',(2.67918713808672,-0.804322716273644,-3.86345880016781));
#9940=CARTESIAN_POINT('Ctrl Pts',(2.68145238734384,-0.806738888177693,-3.86323267942849));
#9941=CARTESIAN_POINT('Ctrl Pts',(2.68585148340174,-0.811391583793172,-3.86279702739081));
#9942=CARTESIAN_POINT('Ctrl Pts',(2.68798397528699,-0.813629297225322,-3.86258740518227));
#9943=CARTESIAN_POINT('Ctrl Pts',(2.6927227766992,-0.818562883000912,-3.86212496478452));
#9944=CARTESIAN_POINT('Ctrl Pts',(2.69533322523354,-0.821254781494435,-3.86187245860051));
#9945=CARTESIAN_POINT('Ctrl Pts',(2.70465371696756,-0.830774687812822,-3.86097860201256));
#9946=CARTESIAN_POINT('Ctrl Pts',(2.71143432135321,-0.837533523395143,-3.86034239227368));
#9947=CARTESIAN_POINT('Ctrl Pts',(2.77433497494493,-0.898721453754918,-3.85455920813305));
#9948=CARTESIAN_POINT('Ctrl Pts',(2.83567013750935,-0.947526894879376,-3.84976431458468));
#9949=CARTESIAN_POINT('Ctrl Pts',(2.9470042952222,-1.01929659580887,-3.84156873551229));
#9950=CARTESIAN_POINT('Ctrl Pts',(2.99458504989597,-1.04550733873365,-3.83820211639131));
#9951=CARTESIAN_POINT('Ctrl Pts',(3.06215856294847,-1.07686193613802,-3.83344580572473));
#9952=CARTESIAN_POINT('Ctrl Pts',(3.08073279744557,-1.08490541883781,-3.83214132927302));
#9953=CARTESIAN_POINT('Ctrl Pts',(3.11344332113403,-1.09808030328254,-3.82984201649596));
#9954=CARTESIAN_POINT('Ctrl Pts',(3.12748800353908,-1.10342705366624,-3.82885415929797));
#9955=CARTESIAN_POINT('Ctrl Pts',(3.14834887895483,-1.11091489742362,-3.82738407349395));
#9956=CARTESIAN_POINT('Ctrl Pts',(3.15508877454961,-1.11326518476249,-3.82690868594501));
#9957=CARTESIAN_POINT('Ctrl Pts',(3.16703280325044,-1.11730882220583,-3.82606529455302));
#9958=CARTESIAN_POINT('Ctrl Pts',(3.17222820212774,-1.11902745254394,-3.82569812615088));
#9959=CARTESIAN_POINT('Ctrl Pts',(3.18312552652671,-1.1225482069398,-3.82492725096427));
#9960=CARTESIAN_POINT('Ctrl Pts',(3.18882956372489,-1.1243432315911,-3.82452332607278));
#9961=CARTESIAN_POINT('Ctrl Pts',(3.20383649356018,-1.12894051128053,-3.82345939284191));
#9962=CARTESIAN_POINT('Ctrl Pts',(3.21316066174228,-1.13167117544022,-3.82279710355218));
#9963=CARTESIAN_POINT('Ctrl Pts',(3.25346538739096,-1.14293523677766,-3.81992824848856));
#9964=CARTESIAN_POINT('Ctrl Pts',(3.28475164447928,-1.15031338395358,-3.81768550808439));
#9965=CARTESIAN_POINT('Ctrl Pts',(3.42387585168212,-1.17716861087855,-3.80763731909785));
#9966=CARTESIAN_POINT('Ctrl Pts',(3.53380348514754,-1.18281891820952,-3.79943611846804));
#9967=CARTESIAN_POINT('Ctrl Pts',(3.66029971474918,-1.17167043377599,-3.79030886762797));
#9968=CARTESIAN_POINT('Ctrl Pts',(3.67764737986652,-1.16975219821265,-3.78906568128696));
#9969=CARTESIAN_POINT('Ctrl Pts',(3.70645186261257,-1.165917325074,-3.78702210444013));
#9970=CARTESIAN_POINT('Ctrl Pts',(3.71793410087469,-1.16421555900369,-3.78621298569804));
#9971=CARTESIAN_POINT('Ctrl Pts',(3.73382413508723,-1.16161989665838,-3.78510259201308));
#9972=CARTESIAN_POINT('Ctrl Pts',(3.73825434938933,-1.16087016192049,-3.7847940197792));
#9973=CARTESIAN_POINT('Ctrl Pts',(3.74576394291016,-1.15955504724416,-3.78427280188949));
#9974=CARTESIAN_POINT('Ctrl Pts',(3.74884552901996,-1.15900271333646,-3.78405944573402));
#9975=CARTESIAN_POINT('Ctrl Pts',(3.75517593532824,-1.15784199901858,-3.78362228530786));
#9976=CARTESIAN_POINT('Ctrl Pts',(3.75842444390212,-1.15723222219465,-3.7833985595264));
#9977=CARTESIAN_POINT('Ctrl Pts',(3.76689223287052,-1.1556058030122,-3.78281686364914));
#9978=CARTESIAN_POINT('Ctrl Pts',(3.77210734362133,-1.15456746211805,-3.78246008364174));
#9979=CARTESIAN_POINT('Ctrl Pts',(3.79348007828285,-1.1501614068025,-3.78100329897669));
#9980=CARTESIAN_POINT('Ctrl Pts',(3.80957395855438,-1.14648937147744,-3.77991897405437));
#9981=CARTESIAN_POINT('Ctrl Pts',(3.84436270214127,-1.13777856704782,-3.7775921483107));
#9982=CARTESIAN_POINT('Ctrl Pts',(3.86302134036225,-1.13261470280076,-3.77635501665119));
#9983=CARTESIAN_POINT('Ctrl Pts',(3.94934775508302,-1.10641588465514,-3.77064656442402));
#9984=CARTESIAN_POINT('Ctrl Pts',(4.01515567697647,-1.0797619320866,-3.76633114629972));
#9985=CARTESIAN_POINT('Ctrl Pts',(4.07816926790565,-1.04735428853177,-3.76191690485895));
#9986=CARTESIAN_POINT('Ctrl Pts',(4.07816923053759,-1.04735430775001,-3.66210420774532));
#9987=CARTESIAN_POINT('Ctrl Pts',(4.04844861985459,-1.06263950033389,-3.66422613304709));
#9988=CARTESIAN_POINT('Ctrl Pts',(4.01808480614548,-1.07665583766756,-3.66637966969037));
#9989=CARTESIAN_POINT('Ctrl Pts',(3.9771413196992,-1.09348027249041,-3.66928898261599));
#9990=CARTESIAN_POINT('Ctrl Pts',(3.9670678205978,-1.09745815102189,-3.67000513538608));
#9991=CARTESIAN_POINT('Ctrl Pts',(3.95112338361915,-1.10350153802698,-3.67113993062783));
#9992=CARTESIAN_POINT('Ctrl Pts',(3.94528831817094,-1.10566046794659,-3.67155548449973));
#9993=CARTESIAN_POINT('Ctrl Pts',(3.93433172578966,-1.10961591054872,-3.67233639632326));
#9994=CARTESIAN_POINT('Ctrl Pts',(3.9292143348106,-1.11142345719827,-3.67270138043947));
#9995=CARTESIAN_POINT('Ctrl Pts',(3.91772933681739,-1.11539107618947,-3.67352116899733));
#9996=CARTESIAN_POINT('Ctrl Pts',(3.91135539921351,-1.11753210247141,-3.67397658113456));
#9997=CARTESIAN_POINT('Ctrl Pts',(3.89508930371856,-1.12284137196217,-3.67514007839558));
#9998=CARTESIAN_POINT('Ctrl Pts',(3.88517309685208,-1.1259334881902,-3.67585059333827));
#9999=CARTESIAN_POINT('Ctrl Pts',(3.80299939013408,-1.15036943320402,-3.68174998840933));
#10000=CARTESIAN_POINT('Ctrl Pts',(3.72890066998285,-1.16486156269254,-3.68715976191397));
#10001=CARTESIAN_POINT('Ctrl Pts',(3.59597400316395,-1.17783693902623,-3.69692943800183));
#10002=CARTESIAN_POINT('Ctrl Pts',(3.53766849725277,-1.17918779262541,-3.70123136369423));
#10003=CARTESIAN_POINT('Ctrl Pts',(3.45922160018935,-1.17518497517152,-3.7069020253475));
#10004=CARTESIAN_POINT('Ctrl Pts',(3.43897064712184,-1.17362580168143,-3.70835474100237));
#10005=CARTESIAN_POINT('Ctrl Pts',(3.40587383062965,-1.17021454018066,-3.71070087284032));
#10006=CARTESIAN_POINT('Ctrl Pts',(3.39300078898572,-1.16867255833062,-3.71160638532605));
#10007=CARTESIAN_POINT('Ctrl Pts',(3.37550898727766,-1.16628373541297,-3.71282493220717));
#10008=CARTESIAN_POINT('Ctrl Pts',(3.37086651807613,-1.16562145549307,-3.71314720226167));
#10009=CARTESIAN_POINT('Ctrl Pts',(3.3630935162249,-1.16446517164721,-3.71368473403851));
#10010=CARTESIAN_POINT('Ctrl Pts',(3.35996083661272,-1.16398623434157,-3.71390081027675));
#10011=CARTESIAN_POINT('Ctrl Pts',(3.35400605052876,-1.16305122890294,-3.71431042739958));
#10012=CARTESIAN_POINT('Ctrl Pts',(3.35118362085546,-1.16259752304727,-3.71450410202761));
#10013=CARTESIAN_POINT('Ctrl Pts',(3.3444692137112,-1.16149308829024,-3.71496377401127));
#10014=CARTESIAN_POINT('Ctrl Pts',(3.3405787684138,-1.16083306218068,-3.71522925949236));
#10015=CARTESIAN_POINT('Ctrl Pts',(3.32677780327535,-1.15842026594744,-3.71616823560734));
#10016=CARTESIAN_POINT('Ctrl Pts',(3.31688617931598,-1.15655997338567,-3.7168360851204));
#10017=CARTESIAN_POINT('Ctrl Pts',(3.24861442522589,-1.14281188569118,-3.72141750979336));
#10018=CARTESIAN_POINT('Ctrl Pts',(3.19117834922134,-1.1266344066395,-3.72513186763262));
#10019=CARTESIAN_POINT('Ctrl Pts',(3.072179346441,-1.08313983084812,-3.73298225008632));
#10020=CARTESIAN_POINT('Ctrl Pts',(3.01123910751551,-1.054759687974,-3.73710183304628));
#10021=CARTESIAN_POINT('Ctrl Pts',(2.92322398438618,-1.00422021555506,-3.74355374607896));
#10022=CARTESIAN_POINT('Ctrl Pts',(2.89416644473011,-0.985797908113418,
-3.74577348102382));
#10023=CARTESIAN_POINT('Ctrl Pts',(2.85809108232158,-0.960647159867072,
-3.74867159772587));
#10024=CARTESIAN_POINT('Ctrl Pts',(2.85029123492305,-0.955066516465092,
-3.74930706235956));
#10025=CARTESIAN_POINT('Ctrl Pts',(2.83776269167216,-0.945869177634443,
-3.75034274759836));
#10026=CARTESIAN_POINT('Ctrl Pts',(2.8329916314314,-0.9423107195927,-3.75074074043638));
#10027=CARTESIAN_POINT('Ctrl Pts',(2.82388043338371,-0.935407107718452,
-3.75150782500438));
#10028=CARTESIAN_POINT('Ctrl Pts',(2.81953625700718,-0.932067520522219,
-3.75187669438017));
#10029=CARTESIAN_POINT('Ctrl Pts',(2.80963785389392,-0.92434762760609,-3.75272447564166));
#10030=CARTESIAN_POINT('Ctrl Pts',(2.8040995142685,-0.919947389676309,-3.75320416160331));
#10031=CARTESIAN_POINT('Ctrl Pts',(2.78658021839377,-0.905768916688391,
-3.75473889947827));
#10032=CARTESIAN_POINT('Ctrl Pts',(2.77475248973425,-0.895804824435225,
-3.75580129639469));
#10033=CARTESIAN_POINT('Ctrl Pts',(2.70327046541717,-0.833138235252452,
-3.76238907377542));
#10034=CARTESIAN_POINT('Ctrl Pts',(2.64890026058588,-0.774741861973427,
-3.76815310433015));
#10035=CARTESIAN_POINT('Ctrl Pts',(2.57282732747799,-0.674354202017694,
-3.77739103106325));
#10036=CARTESIAN_POINT('Ctrl Pts',(2.54702083012893,-0.635762553685175,
-3.78080459783862));
#10037=CARTESIAN_POINT('Ctrl Pts',(2.51287734126004,-0.577535816048185,
-3.78568297920743));
#10038=CARTESIAN_POINT('Ctrl Pts',(2.50268866524345,-0.559038171718371,
-3.7871950688076));
#10039=CARTESIAN_POINT('Ctrl Pts',(2.48688643539726,-0.52842916307065,-3.78962575089257));
#10040=CARTESIAN_POINT('Ctrl Pts',(2.48097187246806,-0.516479149832285,
-3.79055747924329));
#10041=CARTESIAN_POINT('Ctrl Pts',(2.47323115548551,-0.500147631308321,
-3.79180520057095));
#10042=CARTESIAN_POINT('Ctrl Pts',(2.47122693711902,-0.495852287053195,
-3.79213099258052));
#10043=CARTESIAN_POINT('Ctrl Pts',(2.46792169721483,-0.488655588196798,
-3.79267275505615));
#10044=CARTESIAN_POINT('Ctrl Pts',(2.46660641339628,-0.485760893170416,
-3.79288956707426));
#10045=CARTESIAN_POINT('Ctrl Pts',(2.46413455682944,-0.480261776050492,
-3.79329932190493));
#10046=CARTESIAN_POINT('Ctrl Pts',(2.4629756907694,-0.477658432169053,-3.79349240647044));
#10047=CARTESIAN_POINT('Ctrl Pts',(2.46024906773894,-0.471472858947253,
-3.79394911020788));
#10048=CARTESIAN_POINT('Ctrl Pts',(2.45868966710349,-0.467886949467087,
-3.79421223296509));
#10049=CARTESIAN_POINT('Ctrl Pts',(2.45326485745182,-0.455240511269034,
-3.79513466435501));
#10050=CARTESIAN_POINT('Ctrl Pts',(2.44949515812842,-0.446139019402175,
-3.79578858715235));
#10051=CARTESIAN_POINT('Ctrl Pts',(2.42015070718981,-0.372697193087162,
-3.80099414988089));
#10052=CARTESIAN_POINT('Ctrl Pts',(2.40017724275753,-0.30625409905891,-3.80527350177618));
#10053=CARTESIAN_POINT('Ctrl Pts',(2.36996520026676,-0.160110655326258,
-3.81450523120774));
#10054=CARTESIAN_POINT('Ctrl Pts',(2.36179525311326,-0.0803519521974262,
-3.81944418741669));
#10055=CARTESIAN_POINT('Ctrl Pts',(2.36176366402195,0.0162853768794864,
-3.82572603094372));
#10056=CARTESIAN_POINT('Ctrl Pts',(2.36211215340961,0.0329532537253749,
-3.82681939802594));
#10057=CARTESIAN_POINT('Ctrl Pts',(2.36310117832572,0.0564132401608757,
-3.8283747806013));
#10058=CARTESIAN_POINT('Ctrl Pts',(2.3634471299522,0.063216280260236,-3.82882776666044));
#10059=CARTESIAN_POINT('Ctrl Pts',(2.36415372310044,0.0750810022526736,
-3.82962136498457));
#10060=CARTESIAN_POINT('Ctrl Pts',(2.36448810225051,0.0801441141953606,
-3.82996116002476));
#10061=CARTESIAN_POINT('Ctrl Pts',(2.36525846034585,0.0907645415065579,
-3.83067638137945));
#10062=CARTESIAN_POINT('Ctrl Pts',(2.36570119609865,0.0963212252669191,
-3.8310520083426));
#10063=CARTESIAN_POINT('Ctrl Pts',(2.36685535434355,0.109614202312183,-3.83195409902611));
#10064=CARTESIAN_POINT('Ctrl Pts',(2.3676039034977,0.117346925179376,-3.83248169915888));
#10065=CARTESIAN_POINT('Ctrl Pts',(2.37045749641022,0.144066154517063,-3.83431489834426));
#10066=CARTESIAN_POINT('Ctrl Pts',(2.3729478252546,0.16300759709244,-3.83563230288415));
#10067=CARTESIAN_POINT('Ctrl Pts',(2.38014251869302,0.209037603783719,-3.83887928813729));
#10068=CARTESIAN_POINT('Ctrl Pts',(2.38533668375326,0.236037128911488,-3.84082281696858));
#10069=CARTESIAN_POINT('Ctrl Pts',(2.41473604672644,0.36445509295537,-3.85025063472687));
#10070=CARTESIAN_POINT('Ctrl Pts',(2.45138854482873,0.462528755992019,-3.85805991057015));
#10071=CARTESIAN_POINT('Ctrl Pts',(2.51050737087764,0.573310564704789,-3.86703725347443));
#10072=CARTESIAN_POINT('Ctrl Pts',(2.52105993057718,0.591854035582738,-3.86854355169125));
#10073=CARTESIAN_POINT('Ctrl Pts',(2.53513277427362,0.61509128959281,-3.87042653631821));
#10074=CARTESIAN_POINT('Ctrl Pts',(2.53819150074025,0.620058245661271,-3.87082874587661));
#10075=CARTESIAN_POINT('Ctrl Pts',(2.54310139283704,0.627900153576863,-3.8714630698678));
#10076=CARTESIAN_POINT('Ctrl Pts',(2.54492834297265,0.630790041628274,-3.87169667964179));
#10077=CARTESIAN_POINT('Ctrl Pts',(2.54842546247159,0.636268853358129,-3.87213922288277));
#10078=CARTESIAN_POINT('Ctrl Pts',(2.5500931929083,0.638859160167936,-3.87234829483588));
#10079=CARTESIAN_POINT('Ctrl Pts',(2.55406060805322,0.644968520217937,-3.87284108596375));
#10080=CARTESIAN_POINT('Ctrl Pts',(2.55636899742934,0.648481848907288,-3.87312423286438));
#10081=CARTESIAN_POINT('Ctrl Pts',(2.56412947459199,0.660156471728367,-3.87406456868759));
#10082=CARTESIAN_POINT('Ctrl Pts',(2.56966493571705,0.668262226576556,-3.87471655080822));
#10083=CARTESIAN_POINT('Ctrl Pts',(2.58330905339852,0.687715037914072,-3.87628151526722));
#10084=CARTESIAN_POINT('Ctrl Pts',(2.59151932480689,0.698989333478457,-3.87718876918013));
#10085=CARTESIAN_POINT('Ctrl Pts',(2.62472078783833,0.742919907260766,-3.88073637672632));
#10086=CARTESIAN_POINT('Ctrl Pts',(2.65121623596041,0.774405887494549,-3.88330745514829));
#10087=CARTESIAN_POINT('Ctrl Pts',(2.746945496837,0.876771730365237,-3.89200681350264));
#10088=CARTESIAN_POINT('Ctrl Pts',(2.82342800962459,0.940272890584698,-3.89804785574503));
#10089=CARTESIAN_POINT('Ctrl Pts',(2.918802157243,1.00100099562416,-3.90543403210144));
#10090=CARTESIAN_POINT('Ctrl Pts',(2.93078694217764,1.00833409532424,-3.90635893675167));
#10091=CARTESIAN_POINT('Ctrl Pts',(2.94883483682975,1.01893798109636,-3.90774850056985));
#10092=CARTESIAN_POINT('Ctrl Pts',(2.95480038857649,1.0223729909505,-3.90820728502022));
#10093=CARTESIAN_POINT('Ctrl Pts',(2.96553460067299,1.0284291520166,-3.9090320542742));
#10094=CARTESIAN_POINT('Ctrl Pts',(2.97029199832814,1.03106994463999,-3.90939733020954));
#10095=CARTESIAN_POINT('Ctrl Pts',(2.98043470030214,1.03660848400049,-3.91017563074714));
#10096=CARTESIAN_POINT('Ctrl Pts',(2.98582459984016,1.03949743271071,-3.91058895103993));
#10097=CARTESIAN_POINT('Ctrl Pts',(3.00038775807169,1.04715778414305,-3.91170512191986));
#10098=CARTESIAN_POINT('Ctrl Pts',(3.00960157928965,1.05185048236449,-3.9124106769385));
#10099=CARTESIAN_POINT('Ctrl Pts',(3.0586297217767,1.07601335970198,-3.91616278125679));
#10100=CARTESIAN_POINT('Ctrl Pts',(3.09945292736343,1.09334360389462,-3.91928115218655));
#10101=CARTESIAN_POINT('Ctrl Pts',(3.19234256433788,1.12673096456194,-3.92636308364059));
#10102=CARTESIAN_POINT('Ctrl Pts',(3.24474379307409,1.14156073096066,-3.93035049972805));
#10103=CARTESIAN_POINT('Ctrl Pts',(3.35768298020661,1.16522612653446,-3.93881898603055));
#10104=CARTESIAN_POINT('Ctrl Pts',(3.41827597922547,1.17308050887551,-3.94328910720124));
#10105=CARTESIAN_POINT('Ctrl Pts',(3.48919871205546,1.17671702860564,-3.94826886702782));
#10106=CARTESIAN_POINT('Ctrl Pts',(3.49919409521934,1.17710195665604,-3.94896475364315));
#10107=CARTESIAN_POINT('Ctrl Pts',(3.51312777543832,1.17746084917022,-3.94992548963286));
#10108=CARTESIAN_POINT('Ctrl Pts',(3.5170625328425,1.17754246490458,-3.95019575639631));
#10109=CARTESIAN_POINT('Ctrl Pts',(3.52385330335688,1.17764927010658,-3.95066032095821));
#10110=CARTESIAN_POINT('Ctrl Pts',(3.52670910415554,1.177683796583,-3.95085511806132));
#10111=CARTESIAN_POINT('Ctrl Pts',(3.53273693236199,1.17773474389974,-3.95126503668306));
#10112=CARTESIAN_POINT('Ctrl Pts',(3.5359089525109,1.17774873880127,-3.9514800172152));
#10113=CARTESIAN_POINT('Ctrl Pts',(3.54378482283516,1.17775166796254,-3.95201206725485));
#10114=CARTESIAN_POINT('Ctrl Pts',(3.54848868684836,1.17772523777653,-3.95232830297985));
#10115=CARTESIAN_POINT('Ctrl Pts',(3.56625975665319,1.17751890722221,-3.95351767410306));
#10116=CARTESIAN_POINT('Ctrl Pts',(3.57932438955163,1.17714969826929,-3.95438110964296));
#10117=CARTESIAN_POINT('Ctrl Pts',(3.61289435699904,1.17564143396813,-3.95657778478632));
#10118=CARTESIAN_POINT('Ctrl Pts',(3.63338151890948,1.1741833988167,-3.95789731202981));
#10119=CARTESIAN_POINT('Ctrl Pts',(3.71131820664477,1.16658366532871,-3.96287157829586));
#10120=CARTESIAN_POINT('Ctrl Pts',(3.76832811670062,1.15675390984114,-3.96641880997522));
#10121=CARTESIAN_POINT('Ctrl Pts',(3.89759001960959,1.12453171523331,-3.97466756075121));
#10122=CARTESIAN_POINT('Ctrl Pts',(3.9688580014888,1.09929625483355,-3.97937923449006));
#10123=CARTESIAN_POINT('Ctrl Pts',(4.04663302212342,1.06303263432097,-3.98501124989341));
#10124=CARTESIAN_POINT('Ctrl Pts',(4.05598868487624,1.05851880825231,-3.98569695866126));
#10125=CARTESIAN_POINT('Ctrl Pts',(4.07130005923392,1.05088021881746,-3.98683347443966));
#10126=CARTESIAN_POINT('Ctrl Pts',(4.07729101248484,1.04782707986891,-3.98728182259133));
#10127=CARTESIAN_POINT('Ctrl Pts',(4.08806964381035,1.04221723464326,-3.98809527369389));
#10128=CARTESIAN_POINT('Ctrl Pts',(4.09286644973831,1.03967839819818,-3.98845974720784));
#10129=CARTESIAN_POINT('Ctrl Pts',(4.10312405748324,1.03415819204342,-3.98924454397651));
#10130=CARTESIAN_POINT('Ctrl Pts',(4.10857910494799,1.0311665345298,-3.9896652202357));
#10131=CARTESIAN_POINT('Ctrl Pts',(4.12346407029455,1.02284923605826,-3.99082238133443));
#10132=CARTESIAN_POINT('Ctrl Pts',(4.13284443960847,1.01743663925843,-3.99156192302487));
#10133=CARTESIAN_POINT('Ctrl Pts',(4.18795513940158,0.984615729432178,-3.99596961974173));
#10134=CARTESIAN_POINT('Ctrl Pts',(4.2318497925435,0.954261059497406,-3.99974361111364));
#10135=CARTESIAN_POINT('Ctrl Pts',(4.31105842730863,0.89113667168131,-4.0070639731912));
#10136=CARTESIAN_POINT('Ctrl Pts',(4.34671963136999,0.858967033756197,-4.01058800950391));
#10137=CARTESIAN_POINT('Ctrl Pts',(4.40008695209897,0.804558893169404,-4.01617962053957));
#10138=CARTESIAN_POINT('Ctrl Pts',(4.41912598661287,0.783698831287555,-4.0182473517035));
#10139=CARTESIAN_POINT('Ctrl Pts',(4.45981447821357,0.735765800171875,-4.02280590525872));
#10140=CARTESIAN_POINT('Ctrl Pts',(4.48105793276918,0.708378440831675,-4.02528430910809));
#10141=CARTESIAN_POINT('Ctrl Pts',(4.5045653934219,0.675142478559903,-4.02811381200472));
#10142=CARTESIAN_POINT('Ctrl Pts',(4.50802773161558,0.670166209841275,-4.02853295335212));
#10143=CARTESIAN_POINT('Ctrl Pts',(4.51361190163298,0.662006654884104,-4.02921261948849));
#10144=CARTESIAN_POINT('Ctrl Pts',(4.51575686841944,0.658839447545405,-4.02947459359533));
#10145=CARTESIAN_POINT('Ctrl Pts',(4.51957961162135,0.653135215262649,-4.02994303597782));
#10146=CARTESIAN_POINT('Ctrl Pts',(4.52126302077772,0.65060209832433,-4.03014986789553));
#10147=CARTESIAN_POINT('Ctrl Pts',(4.52495107670906,0.645005570601507,-4.03060420868494));
#10148=CARTESIAN_POINT('Ctrl Pts',(4.52695126317326,0.64193932008488,-4.03085142607382));
#10149=CARTESIAN_POINT('Ctrl Pts',(4.53271095042371,0.633019203839182,-4.03156582615065));
#10150=CARTESIAN_POINT('Ctrl Pts',(4.5364329998611,0.627141168991839,-4.03203064783547));
#10151=CARTESIAN_POINT('Ctrl Pts',(4.56761767406544,0.576913614461229,-4.03595541886596));
#10152=CARTESIAN_POINT('Ctrl Pts',(4.5921617246552,0.53081160626499,-4.03924908255017));
#10153=CARTESIAN_POINT('Ctrl Pts',(4.64766320971026,0.407450785301738,-4.04767541787365));
#10154=CARTESIAN_POINT('Ctrl Pts',(4.67363991946275,0.3282820287332,-4.0527318918661));
#10155=CARTESIAN_POINT('Ctrl Pts',(4.69755572356987,0.216800752261754,-4.0600032591527));
#10156=CARTESIAN_POINT('Ctrl Pts',(4.70284865187255,0.186320911727268,-4.06200379042932));
#10157=CARTESIAN_POINT('Ctrl Pts',(4.70820254723277,0.146170427590695,-4.06467318821915));
#10158=CARTESIAN_POINT('Ctrl Pts',(4.7093532485695,0.136655953194657,-4.06530820480776));
#10159=CARTESIAN_POINT('Ctrl Pts',(4.71102998547545,0.121213033422497,-4.06634334019044));
#10160=CARTESIAN_POINT('Ctrl Pts',(4.71162743772298,0.115292656495342,-4.06674123567543));
#10161=CARTESIAN_POINT('Ctrl Pts',(4.71268887130824,0.103911808323198,-4.0675082561521));
#10162=CARTESIAN_POINT('Ctrl Pts',(4.71315965632523,0.0984521151681194,
-4.06787715969394));
#10163=CARTESIAN_POINT('Ctrl Pts',(4.71416065330249,0.0858136464931614,
-4.06873339917269));
#10164=CARTESIAN_POINT('Ctrl Pts',(4.71466318223655,0.0786329614264221,
-4.06922157859461));
#10165=CARTESIAN_POINT('Ctrl Pts',(4.71605392715649,0.0557502054716263,
-4.07078291415765));
#10166=CARTESIAN_POINT('Ctrl Pts',(4.7166934359112,0.0400353133819916,-4.07186366221968));
#10167=CARTESIAN_POINT('Ctrl Pts',(4.71745666545541,0.00307141003010868,
-4.07442690568669));
#10168=CARTESIAN_POINT('Ctrl Pts',(4.71732037574729,-0.0181769021506357,
-4.07591682543126));
#10169=CARTESIAN_POINT('Ctrl Pts',(4.71463514345411,-0.0983813380987575,
-4.08160331385886));
#10170=CARTESIAN_POINT('Ctrl Pts',(4.70823197613073,-0.157115915930673,
-4.08590110161006));
#10171=CARTESIAN_POINT('Ctrl Pts',(4.6844977053795,-0.284873298397203,-4.09543305152185));
#10172=CARTESIAN_POINT('Ctrl Pts',(4.66526075372894,-0.353321853443469,
-4.10066342150063));
#10173=CARTESIAN_POINT('Ctrl Pts',(4.63649494189315,-0.428759229392006,
-4.10632182334878));
#10174=CARTESIAN_POINT('Ctrl Pts',(4.63289901592379,-0.437847975619643,
-4.10700154852122));
#10175=CARTESIAN_POINT('Ctrl Pts',(4.62771144039552,-0.450497029118683,
-4.10794371151065));
#10176=CARTESIAN_POINT('Ctrl Pts',(4.62621474454141,-0.454095496898909,
-4.10821130522183));
#10177=CARTESIAN_POINT('Ctrl Pts',(4.62359407183916,-0.460309148342149,
-4.10867253232959));
#10178=CARTESIAN_POINT('Ctrl Pts',(4.62247843733562,-0.462927781455639,
-4.10886664879161));
#10179=CARTESIAN_POINT('Ctrl Pts',(4.62009496224947,-0.468466536049767,
-4.10927664100431));
#10180=CARTESIAN_POINT('Ctrl Pts',(4.6188247532074,-0.471385613965797,-4.10949236776013));
#10181=CARTESIAN_POINT('Ctrl Pts',(4.6156262748807,-0.478655355971944,-4.11002882959558));
#10182=CARTESIAN_POINT('Ctrl Pts',(4.6136834183443,-0.482999607611767,-4.11034870036592));
#10183=CARTESIAN_POINT('Ctrl Pts',(4.60613941028242,-0.499597426427108,
-4.11156853933936));
#10184=CARTESIAN_POINT('Ctrl Pts',(4.60035423009635,-0.511766880711835,
-4.11245815606025));
#10185=CARTESIAN_POINT('Ctrl Pts',(4.58483179596218,-0.543024275717131,
-4.11473756001972));
#10186=CARTESIAN_POINT('Ctrl Pts',(4.57477995345353,-0.561951131570074,
-4.11611230060897));
#10187=CARTESIAN_POINT('Ctrl Pts',(4.5362337869681,-0.629981713175678,-4.12107138806634));
#10188=CARTESIAN_POINT('Ctrl Pts',(4.5047154462433,-0.677284183241362,-4.12455703420347));
#10189=CARTESIAN_POINT('Ctrl Pts',(4.42391368575104,-0.781388509308156,
-4.13271764382273));
#10190=CARTESIAN_POINT('Ctrl Pts',(4.37237127889971,-0.836108158790844,
-4.13740404485252));
#10191=CARTESIAN_POINT('Ctrl Pts',(4.30816407226216,-0.892405715595032,
-4.14300835080058));
#10192=CARTESIAN_POINT('Ctrl Pts',(4.30025742242843,-0.899155297470207,
-4.14369458669386));
#10193=CARTESIAN_POINT('Ctrl Pts',(4.28708932886012,-0.910098339529067,
-4.1448317960199));
#10194=CARTESIAN_POINT('Ctrl Pts',(4.28187935224092,-0.914353043386512,
-4.14528030531816));
#10195=CARTESIAN_POINT('Ctrl Pts',(4.272400278373,-0.921959665791854,-4.14609392861899));
#10196=CARTESIAN_POINT('Ctrl Pts',(4.26814388388235,-0.925327169173477,
-4.14645841195714));
#10197=CARTESIAN_POINT('Ctrl Pts',(4.25896009315414,-0.932490393514595,
-4.14724309603075));
#10198=CARTESIAN_POINT('Ctrl Pts',(4.25402561818826,-0.936276727267058,
-4.1476636488251));
#10199=CARTESIAN_POINT('Ctrl Pts',(4.24042427079647,-0.946543205108173,
-4.14882011922744));
#10200=CARTESIAN_POINT('Ctrl Pts',(4.23169789337818,-0.952943126791585,
-4.14955908759421));
#10201=CARTESIAN_POINT('Ctrl Pts',(4.17960771115787,-0.990053053102572,
-4.15395390652374));
#10202=CARTESIAN_POINT('Ctrl Pts',(4.13430009814544,-1.01791580728556,-4.15771485253991));
#10203=CARTESIAN_POINT('Ctrl Pts',(4.08424467547647,-1.04421298248778,-4.16180092982385));
#10204=CARTESIAN_POINT('Ctrl Pts',(4.08121028447338,-1.04579030560513,-4.16204835369644));
#10205=CARTESIAN_POINT('Ctrl Pts',(4.07816926526045,-1.04735428989218,-4.16229603312229));
#10206=CARTESIAN_POINT('Origin',(3.53951905042299,8.32667268468867E-16,
0.924367114736157));
#10207=CARTESIAN_POINT('',(4.07816946571175,-1.04735418680084,-4.76238152739268));
#10208=CARTESIAN_POINT('',(4.07816926754731,-1.04735428871606,-4.66391540717653));
#10209=CARTESIAN_POINT('',(4.07816926754759,-1.04735428871592,0.924367114736157));
#10210=CARTESIAN_POINT('Ctrl Pts',(4.07816946571175,-1.04735418680084,-4.76238152739268));
#10211=CARTESIAN_POINT('Ctrl Pts',(4.1238246947715,-1.02387387001492,-4.75872475031135));
#10212=CARTESIAN_POINT('Ctrl Pts',(4.16791639040916,-0.997422887860836,
-4.75498284712457));
#10213=CARTESIAN_POINT('Ctrl Pts',(4.2352999419459,-0.950746764474624,-4.74897178872223));
#10214=CARTESIAN_POINT('Ctrl Pts',(4.25975379432268,-0.932358515856194,
-4.74672343589551));
#10215=CARTESIAN_POINT('Ctrl Pts',(4.32002382529312,-0.883250431994198,
-4.74104387231585));
#10216=CARTESIAN_POINT('Ctrl Pts',(4.35476568563751,-0.851289022416631,
-4.73763586798109));
#10217=CARTESIAN_POINT('Ctrl Pts',(4.39225537096927,-0.81239324041436,-4.73387966196873));
#10218=CARTESIAN_POINT('Ctrl Pts',(4.3969673253232,-0.807418398921939,-4.733406051962));
#10219=CARTESIAN_POINT('Ctrl Pts',(4.4041150996941,-0.799738693321236,-4.73268567264392));
#10220=CARTESIAN_POINT('Ctrl Pts',(4.4065821485723,-0.797063291551279,-4.73243667380822));
#10221=CARTESIAN_POINT('Ctrl Pts',(4.41108942919161,-0.792129660296022,
-4.73198115996995));
#10222=CARTESIAN_POINT('Ctrl Pts',(4.41313331394922,-0.789874953933117,
-4.73177438116093));
#10223=CARTESIAN_POINT('Ctrl Pts',(4.4177448111186,-0.784747995926978,-4.73130731525029));
#10224=CARTESIAN_POINT('Ctrl Pts',(4.4203070864187,-0.781871051108427,-4.73104742012281));
#10225=CARTESIAN_POINT('Ctrl Pts',(4.42692415251358,-0.774367543361832,
-4.73037508745562));
#10226=CARTESIAN_POINT('Ctrl Pts',(4.43095695452565,-0.769721621456751,
-4.72996419124905));
#10227=CARTESIAN_POINT('Ctrl Pts',(4.4381340580166,-0.76132129092274,-4.72923040728557));
#10228=CARTESIAN_POINT('Ctrl Pts',(4.44129165541683,-0.757578517782859,
-4.72890667901163));
#10229=CARTESIAN_POINT('Ctrl Pts',(4.48956575480433,-0.699628624190789,
-4.7239415697203));
#10230=CARTESIAN_POINT('Ctrl Pts',(4.52975368333266,-0.641488184859085,
-4.71958737884043));
#10231=CARTESIAN_POINT('Ctrl Pts',(4.59370219690835,-0.528495972568149,
-4.71155631277819));
#10232=CARTESIAN_POINT('Ctrl Pts',(4.61896435276189,-0.474770765827193,
-4.70789364112963));
#10233=CARTESIAN_POINT('Ctrl Pts',(4.64765982860039,-0.399465858020155,
-4.70275788393481));
#10234=CARTESIAN_POINT('Ctrl Pts',(4.6547040933971,-0.379356289809559,-4.70138686441829));
#10235=CARTESIAN_POINT('Ctrl Pts',(4.66600392484798,-0.344057108959871,
-4.69897265587932));
#10236=CARTESIAN_POINT('Ctrl Pts',(4.6705070366421,-0.328952281353088,-4.69793725027693));
#10237=CARTESIAN_POINT('Ctrl Pts',(4.67662500865674,-0.306817559307883,
-4.69641438477839));
#10238=CARTESIAN_POINT('Ctrl Pts',(4.67848068322941,-0.299855582053656,
-4.69593461202283));
#10239=CARTESIAN_POINT('Ctrl Pts',(4.68163547460494,-0.28756770408172,-4.69508622319637));
#10240=CARTESIAN_POINT('Ctrl Pts',(4.68296151637903,-0.282248890403064,
-4.69471847633296));
#10241=CARTESIAN_POINT('Ctrl Pts',(4.68564910064335,-0.271139003953795,
-4.69394915286868));
#10242=CARTESIAN_POINT('Ctrl Pts',(4.68700398954536,-0.265346497493998,
-4.69354737666264));
#10243=CARTESIAN_POINT('Ctrl Pts',(4.69042468190771,-0.250205803618211,
-4.6924953408747));
#10244=CARTESIAN_POINT('Ctrl Pts',(4.69242045126806,-0.240842411741294,
-4.69184289267613));
#10245=CARTESIAN_POINT('Ctrl Pts',(4.70035920076625,-0.201234311809141,
-4.6890745483797));
#10246=CARTESIAN_POINT('Ctrl Pts',(4.70522735884054,-0.170789169666245,
-4.68692554824044));
#10247=CARTESIAN_POINT('Ctrl Pts',(4.71879790977702,-0.0575925486884402,
-4.67885281023103));
#10248=CARTESIAN_POINT('Ctrl Pts',(4.71991974477076,0.0258138003403826,
-4.67272135094934));
#10249=CARTESIAN_POINT('Ctrl Pts',(4.70743430651301,0.160604102838441,-4.66281207693023));
#10250=CARTESIAN_POINT('Ctrl Pts',(4.69916917891795,0.212208870744189,-4.6590249514404));
#10251=CARTESIAN_POINT('Ctrl Pts',(4.685951249501,0.269882742669623,-4.65490958087788));
#10252=CARTESIAN_POINT('Ctrl Pts',(4.68433667025753,0.276651595047297,-4.65442848822193));
#10253=CARTESIAN_POINT('Ctrl Pts',(4.68178106355983,0.286959862182702,-4.65369915039173));
#10254=CARTESIAN_POINT('Ctrl Pts',(4.68088339844669,0.290509716078846,-4.65344859169957));
#10255=CARTESIAN_POINT('Ctrl Pts',(4.6792096715083,0.297001017343397,-4.65299159445252));
#10256=CARTESIAN_POINT('Ctrl Pts',(4.67843876660333,0.299943655767906,-4.65278487989882));
#10257=CARTESIAN_POINT('Ctrl Pts',(4.67667258082573,0.306580408305435,-4.65231966270194));
#10258=CARTESIAN_POINT('Ctrl Pts',(4.67567069636531,0.310272681555549,-4.65206153818263));
#10259=CARTESIAN_POINT('Ctrl Pts',(4.67303457660165,0.319803649209355,-4.65139687125989));
#10260=CARTESIAN_POINT('Ctrl Pts',(4.67137319128884,0.325634810421166,-4.65099181272067));
#10261=CARTESIAN_POINT('Ctrl Pts',(4.65991569380577,0.364701175228601,-4.64828718311037));
#10262=CARTESIAN_POINT('Ctrl Pts',(4.64870106091063,0.397506425981322,-4.64606017966695));
#10263=CARTESIAN_POINT('Ctrl Pts',(4.62576276797231,0.45603194171076,-4.64208820862212));
#10264=CARTESIAN_POINT('Ctrl Pts',(4.61453037715098,0.48191421850553,-4.64033201442321));
#10265=CARTESIAN_POINT('Ctrl Pts',(4.58172188548151,0.550642952029911,-4.63561006395663));
#10266=CARTESIAN_POINT('Ctrl Pts',(4.55844147314865,0.592614051619709,-4.63266126320182));
#10267=CARTESIAN_POINT('Ctrl Pts',(4.50398848110103,0.678041773187614,-4.62632615764673));
#10268=CARTESIAN_POINT('Ctrl Pts',(4.47228843409243,0.721028515699199,-4.62293442276487));
#10269=CARTESIAN_POINT('Ctrl Pts',(4.43078056935493,0.769977478529743,-4.61871635005542));
#10270=CARTESIAN_POINT('Ctrl Pts',(4.42366093030718,0.778142362314284,-4.61800003007169));
#10271=CARTESIAN_POINT('Ctrl Pts',(4.41227582210453,0.790840946984347,-4.6168649893465));
#10272=CARTESIAN_POINT('Ctrl Pts',(4.40808519070023,0.795441162752092,-4.61644935882164));
#10273=CARTESIAN_POINT('Ctrl Pts',(4.40017123992361,0.803991502048321,-4.61566831401971));
#10274=CARTESIAN_POINT('Ctrl Pts',(4.39645667032949,0.807949528471788,-4.61530327379224));
#10275=CARTESIAN_POINT('Ctrl Pts',(4.38807922392196,0.816753277707682,-4.61448337298019));
#10276=CARTESIAN_POINT('Ctrl Pts',(4.38340196886911,0.821584993416335,-4.61402790462501));
#10277=CARTESIAN_POINT('Ctrl Pts',(4.37139495021376,0.833777822828424,-4.61286428822969));
#10278=CARTESIAN_POINT('Ctrl Pts',(4.36400883136035,0.841082373874477,-4.61215371007682));
#10279=CARTESIAN_POINT('Ctrl Pts',(4.30215082478109,0.900659421815302,-4.60624379587351));
#10280=CARTESIAN_POINT('Ctrl Pts',(4.24287507936599,0.947671371370007,-4.60082261416592));
#10281=CARTESIAN_POINT('Ctrl Pts',(4.13093969741506,1.02013027262249,-4.59106833800458));
#10282=CARTESIAN_POINT('Ctrl Pts',(4.08010624888138,1.04795509911427,-4.58679405682858));
#10283=CARTESIAN_POINT('Ctrl Pts',(4.00882890120997,1.08039859683487,-4.58113930347216));
#10284=CARTESIAN_POINT('Ctrl Pts',(3.99000679871422,1.08838125292876,-4.57967673296068));
#10285=CARTESIAN_POINT('Ctrl Pts',(3.95886544462656,1.10064223438424,-4.57731650350475));
#10286=CARTESIAN_POINT('Ctrl Pts',(3.94666652491785,1.10521296392672,-4.57640657905525));
#10287=CARTESIAN_POINT('Ctrl Pts',(3.92996727155447,1.11115585025934,-4.5751830844287));
#10288=CARTESIAN_POINT('Ctrl Pts',(3.92553138983615,1.11270463855083,-4.57486018521342));
#10289=CARTESIAN_POINT('Ctrl Pts',(3.91808610542428,1.11525427768112,-4.57432187502797));
#10290=CARTESIAN_POINT('Ctrl Pts',(3.91508175158232,1.11626958092452,-4.57410564486279));
#10291=CARTESIAN_POINT('Ctrl Pts',(3.9093624494946,1.11817668027466,-4.5736959431407));
#10292=CARTESIAN_POINT('Ctrl Pts',(3.90664830748703,1.11907074718166,-4.57350233647787));
#10293=CARTESIAN_POINT('Ctrl Pts',(3.90018362210851,1.12117423178074,-4.57304308390726));
#10294=CARTESIAN_POINT('Ctrl Pts',(3.89643018005682,1.12237473150809,-4.57277794747231));
#10295=CARTESIAN_POINT('Ctrl Pts',(3.8831013744508,1.12656418737,-4.57184153023339));
#10296=CARTESIAN_POINT('Ctrl Pts',(3.87349360583694,1.12944973078449,-4.57117585026772));
#10297=CARTESIAN_POINT('Ctrl Pts',(3.80607251562621,1.14876300806629,-4.56656177230268));
#10298=CARTESIAN_POINT('Ctrl Pts',(3.74710528944598,1.1608690782246,-4.56281639306572));
#10299=CARTESIAN_POINT('Ctrl Pts',(3.62350441213244,1.1765194676904,-4.55509780781357));
#10300=CARTESIAN_POINT('Ctrl Pts',(3.55899030526028,1.17935234291728,-4.55113797056606));
#10301=CARTESIAN_POINT('Ctrl Pts',(3.45836278618677,1.17550908349376,-4.54474872733253));
#10302=CARTESIAN_POINT('Ctrl Pts',(3.42224176952475,1.172456217751,-4.54241368065164));
#10303=CARTESIAN_POINT('Ctrl Pts',(3.3766537614248,1.16647547415376,-4.53938475671786));
#10304=CARTESIAN_POINT('Ctrl Pts',(3.36700250241469,1.16508719220557,-4.53873887477249));
#10305=CARTESIAN_POINT('Ctrl Pts',(3.3514544565316,1.16265326736094,-4.53769036111547));
#10306=CARTESIAN_POINT('Ctrl Pts',(3.34554632888212,1.16168218228574,-4.53729006153443));
#10307=CARTESIAN_POINT('Ctrl Pts',(3.3342551365963,1.15973777677597,-4.53652133093436));
#10308=CARTESIAN_POINT('Ctrl Pts',(3.32887093221674,1.15877191619635,-4.53615314293425));
#10309=CARTESIAN_POINT('Ctrl Pts',(3.31660915876159,1.1564840207008,-4.53531085702529));
#10310=CARTESIAN_POINT('Ctrl Pts',(3.30973631576003,1.15513808746904,-4.53483601966663));
#10311=CARTESIAN_POINT('Ctrl Pts',(3.28810787555828,1.15070185408713,-4.53333289264715));
#10312=CARTESIAN_POINT('Ctrl Pts',(3.27339988648215,1.14738959814153,-4.53229767962789));
#10313=CARTESIAN_POINT('Ctrl Pts',(3.17272848711102,1.12267855276493,-4.52511871423584));
#10314=CARTESIAN_POINT('Ctrl Pts',(3.0893694931513,1.09192588335594,-4.51867178672263));
#10315=CARTESIAN_POINT('Ctrl Pts',(2.99292161076762,1.04340933630333,-4.51074810682237));
#10316=CARTESIAN_POINT('Ctrl Pts',(2.97580012812239,1.03425953956536,-4.50932368888764));
#10317=CARTESIAN_POINT('Ctrl Pts',(2.92974969565556,1.00816660771333,-4.5054538473849));
#10318=CARTESIAN_POINT('Ctrl Pts',(2.9013035857772,0.990403907151046,-4.50302019637042));
#10319=CARTESIAN_POINT('Ctrl Pts',(2.85855157627035,0.961100165392884,-4.4993323716793));
#10320=CARTESIAN_POINT('Ctrl Pts',(2.84369318876685,0.950398174632091,-4.49804477577549));
#10321=CARTESIAN_POINT('Ctrl Pts',(2.82484564468024,0.936143843841808,-4.49640974199378));
#10322=CARTESIAN_POINT('Ctrl Pts',(2.82062357492806,0.932905499634276,-4.49604336134894));
#10323=CARTESIAN_POINT('Ctrl Pts',(2.81381399739052,0.927608844184126,-4.49545245028938));
#10324=CARTESIAN_POINT('Ctrl Pts',(2.81121301411879,0.925568101207468,-4.49522674788133));
#10325=CARTESIAN_POINT('Ctrl Pts',(2.80619428324002,0.921596127860086,-4.49479130272333));
#10326=CARTESIAN_POINT('Ctrl Pts',(2.80377551499016,0.919666291316708,-4.49458147296478));
#10327=CARTESIAN_POINT('Ctrl Pts',(2.79843241332152,0.915368677880096,-4.49411796106471));
#10328=CARTESIAN_POINT('Ctrl Pts',(2.79551173693431,0.912996351897627,-4.49386459628896));
#10329=CARTESIAN_POINT('Ctrl Pts',(2.78543378269944,0.904730034509634,-4.49299015633349));
#10330=CARTESIAN_POINT('Ctrl Pts',(2.77833454508543,0.898765368877215,-4.49237383639267));
#10331=CARTESIAN_POINT('Ctrl Pts',(2.70974674604248,0.839743291540491,-4.48640764485951));
#10332=CARTESIAN_POINT('Ctrl Pts',(2.65382227632774,0.780535743997938,-4.4814396272649));
#10333=CARTESIAN_POINT('Ctrl Pts',(2.57262647582614,0.674500209030629,-4.47317347145686));
#10334=CARTESIAN_POINT('Ctrl Pts',(2.54362590630552,0.630894624230979,-4.46992205464854));
#10335=CARTESIAN_POINT('Ctrl Pts',(2.50777661473052,0.568326282383951,-4.46531426749584));
#10336=CARTESIAN_POINT('Ctrl Pts',(2.49836714992258,0.550899147073555,-4.46403703316848));
#10337=CARTESIAN_POINT('Ctrl Pts',(2.48265645345692,0.519960067433883,-4.4617735734591));
#10338=CARTESIAN_POINT('Ctrl Pts',(2.47616396689979,0.506550051363631,-4.46079383024674));
#10339=CARTESIAN_POINT('Ctrl Pts',(2.46697818280256,0.486621823556924,-4.45933794604063));
#10340=CARTESIAN_POINT('Ctrl Pts',(2.46408608317694,0.480196461072343,-4.45886854933517));
#10341=CARTESIAN_POINT('Ctrl Pts',(2.45905545460417,0.468746515894298,-4.45803192760792));
#10342=CARTESIAN_POINT('Ctrl Pts',(2.45689386858019,0.463732241686929,-4.45766549209573));
#10343=CARTESIAN_POINT('Ctrl Pts',(2.45242051552263,0.453153554073311,-4.45689221362561));
#10344=CARTESIAN_POINT('Ctrl Pts',(2.45011643246739,0.447586083135522,-4.45648512597225));
#10345=CARTESIAN_POINT('Ctrl Pts',(2.44413054367867,0.432802011534879,-4.45540368601457));
#10346=CARTESIAN_POINT('Ctrl Pts',(2.44052241073127,0.423556297778087,-4.45472691424769));
#10347=CARTESIAN_POINT('Ctrl Pts',(2.42502190391518,0.382304783248453,-4.45170457801411));
#10348=CARTESIAN_POINT('Ctrl Pts',(2.41440885336671,0.349839212051453,-4.44931787050946));
#10349=CARTESIAN_POINT('Ctrl Pts',(2.37633410099366,0.213582501721775,-4.43926254119206));
#10350=CARTESIAN_POINT('Ctrl Pts',(2.36171861433284,0.106759320706611,-4.43123006619689));
#10351=CARTESIAN_POINT('Ctrl Pts',(2.36178118377105,-0.0260274178282911,
-4.42168786245795));
#10352=CARTESIAN_POINT('Ctrl Pts',(2.36261956795491,-0.0514950397899183,
-4.41988115543017));
#10353=CARTESIAN_POINT('Ctrl Pts',(2.36468223135748,-0.0830108380322754,
-4.41768959195174));
#10354=CARTESIAN_POINT('Ctrl Pts',(2.3651284275498,-0.089101176061268,-4.41726813729475));
#10355=CARTESIAN_POINT('Ctrl Pts',(2.36590606748946,-0.0986913546338751,
-4.41660801986475));
#10356=CARTESIAN_POINT('Ctrl Pts',(2.36620583704834,-0.102193548353958,
-4.41636769692345));
#10357=CARTESIAN_POINT('Ctrl Pts',(2.36676819616081,-0.108434616480967,
-4.41594081626785));
#10358=CARTESIAN_POINT('Ctrl Pts',(2.36702470305547,-0.111173908155267,
-4.41575393459828));
#10359=CARTESIAN_POINT('Ctrl Pts',(2.36766375870601,-0.117750183481974,
-4.41530641647577));
#10360=CARTESIAN_POINT('Ctrl Pts',(2.36805555386257,-0.121586215164551,
-4.41504629315816));
#10361=CARTESIAN_POINT('Ctrl Pts',(2.36930938676032,-0.133293286129065,
-4.41425505170988));
#10362=CARTESIAN_POINT('Ctrl Pts',(2.37023198647703,-0.141157810678305,
-4.41372713633098));
#10363=CARTESIAN_POINT('Ctrl Pts',(2.37256737398493,-0.159467651165253,
-4.41250526373565));
#10364=CARTESIAN_POINT('Ctrl Pts',(2.37404121832908,-0.169904640266484,
-4.41181424663582));
#10365=CARTESIAN_POINT('Ctrl Pts',(2.37971133060692,-0.206501852524029,
-4.40940604086706));
#10366=CARTESIAN_POINT('Ctrl Pts',(2.38465017131869,-0.232540369503318,
-4.40771928913578));
#10367=CARTESIAN_POINT('Ctrl Pts',(2.40761636396558,-0.334669910104225,
-4.40113243263604));
#10368=CARTESIAN_POINT('Ctrl Pts',(2.43232199428828,-0.409051428995215,
-4.3963869447157));
#10369=CARTESIAN_POINT('Ctrl Pts',(2.48337198574969,-0.523310008623693,
-4.38852799588136));
#10370=CARTESIAN_POINT('Ctrl Pts',(2.50507159987843,-0.564993516413902,
-4.38553011154634));
#10371=CARTESIAN_POINT('Ctrl Pts',(2.53472338837958,-0.614488637085034,
-4.38173836041264));
#10372=CARTESIAN_POINT('Ctrl Pts',(2.5403734212286,-0.623633391305754,-4.38102767055524));
#10373=CARTESIAN_POINT('Ctrl Pts',(2.54951440475064,-0.637985219207013,
-4.37989546916092));
#10374=CARTESIAN_POINT('Ctrl Pts',(2.55292320773736,-0.64324410530969,-4.37947695451095));
#10375=CARTESIAN_POINT('Ctrl Pts',(2.55906168205516,-0.652550567225135,
-4.37872967607215));
#10376=CARTESIAN_POINT('Ctrl Pts',(2.56177487480144,-0.656608878848639,
-4.37840152752093));
#10377=CARTESIAN_POINT('Ctrl Pts',(2.56811813037439,-0.665970431790652,
-4.3776391963065));
#10378=CARTESIAN_POINT('Ctrl Pts',(2.57176649839303,-0.671261021289354,
-4.37720433647599));
#10379=CARTESIAN_POINT('Ctrl Pts',(2.58222903663871,-0.686170418788252,
-4.37596719106977));
#10380=CARTESIAN_POINT('Ctrl Pts',(2.58914440931673,-0.695716923862671,
-4.37516110731957));
#10381=CARTESIAN_POINT('Ctrl Pts',(2.64607921557227,-0.771880863593361,
-4.36861424258325));
#10382=CARTESIAN_POINT('Ctrl Pts',(2.70288536552584,-0.833110917589799,
-4.3626008455239));
#10383=CARTESIAN_POINT('Ctrl Pts',(2.821787717027,-0.936749928707592,-4.35103695183046));
#10384=CARTESIAN_POINT('Ctrl Pts',(2.88243204106732,-0.980243454152859,
-4.34553716821826));
#10385=CARTESIAN_POINT('Ctrl Pts',(2.95509337063497,-1.02256256739274,-4.33964601278877));
#10386=CARTESIAN_POINT('Ctrl Pts',(2.96346433341195,-1.02730159018917,-4.33897723883132));
#10387=CARTESIAN_POINT('Ctrl Pts',(2.97528465929047,-1.03380346318538,-4.33804767069479));
#10388=CARTESIAN_POINT('Ctrl Pts',(2.97868581417824,-1.03565251451142,-4.33778189455228));
#10389=CARTESIAN_POINT('Ctrl Pts',(2.98484650193509,-1.03896254745117,-4.33730361903064));
#10390=CARTESIAN_POINT('Ctrl Pts',(2.98760283921663,-1.04042938619351,-4.33709076235831));
#10391=CARTESIAN_POINT('Ctrl Pts',(2.99324952702244,-1.0434056268094,-4.33665704795359));
#10392=CARTESIAN_POINT('Ctrl Pts',(2.99614036412811,-1.0449140147353,-4.33643625278272));
#10393=CARTESIAN_POINT('Ctrl Pts',(3.00358211682221,-1.04875775542582,-4.33587096709932));
#10394=CARTESIAN_POINT('Ctrl Pts',(3.00814210817067,-1.0510755320086,-4.3355275448279));
#10395=CARTESIAN_POINT('Ctrl Pts',(3.02735982112843,-1.06068657965286,-4.33409200649674));
#10396=CARTESIAN_POINT('Ctrl Pts',(3.04215449354165,-1.06770391955412,-4.33301550847004));
#10397=CARTESIAN_POINT('Ctrl Pts',(3.08293610833501,-1.08601550943427,-4.3301126263949));
#10398=CARTESIAN_POINT('Ctrl Pts',(3.10919280319622,-1.09668464625338,-4.3283135884314));
#10399=CARTESIAN_POINT('Ctrl Pts',(3.21661103250613,-1.1358800355342,-4.32113582233972));
#10400=CARTESIAN_POINT('Ctrl Pts',(3.30039712128703,-1.15642306316942,-4.31592820504046));
#10401=CARTESIAN_POINT('Ctrl Pts',(3.42293373409073,-1.17256780104991,-4.30810182028285));
#10402=CARTESIAN_POINT('Ctrl Pts',(3.46040283498772,-1.17569025205965,-4.30568450785861));
#10403=CARTESIAN_POINT('Ctrl Pts',(3.50818498931754,-1.17737760879424,-4.30253817323958));
#10404=CARTESIAN_POINT('Ctrl Pts',(3.51841953553587,-1.17760547583808,-4.30186061783616));
#10405=CARTESIAN_POINT('Ctrl Pts',(3.53474874289516,-1.17775610272775,-4.30077319581822));
#10406=CARTESIAN_POINT('Ctrl Pts',(3.54084223776515,-1.17776501907845,-4.30036599122266));
#10407=CARTESIAN_POINT('Ctrl Pts',(3.55238136229922,-1.17769235488938,-4.29959207029288));
#10408=CARTESIAN_POINT('Ctrl Pts',(3.55782690913985,-1.1776202878829,-4.29922565772469));
#10409=CARTESIAN_POINT('Ctrl Pts',(3.57019323854404,-1.17737083542516,-4.29839078810382));
#10410=CARTESIAN_POINT('Ctrl Pts',(3.57711329750726,-1.17717019116737,-4.29792162507653));
#10411=CARTESIAN_POINT('Ctrl Pts',(3.59826989956933,-1.17637002461012,-4.29648098961761));
#10412=CARTESIAN_POINT('Ctrl Pts',(3.61249722485612,-1.17557315905028,-4.29550349020484));
#10413=CARTESIAN_POINT('Ctrl Pts',(3.68125472776603,-1.17046914231167,-4.29073529620166));
#10414=CARTESIAN_POINT('Ctrl Pts',(3.73544722109135,-1.1626253247207,-4.28683795613902));
#10415=CARTESIAN_POINT('Ctrl Pts',(3.87200461050891,-1.13304029791378,-4.27669384363175));
#10416=CARTESIAN_POINT('Ctrl Pts',(3.95291985471189,-1.10608616546657,-4.2703599530123));
#10417=CARTESIAN_POINT('Ctrl Pts',(4.04638062721946,-1.06325075396286,-4.26301792008229));
#10418=CARTESIAN_POINT('Ctrl Pts',(4.06236558022085,-1.05548206334191,-4.26176216134083));
#10419=CARTESIAN_POINT('Ctrl Pts',(4.07816926766421,-1.04735428865594,-4.2605248066102));
#10420=CARTESIAN_POINT('',(2.36176954983345,0.00105548582028932,-4.32555179375738));
#10421=CARTESIAN_POINT('Ctrl Pts',(4.07816926526045,-1.04735428989218,-4.16229603312229));
#10422=CARTESIAN_POINT('Ctrl Pts',(4.03842873019156,-1.06779269164334,-4.16553274825607));
#10423=CARTESIAN_POINT('Ctrl Pts',(3.99755637743545,-1.08595305923346,-4.16881511342479));
#10424=CARTESIAN_POINT('Ctrl Pts',(3.9292887858117,-1.11174402647986,-4.17416938912811));
#10425=CARTESIAN_POINT('Ctrl Pts',(3.9024746683188,-1.12078478808358,-4.1762411837762));
#10426=CARTESIAN_POINT('Ctrl Pts',(3.8421510273945,-1.13873149645923,-4.18080431744579));
#10427=CARTESIAN_POINT('Ctrl Pts',(3.80851831929176,-1.14714228561079,-4.18328330394645));
#10428=CARTESIAN_POINT('Ctrl Pts',(3.76862008123459,-1.15526816455367,-4.18611338118691));
#10429=CARTESIAN_POINT('Ctrl Pts',(3.76267029062669,-1.15643216066189,-4.18653254488164));
#10430=CARTESIAN_POINT('Ctrl Pts',(3.75295203356498,-1.15825560923789,-4.1872122398664));
#10431=CARTESIAN_POINT('Ctrl Pts',(3.74918896285268,-1.15894271794807,-4.18747422067267));
#10432=CARTESIAN_POINT('Ctrl Pts',(3.7424279137746,-1.16014322660198,-4.1879426700595));
#10433=CARTESIAN_POINT('Ctrl Pts',(3.73943124288457,-1.1606633573098,-4.18814950233272));
#10434=CARTESIAN_POINT('Ctrl Pts',(3.73282321093215,-1.16178395817205,-4.18860383800169));
#10435=CARTESIAN_POINT('Ctrl Pts',(3.72921104802691,-1.16237920270958,-4.1888510499588));
#10436=CARTESIAN_POINT('Ctrl Pts',(3.71872685249991,-1.16405670861132,-4.1895654184471));
#10437=CARTESIAN_POINT('Ctrl Pts',(3.71184778945889,-1.16509496122081,-4.1900302142957));
#10438=CARTESIAN_POINT('Ctrl Pts',(3.65333467248538,-1.17339671938536,-4.1939535373333));
#10439=CARTESIAN_POINT('Ctrl Pts',(3.60127289576342,-1.17728576838526,-4.19724591676357));
#10440=CARTESIAN_POINT('Ctrl Pts',(3.46609504889203,-1.17838760177226,-4.20566682200954));
#10441=CARTESIAN_POINT('Ctrl Pts',(3.38323679052929,-1.17028368310989,-4.21071921608285));
#10442=CARTESIAN_POINT('Ctrl Pts',(3.27155694966704,-1.1472804337431,-4.2179903911338));
#10443=CARTESIAN_POINT('Ctrl Pts',(3.24145512439798,-1.13983056486589,-4.21999557709433));
#10444=CARTESIAN_POINT('Ctrl Pts',(3.20247165595037,-1.12853272570261,-4.22267031257472));
#10445=CARTESIAN_POINT('Ctrl Pts',(3.19329243811487,-1.12575049770806,-4.22330583709509));
#10446=CARTESIAN_POINT('Ctrl Pts',(3.17847371302215,-1.12106054919905,-4.22434159583032));
#10447=CARTESIAN_POINT('Ctrl Pts',(3.1728127686685,-1.11922160064533,-4.22473960168163));
#10448=CARTESIAN_POINT('Ctrl Pts',(3.1619677169476,-1.11560749247629,-4.22550669483037));
#10449=CARTESIAN_POINT('Ctrl Pts',(3.15678157008866,-1.1138389049072,-4.22587555965276));
#10450=CARTESIAN_POINT('Ctrl Pts',(3.14521420798989,-1.109803860669,-4.22670294700959));
#10451=CARTESIAN_POINT('Ctrl Pts',(3.13883986130714,-1.10751844319511,-4.2271620801068));
#10452=CARTESIAN_POINT('Ctrl Pts',(3.11885634526022,-1.10015858259009,-4.22861172611622));
#10453=CARTESIAN_POINT('Ctrl Pts',(3.10532157626562,-1.0948874550087,-4.22960865465041));
#10454=CARTESIAN_POINT('Ctrl Pts',(3.07396924328436,-1.08200450339694,-4.23195442351519));
#10455=CARTESIAN_POINT('Ctrl Pts',(3.05623557979995,-1.07420081041973,-4.23330928520239));
#10456=CARTESIAN_POINT('Ctrl Pts',(2.99304099547762,-1.04451045178818,-4.2382402260481));
#10457=CARTESIAN_POINT('Ctrl Pts',(2.94880912494815,-1.02014761218482,-4.2418902519446));
#10458=CARTESIAN_POINT('Ctrl Pts',(2.83619086249014,-0.948332497442498,
-4.25165923718373));
#10459=CARTESIAN_POINT('Ctrl Pts',(2.77102725109173,-0.896341015665466,
-4.25783057899671));
#10460=CARTESIAN_POINT('Ctrl Pts',(2.7049714878899,-0.831095472775577,-4.26433674777524));
#10461=CARTESIAN_POINT('Ctrl Pts',(2.69814859850046,-0.824187537393891,
-4.26501188448792));
#10462=CARTESIAN_POINT('Ctrl Pts',(2.68871514924872,-0.814397253743633,
-4.26594876362327));
#10463=CARTESIAN_POINT('Ctrl Pts',(2.68603247353762,-0.811585380170657,
-4.26621558880821));
#10464=CARTESIAN_POINT('Ctrl Pts',(2.68141102118401,-0.806693100691683,
-4.26667585860686));
#10465=CARTESIAN_POINT('Ctrl Pts',(2.67946579057232,-0.804618878231609,
-4.26686978163389));
#10466=CARTESIAN_POINT('Ctrl Pts',(2.6753564976189,-0.800205161704783,-4.26727980749679));
#10467=CARTESIAN_POINT('Ctrl Pts',(2.67319437850884,-0.797863886786371,
-4.26749575899937));
#10468=CARTESIAN_POINT('Ctrl Pts',(2.66884822288553,-0.793119107640423,
-4.2679303576441));
#10469=CARTESIAN_POINT('Ctrl Pts',(2.66666456611978,-0.790715282944737,
-4.26814897653004));
#10470=CARTESIAN_POINT('Ctrl Pts',(2.65847382333725,-0.781623428425936,
-4.26897013137225));
#10471=CARTESIAN_POINT('Ctrl Pts',(2.65253324175446,-0.774875514687234,
-4.26956800864679));
#10472=CARTESIAN_POINT('Ctrl Pts',(2.6198939868497,-0.736933272474278,-4.27287033166498));
#10473=CARTESIAN_POINT('Ctrl Pts',(2.59476068760359,-0.704424075175968,
-4.27547977097146));
#10474=CARTESIAN_POINT('Ctrl Pts',(2.53827653098532,-0.622885875337787,
-4.28169076046831));
#10475=CARTESIAN_POINT('Ctrl Pts',(2.50876018827381,-0.572721454260407,
-4.28524823622344));
#10476=CARTESIAN_POINT('Ctrl Pts',(2.45648478836044,-0.466635527591634,
-4.29261140101451));
#10477=CARTESIAN_POINT('Ctrl Pts',(2.43407624211017,-0.410739224321567,
-4.29641172537716));
#10478=CARTESIAN_POINT('Ctrl Pts',(2.41294152163777,-0.343546816669302,
-4.30103540528726));
#10479=CARTESIAN_POINT('Ctrl Pts',(2.40997758911924,-0.333672623777673,
-4.30171604188615));
#10480=CARTESIAN_POINT('Ctrl Pts',(2.40530183598868,-0.317318872946005,
-4.30284588286288));
#10481=CARTESIAN_POINT('Ctrl Pts',(2.40351497600178,-0.310861217314879,
-4.30329267889362));
#10482=CARTESIAN_POINT('Ctrl Pts',(2.40038109898855,-0.299147501021571,
-4.30410447596302));
#10483=CARTESIAN_POINT('Ctrl Pts',(2.39901510796192,-0.293896674553662,
-4.3044688593917));
#10484=CARTESIAN_POINT('Ctrl Pts',(2.39615645014559,-0.282587953844677,
-4.30525476346907));
#10485=CARTESIAN_POINT('Ctrl Pts',(2.39467554785014,-0.276527285095791,
-4.30567664633791));
#10486=CARTESIAN_POINT('Ctrl Pts',(2.39174467597918,-0.264105308721656,
-4.30654286851939));
#10487=CARTESIAN_POINT('Ctrl Pts',(2.39029927535561,-0.257743155773501,
-4.30698733670704));
#10488=CARTESIAN_POINT('Ctrl Pts',(2.38677856568495,-0.241627546435829,
-4.30811538131316));
#10489=CARTESIAN_POINT('Ctrl Pts',(2.38477416347312,-0.231859293229989,
-4.30880115038773));
#10490=CARTESIAN_POINT('Ctrl Pts',(2.36877311963858,-0.148518657131392,
-4.31467022141069));
#10491=CARTESIAN_POINT('Ctrl Pts',(2.36170241876881,-0.0738064342619328,
-4.32006890540583));
#10492=CARTESIAN_POINT('Ctrl Pts',(2.36176952358042,0.00105570928602091,
-4.32555176752495));
#10493=CARTESIAN_POINT('Ctrl Pts',(2.36176952338293,0.00105548894706701,
-4.32555175138744));
#10494=CARTESIAN_POINT('Ctrl Pts',(2.36183394678726,0.0729412573325759,
-4.3308166253243));
#10495=CARTESIAN_POINT('Ctrl Pts',(2.36847963152645,0.14467607557027,-4.33613413493838));
#10496=CARTESIAN_POINT('Ctrl Pts',(2.38348249949644,0.225338683748339,-4.34194114727436));
#10497=CARTESIAN_POINT('Ctrl Pts',(2.38546694400475,0.235290842856999,-4.34265435503951));
#10498=CARTESIAN_POINT('Ctrl Pts',(2.38871217779652,0.250535789214435,-4.34374062493111));
#10499=CARTESIAN_POINT('Ctrl Pts',(2.38988137145093,0.255847316902987,-4.34411792458011));
#10500=CARTESIAN_POINT('Ctrl Pts',(2.39213032186502,0.265737262467958,-4.34481802849396));
#10501=CARTESIAN_POINT('Ctrl Pts',(2.39320079076264,0.270317658584731,-4.3451413002702));
#10502=CARTESIAN_POINT('Ctrl Pts',(2.39503904195511,0.277975959409702,-4.34568003428197));
#10503=CARTESIAN_POINT('Ctrl Pts',(2.39579186011124,0.281057358398529,-4.34589631870806));
#10504=CARTESIAN_POINT('Ctrl Pts',(2.39724614751359,0.286907362079868,-4.34630596974061));
#10505=CARTESIAN_POINT('Ctrl Pts',(2.39794525055704,0.289676507571524,-4.34649947238966));
#10506=CARTESIAN_POINT('Ctrl Pts',(2.39963166297419,0.296255456198783,-4.34695828366771));
#10507=CARTESIAN_POINT('Ctrl Pts',(2.40062801707942,0.300062937838093,-4.34722308490851));
#10508=CARTESIAN_POINT('Ctrl Pts',(2.40422414701941,0.313529256182683,-4.34815728113886));
#10509=CARTESIAN_POINT('Ctrl Pts',(2.40692794912355,0.323160216744212,-4.34882110926691));
#10510=CARTESIAN_POINT('Ctrl Pts',(2.42696954402347,0.391204947348311,-4.35348828969844));
#10511=CARTESIAN_POINT('Ctrl Pts',(2.44869711854392,0.448237836797384,-4.35728266093201));
#10512=CARTESIAN_POINT('Ctrl Pts',(2.50193984352266,0.560868728473025,-4.36499926713142));
#10513=CARTESIAN_POINT('Ctrl Pts',(2.53375147688438,0.616096914193811,-4.36890952225803));
#10514=CARTESIAN_POINT('Ctrl Pts',(2.59043626803981,0.698319538448475,-4.37524568888485));
#10515=CARTESIAN_POINT('Ctrl Pts',(2.61236937664674,0.72718731189892,-4.37758094089741));
#10516=CARTESIAN_POINT('Ctrl Pts',(2.64159123071168,0.762173299544365,-4.38058374496643));
#10517=CARTESIAN_POINT('Ctrl Pts',(2.64767095008627,0.769278535775692,-4.38120301094996));
#10518=CARTESIAN_POINT('Ctrl Pts',(2.65784986421826,0.780891553448013,-4.38223134897906));
#10519=CARTESIAN_POINT('Ctrl Pts',(2.66190065301687,0.785441352571194,-4.38263843901499));
#10520=CARTESIAN_POINT('Ctrl Pts',(2.66963886772805,0.79399822531299,-4.38341219774291));
#10521=CARTESIAN_POINT('Ctrl Pts',(2.67331915499885,0.798011562263318,-4.38377856320098));
#10522=CARTESIAN_POINT('Ctrl Pts',(2.68174149435467,0.807069177541713,-4.38461340160357));
#10523=CARTESIAN_POINT('Ctrl Pts',(2.68650042352199,0.812097415124681,-4.38508258095322));
#10524=CARTESIAN_POINT('Ctrl Pts',(2.70119193678458,0.827348702789837,-4.38652354180177));
#10525=CARTESIAN_POINT('Ctrl Pts',(2.71126569473357,0.837433324734496,-4.38750135514587));
#10526=CARTESIAN_POINT('Ctrl Pts',(2.78884448683518,0.912326504248746,-4.39495873255046));
#10527=CARTESIAN_POINT('Ctrl Pts',(2.86366331523872,0.969053290894656,-4.40178300698536));
#10528=CARTESIAN_POINT('Ctrl Pts',(2.98314851466393,1.0390210823148,-4.41194389047282));
#10529=CARTESIAN_POINT('Ctrl Pts',(3.02318197688122,1.05948548559944,-4.4152342799495));
#10530=CARTESIAN_POINT('Ctrl Pts',(3.07773889826031,1.08354521867975,-4.41949861387452));
#10531=CARTESIAN_POINT('Ctrl Pts',(3.09129951992364,1.08922469892963,-4.42054113177716));
#10532=CARTESIAN_POINT('Ctrl Pts',(3.11436202435343,1.09838008782103,-4.42228101421727));
#10533=CARTESIAN_POINT('Ctrl Pts',(3.12380854868405,1.10199006799592,-4.42298446086923));
#10534=CARTESIAN_POINT('Ctrl Pts',(3.13734845472276,1.10696543321352,-4.42397849635867));
#10535=CARTESIAN_POINT('Ctrl Pts',(3.14140434561515,1.10843057593146,-4.42427445501353));
#10536=CARTESIAN_POINT('Ctrl Pts',(3.1483876930897,1.1109099518838,-4.42478082434258));
#10537=CARTESIAN_POINT('Ctrl Pts',(3.15131124679629,1.11193496303143,-4.42499185142925));
#10538=CARTESIAN_POINT('Ctrl Pts',(3.15742425779173,1.11405116328907,-4.42543105323434));
#10539=CARTESIAN_POINT('Ctrl Pts',(3.16061438774708,1.11514020746468,-4.42565910479114));
#10540=CARTESIAN_POINT('Ctrl Pts',(3.16913127398431,1.11800692799571,-4.42626499779542));
#10541=CARTESIAN_POINT('Ctrl Pts',(3.17446622338382,1.11976025673737,-4.42664146055877));
#10542=CARTESIAN_POINT('Ctrl Pts',(3.19803340228195,1.12731926491622,-4.42829185018616));
#10543=CARTESIAN_POINT('Ctrl Pts',(3.21639414205139,1.13271866213725,-4.42954443600009));
#10544=CARTESIAN_POINT('Ctrl Pts',(3.31806433321148,1.15994342534524,-4.43634070379639));
#10545=CARTESIAN_POINT('Ctrl Pts',(3.4034492200047,1.17302985393893,-4.44155319599446));
#10546=CARTESIAN_POINT('Ctrl Pts',(3.54462475894067,1.17903039484465,-4.45035176304717));
#10547=CARTESIAN_POINT('Ctrl Pts',(3.59983477587177,1.17749720922757,-4.45383414458074));
#10548=CARTESIAN_POINT('Ctrl Pts',(3.66896987633567,1.17070161835792,-4.45837016550041));
#10549=CARTESIAN_POINT('Ctrl Pts',(3.68318252799158,1.16904258774411,-4.45931180626223));
#10550=CARTESIAN_POINT('Ctrl Pts',(3.70423214420707,1.16619583953559,-4.46072162768333));
#10551=CARTESIAN_POINT('Ctrl Pts',(3.7110948776815,1.16520593521907,-4.46118367431222));
#10552=CARTESIAN_POINT('Ctrl Pts',(3.72333194978885,1.16333036775391,-4.46201204362349));
#10553=CARTESIAN_POINT('Ctrl Pts',(3.72870968307208,1.16246790464474,-4.46237763259274));
#10554=CARTESIAN_POINT('Ctrl Pts',(3.74008315845333,1.16056285296851,-4.46315420382506));
#10555=CARTESIAN_POINT('Ctrl Pts',(3.74607717074026,1.15951103386453,-4.46356546531935));
#10556=CARTESIAN_POINT('Ctrl Pts',(3.76209856411653,1.15657145584035,-4.46467021137427));
#10557=CARTESIAN_POINT('Ctrl Pts',(3.77210982485208,1.15459979762217,-4.46536630540517));
#10558=CARTESIAN_POINT('Ctrl Pts',(3.81845848590619,1.14484445084483,-4.46861670435287));
#10559=CARTESIAN_POINT('Ctrl Pts',(3.85443657842567,1.13547455074788,-4.47122023140523));
#10560=CARTESIAN_POINT('Ctrl Pts',(3.97241210693093,1.0987112855891,-4.4800309491002));
#10561=CARTESIAN_POINT('Ctrl Pts',(4.05183033175571,1.06400050138129,-4.48643607373497));
#10562=CARTESIAN_POINT('Ctrl Pts',(4.15133465569593,1.00676845573574,-4.49479825325177));
#10563=CARTESIAN_POINT('Ctrl Pts',(4.17542621254354,0.991727459659717,-4.49684922187467));
#10564=CARTESIAN_POINT('Ctrl Pts',(4.21253583813431,0.966650013184072,-4.50002644874795));
#10565=CARTESIAN_POINT('Ctrl Pts',(4.22592734503419,0.957187319596748,-4.50117683386415));
#10566=CARTESIAN_POINT('Ctrl Pts',(4.24323420439615,0.944407872488963,-4.50266427535948));
#10567=CARTESIAN_POINT('Ctrl Pts',(4.24733095185915,0.941341363238803,-4.5030164231688));
#10568=CARTESIAN_POINT('Ctrl Pts',(4.25400534076225,0.936277221744721,-4.50359005184909));
#10569=CARTESIAN_POINT('Ctrl Pts',(4.2565948496467,0.934295453198158,-4.50381258463187));
#10570=CARTESIAN_POINT('Ctrl Pts',(4.26164698475302,0.930395642610353,-4.50424664910969));
#10571=CARTESIAN_POINT('Ctrl Pts',(4.26411026411439,0.928478528956926,-4.50445823753851));
#10572=CARTESIAN_POINT('Ctrl Pts',(4.26960959880018,0.924163309009259,-4.50493057557591));
#10573=CARTESIAN_POINT('Ctrl Pts',(4.27264154617054,0.921759967576544,-4.50519096350377));
#10574=CARTESIAN_POINT('Ctrl Pts',(4.28316075951896,0.913336939282048,-4.50609449601116));
#10575=CARTESIAN_POINT('Ctrl Pts',(4.29058641350802,0.907240423900407,-4.50673253875443));
#10576=CARTESIAN_POINT('Ctrl Pts',(4.35498557928602,0.853035563823585,-4.51227640933967));
#10577=CARTESIAN_POINT('Ctrl Pts',(4.40735353745325,0.79970107902609,-4.51686389823039));
#10578=CARTESIAN_POINT('Ctrl Pts',(4.48995908414947,0.697824443301773,-4.52497689603592));
#10579=CARTESIAN_POINT('Ctrl Pts',(4.52237310957322,0.651377358922156,-4.52847971136735));
#10580=CARTESIAN_POINT('Ctrl Pts',(4.56193708787925,0.584967081846571,-4.53341099384109));
#10581=CARTESIAN_POINT('Ctrl Pts',(4.57207810363457,0.566874638875244,-4.53474666413505));
#10582=CARTESIAN_POINT('Ctrl Pts',(4.5889255949637,0.53486379547339,-4.53710415560737));
#10583=CARTESIAN_POINT('Ctrl Pts',(4.59584582403614,0.521063419225569,-4.5381186986392));
#10584=CARTESIAN_POINT('Ctrl Pts',(4.6055693600665,0.500682392057368,-4.53961644974872));
#10585=CARTESIAN_POINT('Ctrl Pts',(4.60858734538229,0.494205521374071,-4.54009233081125));
#10586=CARTESIAN_POINT('Ctrl Pts',(4.61381234188122,0.482720349644697,-4.54093623518798));
#10587=CARTESIAN_POINT('Ctrl Pts',(4.61604375034683,0.477723330771751,-4.54130341896364));
#10588=CARTESIAN_POINT('Ctrl Pts',(4.62063829440744,0.467238633339539,-4.54207396180983));
#10589=CARTESIAN_POINT('Ctrl Pts',(4.62299465324799,0.461748173806508,-4.54247753647737));
#10590=CARTESIAN_POINT('Ctrl Pts',(4.62906485144233,0.447301919183366,-4.54353971388447));
#10591=CARTESIAN_POINT('Ctrl Pts',(4.6327099934989,0.438317934443671,-4.54420058445679));
#10592=CARTESIAN_POINT('Ctrl Pts',(4.64788967505092,0.399537801187319,-4.54705532862281));
#10593=CARTESIAN_POINT('Ctrl Pts',(4.65831906587027,0.369326530362815,-4.54928493984713));
#10594=CARTESIAN_POINT('Ctrl Pts',(4.69389293834458,0.250864131426148,-4.55805453238249));
#10595=CARTESIAN_POINT('Ctrl Pts',(4.70991929931431,0.160221840005983,-4.56485303807176));
#10596=CARTESIAN_POINT('Ctrl Pts',(4.71695580110238,0.0397220695454684,
-4.57365051969951));
#10597=CARTESIAN_POINT('Ctrl Pts',(4.71757685012782,0.0107326568825134,
-4.57574570900212));
#10598=CARTESIAN_POINT('Ctrl Pts',(4.71686996105628,-0.0348756478035519,
-4.5789826953634));
#10599=CARTESIAN_POINT('Ctrl Pts',(4.71626031493139,-0.0514931435986362,
-4.58014963543668));
#10600=CARTESIAN_POINT('Ctrl Pts',(4.71500161198726,-0.0732274486540218,
-4.58165498810216));
#10601=CARTESIAN_POINT('Ctrl Pts',(4.71467063568214,-0.07835984867642,-4.58200893541007));
#10602=CARTESIAN_POINT('Ctrl Pts',(4.71407448855711,-0.0867482258372043,
-4.58258474546325));
#10603=CARTESIAN_POINT('Ctrl Pts',(4.71382937740384,-0.0900054917435229,
-4.58280767506943));
#10604=CARTESIAN_POINT('Ctrl Pts',(4.71332385256295,-0.0963694330864966,
-4.58324188002917));
#10605=CARTESIAN_POINT('Ctrl Pts',(4.71306465099221,-0.0994761523842213,
-4.58345321605845));
#10606=CARTESIAN_POINT('Ctrl Pts',(4.71245740586505,-0.106421484809332,
-4.58392433265226));
#10607=CARTESIAN_POINT('Ctrl Pts',(4.7121028450712,-0.110259528669526,-4.58418375762949));
#10608=CARTESIAN_POINT('Ctrl Pts',(4.71080695372752,-0.123573400928585,
-4.585080711798));
#10609=CARTESIAN_POINT('Ctrl Pts',(4.70976952017576,-0.13303980612306,-4.58571323605646));
#10610=CARTESIAN_POINT('Ctrl Pts',(4.69946363467642,-0.21759551932588,-4.59132461838758));
#10611=CARTESIAN_POINT('Ctrl Pts',(4.68309297948722,-0.291652564604074,
-4.59597497668237));
#10612=CARTESIAN_POINT('Ctrl Pts',(4.64247351184896,-0.4167841101214,-4.60411315894722));
#10613=CARTESIAN_POINT('Ctrl Pts',(4.62146083832885,-0.468635108910132,
-4.60757532613088));
#10614=CARTESIAN_POINT('Ctrl Pts',(4.58777874691445,-0.537280779495973,
-4.61245439098281));
#10615=CARTESIAN_POINT('Ctrl Pts',(4.57822596268234,-0.555523990107598,
-4.61378084252605));
#10616=CARTESIAN_POINT('Ctrl Pts',(4.56072428660126,-0.586916207472989,
-4.61612352438308));
#10617=CARTESIAN_POINT('Ctrl Pts',(4.55298706445551,-0.600177738814442,
-4.61713260540244));
#10618=CARTESIAN_POINT('Ctrl Pts',(4.54128037417088,-0.619370768445844,
-4.618623786095));
#10619=CARTESIAN_POINT('Ctrl Pts',(4.53751250796105,-0.62542381912913,-4.61909865172497));
#10620=CARTESIAN_POINT('Ctrl Pts',(4.53075700789496,-0.63605998194878,-4.6199414027435));
#10621=CARTESIAN_POINT('Ctrl Pts',(4.52779193876714,-0.6406572292671,-4.62030845639633));
#10622=CARTESIAN_POINT('Ctrl Pts',(4.5215176569622,-0.650238098938151,-4.62107937750852));
#10623=CARTESIAN_POINT('Ctrl Pts',(4.51820229420364,-0.655217486505259,
-4.62148346493585));
#10624=CARTESIAN_POINT('Ctrl Pts',(4.50939568762503,-0.668228274093998,
-4.62254848076225));
#10625=CARTESIAN_POINT('Ctrl Pts',(4.50384270393942,-0.676217124235428,
-4.62321169918651));
#10626=CARTESIAN_POINT('Ctrl Pts',(4.47944814397458,-0.710400957820557,
-4.62609068114484));
#10627=CARTESIAN_POINT('Ctrl Pts',(4.45963503736907,-0.735882087728136,
-4.62834293907587));
#10628=CARTESIAN_POINT('Ctrl Pts',(4.38589359421848,-0.823078777287632,
-4.63644251929911));
#10629=CARTESIAN_POINT('Ctrl Pts',(4.32660521756055,-0.879943626302029,
-4.64248368260475));
#10630=CARTESIAN_POINT('Ctrl Pts',(4.22106376312065,-0.961907566959175,
-4.65226416754916));
#10631=CARTESIAN_POINT('Ctrl Pts',(4.17817032352177,-0.990906247482976,
-4.65601472483297));
#10632=CARTESIAN_POINT('Ctrl Pts',(4.12750443208351,-1.02049818102455,-4.66009558767205));
#10633=CARTESIAN_POINT('Ctrl Pts',(4.12147313663783,-1.02394960515021,-4.66057599720942));
#10634=CARTESIAN_POINT('Ctrl Pts',(4.11221961682113,-1.0291367805158,-4.66130449417721));
#10635=CARTESIAN_POINT('Ctrl Pts',(4.10901938995273,-1.03091115812828,-4.66155488756773));
#10636=CARTESIAN_POINT('Ctrl Pts',(4.10314398640771,-1.03413308873951,-4.66201169197118));
#10637=CARTESIAN_POINT('Ctrl Pts',(4.10047146243859,-1.0355851995795,-4.66221837792203));
#10638=CARTESIAN_POINT('Ctrl Pts',(4.09442338332127,-1.03884112878983,-4.66268366270804));
#10639=CARTESIAN_POINT('Ctrl Pts',(4.09104464166341,-1.04063885799809,-4.66294188247286));
#10640=CARTESIAN_POINT('Ctrl Pts',(4.08450203439169,-1.04407917172129,-4.66343872289608));
#10641=CARTESIAN_POINT('Ctrl Pts',(4.08133937867713,-1.04572391295231,-4.66367746909161));
#10642=CARTESIAN_POINT('Ctrl Pts',(4.07816926754726,-1.04735428871609,-4.66391540717654));
#10643=CARTESIAN_POINT('Origin',(3.53951905042299,8.32667268468867E-16,
0.924367114736157));
#10644=CARTESIAN_POINT('',(4.07816965980385,-1.04735408697996,-5.26199342056381));
#10645=CARTESIAN_POINT('',(4.07816923100673,-1.04735430750874,-5.16216634940201));
#10646=CARTESIAN_POINT('',(4.07816926754759,-1.04735428871592,0.924367114736157));
#10647=CARTESIAN_POINT('',(2.3617694621724,-0.000540025086465901,-4.92534712819671));
#10648=CARTESIAN_POINT('Ctrl Pts',(4.07816965980385,-1.04735408697996,-5.26199342056381));
#10649=CARTESIAN_POINT('Ctrl Pts',(4.12181072239703,-1.02490963839082,-5.25892790966009));
#10650=CARTESIAN_POINT('Ctrl Pts',(4.16404503060095,-0.999739693094997,
-5.25581515735499));
#10651=CARTESIAN_POINT('Ctrl Pts',(4.21653578388376,-0.963821510535766,
-5.25166303093834));
#10652=CARTESIAN_POINT('Ctrl Pts',(4.22830102561051,-0.955449068569838,
-5.25071292378843));
#10653=CARTESIAN_POINT('Ctrl Pts',(4.24550409185827,-0.942724041252379,
-5.24929282208923));
#10654=CARTESIAN_POINT('Ctrl Pts',(4.25106232125615,-0.938535916699573,
-5.24882909447093));
#10655=CARTESIAN_POINT('Ctrl Pts',(4.26090649012893,-0.930980626784435,
-5.2479988102137));
#10656=CARTESIAN_POINT('Ctrl Pts',(4.26520682443458,-0.927632480328237,
-5.24763299978676));
#10657=CARTESIAN_POINT('Ctrl Pts',(4.27424915135843,-0.920490964716445,
-5.24685711135079));
#10658=CARTESIAN_POINT('Ctrl Pts',(4.27898534000884,-0.916690537492991,
-5.24644676191384));
#10659=CARTESIAN_POINT('Ctrl Pts',(4.29155148404351,-0.906446417916009,
-5.24534725552976));
#10660=CARTESIAN_POINT('Ctrl Pts',(4.29932781777987,-0.899938062128318,
-5.24465553281595));
#10661=CARTESIAN_POINT('Ctrl Pts',(4.3383579916116,-0.866405498964806,-5.24112476558359));
#10662=CARTESIAN_POINT('Ctrl Pts',(4.36825486627107,-0.837853436406766,
-5.23822373770836));
#10663=CARTESIAN_POINT('Ctrl Pts',(4.46678938675016,-0.733308294601039,
-5.2279449652619));
#10664=CARTESIAN_POINT('Ctrl Pts',(4.52697344195916,-0.650001329079335,
-5.22028621760055));
#10665=CARTESIAN_POINT('Ctrl Pts',(4.58665020397976,-0.539581865519443,
-5.21129135290743));
#10666=CARTESIAN_POINT('Ctrl Pts',(4.59706661343969,-0.518869508816685,
-5.2096513520831));
#10667=CARTESIAN_POINT('Ctrl Pts',(4.60940106064836,-0.492426156105455,
-5.20762781222354));
#10668=CARTESIAN_POINT('Ctrl Pts',(4.61189493878861,-0.486971244410699,
-5.20721407088753));
#10669=CARTESIAN_POINT('Ctrl Pts',(4.61575977668403,-0.47834391561347,-5.20656577028571));
#10670=CARTESIAN_POINT('Ctrl Pts',(4.61715859028351,-0.475184201518537,
-5.20632960542054));
#10671=CARTESIAN_POINT('Ctrl Pts',(4.61977429803975,-0.469204745918405,
-5.20588514589748));
#10672=CARTESIAN_POINT('Ctrl Pts',(4.62099406123722,-0.466386422201719,
-5.20567669131505));
#10673=CARTESIAN_POINT('Ctrl Pts',(4.62382938100447,-0.459764338565198,
-5.2051892680157));
#10674=CARTESIAN_POINT('Ctrl Pts',(4.6254359592854,-0.455956805363756,-5.2049108348728));
#10675=CARTESIAN_POINT('Ctrl Pts',(4.63063246104493,-0.443458014576272,
-5.20400254454878));
#10676=CARTESIAN_POINT('Ctrl Pts',(4.63413845186622,-0.434731946387427,
-5.20337742073631));
#10677=CARTESIAN_POINT('Ctrl Pts',(4.65302503345263,-0.386047474049979,
-5.19993447420054));
#10678=CARTESIAN_POINT('Ctrl Pts',(4.66632395000198,-0.345311104233059,
-5.19721932173884));
#10679=CARTESIAN_POINT('Ctrl Pts',(4.68470474709112,-0.276498392960429,
-5.19276664346341));
#10680=CARTESIAN_POINT('Ctrl Pts',(4.69103918212133,-0.248803330221722,
-5.19100949129946));
#10681=CARTESIAN_POINT('Ctrl Pts',(4.71161889630559,-0.141030778264493,
-5.18422252239453));
#10682=CARTESIAN_POINT('Ctrl Pts',(4.71855660318823,-0.0598008844888874,
-5.17919608584553));
#10683=CARTESIAN_POINT('Ctrl Pts',(4.71679165907389,0.0369037688813997,
-5.17289241417119));
#10684=CARTESIAN_POINT('Ctrl Pts',(4.71620782193635,0.0523085313992264,
-5.17187931924319));
#10685=CARTESIAN_POINT('Ctrl Pts',(4.71491573126955,0.0747504037471623,
-5.17038835889738));
#10686=CARTESIAN_POINT('Ctrl Pts',(4.71444616733386,0.0818000398237494,
-5.1699178370322));
#10687=CARTESIAN_POINT('Ctrl Pts',(4.7134998992822,0.0943082614614065,-5.16907894154682));
#10688=CARTESIAN_POINT('Ctrl Pts',(4.71304847382315,0.0997685940210485,
-5.16871135976159));
#10689=CARTESIAN_POINT('Ctrl Pts',(4.71202671718992,0.11115900144885,-5.16794161908197));
#10690=CARTESIAN_POINT('Ctrl Pts',(4.71144945963075,0.117088282746944,-5.16753925548609));
#10691=CARTESIAN_POINT('Ctrl Pts',(4.70982325574268,0.132572731377017,-5.1664839664535));
#10692=CARTESIAN_POINT('Ctrl Pts',(4.70870228553757,0.142119721793125,-5.16582882729535));
#10693=CARTESIAN_POINT('Ctrl Pts',(4.70300572130557,0.185991816294285,-5.16279674980042));
#10694=CARTESIAN_POINT('Ctrl Pts',(4.69703495084384,0.220115206402822,-5.1603770833594));
#10695=CARTESIAN_POINT('Ctrl Pts',(4.67491572539615,0.320296060508006,-5.1530861452875));
#10696=CARTESIAN_POINT('Ctrl Pts',(4.65454413600666,0.385269186302499,-5.14810366116571));
#10697=CARTESIAN_POINT('Ctrl Pts',(4.61912076825343,0.471367557034039,-5.14127225520403));
#10698=CARTESIAN_POINT('Ctrl Pts',(4.60881180679766,0.494307902040265,-5.13942974161785));
#10699=CARTESIAN_POINT('Ctrl Pts',(4.59034790793633,0.532109237774679,-5.13637080484718));
#10700=CARTESIAN_POINT('Ctrl Pts',(4.58259232458584,0.547156025623537,-5.13514696889147));
#10701=CARTESIAN_POINT('Ctrl Pts',(4.56348996893813,0.582333550366112,-5.1322785551833));
#10702=CARTESIAN_POINT('Ctrl Pts',(4.55186918339786,0.602309044835768,-5.1306439375619));
#10703=CARTESIAN_POINT('Ctrl Pts',(4.53650348460343,0.627019136375058,-5.1286260273197));
#10704=CARTESIAN_POINT('Ctrl Pts',(4.53330075935997,0.632082967781581,-5.12821272777133));
#10705=CARTESIAN_POINT('Ctrl Pts',(4.52819092818517,0.640027273659789,-5.12756496140902));
#10706=CARTESIAN_POINT('Ctrl Pts',(4.52630960927651,0.642924090884075,-5.1273288932832));
#10707=CARTESIAN_POINT('Ctrl Pts',(4.5227313758944,0.648381075324588,-5.12688450712173));
#10708=CARTESIAN_POINT('Ctrl Pts',(4.52103720391257,0.650942862624202,-5.12667602997595));
#10709=CARTESIAN_POINT('Ctrl Pts',(4.51703851400971,0.656938246800565,-5.12618840839514));
#10710=CARTESIAN_POINT('Ctrl Pts',(4.51472590938022,0.660366372049791,-5.12590980088357));
#10711=CARTESIAN_POINT('Ctrl Pts',(4.50708709394372,0.671562244012291,-5.12500034459764));
#10712=CARTESIAN_POINT('Ctrl Pts',(4.50168559651082,0.679278527388979,-5.12437424598452));
#10713=CARTESIAN_POINT('Ctrl Pts',(4.47113727625992,0.721822558033856,-5.12092114835691));
#10714=CARTESIAN_POINT('Ctrl Pts',(4.44418948728184,0.755322808632546,-5.11819748398923));
#10715=CARTESIAN_POINT('Ctrl Pts',(4.39568850609399,0.809286419043412,-5.11366212219573));
#10716=CARTESIAN_POINT('Ctrl Pts',(4.375085813339,0.830541332681467,-5.11183225718775));
#10717=CARTESIAN_POINT('Ctrl Pts',(4.29597236301118,0.906232437590899,-5.10505978450021));
#10718=CARTESIAN_POINT('Ctrl Pts',(4.23277743782858,0.955442124826888,-5.10011581106505));
#10719=CARTESIAN_POINT('Ctrl Pts',(4.15199566313185,1.00608468363147,-5.09390234427455));
#10720=CARTESIAN_POINT('Ctrl Pts',(4.13873925710877,1.0140360445229,-5.09288651473095));
#10721=CARTESIAN_POINT('Ctrl Pts',(4.11919478559555,1.02524198637415,-5.09139227222458));
#10722=CARTESIAN_POINT('Ctrl Pts',(4.11302742834247,1.02870463466391,-5.0909212496014));
#10723=CARTESIAN_POINT('Ctrl Pts',(4.10202692900307,1.03475116840081,-5.09008177993314));
#10724=CARTESIAN_POINT('Ctrl Pts',(4.09720619585746,1.03735728659822,-5.08971412849348));
#10725=CARTESIAN_POINT('Ctrl Pts',(4.08711050211186,1.04272436978215,-5.08894456617716));
#10726=CARTESIAN_POINT('Ctrl Pts',(4.08183245418757,1.04547916246757,-5.08854245276601));
#10727=CARTESIAN_POINT('Ctrl Pts',(4.06799348499323,1.05256919786595,-5.0874885492809));
#10728=CARTESIAN_POINT('Ctrl Pts',(4.05940021302137,1.05683996499785,-5.08683455619067));
#10729=CARTESIAN_POINT('Ctrl Pts',(4.01972822894387,1.07595559461547,-5.08381651801301));
#10730=CARTESIAN_POINT('Ctrl Pts',(3.98806270602655,1.08953635420821,-5.08141023025321));
#10731=CARTESIAN_POINT('Ctrl Pts',(3.89290739331601,1.12549514686094,-5.07418262163846));
#10732=CARTESIAN_POINT('Ctrl Pts',(3.82804800739374,1.14384082649897,-5.06925257873283));
#10733=CARTESIAN_POINT('Ctrl Pts',(3.7036443792427,1.1677703374829,-5.05995623275433));
#10734=CARTESIAN_POINT('Ctrl Pts',(3.64453169197281,1.17456308823098,-5.05560708651603));
#10735=CARTESIAN_POINT('Ctrl Pts',(3.57514463852517,1.17725367404128,-5.05073772466424));
#10736=CARTESIAN_POINT('Ctrl Pts',(3.56513055737188,1.17751410304252,-5.05004079967255));
#10737=CARTESIAN_POINT('Ctrl Pts',(3.55117601957179,1.17769889518903,-5.04907884791963));
#10738=CARTESIAN_POINT('Ctrl Pts',(3.54723776306123,1.17773129161456,-5.04880838697305));
#10739=CARTESIAN_POINT('Ctrl Pts',(3.540442403854,1.17775310321496,-5.04834355983019));
#10740=CARTESIAN_POINT('Ctrl Pts',(3.53758539678206,1.17775187800398,-5.04814869325288));
#10741=CARTESIAN_POINT('Ctrl Pts',(3.53155650614656,1.17772735442585,-5.04773871102051));
#10742=CARTESIAN_POINT('Ctrl Pts',(3.52838466048035,1.1777016384777,-5.04752373595874));
#10743=CARTESIAN_POINT('Ctrl Pts',(3.52051163681021,1.17760599780551,-5.04699183561268));
#10744=CARTESIAN_POINT('Ctrl Pts',(3.51581063687405,1.17752073477916,-5.04667574276497));
#10745=CARTESIAN_POINT('Ctrl Pts',(3.49806462841056,1.17709255317963,-5.04548777109785));
#10746=CARTESIAN_POINT('Ctrl Pts',(3.48502454462631,1.17656097652151,-5.0446255618208));
#10747=CARTESIAN_POINT('Ctrl Pts',(3.45153696241877,1.17463787613255,-5.04243279189006));
#10748=CARTESIAN_POINT('Ctrl Pts',(3.43111149806204,1.17292919227403,-5.04111588118099));
#10749=CARTESIAN_POINT('Ctrl Pts',(3.35327263201899,1.16436668618449,-5.03614110683995));
#10750=CARTESIAN_POINT('Ctrl Pts',(3.29634548165766,1.15382187783944,-5.03259116118402));
#10751=CARTESIAN_POINT('Ctrl Pts',(3.16743493356829,1.11997436303171,-5.02433857426702));
#10752=CARTESIAN_POINT('Ctrl Pts',(3.09647047652549,1.09384410115273,-5.0196258414921));
#10753=CARTESIAN_POINT('Ctrl Pts',(3.01913711947947,1.05660098896032,-5.0139925152941));
#10754=CARTESIAN_POINT('Ctrl Pts',(3.00983689102419,1.05196948755356,-5.01330667541189));
#10755=CARTESIAN_POINT('Ctrl Pts',(2.99461953520751,1.04413830961879,-5.01216995053619));
#10756=CARTESIAN_POINT('Ctrl Pts',(2.98866625697952,1.04100984054052,-5.01172152542976));
#10757=CARTESIAN_POINT('Ctrl Pts',(2.97818577263532,1.03538723511854,-5.01092532310437));
#10758=CARTESIAN_POINT('Ctrl Pts',(2.97364754066414,1.03291394045555,-5.01057828259718));
#10759=CARTESIAN_POINT('Ctrl Pts',(2.96388529930138,1.02750996357235,-5.00982676111007));
#10760=CARTESIAN_POINT('Ctrl Pts',(2.9586670943763,1.02456915019964,-5.00942192931476));
#10761=CARTESIAN_POINT('Ctrl Pts',(2.94798962802038,1.01844388514554,-5.00858702203782));
#10762=CARTESIAN_POINT('Ctrl Pts',(2.9425331218931,1.01525504342289,-5.00815679950824));
#10763=CARTESIAN_POINT('Ctrl Pts',(2.92896179358082,1.00717657580366,-5.00707770216163));
#10764=CARTESIAN_POINT('Ctrl Pts',(2.92087993178016,1.00223273272737,-5.00642690454264));
#10765=CARTESIAN_POINT('Ctrl Pts',(2.89813458345643,0.987938990756681,-5.00457161794335));
#10766=CARTESIAN_POINT('Ctrl Pts',(2.88361782231235,0.978361389566877,-5.00335910521856));
#10767=CARTESIAN_POINT('Ctrl Pts',(2.83441198463984,0.944309867614952,-4.99914917682155));
#10768=CARTESIAN_POINT('Ctrl Pts',(2.8008398717433,0.918286191794954,-4.99609953176539));
#10769=CARTESIAN_POINT('Ctrl Pts',(2.72189126543553,0.849953113278,-4.98850243575755));
#10770=CARTESIAN_POINT('Ctrl Pts',(2.67830960434367,0.805762713450463,-4.98391948335111));
#10771=CARTESIAN_POINT('Ctrl Pts',(2.62935760230804,0.747595313268514,-4.97839474099661));
#10772=CARTESIAN_POINT('Ctrl Pts',(2.62050038630224,0.736679939528711,-4.97737817840808));
#10773=CARTESIAN_POINT('Ctrl Pts',(2.59652165156743,0.706023510672077,-4.97458328105213));
#10774=CARTESIAN_POINT('Ctrl Pts',(2.58182558212455,0.685956792730309,-4.97282080439739));
#10775=CARTESIAN_POINT('Ctrl Pts',(2.56434953644656,0.660436394917194,-4.97067482939049));
#10776=CARTESIAN_POINT('Ctrl Pts',(2.56096292456356,0.655408060055201,-4.97025647199444));
#10777=CARTESIAN_POINT('Ctrl Pts',(2.55567984455888,0.647431666814539,-4.96960012831129));
#10778=CARTESIAN_POINT('Ctrl Pts',(2.55375750923817,0.644500993729968,-4.96936051204091));
#10779=CARTESIAN_POINT('Ctrl Pts',(2.55034861433473,0.639253071728064,-4.96893423068016));
#10780=CARTESIAN_POINT('Ctrl Pts',(2.54885709992483,0.63693919757697,-4.96874724725859));
#10781=CARTESIAN_POINT('Ctrl Pts',(2.54528799277041,0.631359365591405,-4.96829864277084));
#10782=CARTESIAN_POINT('Ctrl Pts',(2.54321837120998,0.628088371321061,-4.9680375421102));
#10783=CARTESIAN_POINT('Ctrl Pts',(2.53692426249731,0.618031268978648,-4.9672403027451));
#10784=CARTESIAN_POINT('Ctrl Pts',(2.53275259825284,0.61121213796607,-4.96670743786144));
#10785=CARTESIAN_POINT('Ctrl Pts',(2.52317564995829,0.595193238280242,-4.96547224342799));
#10786=CARTESIAN_POINT('Ctrl Pts',(2.51782523327688,0.585961312822027,-4.96477294320863));
#10787=CARTESIAN_POINT('Ctrl Pts',(2.4993872981812,0.553126833967579,-4.96232515490447));
#10788=CARTESIAN_POINT('Ctrl Pts',(2.48698554113814,0.529147206672973,-4.96060819549297));
#10789=CARTESIAN_POINT('Ctrl Pts',(2.43299941665534,0.415337533251348,-4.95268731264139));
#10790=CARTESIAN_POINT('Ctrl Pts',(2.40202262557602,0.320926229393458,-4.9467268254807));
#10791=CARTESIAN_POINT('Ctrl Pts',(2.37780790036989,0.195789132497261,-4.93857492600095));
#10792=CARTESIAN_POINT('Ctrl Pts',(2.37341359649751,0.167642610946875,-4.93672864877239));
#10793=CARTESIAN_POINT('Ctrl Pts',(2.36894287836191,0.130127094051754,-4.93423722545964));
#10794=CARTESIAN_POINT('Ctrl Pts',(2.36795141062971,0.120875524460372,-4.93362040694766));
#10795=CARTESIAN_POINT('Ctrl Pts',(2.36651146449389,0.10574952665702,-4.93260754936065));
#10796=CARTESIAN_POINT('Ctrl Pts',(2.36599725113855,0.0998816474920488,
-4.9322135551601));
#10797=CARTESIAN_POINT('Ctrl Pts',(2.36511081596282,0.0888119204264973,
-4.93146815585098));
#10798=CARTESIAN_POINT('Ctrl Pts',(2.36472908438211,0.0836109596068005,
-4.93111705473318));
#10799=CARTESIAN_POINT('Ctrl Pts',(2.36402603852109,0.0730740450178941,
-4.93040387614608));
#10800=CARTESIAN_POINT('Ctrl Pts',(2.36370648662251,0.0677381005423877,
-4.93004175260206));
#10801=CARTESIAN_POINT('Ctrl Pts',(2.36293200124268,0.0531408975087039,
-4.92904838308185));
#10802=CARTESIAN_POINT('Ctrl Pts',(2.36255010438768,0.0438763128627383,
-4.92841490227299));
#10803=CARTESIAN_POINT('Ctrl Pts',(2.3619332874832,0.0228946380504665,-4.92697314292768));
#10804=CARTESIAN_POINT('Ctrl Pts',(2.36176379052719,0.011176820686237,-4.92616293648505));
#10805=CARTESIAN_POINT('Ctrl Pts',(2.36176917474948,-0.000541157121145007,
-4.92534754912936));
#10806=CARTESIAN_POINT('Ctrl Pts',(2.3617691742458,-0.000540059816761217,
-4.92534762548451));
#10807=CARTESIAN_POINT('Ctrl Pts',(2.36181898604999,-0.1091684828109,-4.91778879502375));
#10808=CARTESIAN_POINT('Ctrl Pts',(2.3768982642571,-0.21725951079595,-4.90975117149892));
#10809=CARTESIAN_POINT('Ctrl Pts',(2.41479228157621,-0.350702095365063,
-4.89963175039954));
#10810=CARTESIAN_POINT('Ctrl Pts',(2.42412918804696,-0.379352030733392,
-4.89745194885264));
#10811=CARTESIAN_POINT('Ctrl Pts',(2.44045962029353,-0.423620709524443,
-4.8941011523857));
#10812=CARTESIAN_POINT('Ctrl Pts',(2.44671182077197,-0.439498089175984,
-4.89290302787093));
#10813=CARTESIAN_POINT('Ctrl Pts',(2.45531365661753,-0.46002246942175,-4.89136398367663));
#10814=CARTESIAN_POINT('Ctrl Pts',(2.45735178281537,-0.464796746716891,
-4.89100667874334));
#10815=CARTESIAN_POINT('Ctrl Pts',(2.46072808667034,-0.472563074918726,
-4.89042677503478));
#10816=CARTESIAN_POINT('Ctrl Pts',(2.46204727782729,-0.475563227319261,
-4.89020308145298));
#10817=CARTESIAN_POINT('Ctrl Pts',(2.46464316677656,-0.481400640495505,
-4.88976852858433));
#10818=CARTESIAN_POINT('Ctrl Pts',(2.46591860598063,-0.484238399890764,
-4.88955760145916));
#10819=CARTESIAN_POINT('Ctrl Pts',(2.46908867480344,-0.491217480424574,
-4.88903957602262));
#10820=CARTESIAN_POINT('Ctrl Pts',(2.47099613475291,-0.495352987793376,
-4.88873324326063));
#10821=CARTESIAN_POINT('Ctrl Pts',(2.4765980270547,-0.507315351744546,-4.88784867206811));
#10822=CARTESIAN_POINT('Ctrl Pts',(2.48035489525971,-0.515112872116006,
-4.88727398096347));
#10823=CARTESIAN_POINT('Ctrl Pts',(2.51915839094289,-0.59343115205462,-4.88151403766226));
#10824=CARTESIAN_POINT('Ctrl Pts',(2.56111356399941,-0.660320194402181,
-4.87668683277672));
#10825=CARTESIAN_POINT('Ctrl Pts',(2.65186312867384,-0.777138526529026,
-4.86753387797304));
#10826=CARTESIAN_POINT('Ctrl Pts',(2.69901022010504,-0.827901417128617,
-4.86323554845166));
#10827=CARTESIAN_POINT('Ctrl Pts',(2.75967865557678,-0.882667821003851,
-4.85793415668721));
#10828=CARTESIAN_POINT('Ctrl Pts',(2.76915705345247,-0.890952242532075,
-4.85711216872654));
#10829=CARTESIAN_POINT('Ctrl Pts',(2.78456444155176,-0.903989099496904,
-4.85578457188405));
#10830=CARTESIAN_POINT('Ctrl Pts',(2.79040995131818,-0.908838988332221,
-4.85528280811798));
#10831=CARTESIAN_POINT('Ctrl Pts',(2.80153794472927,-0.917891338641795,
-4.85433091741403));
#10832=CARTESIAN_POINT('Ctrl Pts',(2.80681046243589,-0.922105603404551,
-4.85388127793458));
#10833=CARTESIAN_POINT('Ctrl Pts',(2.81217361515792,-0.926317270244198,
-4.85342519085826));
#10834=CARTESIAN_POINT('Ctrl Pts',(2.81222841116074,-0.926360293511715,
-4.85342053109387));
#10835=CARTESIAN_POINT('Ctrl Pts',(2.81234195190683,-0.926449424129804,
-4.8534108760487));
#10836=CARTESIAN_POINT('Ctrl Pts',(2.81240069721753,-0.926495530754796,
-4.85340588073968));
#10837=CARTESIAN_POINT('Ctrl Pts',(2.81252257883423,-0.92659117157316,-4.85339551706046));
#10838=CARTESIAN_POINT('Ctrl Pts',(2.81258571581292,-0.926640704897272,
-4.85339014865691));
#10839=CARTESIAN_POINT('Ctrl Pts',(2.81271689344659,-0.926743597005745,
-4.85337899527));
#10840=CARTESIAN_POINT('Ctrl Pts',(2.81278493491908,-0.926796954752999,
-4.85337321024575));
#10841=CARTESIAN_POINT('Ctrl Pts',(2.81292651962749,-0.926907959521318,
-4.85336117285522));
#10842=CARTESIAN_POINT('Ctrl Pts',(2.81300006384146,-0.92696560527795,-4.8533549204404));
#10843=CARTESIAN_POINT('Ctrl Pts',(2.81315335640737,-0.92708573029719,-4.85334188866281));
#10844=CARTESIAN_POINT('Ctrl Pts',(2.81323310596572,-0.927148208026781,
-4.85333510923968));
#10845=CARTESIAN_POINT('Ctrl Pts',(2.81339964028152,-0.927278640358562,
-4.85332095292847));
#10846=CARTESIAN_POINT('Ctrl Pts',(2.8134864265113,-0.927346593062875,-4.85331357596712));
#10847=CARTESIAN_POINT('Ctrl Pts',(2.81366802544857,-0.927488742000743,
-4.85329814048013));
#10848=CARTESIAN_POINT('Ctrl Pts',(2.81376283999231,-0.927562935878647,
-4.85329008186285));
#10849=CARTESIAN_POINT('Ctrl Pts',(2.81396168866049,-0.927718488947303,
-4.85327318185809));
#10850=CARTESIAN_POINT('Ctrl Pts',(2.81406572508664,-0.927799845171807,
-4.85326434035588));
#10851=CARTESIAN_POINT('Ctrl Pts',(2.81428446787926,-0.927970842201228,
-4.85324575157455));
#10852=CARTESIAN_POINT('Ctrl Pts',(2.81439917718112,-0.928060479237587,
-4.85323600414871));
#10853=CARTESIAN_POINT('Ctrl Pts',(2.81464104860361,-0.928249412069959,
-4.85321545234029));
#10854=CARTESIAN_POINT('Ctrl Pts',(2.81476821450138,-0.928348702999451,
-4.85320464776902));
#10855=CARTESIAN_POINT('Ctrl Pts',(2.81503721832761,-0.928558651796912,
-4.85318179352913));
#10856=CARTESIAN_POINT('Ctrl Pts',(2.8151790612019,-0.928669303292786,-4.85316974361315));
#10857=CARTESIAN_POINT('Ctrl Pts',(2.81548022081617,-0.928904126657907,
-4.8531441612025));
#10858=CARTESIAN_POINT('Ctrl Pts',(2.81563954414395,-0.929028290037307,
-4.85313062837795));
#10859=CARTESIAN_POINT('Ctrl Pts',(2.81597925999633,-0.929292895934835,
-4.8531017754874));
#10860=CARTESIAN_POINT('Ctrl Pts',(2.81615966146351,-0.92943332690928,-4.85308645497331));
#10861=CARTESIAN_POINT('Ctrl Pts',(2.81642629426616,-0.929640758797993,
-4.853063813394));
#10862=CARTESIAN_POINT('Ctrl Pts',(2.81651249413298,-0.929707800325802,
-4.85305649390827));
#10863=CARTESIAN_POINT('Ctrl Pts',(2.81678542558222,-0.929920010520886,
-4.8530333195128));
#10864=CARTESIAN_POINT('Ctrl Pts',(2.8169721914822,-0.930065134857392,-4.85301746287995));
#10865=CARTESIAN_POINT('Ctrl Pts',(2.82133725349274,-0.933454848709381,
-4.8526468995239));
#10866=CARTESIAN_POINT('Ctrl Pts',(2.82553726016308,-0.93667126017307,-4.85229110269391));
#10867=CARTESIAN_POINT('Ctrl Pts',(2.83512969130231,-0.943915246063989,
-4.85148011500952));
#10868=CARTESIAN_POINT('Ctrl Pts',(2.84053521770156,-0.947925081078398,
-4.85102425483084));
#10869=CARTESIAN_POINT('Ctrl Pts',(2.85438557342324,-0.95801642871208,-4.84985895889958));
#10870=CARTESIAN_POINT('Ctrl Pts',(2.86287703639412,-0.964032640419206,
-4.84914708093828));
#10871=CARTESIAN_POINT('Ctrl Pts',(2.93360151719623,-1.01274625456824,-4.84323727408815));
#10872=CARTESIAN_POINT('Ctrl Pts',(2.99971556311497,-1.04947574867174,-4.83781768434997));
#10873=CARTESIAN_POINT('Ctrl Pts',(3.12194767035934,-1.10276067581353,-4.82806332631947));
#10874=CARTESIAN_POINT('Ctrl Pts',(3.17665399657629,-1.12195194797886,-4.8237872403041));
#10875=CARTESIAN_POINT('Ctrl Pts',(3.25226223265107,-1.1423639737446,-4.81813256979602));
#10876=CARTESIAN_POINT('Ctrl Pts',(3.27211006870983,-1.14717237723388,-4.81667168507945));
#10877=CARTESIAN_POINT('Ctrl Pts',(3.30479848613688,-1.15419699747518,-4.81431386124434));
#10878=CARTESIAN_POINT('Ctrl Pts',(3.3175680978176,-1.1567204770445,-4.81340468577313));
#10879=CARTESIAN_POINT('Ctrl Pts',(3.33499980239412,-1.15986594073542,-4.81218202566516));
#10880=CARTESIAN_POINT('Ctrl Pts',(3.33962709298689,-1.16067236140287,-4.81185922793262));
#10881=CARTESIAN_POINT('Ctrl Pts',(3.3473862022155,-1.16197680087145,-4.81132103954564));
#10882=CARTESIAN_POINT('Ctrl Pts',(3.35051539252966,-1.16248988606737,-4.81110483047383));
#10883=CARTESIAN_POINT('Ctrl Pts',(3.3564686906733,-1.16344135884289,-4.81069513219727));
#10884=CARTESIAN_POINT('Ctrl Pts',(3.3592923729147,-1.16388211380205,-4.8105015081195));
#10885=CARTESIAN_POINT('Ctrl Pts',(3.36601440233178,-1.16490632096715,-4.81004216838426));
#10886=CARTESIAN_POINT('Ctrl Pts',(3.36991416040227,-1.16548049401373,-4.80977696265404));
#10887=CARTESIAN_POINT('Ctrl Pts',(3.38375419949886,-1.16744726644796,-4.80884005592069));
#10888=CARTESIAN_POINT('Ctrl Pts',(3.39370965490633,-1.16873240962715,-4.80817396338375));
#10889=CARTESIAN_POINT('Ctrl Pts',(3.46327460914987,-1.17680973789604,-4.80356656716596));
#10890=CARTESIAN_POINT('Ctrl Pts',(3.52331819541534,-1.17916655427905,-4.799827506927));
#10891=CARTESIAN_POINT('Ctrl Pts',(3.65005907296692,-1.17445336707883,-4.79196989567312));
#10892=CARTESIAN_POINT('Ctrl Pts',(3.71649539435003,-1.16629266550261,-4.78786703465103));
#10893=CARTESIAN_POINT('Ctrl Pts',(3.81545848963402,-1.14548238035953,-4.78143785346733));
#10894=CARTESIAN_POINT('Ctrl Pts',(3.84870985800779,-1.13695785148989,-4.77922304202997));
#10895=CARTESIAN_POINT('Ctrl Pts',(3.89071094569065,-1.12421135815636,-4.77633045465986));
#10896=CARTESIAN_POINT('Ctrl Pts',(3.89984785013332,-1.12131622314379,-4.77569538513455));
#10897=CARTESIAN_POINT('Ctrl Pts',(3.91459906501985,-1.11644321948396,-4.77466014454029));
#10898=CARTESIAN_POINT('Ctrl Pts',(3.92023562499971,-1.1145336995018,-4.77426219702932));
#10899=CARTESIAN_POINT('Ctrl Pts',(3.93103499238363,-1.11078367369686,-4.7734950626842));
#10900=CARTESIAN_POINT('Ctrl Pts',(3.93619991026364,-1.10894968157025,-4.77312609727508));
#10901=CARTESIAN_POINT('Ctrl Pts',(3.94800527484999,-1.10466473120827,-4.77227789947044));
#10902=CARTESIAN_POINT('Ctrl Pts',(3.95463674959023,-1.10218984570484,-4.77179789100892));
#10903=CARTESIAN_POINT('Ctrl Pts',(3.97570533521537,-1.09410988024924,-4.77026129596531));
#10904=CARTESIAN_POINT('Ctrl Pts',(3.99005386349495,-1.08827994916449,-4.76919734025277));
#10905=CARTESIAN_POINT('Ctrl Pts',(4.02932237438677,-1.07141513801035,-4.76623557462156));
#10906=CARTESIAN_POINT('Ctrl Pts',(4.05396561751214,-1.05980213712042,-4.76432014601751));
#10907=CARTESIAN_POINT('Ctrl Pts',(4.07816946571175,-1.04735418680084,-4.76238152739268));
#10908=CARTESIAN_POINT('Ctrl Pts',(4.07816926754726,-1.04735428871609,-4.66391540717654));
#10909=CARTESIAN_POINT('Ctrl Pts',(4.07594237517118,-1.04849957076134,-4.66408255037298));
#10910=CARTESIAN_POINT('Ctrl Pts',(4.07371180386683,-1.04963776406353,-4.66424929480144));
#10911=CARTESIAN_POINT('Ctrl Pts',(4.04042211211563,-1.06649088614516,-4.66672805048002));
#10912=CARTESIAN_POINT('Ctrl Pts',(4.0086815204711,-1.08083013267527,-4.66896494141043));
#10913=CARTESIAN_POINT('Ctrl Pts',(3.95009147986544,-1.10423040334051,-4.67295075052231));
#10914=CARTESIAN_POINT('Ctrl Pts',(3.92346369370455,-1.11376888769826,-4.6747110445444));
#10915=CARTESIAN_POINT('Ctrl Pts',(3.83337807483642,-1.14242368521899,-4.68057183162995));
#10916=CARTESIAN_POINT('Ctrl Pts',(3.76865968539658,-1.15714263997218,-4.68463580821676));
#10917=CARTESIAN_POINT('Ctrl Pts',(3.66663614832824,-1.17144706502294,-4.69116873956656));
#10918=CARTESIAN_POINT('Ctrl Pts',(3.63000799642946,-1.17484395378423,-4.69353720779345));
#10919=CARTESIAN_POINT('Ctrl Pts',(3.58349994369115,-1.17696926980004,-4.69660390671092));
#10920=CARTESIAN_POINT('Ctrl Pts',(3.57371140871894,-1.17729429377407,-4.69725261074648));
#10921=CARTESIAN_POINT('Ctrl Pts',(3.55792522256068,-1.17762142918079,-4.69830454967573));
#10922=CARTESIAN_POINT('Ctrl Pts',(3.55192948374963,-1.17769987540759,-4.69870542348624));
#10923=CARTESIAN_POINT('Ctrl Pts',(3.54046693973192,-1.17776230546359,-4.69947448198897));
#10924=CARTESIAN_POINT('Ctrl Pts',(3.53500031929333,-1.17775401761402,-4.69984241798241));
#10925=CARTESIAN_POINT('Ctrl Pts',(3.52255137258316,-1.17764847108797,-4.70068304766807));
#10926=CARTESIAN_POINT('Ctrl Pts',(3.51556951052194,-1.17752717142828,-4.70115647112397));
#10927=CARTESIAN_POINT('Ctrl Pts',(3.49362664586136,-1.17695071446321,-4.70265076676722));
#10928=CARTESIAN_POINT('Ctrl Pts',(3.47867350584121,-1.17627245187627,-4.70367844800702));
#10929=CARTESIAN_POINT('Ctrl Pts',(3.37381403098154,-1.16951136556598,-4.71095425256885));
#10930=CARTESIAN_POINT('Ctrl Pts',(3.28486878464908,-1.15341330796791,-4.71751751035369));
#10931=CARTESIAN_POINT('Ctrl Pts',(3.13648430369497,-1.10854656736093,-4.7288945734192));
#10932=CARTESIAN_POINT('Ctrl Pts',(3.07597624575129,-1.08463928832256,-4.7336563320011));
#10933=CARTESIAN_POINT('Ctrl Pts',(3.01038139189544,-1.0522242280023,-4.73876251140944));
#10934=CARTESIAN_POINT('Ctrl Pts',(3.00305789832098,-1.04850938449694,-4.73933167849372));
#10935=CARTESIAN_POINT('Ctrl Pts',(2.99230306569419,-1.04291180642469,-4.74016551164074));
#10936=CARTESIAN_POINT('Ctrl Pts',(2.98884148492761,-1.04108817584861,-4.74043358055913));
#10937=CARTESIAN_POINT('Ctrl Pts',(2.982700608023,-1.03781384020369,-4.74090849801768));
#10938=CARTESIAN_POINT('Ctrl Pts',(2.98001778785014,-1.03636995451515,-4.74111575597655));
#10939=CARTESIAN_POINT('Ctrl Pts',(2.97418454116829,-1.03320126512422,-4.74156589831628));
#10940=CARTESIAN_POINT('Ctrl Pts',(2.97103638544072,-1.03147245338185,-4.7418085289892));
#10941=CARTESIAN_POINT('Ctrl Pts',(2.96226074820748,-1.0266009248748,-4.74248415282486));
#10942=CARTESIAN_POINT('Ctrl Pts',(2.95665097989623,-1.02342631557843,-4.74291520800155));
#10943=CARTESIAN_POINT('Ctrl Pts',(2.92427927831815,-1.00475441370576,-4.74539948592566));
#10944=CARTESIAN_POINT('Ctrl Pts',(2.89810743256667,-0.988252457315542,
-4.74739543981475));
#10945=CARTESIAN_POINT('Ctrl Pts',(2.81874821178269,-0.933731936282084,
-4.75350587934091));
#10946=CARTESIAN_POINT('Ctrl Pts',(2.76805383453747,-0.892305073729162,
-4.75750011858764));
#10947=CARTESIAN_POINT('Ctrl Pts',(2.68017429558994,-0.807374732461095,
-4.76508590753014));
#10948=CARTESIAN_POINT('Ctrl Pts',(2.64221148736273,-0.764961088451493,
-4.76865181562321));
#10949=CARTESIAN_POINT('Ctrl Pts',(2.59639385165059,-0.705647021776681,
-4.77351572210995));
#10950=CARTESIAN_POINT('Ctrl Pts',(2.58565828138658,-0.691066159061978,
-4.77470201729709));
#10951=CARTESIAN_POINT('Ctrl Pts',(2.57089487314005,-0.670015039881867,
-4.77640499125867));
#10952=CARTESIAN_POINT('Ctrl Pts',(2.56658680154747,-0.663743764608143,
-4.77691111934945));
#10953=CARTESIAN_POINT('Ctrl Pts',(2.55924430036471,-0.652830169326876,
-4.77779008900089));
#10954=CARTESIAN_POINT('Ctrl Pts',(2.55618130525719,-0.648207291479624,
-4.77816185457187));
#10955=CARTESIAN_POINT('Ctrl Pts',(2.55036007655923,-0.639285285181651,
-4.77887837605372));
#10956=CARTESIAN_POINT('Ctrl Pts',(2.54759693251548,-0.634989497563756,
-4.77922294012964));
#10957=CARTESIAN_POINT('Ctrl Pts',(2.5411411174682,-0.62480784549932,-4.78003867619195));
#10958=CARTESIAN_POINT('Ctrl Pts',(2.53747245154041,-0.618907061594607,
-4.78051070968078));
#10959=CARTESIAN_POINT('Ctrl Pts',(2.52665496992359,-0.60115959798838,-4.78192845602149));
#10960=CARTESIAN_POINT('Ctrl Pts',(2.51966269772991,-0.589219398436419,
-4.78287971914512));
#10961=CARTESIAN_POINT('Ctrl Pts',(2.4722993367599,-0.504970634263997,-4.78957636750384));
#10962=CARTESIAN_POINT('Ctrl Pts',(2.43945026368169,-0.42871575861482,-4.79558411563196));
#10963=CARTESIAN_POINT('Ctrl Pts',(2.40738734594908,-0.325589333328425,
-4.80350798074462));
#10964=CARTESIAN_POINT('Ctrl Pts',(2.40067753052457,-0.301281637022407,
-4.80535980599111));
#10965=CARTESIAN_POINT('Ctrl Pts',(2.38432607889428,-0.233651103097251,
-4.81044600652398));
#10966=CARTESIAN_POINT('Ctrl Pts',(2.376343426479,-0.189965581231032,-4.81365869338497));
#10967=CARTESIAN_POINT('Ctrl Pts',(2.36965958782558,-0.136438239716641,
-4.81743560495512));
#10968=CARTESIAN_POINT('Ctrl Pts',(2.36859003216975,-0.126932282345681,
-4.81810024147724));
#10969=CARTESIAN_POINT('Ctrl Pts',(2.36722159069247,-0.11327417371505,-4.8190454584071));
#10970=CARTESIAN_POINT('Ctrl Pts',(2.36682874431602,-0.109132120882722,
-4.81933083023163));
#10971=CARTESIAN_POINT('Ctrl Pts',(2.36618378468905,-0.101925800603485,
-4.81982499208126));
#10972=CARTESIAN_POINT('Ctrl Pts',(2.36592170833022,-0.0988625013259678,
-4.8200343200167));
#10973=CARTESIAN_POINT('Ctrl Pts',(2.36539180889145,-0.092369459952888,
-4.82047643419576));
#10974=CARTESIAN_POINT('Ctrl Pts',(2.36512701428202,-0.0889395449169065,
-4.82070905396838));
#10975=CARTESIAN_POINT('Ctrl Pts',(2.36444676922117,-0.079594922763808,
-4.82134041675857));
#10976=CARTESIAN_POINT('Ctrl Pts',(2.36406094202169,-0.0736780619804741,
-4.82173757126383));
#10977=CARTESIAN_POINT('Ctrl Pts',(2.36243157575517,-0.0454039588929165,
-4.82362400025371));
#10978=CARTESIAN_POINT('Ctrl Pts',(2.36178101448085,-0.0230155722425881,
-4.82508373987338));
#10979=CARTESIAN_POINT('Ctrl Pts',(2.36174401658426,0.0471985237747278,
-4.829593103011));
#10980=CARTESIAN_POINT('Ctrl Pts',(2.3646311847031,0.0949786277497044,-4.83256307013559));
#10981=CARTESIAN_POINT('Ctrl Pts',(2.3811127466578,0.230240856367583,-4.8409985176109));
#10982=CARTESIAN_POINT('Ctrl Pts',(2.40166106301473,0.316532919826317,-4.84643564789581));
#10983=CARTESIAN_POINT('Ctrl Pts',(2.43679006200633,0.413897779696194,-4.85318542095783));
#10984=CARTESIAN_POINT('Ctrl Pts',(2.44218128664968,0.427986439667305,-4.85417716662488));
#10985=CARTESIAN_POINT('Ctrl Pts',(2.45046987214241,0.448459597062111,-4.85564243623371));
#10986=CARTESIAN_POINT('Ctrl Pts',(2.45315615543315,0.454928323754113,-4.85610897651905));
#10987=CARTESIAN_POINT('Ctrl Pts',(2.45804259059345,0.466405023252212,-4.85694327579659));
#10988=CARTESIAN_POINT('Ctrl Pts',(2.4602202495084,0.471422396056728,-4.85731027257533));
#10989=CARTESIAN_POINT('Ctrl Pts',(2.46485398363867,0.481898207369978,-4.85808136374389));
#10990=CARTESIAN_POINT('Ctrl Pts',(2.46731687334954,0.487353441797358,-4.85848568004611));
#10991=CARTESIAN_POINT('Ctrl Pts',(2.47389833630932,0.501639816882176,-4.85955196275789));
#10992=CARTESIAN_POINT('Ctrl Pts',(2.47808504058831,0.5104388749908,-4.86021622912454));
#10993=CARTESIAN_POINT('Ctrl Pts',(2.49832540071275,0.551651311248119,-4.86336397318484));
#10994=CARTESIAN_POINT('Ctrl Pts',(2.51575599386501,0.583362757437863,-4.86589429827743));
#10995=CARTESIAN_POINT('Ctrl Pts',(2.56813394305839,0.66905648477249,-4.87304338174069));
#10996=CARTESIAN_POINT('Ctrl Pts',(2.60608093576134,0.721052920950755,-4.87775116002841));
#10997=CARTESIAN_POINT('Ctrl Pts',(2.68755045370288,0.815409888972056,-4.8868996745501));
#10998=CARTESIAN_POINT('Ctrl Pts',(2.73048932778562,0.858030384853922,-4.8913244050864));
#10999=CARTESIAN_POINT('Ctrl Pts',(2.78414315453906,0.903660695744325,-4.89626348002543));
#11000=CARTESIAN_POINT('Ctrl Pts',(2.79185635786389,0.910052697294059,-4.89696041008659));
#11001=CARTESIAN_POINT('Ctrl Pts',(2.80271440234051,0.918819612625345,-4.89792234319587));
#11002=CARTESIAN_POINT('Ctrl Pts',(2.80579076202136,0.921278117559275,-4.89819278072557));
#11003=CARTESIAN_POINT('Ctrl Pts',(2.81111989604328,0.925493324914357,-4.8986575588927));
#11004=CARTESIAN_POINT('Ctrl Pts',(2.81336681279798,0.927257327174282,-4.89885239987541));
#11005=CARTESIAN_POINT('Ctrl Pts',(2.81812169032928,0.930962388345032,-4.89926231600909));
#11006=CARTESIAN_POINT('Ctrl Pts',(2.82063111368446,0.932901524552633,-4.89947725067882));
#11007=CARTESIAN_POINT('Ctrl Pts',(2.82687926435044,0.937689549601756,-4.90000902738763));
#11008=CARTESIAN_POINT('Ctrl Pts',(2.83062732232272,0.94052627598783,-4.90032503752866));
#11009=CARTESIAN_POINT('Ctrl Pts',(2.84483978053464,0.951149781903242,-4.90151254062941));
#11010=CARTESIAN_POINT('Ctrl Pts',(2.85541676486228,0.958785321776503,-4.90237437294793));
#11011=CARTESIAN_POINT('Ctrl Pts',(2.88292124661867,0.977953898020603,-4.90456601645266));
#11012=CARTESIAN_POINT('Ctrl Pts',(2.90002714399,0.989224293938772,-4.90588219422197));
#11013=CARTESIAN_POINT('Ctrl Pts',(2.9665208201606,1.03058819911785,-4.91085715353935));
#11014=CARTESIAN_POINT('Ctrl Pts',(3.01780819301119,1.0574769938129,-4.91440789604782));
#11015=CARTESIAN_POINT('Ctrl Pts',(3.14010377862566,1.11052160963622,-4.92266194772751));
#11016=CARTESIAN_POINT('Ctrl Pts',(3.21205779908429,1.1338243803949,-4.9273753365722));
#11017=CARTESIAN_POINT('Ctrl Pts',(3.29588425755089,1.1523215915183,-4.93300927013435));
#11018=CARTESIAN_POINT('Ctrl Pts',(3.30605663399126,1.15442550712546,-4.93369498093768));
#11019=CARTESIAN_POINT('Ctrl Pts',(3.3228574078038,1.15766921371327,-4.93483149939424));
#11020=CARTESIAN_POINT('Ctrl Pts',(3.3294702419773,1.1588872985261,-4.93527984816823));
#11021=CARTESIAN_POINT('Ctrl Pts',(3.34143872464283,1.16098609045903,-4.93609329993561));
#11022=CARTESIAN_POINT('Ctrl Pts',(3.34679075643416,1.16188653521442,-4.93645777348734));
#11023=CARTESIAN_POINT('Ctrl Pts',(3.35829104697559,1.16373973930365,-4.93724256981999));
#11024=CARTESIAN_POINT('Ctrl Pts',(3.36444099136388,1.16468083213406,-4.93766324560173));
#11025=CARTESIAN_POINT('Ctrl Pts',(3.38131574953266,1.16712641167665,-4.9388204040293));
#11026=CARTESIAN_POINT('Ctrl Pts',(3.39205408767386,1.16853173531024,-4.93955994350245));
#11027=CARTESIAN_POINT('Ctrl Pts',(3.45576337635456,1.1759772147161,-4.94396759026165));
#11028=CARTESIAN_POINT('Ctrl Pts',(3.50906807416584,1.17856212843965,-4.94774153101322));
#11029=CARTESIAN_POINT('Ctrl Pts',(3.61033405240667,1.17659800293228,-4.95506187508456));
#11030=CARTESIAN_POINT('Ctrl Pts',(3.65820619677908,1.17273635210013,-4.95858594720604));
#11031=CARTESIAN_POINT('Ctrl Pts',(3.73365671957204,1.16198223156333,-4.96417761414976));
#11032=CARTESIAN_POINT('Ctrl Pts',(3.76145538193309,1.15699459816853,-4.96624536504702));
#11033=CARTESIAN_POINT('Ctrl Pts',(3.82290217532677,1.14367346340159,-4.97080393714518));
#11034=CARTESIAN_POINT('Ctrl Pts',(3.85641908781445,1.13484353457212,-4.97328234020087));
#11035=CARTESIAN_POINT('Ctrl Pts',(3.89528922304976,1.12274636261065,-4.97611184231512));
#11036=CARTESIAN_POINT('Ctrl Pts',(3.90106355613962,1.12090025637399,-4.97653098363207));
#11037=CARTESIAN_POINT('Ctrl Pts',(3.91045784998563,1.11781666693035,-4.97721064972915));
#11038=CARTESIAN_POINT('Ctrl Pts',(3.91408640416377,1.11660601486784,-4.97747262382686));
#11039=CARTESIAN_POINT('Ctrl Pts',(3.92058945564488,1.11440103162938,-4.97794106619979));
#11040=CARTESIAN_POINT('Ctrl Pts',(3.9234660493333,1.11341322773696,-4.97814789811702));
#11041=CARTESIAN_POINT('Ctrl Pts',(3.92979668368952,1.11121187606592,-4.97860223891341));
#11042=CARTESIAN_POINT('Ctrl Pts',(3.93324890939516,1.10999336196327,-4.97884945630969));
#11043=CARTESIAN_POINT('Ctrl Pts',(3.94324494394163,1.10641261090348,-4.97956385642956));
#11044=CARTESIAN_POINT('Ctrl Pts',(3.94977371094593,1.1040084157086,-4.98002867814957));
#11045=CARTESIAN_POINT('Ctrl Pts',(4.00506944076144,1.08308768601547,-4.98395345115396));
#11046=CARTESIAN_POINT('Ctrl Pts',(4.05258455145938,1.06140536821004,-4.98724711658884));
#11047=CARTESIAN_POINT('Ctrl Pts',(4.17164865522746,0.997201983320257,-4.99567345831521));
#11048=CARTESIAN_POINT('Ctrl Pts',(4.24040421909818,0.950136426472314,-5.00072993691118));
#11049=CARTESIAN_POINT('Ctrl Pts',(4.32716778581371,0.87616263716116,-5.00800130417276));
#11050=CARTESIAN_POINT('Ctrl Pts',(4.34990039028731,0.855180286455938,-5.01000182993786));
#11051=CARTESIAN_POINT('Ctrl Pts',(4.37856066632914,0.826556759223605,-5.01267122140765));
#11052=CARTESIAN_POINT('Ctrl Pts',(4.38525861238371,0.819702076277839,-5.01330623739476));
#11053=CARTESIAN_POINT('Ctrl Pts',(4.39597841446718,0.808460158657226,-5.01434137203927));
#11054=CARTESIAN_POINT('Ctrl Pts',(4.40005206822568,0.804122747761935,-5.01473926739358));
#11055=CARTESIAN_POINT('Ctrl Pts',(4.40781380533997,0.795731934218784,-5.01550628778432));
#11056=CARTESIAN_POINT('Ctrl Pts',(4.41150681758084,0.791683285624797,-5.01587519137215));
#11057=CARTESIAN_POINT('Ctrl Pts',(4.41998514415882,0.782257205135081,-5.0167314312037));
#11058=CARTESIAN_POINT('Ctrl Pts',(4.42474963970937,0.776861427163581,-5.01721961093467));
#11059=CARTESIAN_POINT('Ctrl Pts',(4.43976544584706,0.75953856378957,-5.01878094850704));
#11060=CARTESIAN_POINT('Ctrl Pts',(4.44982708297487,0.747450096538627,-5.01986169829694));
#11061=CARTESIAN_POINT('Ctrl Pts',(4.47290531154009,0.718565618349747,-5.02242494659652));
#11062=CARTESIAN_POINT('Ctrl Pts',(4.48571503494254,0.701612088290005,-5.02391486948382));
#11063=CARTESIAN_POINT('Ctrl Pts',(4.53234344503568,0.636299038446352,-5.02960137648408));
#11064=CARTESIAN_POINT('Ctrl Pts',(4.56296725837986,0.585772229158071,-5.0338991803957));
#11065=CARTESIAN_POINT('Ctrl Pts',(4.62179279736881,0.469906809288292,-5.04343112368654));
#11066=CARTESIAN_POINT('Ctrl Pts',(4.64813228953771,0.403865518499825,-5.04866147002493));
#11067=CARTESIAN_POINT('Ctrl Pts',(4.67115501107625,0.32648221392716,-5.05431985113295));
#11068=CARTESIAN_POINT('Ctrl Pts',(4.67382544033851,0.31707982072097,-5.05499957702466));
#11069=CARTESIAN_POINT('Ctrl Pts',(4.67739662796914,0.303882986312167,-5.05594174084201));
#11070=CARTESIAN_POINT('Ctrl Pts',(4.67839597714514,0.300115973771326,-5.05620933467332));
#11071=CARTESIAN_POINT('Ctrl Pts',(4.68009281730321,0.293589247781774,-5.05667056193083));
#11072=CARTESIAN_POINT('Ctrl Pts',(4.68079902900792,0.290831867286321,-5.05686467842316));
#11073=CARTESIAN_POINT('Ctrl Pts',(4.682273894142,0.284985199214715,-5.05727467063104));
#11074=CARTESIAN_POINT('Ctrl Pts',(4.68304003264503,0.281895300300368,-5.05749039735209));
#11075=CARTESIAN_POINT('Ctrl Pts',(4.68492015832999,0.274178792600658,-5.05802685898348));
#11076=CARTESIAN_POINT('Ctrl Pts',(4.68601866517052,0.26954840682987,-5.05834672958593));
#11077=CARTESIAN_POINT('Ctrl Pts',(4.69011954729817,0.251783789469712,-5.05956656713604));
#11078=CARTESIAN_POINT('Ctrl Pts',(4.69292467254144,0.238604461361061,-5.06045618263244));
#11079=CARTESIAN_POINT('Ctrl Pts',(4.69960316471049,0.204350057448847,-5.06273558269781));
#11080=CARTESIAN_POINT('Ctrl Pts',(4.70312882616146,0.183211625227725,-5.06411032068186));
#11081=CARTESIAN_POINT('Ctrl Pts',(4.7138833174533,0.105762915398194,-5.06906940637668));
#11082=CARTESIAN_POINT('Ctrl Pts',(4.71761607580232,0.0490443384848221,
-5.07255505310615));
#11083=CARTESIAN_POINT('Ctrl Pts',(4.71675170872838,-0.0827354315696169,
-5.08071566725665));
#11084=CARTESIAN_POINT('Ctrl Pts',(4.70909511443206,-0.157516755015795,
-5.08540207221873));
#11085=CARTESIAN_POINT('Ctrl Pts',(4.69234225810892,-0.241250456079762,
-5.0910063822924));
#11086=CARTESIAN_POINT('Ctrl Pts',(4.69016798173377,-0.251416300976573,
-5.09169261791472));
#11087=CARTESIAN_POINT('Ctrl Pts',(4.68636566296886,-0.268110343125979,
-5.09282982688427));
#11088=CARTESIAN_POINT('Ctrl Pts',(4.68481571720163,-0.274655876897023,
-5.09327833609971));
#11089=CARTESIAN_POINT('Ctrl Pts',(4.6819140121794,-0.286458148742733,-5.09409195931201));
#11090=CARTESIAN_POINT('Ctrl Pts',(4.68058181338018,-0.291719538145418,
-5.09445644264509));
#11091=CARTESIAN_POINT('Ctrl Pts',(4.67764499153434,-0.30299024760524,-5.09524112677651));
#11092=CARTESIAN_POINT('Ctrl Pts',(4.67602904118461,-0.308996417959883,
-5.09566167963423));
#11093=CARTESIAN_POINT('Ctrl Pts',(4.67147140981349,-0.325416691712802,
-5.09681815039107));
#11094=CARTESIAN_POINT('Ctrl Pts',(4.66843371198944,-0.335803276526833,
-5.0975571190521));
#11095=CARTESIAN_POINT('Ctrl Pts',(4.64963634002357,-0.396935957768268,
-5.10195194457051));
#11096=CARTESIAN_POINT('Ctrl Pts',(4.63060233275566,-0.446603141658404,
-5.10571289725965));
#11097=CARTESIAN_POINT('Ctrl Pts',(4.58806951823101,-0.538471856962764,
-5.1130288020892));
#11098=CARTESIAN_POINT('Ctrl Pts',(4.56519964453649,-0.580851876318216,
-5.11656225081209));
#11099=CARTESIAN_POINT('Ctrl Pts',(4.52487129943661,-0.645736921039312,
-5.1221674246078));
#11100=CARTESIAN_POINT('Ctrl Pts',(4.50907789240489,-0.66921668575073,-5.1242392176676));
#11101=CARTESIAN_POINT('Ctrl Pts',(4.4720931256705,-0.720139658713265,-5.12880234908559));
#11102=CARTESIAN_POINT('Ctrl Pts',(4.45050292872451,-0.747264613724035,
-5.13128133490666));
#11103=CARTESIAN_POINT('Ctrl Pts',(4.42376484515356,-0.777972485918973,
-5.13411141147721));
#11104=CARTESIAN_POINT('Ctrl Pts',(4.41974850969115,-0.782513844765413,
-5.13453057514588));
#11105=CARTESIAN_POINT('Ctrl Pts',(4.41314101893004,-0.789869831532346,
-5.135210270097));
#11106=CARTESIAN_POINT('Ctrl Pts',(4.41057096132481,-0.79270313748375,-5.13547225089546));
#11107=CARTESIAN_POINT('Ctrl Pts',(4.40593270427108,-0.797766691133861,
-5.13594070027414));
#11108=CARTESIAN_POINT('Ctrl Pts',(4.4038696348932,-0.800001488012628,-5.13614753254693));
#11109=CARTESIAN_POINT('Ctrl Pts',(4.39930428958679,-0.804908570244363,
-5.13660186822187));
#11110=CARTESIAN_POINT('Ctrl Pts',(4.39679820010056,-0.807577194066002,
-5.13684908018532));
#11111=CARTESIAN_POINT('Ctrl Pts',(4.38949384653271,-0.815282958961408,
-5.13756344871047));
#11112=CARTESIAN_POINT('Ctrl Pts',(4.38466324534603,-0.820289432306725,
-5.13802824458919));
#11113=CARTESIAN_POINT('Ctrl Pts',(4.34325230834112,-0.862453888401102,
-5.14195156931448));
#11114=CARTESIAN_POINT('Ctrl Pts',(4.30428086816322,-0.897192667489721,
-5.1452439502416));
#11115=CARTESIAN_POINT('Ctrl Pts',(4.20526894619093,-0.974294721189144,
-5.15306117737643));
#11116=CARTESIAN_POINT('Ctrl Pts',(4.14334526395964,-1.01383453137555,-5.15753270343064));
#11117=CARTESIAN_POINT('Ctrl Pts',(4.07816923100673,-1.04735430750874,-5.16216634940201));
#11118=CARTESIAN_POINT('Origin',(3.53951905042299,8.32667268468867E-16,
0.924367114736157));
#11119=CARTESIAN_POINT('',(4.07816926754817,-1.04735428871561,-5.76049882461148));
#11120=CARTESIAN_POINT('',(4.07816910321358,-1.04735437323224,-5.66222605418069));
#11121=CARTESIAN_POINT('',(4.07816926754759,-1.04735428871592,0.924367114736157));
#11122=CARTESIAN_POINT('Ctrl Pts',(4.07816926754817,-1.04735428871561,-5.76049882461148));
#11123=CARTESIAN_POINT('Ctrl Pts',(4.08187797021829,-1.04544691742776,-5.7602109730814));
#11124=CARTESIAN_POINT('Ctrl Pts',(4.08557659149742,-1.04351982170539,-5.75992423025184));
#11125=CARTESIAN_POINT('Ctrl Pts',(4.0921535430674,-1.04004848361736,-5.75941502498637));
#11126=CARTESIAN_POINT('Ctrl Pts',(4.0950358034973,-1.03851185282131,-5.75919210917261));
#11127=CARTESIAN_POINT('Ctrl Pts',(4.10065735843889,-1.03548471091922,-5.75875785247854));
#11128=CARTESIAN_POINT('Ctrl Pts',(4.1033971772514,-1.03399528321234,-5.75854645139605));
#11129=CARTESIAN_POINT('Ctrl Pts',(4.10951216720323,-1.03063950239022,-5.75807510583635));
#11130=CARTESIAN_POINT('Ctrl Pts',(4.11288418351973,-1.02876739948968,-5.75781551783258));
#11131=CARTESIAN_POINT('Ctrl Pts',(4.1245602271969,-1.0222097597932,-5.75691758717413));
#11132=CARTESIAN_POINT('Ctrl Pts',(4.13281677414963,-1.01743982462621,-5.75628426325137));
#11133=CARTESIAN_POINT('Ctrl Pts',(4.20590408407458,-0.974023855332084,
-5.75068435481918));
#11134=CARTESIAN_POINT('Ctrl Pts',(4.26694757189161,-0.929323684561039,
-5.74604456307055));
#11135=CARTESIAN_POINT('Ctrl Pts',(4.36509400579341,-0.841817399823423,
-5.73791063778276));
#11136=CARTESIAN_POINT('Ctrl Pts',(4.4041764651071,-0.801621765672082,-5.73444162186334));
#11137=CARTESIAN_POINT('Ctrl Pts',(4.45353200338592,-0.743034592168187,
-5.72955373113003));
#11138=CARTESIAN_POINT('Ctrl Pts',(4.46639760688376,-0.726922382736174,
-5.7282256810086));
#11139=CARTESIAN_POINT('Ctrl Pts',(4.4881039329886,-0.698224859840442,-5.72588040195009));
#11140=CARTESIAN_POINT('Ctrl Pts',(4.49713350583108,-0.685788417565081,
-5.72487034405517));
#11141=CARTESIAN_POINT('Ctrl Pts',(4.50999413973082,-0.667326043785865,
-5.72337794449112));
#11142=CARTESIAN_POINT('Ctrl Pts',(4.51401810663431,-0.66143596317433,-5.72290285309094));
#11143=CARTESIAN_POINT('Ctrl Pts',(4.52103366408996,-0.65096395058456,-5.72205979796052));
#11144=CARTESIAN_POINT('Ctrl Pts',(4.52404732127105,-0.646397001834558,
-5.72169266739557));
#11145=CARTESIAN_POINT('Ctrl Pts',(4.53028885661337,-0.63679355978032,-5.72092168133152));
#11146=CARTESIAN_POINT('Ctrl Pts',(4.53351039682175,-0.631753154043889,
-5.72051760644787));
#11147=CARTESIAN_POINT('Ctrl Pts',(4.54186840199153,-0.618454062256777,
-5.71945284293456));
#11148=CARTESIAN_POINT('Ctrl Pts',(4.54694112024298,-0.610156056360615,
-5.71878986685697));
#11149=CARTESIAN_POINT('Ctrl Pts',(4.56837709552367,-0.57409469829039,-5.715913935312));
#11150=CARTESIAN_POINT('Ctrl Pts',(4.58369840858914,-0.545731365712486,
-5.71366458384287));
#11151=CARTESIAN_POINT('Ctrl Pts',(4.64285297026951,-0.424587807314039,
-5.70410312700539));
#11152=CARTESIAN_POINT('Ctrl Pts',(4.67562736878406,-0.326914693602247,
-5.6964529405097));
#11153=CARTESIAN_POINT('Ctrl Pts',(4.69949361741635,-0.204996112739021,
-5.68746766158048));
#11154=CARTESIAN_POINT('Ctrl Pts',(4.70306836807499,-0.183623260953599,
-5.68591494403306));
#11155=CARTESIAN_POINT('Ctrl Pts',(4.70792153912013,-0.148711527529558,
-5.68342666138627));
#11156=CARTESIAN_POINT('Ctrl Pts',(4.70955873143027,-0.135228245804641,
-5.68247722908563));
#11157=CARTESIAN_POINT('Ctrl Pts',(4.71145576148858,-0.116970915556129,
-5.6812098309718));
#11158=CARTESIAN_POINT('Ctrl Pts',(4.71192024703539,-0.112219811000617,
-5.68088167733769));
#11159=CARTESIAN_POINT('Ctrl Pts',(4.71264663212656,-0.104292356197923,
-5.68033704921217));
#11160=CARTESIAN_POINT('Ctrl Pts',(4.71292454502956,-0.101117577404194,
-5.68011971509213));
#11161=CARTESIAN_POINT('Ctrl Pts',(4.71342611637666,-0.0951070651807408,
-5.67970977738906));
#11162=CARTESIAN_POINT('Ctrl Pts',(4.71365239347741,-0.0922715910167022,
-5.67951702687181));
#11163=CARTESIAN_POINT('Ctrl Pts',(4.71416367599844,-0.0855580854412196,
-5.67906210678509));
#11164=CARTESIAN_POINT('Ctrl Pts',(4.71443975529531,-0.0816793774734788,
-5.67880042413697));
#11165=CARTESIAN_POINT('Ctrl Pts',(4.7153453324281,-0.0680004129323329,
-5.67788136728897));
#11166=CARTESIAN_POINT('Ctrl Pts',(4.71587148298568,-0.0581933969691904,
-5.67722935507856));
#11167=CARTESIAN_POINT('Ctrl Pts',(4.71917359912949,0.0221236688189603,
-5.67193755633074));
#11168=CARTESIAN_POINT('Ctrl Pts',(4.71573051204669,0.0927560213869958,
-5.66758116501317));
#11169=CARTESIAN_POINT('Ctrl Pts',(4.70220420960147,0.189753681766197,-5.6615231504757));
#11170=CARTESIAN_POINT('Ctrl Pts',(4.69748385131342,0.21670423472124,-5.65983245808009));
#11171=CARTESIAN_POINT('Ctrl Pts',(4.6803833773342,0.29763991504475,-5.65468216482137));
#11172=CARTESIAN_POINT('Ctrl Pts',(4.66513246507091,0.350933452613339,-5.6511877373165));
#11173=CARTESIAN_POINT('Ctrl Pts',(4.64128702055945,0.416422732710736,-5.64663709518971));
#11174=CARTESIAN_POINT('Ctrl Pts',(4.63613717342558,0.42980136769828,-5.64569374705179));
#11175=CARTESIAN_POINT('Ctrl Pts',(4.62813390331266,0.449511869367758,-5.64428181793294));
#11176=CARTESIAN_POINT('Ctrl Pts',(4.6254664755146,0.455918200029565,-5.6438193974));
#11177=CARTESIAN_POINT('Ctrl Pts',(4.62060420778169,0.467311056885394,-5.64299056394301));
#11178=CARTESIAN_POINT('Ctrl Pts',(4.61843107060644,0.472306671931109,-5.64262488726538));
#11179=CARTESIAN_POINT('Ctrl Pts',(4.61375786272512,0.482848889929473,-5.64184834642741));
#11180=CARTESIAN_POINT('Ctrl Pts',(4.61124932293543,0.488391540617809,-5.64143720443628));
#11181=CARTESIAN_POINT('Ctrl Pts',(4.60442340864151,0.503167630464035,-5.64033330433663));
#11182=CARTESIAN_POINT('Ctrl Pts',(4.60002900316412,0.51236469951574,-5.63963794435653));
#11183=CARTESIAN_POINT('Ctrl Pts',(4.57912584711362,0.554691690831046,-5.63639839525907));
#11184=CARTESIAN_POINT('Ctrl Pts',(4.56118206338029,0.587085459727697,-5.63380539522078));
#11185=CARTESIAN_POINT('Ctrl Pts',(4.50080424386323,0.684910158569189,-5.62561004491299));
#11186=CARTESIAN_POINT('Ctrl Pts',(4.45338256230509,0.747008867384006,-5.61985722810707));
#11187=CARTESIAN_POINT('Ctrl Pts',(4.36598167253843,0.840574132074291,-5.61049174841205));
#11188=CARTESIAN_POINT('Ctrl Pts',(4.32947457570331,0.874972456660877,-5.60686257165182));
#11189=CARTESIAN_POINT('Ctrl Pts',(4.28555602926795,0.911357088863594,-5.60289629057012));
#11190=CARTESIAN_POINT('Ctrl Pts',(4.28019000214669,0.915723464946005,-5.60241805397284));
#11191=CARTESIAN_POINT('Ctrl Pts',(4.27193198134609,0.922322994137551,-5.60169213411281));
#11192=CARTESIAN_POINT('Ctrl Pts',(4.26906766433747,0.924590302644373,-5.60144216954969));
#11193=CARTESIAN_POINT('Ctrl Pts',(4.26379853065051,0.928721461643172,-5.6009857401457));
#11194=CARTESIAN_POINT('Ctrl Pts',(4.26139703398494,0.930589327297677,-5.60077900394143));
#11195=CARTESIAN_POINT('Ctrl Pts',(4.25595140505116,0.934791129956243,-5.60031309520597));
#11196=CARTESIAN_POINT('Ctrl Pts',(4.25290309109886,0.937119515831706,-5.60005430600372));
#11197=CARTESIAN_POINT('Ctrl Pts',(4.24498070036995,0.943109796148837,-5.59938676436009));
#11198=CARTESIAN_POINT('Ctrl Pts',(4.24008939695203,0.946748868803118,-5.59897951721716));
#11199=CARTESIAN_POINT('Ctrl Pts',(4.20653678410166,0.971309196386732,-5.59621746260358));
#11200=CARTESIAN_POINT('Ctrl Pts',(4.1769678758686,0.990966066580671,-5.593938803187));
#11201=CARTESIAN_POINT('Ctrl Pts',(4.1236633269368,1.02302689362179,-5.59001188727124));
#11202=CARTESIAN_POINT('Ctrl Pts',(4.10031071697327,1.0360122437924,-5.58834834205699));
#11203=CARTESIAN_POINT('Ctrl Pts',(4.0149451061379,1.07974731373108,-5.58240010731714));
#11204=CARTESIAN_POINT('Ctrl Pts',(3.95069627641039,1.10581053528477,-5.5781586868987));
#11205=CARTESIAN_POINT('Ctrl Pts',(3.86237914718799,1.13286947952707,-5.57229031259537));
#11206=CARTESIAN_POINT('Ctrl Pts',(3.84003153921409,1.13900133542013,-5.57080326312618));
#11207=CARTESIAN_POINT('Ctrl Pts',(3.80119010815015,1.14843618571334,-5.56820406305948));
#11208=CARTESIAN_POINT('Ctrl Pts',(3.78477927048749,1.15205242659533,-5.56710148814794));
#11209=CARTESIAN_POINT('Ctrl Pts',(3.76104852165796,1.15675164212147,-5.56549817696128));
#11210=CARTESIAN_POINT('Ctrl Pts',(3.75378650553274,1.15811878566181,-5.56500634661502));
#11211=CARTESIAN_POINT('Ctrl Pts',(3.74108842812285,1.1603857995812,-5.56414405906378));
#11212=CARTESIAN_POINT('Ctrl Pts',(3.73565796752716,1.16131603852538,-5.56377456470146));
#11213=CARTESIAN_POINT('Ctrl Pts',(3.72512620924544,1.16304415374054,-5.56305647579265));
#11214=CARTESIAN_POINT('Ctrl Pts',(3.72002578973926,1.16384665508634,-5.56270803512962));
#11215=CARTESIAN_POINT('Ctrl Pts',(3.70643205950566,1.16589398957059,-5.5617774757776));
#11216=CARTESIAN_POINT('Ctrl Pts',(3.69793026970683,1.16707952872154,-5.56119352437753));
#11217=CARTESIAN_POINT('Ctrl Pts',(3.66670418889264,1.17108639498765,-5.55904111579447));
#11218=CARTESIAN_POINT('Ctrl Pts',(3.64391321872698,1.17333760505385,-5.55745523764452));
#11219=CARTESIAN_POINT('Ctrl Pts',(3.51977541046958,1.18195421843716,-5.5487308679879));
#11220=CARTESIAN_POINT('Ctrl Pts',(3.41800597233407,1.17585429781606,-5.54121423498232));
#11221=CARTESIAN_POINT('Ctrl Pts',(3.28877692812439,1.15114172511511,-5.53161666038536));
#11222=CARTESIAN_POINT('Ctrl Pts',(3.25947335182741,1.14436599608088,-5.52944104699182));
#11223=CARTESIAN_POINT('Ctrl Pts',(3.21940805364577,1.1334704130046,-5.52649260053368));
#11224=CARTESIAN_POINT('Ctrl Pts',(3.20840064848533,1.13030387640634,-5.52568536704231));
#11225=CARTESIAN_POINT('Ctrl Pts',(3.18936118987572,1.12452471241741,-5.52429596647582));
#11226=CARTESIAN_POINT('Ctrl Pts',(3.18130794977989,1.12198537144151,-5.52371044199923));
#11227=CARTESIAN_POINT('Ctrl Pts',(3.16952152012374,1.11812903937646,-5.52285736138255));
#11228=CARTESIAN_POINT('Ctrl Pts',(3.16576676330985,1.11687955937425,-5.52258617996448));
#11229=CARTESIAN_POINT('Ctrl Pts',(3.15915449739544,1.11464209941013,-5.5221097332622));
#11230=CARTESIAN_POINT('Ctrl Pts',(3.15629441392398,1.11366201412777,-5.5219040235197));
#11231=CARTESIAN_POINT('Ctrl Pts',(3.15008452685253,1.11150727139893,-5.52145820897832));
#11232=CARTESIAN_POINT('Ctrl Pts',(3.14673624183696,1.11032847780941,-5.5212183468747));
#11233=CARTESIAN_POINT('Ctrl Pts',(3.13749912224382,1.10702945415866,-5.5205579155664));
#11234=CARTESIAN_POINT('Ctrl Pts',(3.1316216762133,1.10487735581501,-5.52013914740789));
#11235=CARTESIAN_POINT('Ctrl Pts',(3.09979435348579,1.09293480366891,-5.51787792953038));
#11236=CARTESIAN_POINT('Ctrl Pts',(3.07417707657814,1.08227603717349,-5.51608134887564));
#11237=CARTESIAN_POINT('Ctrl Pts',(2.96001171004169,1.0299701053567,-5.50807902160259));
#11238=CARTESIAN_POINT('Ctrl Pts',(2.87648634691669,0.978293121355073,-5.50220561684417));
#11239=CARTESIAN_POINT('Ctrl Pts',(2.76860924777622,0.891319951639726,-5.49345204055826));
#11240=CARTESIAN_POINT('Ctrl Pts',(2.73825861855538,0.8641379241976,-5.49083746251266));
#11241=CARTESIAN_POINT('Ctrl Pts',(2.70221543367556,0.828323419154846,-5.48749274426946));
#11242=CARTESIAN_POINT('Ctrl Pts',(2.69514436495158,0.82111412938354,-5.48682422764823));
#11243=CARTESIAN_POINT('Ctrl Pts',(2.68397740238912,0.809432093422194,-5.4857479111911));
#11244=CARTESIAN_POINT('Ctrl Pts',(2.67982173206068,0.805016983585061,-5.48534267741472));
#11245=CARTESIAN_POINT('Ctrl Pts',(2.67199447980697,0.796571343576881,-5.48457030632363));
#11246=CARTESIAN_POINT('Ctrl Pts',(2.66831642135929,0.792547010233152,-5.48420345578446));
#11247=CARTESIAN_POINT('Ctrl Pts',(2.659996158091,0.783315522386645,-5.48336451722359));
#11248=CARTESIAN_POINT('Ctrl Pts',(2.65537204681401,0.778092409765785,-5.48289169695835));
#11249=CARTESIAN_POINT('Ctrl Pts',(2.64126301155107,0.76186754058363,-5.48142836813775));
#11250=CARTESIAN_POINT('Ctrl Pts',(2.6319353164037,0.750731505820629,-5.48043155259047));
#11251=CARTESIAN_POINT('Ctrl Pts',(2.56321523408886,0.665535869787396,-5.47285818393117));
#11252=CARTESIAN_POINT('Ctrl Pts',(2.51277738798021,0.584723669108077,-5.46592659351282));
#11253=CARTESIAN_POINT('Ctrl Pts',(2.46545831132143,0.483500004215814,-5.45772823416619));
#11254=CARTESIAN_POINT('Ctrl Pts',(2.4586538936309,0.468091072589877,-5.45649369246843));
#11255=CARTESIAN_POINT('Ctrl Pts',(2.44008257185676,0.423469110787301,-5.45296442669784));
#11256=CARTESIAN_POINT('Ctrl Pts',(2.42915290952481,0.393921260158824,-5.45068242777589));
#11257=CARTESIAN_POINT('Ctrl Pts',(2.41398944423184,0.347256351690499,-5.44719518984603));
#11258=CARTESIAN_POINT('Ctrl Pts',(2.40893312800836,0.330423095061284,-5.44596034541842));
#11259=CARTESIAN_POINT('Ctrl Pts',(2.40285897387676,0.308425755885177,-5.44438180528872));
#11260=CARTESIAN_POINT('Ctrl Pts',(2.40149657098967,0.303360207342615,-5.44402069540589));
#11261=CARTESIAN_POINT('Ctrl Pts',(2.39933495208893,0.295103547797664,-5.44343617738116));
#11262=CARTESIAN_POINT('Ctrl Pts',(2.39851520022268,0.291917961967814,-5.44321164229907));
#11263=CARTESIAN_POINT('Ctrl Pts',(2.39694789207287,0.28571986987984,-5.44277673694889));
#11264=CARTESIAN_POINT('Ctrl Pts',(2.39619888504174,0.282707792013207,-5.44256629072002));
#11265=CARTESIAN_POINT('Ctrl Pts',(2.39438954056102,0.275306836420999,-5.44205134654796));
#11266=CARTESIAN_POINT('Ctrl Pts',(2.39334250255954,0.270914693819421,-5.44174759315083));
#11267=CARTESIAN_POINT('Ctrl Pts',(2.39039590650725,0.258231316151745,-5.44087545242379));
#11268=CARTESIAN_POINT('Ctrl Pts',(2.3885608303912,0.249925185453371,-5.44031047211065));
#11269=CARTESIAN_POINT('Ctrl Pts',(2.37023652933059,0.162497560652178,-5.43442131039376));
#11270=CARTESIAN_POINT('Ctrl Pts',(2.36184102968371,0.081886818770969,-5.42947575984217));
#11271=CARTESIAN_POINT('Ctrl Pts',(2.36170060219808,-0.076853429083801,
-5.41965115857095));
#11272=CARTESIAN_POINT('Ctrl Pts',(2.36935922258636,-0.154552289663843,
-5.41479595816134));
#11273=CARTESIAN_POINT('Ctrl Pts',(2.38667217463884,-0.241138361243689,
-5.409001177948));
#11274=CARTESIAN_POINT('Ctrl Pts',(2.38885056288667,-0.251327771583916,
-5.40831339200768));
#11275=CARTESIAN_POINT('Ctrl Pts',(2.39265897433033,-0.268052941995784,
-5.40717410680193));
#11276=CARTESIAN_POINT('Ctrl Pts',(2.39421041201499,-0.274606142455594,
-5.40672508692881));
#11277=CARTESIAN_POINT('Ctrl Pts',(2.39711386709529,-0.286417407576641,
-5.40591086490822));
#11278=CARTESIAN_POINT('Ctrl Pts',(2.39844621198487,-0.291680150079233,
-5.40554629698149));
#11279=CARTESIAN_POINT('Ctrl Pts',(2.40138202360195,-0.302948523881468,
-5.40476179433949));
#11280=CARTESIAN_POINT('Ctrl Pts',(2.40299674058769,-0.308951026269503,
-5.40434151002534));
#11281=CARTESIAN_POINT('Ctrl Pts',(2.40754710119242,-0.325347854318808,
-5.40318672721635));
#11282=CARTESIAN_POINT('Ctrl Pts',(2.41057827428529,-0.335714805536738,
-5.40244919348077));
#11283=CARTESIAN_POINT('Ctrl Pts',(2.42922746280897,-0.396386270078313,
-5.39808783960088));
#11284=CARTESIAN_POINT('Ctrl Pts',(2.44806122956953,-0.445632011384026,
-5.39436084152631));
#11285=CARTESIAN_POINT('Ctrl Pts',(2.50386500754007,-0.566569682512507,
-5.38473903378777));
#11286=CARTESIAN_POINT('Ctrl Pts',(2.5450141752443,-0.636034191557404,-5.37875501912202));
#11287=CARTESIAN_POINT('Ctrl Pts',(2.61159521268414,-0.725973060111868,
-5.37066474697488));
#11288=CARTESIAN_POINT('Ctrl Pts',(2.63126613025116,-0.750437572912024,
-5.36842656594675));
#11289=CARTESIAN_POINT('Ctrl Pts',(2.65614517266138,-0.778965671894448,
-5.36579699003843));
#11290=CARTESIAN_POINT('Ctrl Pts',(2.66043801205456,-0.783807028939528,
-5.36535003425088));
#11291=CARTESIAN_POINT('Ctrl Pts',(2.66717946535301,-0.791284811132123,
-5.36465891038453));
#11292=CARTESIAN_POINT('Ctrl Pts',(2.66960054914071,-0.793945719811108,
-5.36441282502232));
#11293=CARTESIAN_POINT('Ctrl Pts',(2.67409449905466,-0.798839589984025,
-5.36396001357935));
#11294=CARTESIAN_POINT('Ctrl Pts',(2.67616383505845,-0.801075600121314,
-5.36375304667247));
#11295=CARTESIAN_POINT('Ctrl Pts',(2.68090602061594,-0.806160023831496,
-5.36328222341102));
#11296=CARTESIAN_POINT('Ctrl Pts',(2.68358438151723,-0.809003190747652,
-5.36301878660978));
#11297=CARTESIAN_POINT('Ctrl Pts',(2.69191235383771,-0.81775594760654,-5.36220710403092));
#11298=CARTESIAN_POINT('Ctrl Pts',(2.69760953546321,-0.823620227858253,
-5.36166230643215));
#11299=CARTESIAN_POINT('Ctrl Pts',(2.71110311019176,-0.837223235370462,
-5.3603948724688));
#11300=CARTESIAN_POINT('Ctrl Pts',(2.71894772913704,-0.844913274583829,
-5.35967548753292));
#11301=CARTESIAN_POINT('Ctrl Pts',(2.74731345207494,-0.871952276395717,
-5.35713053458738));
#11302=CARTESIAN_POINT('Ctrl Pts',(2.76842167346318,-0.890673642735563,
-5.35533925522086));
#11303=CARTESIAN_POINT('Ctrl Pts',(2.85592957464787,-0.962841104189329,
-5.34821800193056));
#11304=CARTESIAN_POINT('Ctrl Pts',(2.92736595278234,-1.00976567656509,-5.34305707909272));
#11305=CARTESIAN_POINT('Ctrl Pts',(3.03746428937339,-1.06607390707546,-5.33523298199446));
#11306=CARTESIAN_POINT('Ctrl Pts',(3.07251965177669,-1.08188892823429,-5.33276222380301));
#11307=CARTESIAN_POINT('Ctrl Pts',(3.11786854942945,-1.09973270802842,-5.32955570707003));
#11308=CARTESIAN_POINT('Ctrl Pts',(3.12750305218602,-1.10337843928046,-5.32887397826383));
#11309=CARTESIAN_POINT('Ctrl Pts',(3.14292394472285,-1.10898362741727,-5.32778142848127));
#11310=CARTESIAN_POINT('Ctrl Pts',(3.1486800460156,-1.11102530754527,-5.32737331432099));
#11311=CARTESIAN_POINT('Ctrl Pts',(3.1590815479487,-1.1146238695666,-5.32663517410387));
#11312=CARTESIAN_POINT('Ctrl Pts',(3.16372130770967,-1.11619672066612,-5.32630567909582));
#11313=CARTESIAN_POINT('Ctrl Pts',(3.17466507196386,-1.11983062315997,-5.32552787824893));
#11314=CARTESIAN_POINT('Ctrl Pts',(3.18097688613779,-1.12186744470275,-5.3250787966946));
#11315=CARTESIAN_POINT('Ctrl Pts',(3.19950159289169,-1.127673067179,-5.32375917437759));
#11316=CARTESIAN_POINT('Ctrl Pts',(3.21175870416564,-1.13129640280128,-5.32288399234048));
#11317=CARTESIAN_POINT('Ctrl Pts',(3.28691637123713,-1.15218990980757,-5.31750325672743));
#11318=CARTESIAN_POINT('Ctrl Pts',(3.35109297639296,-1.16440661909638,-5.31283836441222));
#11319=CARTESIAN_POINT('Ctrl Pts',(3.4815427068083,-1.17817031081259,-5.3032740446111));
#11320=CARTESIAN_POINT('Ctrl Pts',(3.5476091309705,-1.17956820168689,-5.29838988657289));
#11321=CARTESIAN_POINT('Ctrl Pts',(3.64346970167869,-1.17353924632251,-5.2914541057521));
#11322=CARTESIAN_POINT('Ctrl Pts',(3.67341384531329,-1.17050101662678,-5.28931070605149));
#11323=CARTESIAN_POINT('Ctrl Pts',(3.70954916706981,-1.1654294403968,-5.28677636928521));
#11324=CARTESIAN_POINT('Ctrl Pts',(3.71587976536528,-1.16448826697449,-5.28633434340028));
#11325=CARTESIAN_POINT('Ctrl Pts',(3.72574079816218,-1.16293996018326,-5.28564920427298));
#11326=CARTESIAN_POINT('Ctrl Pts',(3.72927655145256,-1.16236826435742,-5.28540422464926));
#11327=CARTESIAN_POINT('Ctrl Pts',(3.73581670205787,-1.16128015001069,-5.28495241344372));
#11328=CARTESIAN_POINT('Ctrl Pts',(3.73882169674808,-1.16076819837799,-5.28474534983561));
#11329=CARTESIAN_POINT('Ctrl Pts',(3.74569398209677,-1.15956991420605,-5.28427298725828));
#11330=CARTESIAN_POINT('Ctrl Pts',(3.74955985527981,-1.15887589921931,-5.28400811895301));
#11331=CARTESIAN_POINT('Ctrl Pts',(3.76157266207668,-1.15665723149773,-5.28318751018547));
#11332=CARTESIAN_POINT('Ctrl Pts',(3.76970723664417,-1.15506587088829,-5.28263532794448));
#11333=CARTESIAN_POINT('Ctrl Pts',(3.83661038237051,-1.14124278450046,-5.2781177011429));
#11334=CARTESIAN_POINT('Ctrl Pts',(3.89439008077191,-1.1246185530536,-5.27436561515831));
#11335=CARTESIAN_POINT('Ctrl Pts',(3.99427769691301,-1.08740815070123,-5.26775588752701));
#11336=CARTESIAN_POINT('Ctrl Pts',(4.03685409330635,-1.06860254091493,-5.26489557995374));
#11337=CARTESIAN_POINT('Ctrl Pts',(4.07816965980385,-1.04735408697996,-5.26199342056381));
#11338=CARTESIAN_POINT('',(2.36176914077046,-0.000461317087656274,-5.32467780803899));
#11339=CARTESIAN_POINT('Ctrl Pts',(4.07816923100673,-1.04735430750874,-5.16216634940201));
#11340=CARTESIAN_POINT('Ctrl Pts',(4.06954594519216,-1.05178922931881,-5.16277941607337));
#11341=CARTESIAN_POINT('Ctrl Pts',(4.06086571266395,-1.05611877161022,-5.16339511164852));
#11342=CARTESIAN_POINT('Ctrl Pts',(4.02422928907034,-1.07383027455862,-5.16599008202834));
#11343=CARTESIAN_POINT('Ctrl Pts',(3.99580880295806,-1.08621124808923,-5.16799465148405));
#11344=CARTESIAN_POINT('Ctrl Pts',(3.95799837785832,-1.10093691545352,-5.1706686799783));
#11345=CARTESIAN_POINT('Ctrl Pts',(3.94901980326884,-1.10430800222505,-5.17130413723277));
#11346=CARTESIAN_POINT('Ctrl Pts',(3.93440401552854,-1.10959287681835,-5.17233981341572));
#11347=CARTESIAN_POINT('Ctrl Pts',(3.92879158409062,-1.11157428014712,-5.17273780465028));
#11348=CARTESIAN_POINT('Ctrl Pts',(3.91798382177167,-1.11529794418402,-5.1735048881612));
#11349=CARTESIAN_POINT('Ctrl Pts',(3.91279086561634,-1.11704665869182,-5.17387375809825));
#11350=CARTESIAN_POINT('Ctrl Pts',(3.90075138453087,-1.12100759623962,-5.1747297395303));
#11351=CARTESIAN_POINT('Ctrl Pts',(3.89389647247439,-1.12319342448057,-5.17521769286783));
#11352=CARTESIAN_POINT('Ctrl Pts',(3.87201250858318,-1.12995129713792,-5.17677755899423));
#11353=CARTESIAN_POINT('Ctrl Pts',(3.85691235686831,-1.13428536152726,-5.17785704354953));
#11354=CARTESIAN_POINT('Ctrl Pts',(3.82122668420206,-1.1437595538521,-5.18041675377306));
#11355=CARTESIAN_POINT('Ctrl Pts',(3.80058055724751,-1.14864785781617,-5.1819043760131));
#11356=CARTESIAN_POINT('Ctrl Pts',(3.72220228778639,-1.16498294694491,-5.18757730057855));
#11357=CARTESIAN_POINT('Ctrl Pts',(3.66377693921275,-1.1726538325667,-5.19186328929927));
#11358=CARTESIAN_POINT('Ctrl Pts',(3.53396619351954,-1.17988554379157,-5.20139999393195));
#11359=CARTESIAN_POINT('Ctrl Pts',(3.46268409500139,-1.17739497352301,-5.20664755121257));
#11360=CARTESIAN_POINT('Ctrl Pts',(3.38233431058428,-1.16725493270965,-5.21232347803451));
#11361=CARTESIAN_POINT('Ctrl Pts',(3.37262582040075,-1.1659064223766,-5.21300508535927));
#11362=CARTESIAN_POINT('Ctrl Pts',(3.35909531752035,-1.16385455303246,-5.21394812755899));
#11363=CARTESIAN_POINT('Ctrl Pts',(3.35525855932799,-1.1632532899158,-5.21421476270541));
#11364=CARTESIAN_POINT('Ctrl Pts',(3.34861834408074,-1.16217901591583,-5.21467479594472));
#11365=CARTESIAN_POINT('Ctrl Pts',(3.34581352524841,-1.16171481641241,-5.2148686713017));
#11366=CARTESIAN_POINT('Ctrl Pts',(3.33986735586797,-1.16070858738544,-5.21527870637729));
#11367=CARTESIAN_POINT('Ctrl Pts',(3.33672646713476,-1.16016395076476,-5.21549471418181));
#11368=CARTESIAN_POINT('Ctrl Pts',(3.32888218764301,-1.15877090726724,-5.2160328215323));
#11369=CARTESIAN_POINT('Ctrl Pts',(3.32418161675929,-1.15790660034051,-5.21635404532803));
#11370=CARTESIAN_POINT('Ctrl Pts',(3.30610006356069,-1.15446797790832,-5.21758540470949));
#11371=CARTESIAN_POINT('Ctrl Pts',(3.29275826485404,-1.15169001447968,-5.21848493652365));
#11372=CARTESIAN_POINT('Ctrl Pts',(3.2582370480039,-1.14387469091385,-5.22079594981218));
#11373=CARTESIAN_POINT('Ctrl Pts',(3.23714309880603,-1.13848046687896,-5.22219185667478));
#11374=CARTESIAN_POINT('Ctrl Pts',(3.11600526270854,-1.10389780745085,-5.23017686243674));
#11375=CARTESIAN_POINT('Ctrl Pts',(3.02003998118047,-1.06211955896774,-5.2364198330601));
#11376=CARTESIAN_POINT('Ctrl Pts',(2.90448907796051,-0.992359828262857,
-5.24502942516393));
#11377=CARTESIAN_POINT('Ctrl Pts',(2.87879268843153,-0.975439139234408,
-5.24701933167632));
#11378=CARTESIAN_POINT('Ctrl Pts',(2.84601225213423,-0.951963701838311,
-5.24967654751156));
#11379=CARTESIAN_POINT('Ctrl Pts',(2.83830333440822,-0.946299677497521,
-5.25031040477959));
#11380=CARTESIAN_POINT('Ctrl Pts',(2.82591555379399,-0.936963432540757,
-5.25134411747404));
#11381=CARTESIAN_POINT('Ctrl Pts',(2.82119390832007,-0.933348494587354,
-5.2517417611111));
#11382=CARTESIAN_POINT('Ctrl Pts',(2.8123533742184,-0.926473277831047,-5.25249329455644));
#11383=CARTESIAN_POINT('Ctrl Pts',(2.80822851409927,-0.923220886427001,
-5.25284686966135));
#11384=CARTESIAN_POINT('Ctrl Pts',(2.80407572692206,-0.919901181918829,
-5.25320584702733));
#11385=CARTESIAN_POINT('Ctrl Pts',(2.80402585121794,-0.9198613050351,-5.25321015885017));
#11386=CARTESIAN_POINT('Ctrl Pts',(2.79867626710525,-0.915583464329012,
-5.25367268508899));
#11387=CARTESIAN_POINT('Ctrl Pts',(2.79341337937164,-0.911299859561506,
-5.25413270434317));
#11388=CARTESIAN_POINT('Ctrl Pts',(2.78234325708448,-0.902129415389332,
-5.25511110413334));
#11389=CARTESIAN_POINT('Ctrl Pts',(2.77654567677841,-0.89723145874577,-5.25562991832872));
#11390=CARTESIAN_POINT('Ctrl Pts',(2.76126933520918,-0.884070450884006,
-5.25701433163151));
#11391=CARTESIAN_POINT('Ctrl Pts',(2.75187509932375,-0.875711234747423,
-5.25788377987637));
#11392=CARTESIAN_POINT('Ctrl Pts',(2.72335576010973,-0.849503861365732,
-5.26058040448012));
#11393=CARTESIAN_POINT('Ctrl Pts',(2.70469106348343,-0.831168686064245,
-5.26242686756778));
#11394=CARTESIAN_POINT('Ctrl Pts',(2.65458394974946,-0.778554626165861,
-5.26761634042853));
#11395=CARTESIAN_POINT('Ctrl Pts',(2.62453950966349,-0.743013621361341,
-5.27100335456085));
#11396=CARTESIAN_POINT('Ctrl Pts',(2.55176092095107,-0.645791386941205,
-5.27990625261433));
#11397=CARTESIAN_POINT('Ctrl Pts',(2.51267170899475,-0.581634814651451,
-5.28544405643126));
#11398=CARTESIAN_POINT('Ctrl Pts',(2.47576333958393,-0.505579398100091,
-5.29136621820683));
#11399=CARTESIAN_POINT('Ctrl Pts',(2.4716880949209,-0.496914283527631,-5.29203190084747));
#11400=CARTESIAN_POINT('Ctrl Pts',(2.46611739268188,-0.484684298346281,
-5.29295787822271));
#11401=CARTESIAN_POINT('Ctrl Pts',(2.46453324370589,-0.481160580591559,
-5.29322310658612));
#11402=CARTESIAN_POINT('Ctrl Pts',(2.46170120190408,-0.47477729657079,-5.29370066701408));
#11403=CARTESIAN_POINT('Ctrl Pts',(2.46044728053015,-0.471920451078741,
-5.29391335332554));
#11404=CARTESIAN_POINT('Ctrl Pts',(2.45790520166865,-0.466065651054419,
-5.29434704622143));
#11405=CARTESIAN_POINT('Ctrl Pts',(2.45661812699473,-0.463067273304233,
-5.29456798820606));
#11406=CARTESIAN_POINT('Ctrl Pts',(2.45334082313665,-0.455344051664382,
-5.2951342045985));
#11407=CARTESIAN_POINT('Ctrl Pts',(2.45136892829536,-0.450611430090074,
-5.29547840366465));
#11408=CARTESIAN_POINT('Ctrl Pts',(2.44318859744525,-0.43061146081172,-5.29692197235739));
#11409=CARTESIAN_POINT('Ctrl Pts',(2.43726974073351,-0.415226707600595,
-5.2980055041011));
#11410=CARTESIAN_POINT('Ctrl Pts',(2.42196474723824,-0.372808362453588,
-5.30093316575204));
#11411=CARTESIAN_POINT('Ctrl Pts',(2.41323733858201,-0.345548012929315,
-5.30274937538456));
#11412=CARTESIAN_POINT('Ctrl Pts',(2.3765262167229,-0.214631806628227,-5.31128132720297));
#11413=CARTESIAN_POINT('Ctrl Pts',(2.36181118552444,-0.107802247071361,
-5.31773716168021));
#11414=CARTESIAN_POINT('Ctrl Pts',(2.36176914077046,-0.000461317087656274,
-5.32467780803899));
#11415=CARTESIAN_POINT('Ctrl Pts',(2.36176914030695,-0.000460132223236021,
-5.32467788465214));
#11416=CARTESIAN_POINT('Ctrl Pts',(2.36176218208443,0.0173500656714707,
-5.32582948951348));
#11417=CARTESIAN_POINT('Ctrl Pts',(2.36215921809729,0.035157527681886,-5.32699181323502));
#11418=CARTESIAN_POINT('Ctrl Pts',(2.3632691720255,0.0598215599466171,-5.32862005852875));
#11419=CARTESIAN_POINT('Ctrl Pts',(2.36363868602289,0.0666915346234238,
-5.32907556756017));
#11420=CARTESIAN_POINT('Ctrl Pts',(2.3644002772694,0.078861738762373,-5.32988620127089));
#11421=CARTESIAN_POINT('Ctrl Pts',(2.36476808268668,0.0841633358823255,
-5.33024057524318));
#11422=CARTESIAN_POINT('Ctrl Pts',(2.36557001120865,0.0946900465848394,
-5.33094677471049));
#11423=CARTESIAN_POINT('Ctrl Pts',(2.36600317047549,0.0999151119196681,
-5.3312985625889));
#11424=CARTESIAN_POINT('Ctrl Pts',(2.36700216866462,0.111061256840237,-5.33205176524902));
#11425=CARTESIAN_POINT('Ctrl Pts',(2.36757800207991,0.116981270939718,-5.33245348045136));
#11426=CARTESIAN_POINT('Ctrl Pts',(2.36919749596898,0.132416576679595,-5.33350536151939));
#11427=CARTESIAN_POINT('Ctrl Pts',(2.37031234577512,0.141923793023607,-5.33415771540511));
#11428=CARTESIAN_POINT('Ctrl Pts',(2.37550618290751,0.181987410491881,-5.33692625935416));
#11429=CARTESIAN_POINT('Ctrl Pts',(2.38066783325029,0.212388623843495,-5.33907556510917));
#11430=CARTESIAN_POINT('Ctrl Pts',(2.40181113676883,0.312853355052812,-5.34634522342824));
#11431=CARTESIAN_POINT('Ctrl Pts',(2.42300696479493,0.381647643014338,-5.35160907313795));
#11432=CARTESIAN_POINT('Ctrl Pts',(2.46712095405588,0.488880828005473,-5.36011728039088));
#11433=CARTESIAN_POINT('Ctrl Pts',(2.48618966019543,0.528715246695372,-5.3633476902778));
#11434=CARTESIAN_POINT('Ctrl Pts',(2.51445764562731,0.580134262995262,-5.36754283658415));
#11435=CARTESIAN_POINT('Ctrl Pts',(2.52170112289692,0.592750667957972,-5.36857415580377));
#11436=CARTESIAN_POINT('Ctrl Pts',(2.53438378119058,0.613922487675207,-5.37030437269975));
#11437=CARTESIAN_POINT('Ctrl Pts',(2.5397029241979,0.622547557451122,-5.37100909978507));
#11438=CARTESIAN_POINT('Ctrl Pts',(2.54741440164807,0.634698003507631,-5.37200053260632));
#11439=CARTESIAN_POINT('Ctrl Pts',(2.5497153862648,0.638280422394235,-5.37229267667029));
#11440=CARTESIAN_POINT('Ctrl Pts',(2.55371926113885,0.644440361987284,-5.37279461853859));
#11441=CARTESIAN_POINT('Ctrl Pts',(2.55541294259596,0.647023781763348,-5.37300500443261));
#11442=CARTESIAN_POINT('Ctrl Pts',(2.55898890146486,0.652431766350065,-5.37344511852398));
#11443=CARTESIAN_POINT('Ctrl Pts',(2.56087324129983,0.655254884589665,-5.37367470863777));
#11444=CARTESIAN_POINT('Ctrl Pts',(2.56596637797745,0.662814442887124,-5.37428916829446));
#11445=CARTESIAN_POINT('Ctrl Pts',(2.56919757487456,0.667535788630894,-5.37467258993907));
#11446=CARTESIAN_POINT('Ctrl Pts',(2.58397292363304,0.68879118293419,-5.37639811437618));
#11447=CARTESIAN_POINT('Ctrl Pts',(2.59590690287419,0.705051718620397,-5.3777164237304));
#11448=CARTESIAN_POINT('Ctrl Pts',(2.65304360781473,0.778851347227151,-5.3837323719598));
#11449=CARTESIAN_POINT('Ctrl Pts',(2.70313147551925,0.832409768482937,-5.38820095348185));
#11450=CARTESIAN_POINT('Ctrl Pts',(2.79380895083795,0.912863535265693,-5.39571449053853));
#11451=CARTESIAN_POINT('Ctrl Pts',(2.83166270732532,0.942519097487514,-5.39871231668154));
#11452=CARTESIAN_POINT('Ctrl Pts',(2.88670025609378,0.980446920214892,-5.40299124493225));
#11453=CARTESIAN_POINT('Ctrl Pts',(2.902433894309,0.990742644470822,-5.40420574270628));
#11454=CARTESIAN_POINT('Ctrl Pts',(2.92690330446177,1.00593092150125,-5.40608626431453));
#11455=CARTESIAN_POINT('Ctrl Pts',(2.93546662468846,1.0110963001918,-5.40674284887687));
#11456=CARTESIAN_POINT('Ctrl Pts',(2.94973379430735,1.01945629389923,-5.40783491118338));
#11457=CARTESIAN_POINT('Ctrl Pts',(2.95540042169561,1.02271364919015,-5.40826817784132));
#11458=CARTESIAN_POINT('Ctrl Pts',(2.96513402031088,1.02820154260224,-5.40901174861282));
#11459=CARTESIAN_POINT('Ctrl Pts',(2.96918763612002,1.03045555549498,-5.40932122120047));
#11460=CARTESIAN_POINT('Ctrl Pts',(2.97794458271416,1.03525735527898,-5.4099894209425));
#11461=CARTESIAN_POINT('Ctrl Pts',(2.98265215237526,1.03779715295912,-5.41034841851274));
#11462=CARTESIAN_POINT('Ctrl Pts',(2.99270515863957,1.0431327909147,-5.41111469014369));
#11463=CARTESIAN_POINT('Ctrl Pts',(2.99805508422066,1.04591979745029,-5.41152225979603));
#11464=CARTESIAN_POINT('Ctrl Pts',(3.01229375241259,1.05319881003785,-5.41260655109632));
#11465=CARTESIAN_POINT('Ctrl Pts',(3.02121830481511,1.05761929580783,-5.41328571568033));
#11466=CARTESIAN_POINT('Ctrl Pts',(3.06131711267147,1.07685150537706,-5.41633604545866));
#11467=CARTESIAN_POINT('Ctrl Pts',(3.09307459823361,1.09040047183823,-5.41874930666968));
#11468=CARTESIAN_POINT('Ctrl Pts',(3.2190923431032,1.1377360072122,-5.42832076112145));
#11469=CARTESIAN_POINT('Ctrl Pts',(3.31690868400419,1.16084305911693,-5.43578429227747));
#11470=CARTESIAN_POINT('Ctrl Pts',(3.43782525288453,1.17354828775046,-5.44457594973637));
#11471=CARTESIAN_POINT('Ctrl Pts',(3.45926406281154,1.17520911382985,-5.44611638640693));
#11472=CARTESIAN_POINT('Ctrl Pts',(3.49422615156354,1.17695624930548,-5.44858726044562));
#11473=CARTESIAN_POINT('Ctrl Pts',(3.50772609327481,1.17739827853978,-5.44953134280699));
#11474=CARTESIAN_POINT('Ctrl Pts',(3.52599390410295,1.17768196908734,-5.45079277762062));
#11475=CARTESIAN_POINT('Ctrl Pts',(3.5307569668994,1.17772703872595,-5.45112019992988));
#11476=CARTESIAN_POINT('Ctrl Pts',(3.53870456490796,1.17775402310513,-5.45166392419398));
#11477=CARTESIAN_POINT('Ctrl Pts',(3.54188894347072,1.17775192067781,-5.45188108026688));
#11478=CARTESIAN_POINT('Ctrl Pts',(3.54791889706899,1.17772348303803,-5.45229091579987));
#11479=CARTESIAN_POINT('Ctrl Pts',(3.5507644430228,1.17769975015124,-5.45248374065223));
#11480=CARTESIAN_POINT('Ctrl Pts',(3.55750390427682,1.1776191119659,-5.45293912362569));
#11481=CARTESIAN_POINT('Ctrl Pts',(3.56139770870814,1.17755320610843,-5.45320119220142));
#11482=CARTESIAN_POINT('Ctrl Pts',(3.57504488355748,1.17725450006819,-5.45411630001598));
#11483=CARTESIAN_POINT('Ctrl Pts',(3.5847959439077,1.17691981919061,-5.45476406446361));
#11484=CARTESIAN_POINT('Ctrl Pts',(3.66602687351153,1.17312066026462,-5.46011784882681));
#11485=CARTESIAN_POINT('Ctrl Pts',(3.73706861921467,1.16326839096062,-5.46453201091551));
#11486=CARTESIAN_POINT('Ctrl Pts',(3.86383029435777,1.1337319934743,-5.47258287667158));
#11487=CARTESIAN_POINT('Ctrl Pts',(3.91980155044283,1.11620364603449,-5.47620364459922));
#11488=CARTESIAN_POINT('Ctrl Pts',(3.99389843075455,1.08677601058208,-5.4812858656866));
#11489=CARTESIAN_POINT('Ctrl Pts',(4.01334732673234,1.07843840956472,-5.48264772785415));
#11490=CARTESIAN_POINT('Ctrl Pts',(4.04679741904642,1.0630190430275,-5.48504723714126));
#11491=CARTESIAN_POINT('Ctrl Pts',(4.06090151420348,1.05617286369517,-5.48607723312786));
#11492=CARTESIAN_POINT('Ctrl Pts',(4.08126778919107,1.04577963771955,-5.48759355788668));
#11493=CARTESIAN_POINT('Ctrl Pts',(4.08764115927244,1.04245330666869,-5.4880722934461));
#11494=CARTESIAN_POINT('Ctrl Pts',(4.09881712362062,1.03648962550631,-5.48891944990733));
#11495=CARTESIAN_POINT('Ctrl Pts',(4.10363255932552,1.03387669758515,-5.48928700929849));
#11496=CARTESIAN_POINT('Ctrl Pts',(4.11364328508493,1.02835396742885,-5.49005653744723));
#11497=CARTESIAN_POINT('Ctrl Pts',(4.11883507683806,1.02543817875423,-5.49045870973892));
#11498=CARTESIAN_POINT('Ctrl Pts',(4.13234101291831,1.01771773643904,-5.49151312243515));
#11499=CARTESIAN_POINT('Ctrl Pts',(4.14061875806983,1.01285063177031,-5.49216757038399));
#11500=CARTESIAN_POINT('Ctrl Pts',(4.17545454986344,0.991790613991663,-5.49495741811053));
#11501=CARTESIAN_POINT('Ctrl Pts',(4.20142293523542,0.974651485641543,-5.49712657330734));
#11502=CARTESIAN_POINT('Ctrl Pts',(4.31101306282396,0.895921061803214,-5.50668454251924));
#11503=CARTESIAN_POINT('Ctrl Pts',(4.38695770417687,0.824451149262318,-5.51442809527893));
#11504=CARTESIAN_POINT('Ctrl Pts',(4.46626971605132,0.727118307275257,-5.52350995054909));
#11505=CARTESIAN_POINT('Ctrl Pts',(4.47953615140166,0.709884352673366,-5.52506848630949));
#11506=CARTESIAN_POINT('Ctrl Pts',(4.5003218346634,0.681277074820825,-5.5275649641275));
#11507=CARTESIAN_POINT('Ctrl Pts',(4.50813394512856,0.670123621807461,-5.52851688051838));
#11508=CARTESIAN_POINT('Ctrl Pts',(4.51842399668223,0.654876321188191,-5.52978700012526));
#11509=CARTESIAN_POINT('Ctrl Pts',(4.52107264542861,0.650899709609903,-5.53011544670346));
#11510=CARTESIAN_POINT('Ctrl Pts',(4.525447827731,0.644243485056328,-5.53066040453951));
#11511=CARTESIAN_POINT('Ctrl Pts',(4.5271877883482,0.641572822678699,-5.53087777782732));
#11512=CARTESIAN_POINT('Ctrl Pts',(4.53045924655372,0.636506617202525,-5.53128766930372));
#11513=CARTESIAN_POINT('Ctrl Pts',(4.53199294418861,0.634112542598711,-5.53148033514983));
#11514=CARTESIAN_POINT('Ctrl Pts',(4.53560148518286,0.628434510935416,-5.53193490482366));
#11515=CARTESIAN_POINT('Ctrl Pts',(4.53766879720479,0.62514577134661,-5.53219632333358));
#11516=CARTESIAN_POINT('Ctrl Pts',(4.54489631165479,0.613520776955705,-5.53311403632526));
#11517=CARTESIAN_POINT('Ctrl Pts',(4.5499688293379,0.605130102383565,-5.53376498722855));
#11518=CARTESIAN_POINT('Ctrl Pts',(4.59093069200686,0.53542170806235,-5.53908781609312));
#11519=CARTESIAN_POINT('Ctrl Pts',(4.62131379546568,0.471026319230465,-5.54347221653309));
#11520=CARTESIAN_POINT('Ctrl Pts',(4.66593766211988,0.348925689767928,-5.55151342141762));
#11521=CARTESIAN_POINT('Ctrl Pts',(4.68198248282185,0.292138107049691,-5.55515519603111));
#11522=CARTESIAN_POINT('Ctrl Pts',(4.6979351009883,0.213583911850137,-5.5602642443986));
#11523=CARTESIAN_POINT('Ctrl Pts',(4.70159687499713,0.192667804005683,-5.56163068907727));
#11524=CARTESIAN_POINT('Ctrl Pts',(4.70698232404128,0.156114205717943,-5.56403754091896));
#11525=CARTESIAN_POINT('Ctrl Pts',(4.70896178997384,0.140519683769094,-5.56507023063991));
#11526=CARTESIAN_POINT('Ctrl Pts',(4.71139165954182,0.117734631973119,-5.56658979084234));
#11527=CARTESIAN_POINT('Ctrl Pts',(4.7120891921917,0.110571761122995,-5.56706902122872));
#11528=CARTESIAN_POINT('Ctrl Pts',(4.71320212871983,0.0979444839358324,
-5.56791674287458));
#11529=CARTESIAN_POINT('Ctrl Pts',(4.7136451265351,0.0924826787972153,-5.56828436880864));
#11530=CARTESIAN_POINT('Ctrl Pts',(4.71448968572289,0.0810831956584553,
-5.56905372815509));
#11531=CARTESIAN_POINT('Ctrl Pts',(4.71488438850021,0.0751451810903372,
-5.56945566304316));
#11532=CARTESIAN_POINT('Ctrl Pts',(4.71579738451836,0.0596342999625881,
-5.57050876091953));
#11533=CARTESIAN_POINT('Ctrl Pts',(4.71624381656709,0.0500578097297874,
-5.57116212130397));
#11534=CARTESIAN_POINT('Ctrl Pts',(4.71763718277229,0.00953948035335322,
-5.5739405839824));
#11535=CARTESIAN_POINT('Ctrl Pts',(4.71748084156572,-0.0214254082874622,
-5.57609909750216));
#11536=CARTESIAN_POINT('Ctrl Pts',(4.71241285210513,-0.135339396400184,
-5.58417444206101));
#11537=CARTESIAN_POINT('Ctrl Pts',(4.69994979858721,-0.217701048469125,
-5.59029772181375));
#11538=CARTESIAN_POINT('Ctrl Pts',(4.66573224543815,-0.348509682531906,
-5.60019532681509));
#11539=CARTESIAN_POINT('Ctrl Pts',(4.64919481134619,-0.39804040616317,-5.6039791475489));
#11540=CARTESIAN_POINT('Ctrl Pts',(4.62678942015821,-0.452754462394137,
-5.60809134848805));
#11541=CARTESIAN_POINT('Ctrl Pts',(4.62409600643031,-0.459169132747586,
-5.60857233143898));
#11542=CARTESIAN_POINT('Ctrl Pts',(4.61989871430554,-0.468922430823454,
-5.60930151450108));
#11543=CARTESIAN_POINT('Ctrl Pts',(4.61843590318965,-0.472278403055192,
-5.60955202705499));
#11544=CARTESIAN_POINT('Ctrl Pts',(4.61572915396957,-0.478409998010614,
-5.61000894561765));
#11545=CARTESIAN_POINT('Ctrl Pts',(4.61449010808012,-0.481187633692278,
-5.61021562749309));
#11546=CARTESIAN_POINT('Ctrl Pts',(4.61166844272129,-0.487447817537524,
-5.61068077477072));
#11547=CARTESIAN_POINT('Ctrl Pts',(4.61007960850839,-0.490927476041106,
-5.61093886213976));
#11548=CARTESIAN_POINT('Ctrl Pts',(4.60592903017717,-0.499901557667233,
-5.61160343808227));
#11549=CARTESIAN_POINT('Ctrl Pts',(4.60334172924343,-0.505384135208795,
-5.61200844315704));
#11550=CARTESIAN_POINT('Ctrl Pts',(4.58568560902857,-0.542061587197846,
-5.6147126877148));
#11551=CARTESIAN_POINT('Ctrl Pts',(4.56928747413064,-0.5726017214246,-5.61693937957217));
#11552=CARTESIAN_POINT('Ctrl Pts',(4.53712998081129,-0.62662908446548,-5.62091221103024));
#11553=CARTESIAN_POINT('Ctrl Pts',(4.52182749215795,-0.650355152412231,
-5.62266953486143));
#11554=CARTESIAN_POINT('Ctrl Pts',(4.47825271446647,-0.712864378237065,
-5.62739396113424));
#11555=CARTESIAN_POINT('Ctrl Pts',(4.44844014040838,-0.750505744939403,
-5.63034410841217));
#11556=CARTESIAN_POINT('Ctrl Pts',(4.38081643216606,-0.825928274920015,
-5.63667888365917));
#11557=CARTESIAN_POINT('Ctrl Pts',(4.3425662536174,-0.86316447177844,-5.64006883885905));
#11558=CARTESIAN_POINT('Ctrl Pts',(4.29367360988861,-0.9046895931212,-5.64428484399493));
#11559=CARTESIAN_POINT('Ctrl Pts',(4.28532264179532,-0.911586172443673,
-5.64500100448675));
#11560=CARTESIAN_POINT('Ctrl Pts',(4.27202653094454,-0.922261656382174,
-5.64613580920986));
#11561=CARTESIAN_POINT('Ctrl Pts',(4.26714437954487,-0.926118323848458,
-5.6465513647534));
#11562=CARTESIAN_POINT('Ctrl Pts',(4.25794669162269,-0.933266436718698,
-5.6473322780599));
#11563=CARTESIAN_POINT('Ctrl Pts',(4.2536384990577,-0.936567097937192,-5.64769726197379));
#11564=CARTESIAN_POINT('Ctrl Pts',(4.24394208786454,-0.943890066386496,
-5.64851704790031));
#11565=CARTESIAN_POINT('Ctrl Pts',(4.23854196243696,-0.947896217072016,
-5.64897245759095));
#11566=CARTESIAN_POINT('Ctrl Pts',(4.22471328612309,-0.957972759821006,
-5.65013594436673));
#11567=CARTESIAN_POINT('Ctrl Pts',(4.21623833684439,-0.963978186788384,
-5.65084645119532));
#11568=CARTESIAN_POINT('Ctrl Pts',(4.16618808175879,-0.998458963888642,
-5.65502879908426));
#11569=CARTESIAN_POINT('Ctrl Pts',(4.12292517028468,-1.02433651174554,-5.65859284907271));
#11570=CARTESIAN_POINT('Ctrl Pts',(4.07816910321358,-1.04735437323224,-5.66222605418069));
#11571=CARTESIAN_POINT('Origin',(3.53951905042299,8.32667268468867E-16,
0.924367114736157));
#11572=CARTESIAN_POINT('',(4.07816929763934,-1.04735427323984,-6.26232527378825));
#11573=CARTESIAN_POINT('',(4.07816926754759,-1.04735428871591,-6.16392277459278));
#11574=CARTESIAN_POINT('',(4.07816926754759,-1.04735428871592,0.924367114736157));
#11575=CARTESIAN_POINT('',(2.36176914596391,-0.00047439080146823,-5.92346349896571));
#11576=CARTESIAN_POINT('Ctrl Pts',(4.07816929763934,-1.04735427323984,-6.26232527378825));
#11577=CARTESIAN_POINT('Ctrl Pts',(4.09023496895785,-1.0411489452008,-6.26135474120664));
#11578=CARTESIAN_POINT('Ctrl Pts',(4.10219477249534,-1.03473442025141,-6.26037854515567));
#11579=CARTESIAN_POINT('Ctrl Pts',(4.15591265580702,-1.00471610897298,-6.25593093081369));
#11580=CARTESIAN_POINT('Ctrl Pts',(4.19631180554023,-0.978784133249123,
-6.25240843958408));
#11581=CARTESIAN_POINT('Ctrl Pts',(4.25778352792731,-0.933802532810267,
-6.24681982066333));
#11582=CARTESIAN_POINT('Ctrl Pts',(4.27994647057524,-0.91632873992709,-6.24475351838742));
#11583=CARTESIAN_POINT('Ctrl Pts',(4.32788019253289,-0.87566097856935,-6.24019587139681));
#11584=CARTESIAN_POINT('Ctrl Pts',(4.35330024887309,-0.852089253740686,
-6.23771698249531));
#11585=CARTESIAN_POINT('Ctrl Pts',(4.38190563252322,-0.823114006289329,
-6.23488695704736));
#11586=CARTESIAN_POINT('Ctrl Pts',(4.38613184606868,-0.818766510776791,
-6.23446775457701));
#11587=CARTESIAN_POINT('Ctrl Pts',(4.39296976965588,-0.811622799150122,
-6.23378798835348));
#11588=CARTESIAN_POINT('Ctrl Pts',(4.39560169710329,-0.80884621613251,-6.23352597489406));
#11589=CARTESIAN_POINT('Ctrl Pts',(4.40030201720195,-0.80383891424895,-6.23305746059494));
#11590=CARTESIAN_POINT('Ctrl Pts',(4.40237533328976,-0.801612968778922,
-6.23285059601951));
#11591=CARTESIAN_POINT('Ctrl Pts',(4.4069252862916,-0.796689959333669,-6.2323961786076));
#11592=CARTESIAN_POINT('Ctrl Pts',(4.4093979823794,-0.793989366412672,-6.23214891738346));
#11593=CARTESIAN_POINT('Ctrl Pts',(4.41653319784795,-0.786123189220053,
-6.23143437434541));
#11594=CARTESIAN_POINT('Ctrl Pts',(4.42116268032956,-0.780927652881034,
-6.23096945458401));
#11595=CARTESIAN_POINT('Ctrl Pts',(4.46012823840423,-0.736409518276674,
-6.22704195826365));
#11596=CARTESIAN_POINT('Ctrl Pts',(4.49186557160994,-0.694879719389327,
-6.22374591948965));
#11597=CARTESIAN_POINT('Ctrl Pts',(4.56675906252071,-0.582060826952844,
-6.21531085374561));
#11598=CARTESIAN_POINT('Ctrl Pts',(4.60529671783504,-0.508069307664121,
-6.21024808736332));
#11599=CARTESIAN_POINT('Ctrl Pts',(4.64697982004174,-0.401963480249736,
-6.20297687442576));
#11600=CARTESIAN_POINT('Ctrl Pts',(4.65711327379942,-0.372863100348872,
-6.20098400327493));
#11601=CARTESIAN_POINT('Ctrl Pts',(4.66888478841956,-0.334244986214066,
-6.19832333086072));
#11602=CARTESIAN_POINT('Ctrl Pts',(4.6715638691723,-0.325055688189363,-6.19768909172239));
#11603=CARTESIAN_POINT('Ctrl Pts',(4.67572577032009,-0.310104395832672,
-6.19665487016446));
#11604=CARTESIAN_POINT('Ctrl Pts',(4.67727749371054,-0.304361904951789,
-6.19625710304884));
#11605=CARTESIAN_POINT('Ctrl Pts',(4.68017547767282,-0.293305348078831,
-6.19549008695273));
#11606=CARTESIAN_POINT('Ctrl Pts',(4.68152827126876,-0.287993142276344,
-6.19512105771836));
#11607=CARTESIAN_POINT('Ctrl Pts',(4.6845734084807,-0.275676450108379,-6.19426416495626));
#11608=CARTESIAN_POINT('Ctrl Pts',(4.68623863507582,-0.268665550882278,
-6.19377545438209));
#11609=CARTESIAN_POINT('Ctrl Pts',(4.69134182081782,-0.24626800761427,-6.19221091107657));
#11610=CARTESIAN_POINT('Ctrl Pts',(4.6945350807744,-0.230827974661903,-6.19112744335127));
#11611=CARTESIAN_POINT('Ctrl Pts',(4.70131415070436,-0.194374599057004,
-6.18855664629942));
#11612=CARTESIAN_POINT('Ctrl Pts',(4.70464120747205,-0.173319362174652,
-6.18706183393518));
#11613=CARTESIAN_POINT('Ctrl Pts',(4.7150620447811,-0.0933500990174083,
-6.18134660387077));
#11614=CARTESIAN_POINT('Ctrl Pts',(4.71827113560712,-0.0340245659343623,
-6.17702383848102));
#11615=CARTESIAN_POINT('Ctrl Pts',(4.71548489131035,0.0957328978677734,
-6.16750274731688));
#11616=CARTESIAN_POINT('Ctrl Pts',(4.70765258143186,0.165910477065057,-6.16230951768129));
#11617=CARTESIAN_POINT('Ctrl Pts',(4.69163089455348,0.24460159325757,-6.15668100972105));
#11618=CARTESIAN_POINT('Ctrl Pts',(4.68954969955024,0.254206928685382,-6.15599752700367));
#11619=CARTESIAN_POINT('Ctrl Pts',(4.68647754975801,0.267575003137327,-6.15505230289059));
#11620=CARTESIAN_POINT('Ctrl Pts',(4.68558789099588,0.271360268355784,-6.15478533128826));
#11621=CARTESIAN_POINT('Ctrl Pts',(4.6840149862692,0.277906829739487,-6.15432485924397));
#11622=CARTESIAN_POINT('Ctrl Pts',(4.68334046006642,0.280670155991929,-6.15413087961108));
#11623=CARTESIAN_POINT('Ctrl Pts',(4.68188897747402,0.286524289739774,-6.15372079270956));
#11624=CARTESIAN_POINT('Ctrl Pts',(4.68110947314463,0.289614443884628,-6.15350483651458));
#11625=CARTESIAN_POINT('Ctrl Pts',(4.67913101803897,0.297325435688441,-6.15296714395954));
#11626=CARTESIAN_POINT('Ctrl Pts',(4.67791648259323,0.301942278955648,-6.15264628015004));
#11627=CARTESIAN_POINT('Ctrl Pts',(4.67313872392961,0.319665394521243,-6.15141822327237));
#11628=CARTESIAN_POINT('Ctrl Pts',(4.66937680094446,0.332717644775483,-6.15052156033705));
#11629=CARTESIAN_POINT('Ctrl Pts',(4.65902984375411,0.366415212227218,-6.1482197691367));
#11630=CARTESIAN_POINT('Ctrl Pts',(4.65209919136348,0.386949698220904,-6.14683005916396));
#11631=CARTESIAN_POINT('Ctrl Pts',(4.60911685662259,0.503574401638551,-6.13895045862899));
#11632=CARTESIAN_POINT('Ctrl Pts',(4.56119542337881,0.594816078070128,-6.13279828597343));
#11633=CARTESIAN_POINT('Ctrl Pts',(4.48350324151432,0.704999917821411,-6.12421250578414));
#11634=CARTESIAN_POINT('Ctrl Pts',(4.46388623566266,0.730531351248177,-6.12213273950298));
#11635=CARTESIAN_POINT('Ctrl Pts',(4.43701588978873,0.762685381098157,-6.11937209760121));
#11636=CARTESIAN_POINT('Ctrl Pts',(4.43069016383441,0.770067272730883,-6.11872811227026));
#11637=CARTESIAN_POINT('Ctrl Pts',(4.42032615549249,0.781862954258344,-6.11768192736207));
#11638=CARTESIAN_POINT('Ctrl Pts',(4.41634427080329,0.786325865183131,-6.11728204072387));
#11639=CARTESIAN_POINT('Ctrl Pts',(4.40865468574665,0.794813344171872,-6.11651359743817));
#11640=CARTESIAN_POINT('Ctrl Pts',(4.40495258268798,0.798842790642308,-6.11614528005657));
#11641=CARTESIAN_POINT('Ctrl Pts',(4.39635859647735,0.808066808883381,-6.11529394186543));
#11642=CARTESIAN_POINT('Ctrl Pts',(4.39144735827215,0.813242970894683,-6.11481010939629));
#11643=CARTESIAN_POINT('Ctrl Pts',(4.37580358012886,0.829433387577266,-6.11327710661366));
#11644=CARTESIAN_POINT('Ctrl Pts',(4.36490255654542,0.840281850415247,-6.11222072910309));
#11645=CARTESIAN_POINT('Ctrl Pts',(4.33888443132437,0.865179654213928,-6.10972547856839));
#11646=CARTESIAN_POINT('Ctrl Pts',(4.3236046633512,0.879050913690368,-6.10827970605825));
#11647=CARTESIAN_POINT('Ctrl Pts',(4.26546839620884,0.929106010391572,-6.10284944527884));
#11648=CARTESIAN_POINT('Ctrl Pts',(4.22041258014362,0.962612682667298,-6.0987735335591));
#11649=CARTESIAN_POINT('Ctrl Pts',(4.1096343323993,1.03331533686176,-6.08914023447894));
#11650=CARTESIAN_POINT('Ctrl Pts',(4.04237379823384,1.06766615234464,-6.08357204699742));
#11651=CARTESIAN_POINT('Ctrl Pts',(3.96341105184678,1.09886383412478,-6.07762477296247));
#11652=CARTESIAN_POINT('Ctrl Pts',(3.95449185959204,1.10226300714134,-6.07696125378353));
#11653=CARTESIAN_POINT('Ctrl Pts',(3.94191009331509,1.10688364268902,-6.07603775020791));
#11654=CARTESIAN_POINT('Ctrl Pts',(3.93828162347891,1.10819599405154,-6.07577286621487));
#11655=CARTESIAN_POINT('Ctrl Pts',(3.93170860778717,1.11053687056379,-6.07529571892222));
#11656=CARTESIAN_POINT('Ctrl Pts',(3.92876630647829,1.11157157405482,-6.0750831035106));
#11657=CARTESIAN_POINT('Ctrl Pts',(3.92273494563442,1.11366570574782,-6.07464930181903));
#11658=CARTESIAN_POINT('Ctrl Pts',(3.91964553633732,1.11472399358168,-6.07442818176472));
#11659=CARTESIAN_POINT('Ctrl Pts',(3.91168450935162,1.11741412574173,-6.07386107016147));
#11660=CARTESIAN_POINT('Ctrl Pts',(3.90680648024522,1.11902698963564,-6.073516160187));
#11661=CARTESIAN_POINT('Ctrl Pts',(3.88614866036797,1.12570762334384,-6.07206577415419));
#11662=CARTESIAN_POINT('Ctrl Pts',(3.87027250288145,1.13047421978312,-6.07097632146394));
#11663=CARTESIAN_POINT('Ctrl Pts',(3.826501935294,1.14261457581979,-6.06802788090749));
#11664=CARTESIAN_POINT('Ctrl Pts',(3.7984279121614,1.1493013873189,-6.06619729594464));
#11665=CARTESIAN_POINT('Ctrl Pts',(3.68173355665175,1.17260243035188,-6.05873226487686));
#11666=CARTESIAN_POINT('Ctrl Pts',(3.59160002312312,1.18004638063982,-6.05328081782732));
#11667=CARTESIAN_POINT('Ctrl Pts',(3.4681031231792,1.17605748836533,-6.045422827928));
#11668=CARTESIAN_POINT('Ctrl Pts',(3.4347719003372,1.17355833482817,-6.04326617553621));
#11669=CARTESIAN_POINT('Ctrl Pts',(3.39180236078252,1.16849135846763,-6.0404165623393));
#11670=CARTESIAN_POINT('Ctrl Pts',(3.3820256921699,1.16721382258042,-6.03976356927852));
#11671=CARTESIAN_POINT('Ctrl Pts',(3.36631614842783,1.16496006459645,-6.03870632271181));
#11672=CARTESIAN_POINT('Ctrl Pts',(3.36037256105679,1.16406087918425,-6.03830447385833));
#11673=CARTESIAN_POINT('Ctrl Pts',(3.34904024132537,1.16225760463174,-6.03753464015022));
#11674=CARTESIAN_POINT('Ctrl Pts',(3.34365039319316,1.16136143539783,-6.03716691226133));
#11675=CARTESIAN_POINT('Ctrl Pts',(3.33129718361274,1.15921902887461,-6.03632037491132));
#11676=CARTESIAN_POINT('Ctrl Pts',(3.32433848119451,1.15794750380657,-6.03584078445057));
#11677=CARTESIAN_POINT('Ctrl Pts',(3.30261535686581,1.1537755840954,-6.03433486591795));
#11678=CARTESIAN_POINT('Ctrl Pts',(3.2878952924871,1.15065499026485,-6.03330168788211));
#11679=CARTESIAN_POINT('Ctrl Pts',(3.25370060041941,1.14271834499085,-6.0308707016088));
#11680=CARTESIAN_POINT('Ctrl Pts',(3.23428168918236,1.13768513816858,-6.02946646928371));
#11681=CARTESIAN_POINT('Ctrl Pts',(3.16362062670901,1.11743114227027,-6.02426876592153));
#11682=CARTESIAN_POINT('Ctrl Pts',(3.11330712790216,1.09922438801772,-6.02039227058267));
#11683=CARTESIAN_POINT('Ctrl Pts',(2.99166532473383,1.04559622403568,-6.01065627823979));
#11684=CARTESIAN_POINT('Ctrl Pts',(2.92235092134621,1.00624083082896,-6.0047678923588));
#11685=CARTESIAN_POINT('Ctrl Pts',(2.84981253488101,0.954719600240245,-5.99853975550467));
#11686=CARTESIAN_POINT('Ctrl Pts',(2.8421643027805,0.949147492627594,-5.99788240316152));
#11687=CARTESIAN_POINT('Ctrl Pts',(2.83159398420192,0.941249750043009,-5.99697387005026));
#11688=CARTESIAN_POINT('Ctrl Pts',(2.82861479137434,0.939001664940125,-5.99671780099785));
#11689=CARTESIAN_POINT('Ctrl Pts',(2.82319119836403,0.934868439340018,-5.99625169877643));
#11690=CARTESIAN_POINT('Ctrl Pts',(2.82074342770127,0.932987778897274,-5.99604136490264));
#11691=CARTESIAN_POINT('Ctrl Pts',(2.81573090290748,0.929105142132876,-5.9956107426378));
#11692=CARTESIAN_POINT('Ctrl Pts',(2.81316701755263,0.927102137100601,-5.99539052778835));
#11693=CARTESIAN_POINT('Ctrl Pts',(2.80673448666815,0.922033734680722,-5.99483805452521));
#11694=CARTESIAN_POINT('Ctrl Pts',(2.80287670380741,0.918954558221804,-5.99450674135558));
#11695=CARTESIAN_POINT('Ctrl Pts',(2.7943208730998,0.912037028173135,-5.9937717092654));
#11696=CARTESIAN_POINT('Ctrl Pts',(2.78963286005736,0.908186417749585,-5.99336879662046));
#11697=CARTESIAN_POINT('Ctrl Pts',(2.77586143854283,0.896695593604447,-5.99218400117474));
#11698=CARTESIAN_POINT('Ctrl Pts',(2.76686326791718,0.888953880141247,-5.99140828875435));
#11699=CARTESIAN_POINT('Ctrl Pts',(2.73421665808705,0.859995584259759,-5.988581418607));
#11700=CARTESIAN_POINT('Ctrl Pts',(2.71131096530185,0.837959430794632,-5.98657319649999));
#11701=CARTESIAN_POINT('Ctrl Pts',(2.67160936435353,0.796544441714306,-5.98298600219773));
#11702=CARTESIAN_POINT('Ctrl Pts',(2.65450251521094,0.777493446020089,-5.98140049337148));
#11703=CARTESIAN_POINT('Ctrl Pts',(2.58361082598284,0.693170820613504,-5.97458445170998));
#11704=CARTESIAN_POINT('Ctrl Pts',(2.53632793676492,0.62277750278925,-5.96937011291797));
#11705=CARTESIAN_POINT('Ctrl Pts',(2.48996839576904,0.534571163312495,-5.9628743519718));
#11706=CARTESIAN_POINT('Ctrl Pts',(2.48320368584932,0.521076503303184,-5.96188227556779));
#11707=CARTESIAN_POINT('Ctrl Pts',(2.47363591261027,0.501037708494094,-5.96040966482948));
#11708=CARTESIAN_POINT('Ctrl Pts',(2.47062965804543,0.494591864024867,-5.95993606199502));
#11709=CARTESIAN_POINT('Ctrl Pts',(2.46540835448122,0.483126661858874,-5.959093626612));
#11710=CARTESIAN_POINT('Ctrl Pts',(2.46316962898218,0.478118269640409,-5.95872560912309));
#11711=CARTESIAN_POINT('Ctrl Pts',(2.45858173133207,0.467658856001614,-5.95795693048653));
#11712=CARTESIAN_POINT('Ctrl Pts',(2.45623861849636,0.462205362346718,-5.95755607780845));
#11713=CARTESIAN_POINT('Ctrl Pts',(2.45024788695567,0.447966385887117,-5.95650915875833));
#11714=CARTESIAN_POINT('Ctrl Pts',(2.44666536934578,0.439154156302012,-5.95586094303869));
#11715=CARTESIAN_POINT('Ctrl Pts',(2.43094374827078,0.399098195333223,-5.95291243462964));
#11716=CARTESIAN_POINT('Ctrl Pts',(2.42003614690547,0.367391088674902,-5.95057225856815));
#11717=CARTESIAN_POINT('Ctrl Pts',(2.37812953154315,0.226268154702565,-5.94012295799659));
#11718=CARTESIAN_POINT('Ctrl Pts',(2.3617233639395,0.113186697719935,-5.93158837563074));
#11719=CARTESIAN_POINT('Ctrl Pts',(2.36176914596391,-0.00047439080146823,
-5.92346349896571));
#11720=CARTESIAN_POINT('Ctrl Pts',(2.36176914658663,-0.000475934275394455,
-5.92346338863304));
#11721=CARTESIAN_POINT('Ctrl Pts',(2.36177760495954,-0.0214070762438138,
-5.92196716112806));
#11722=CARTESIAN_POINT('Ctrl Pts',(2.3623440511716,-0.0423361050014404,
-5.92048893771383));
#11723=CARTESIAN_POINT('Ctrl Pts',(2.36370274366909,-0.0676029612356144,
-5.91873422110888));
#11724=CARTESIAN_POINT('Ctrl Pts',(2.36396159790513,-0.0719640527127362,
-5.91843243505327));
#11725=CARTESIAN_POINT('Ctrl Pts',(2.36444920185137,-0.0794724480462547,
-5.91791483065283));
#11726=CARTESIAN_POINT('Ctrl Pts',(2.36466634244599,-0.0826204221579617,
-5.91769841766443));
#11727=CARTESIAN_POINT('Ctrl Pts',(2.36510396526883,-0.0886138533579433,
-5.91728757574057));
#11728=CARTESIAN_POINT('Ctrl Pts',(2.36532214384525,-0.0914594575013904,
-5.91709302330615));
#11729=CARTESIAN_POINT('Ctrl Pts',(2.36577866569802,-0.0971425736467546,
-5.91670552777087));
#11730=CARTESIAN_POINT('Ctrl Pts',(2.36601695921495,-0.0999800616037671,
-5.91651258241162));
#11731=CARTESIAN_POINT('Ctrl Pts',(2.36660605016895,-0.106702248326651,
-5.91605666773188));
#11732=CARTESIAN_POINT('Ctrl Pts',(2.36696586203937,-0.110586153962821,
-5.91579419050447));
#11733=CARTESIAN_POINT('Ctrl Pts',(2.36829937255023,-0.124241523053148,
-5.9148744267966));
#11734=CARTESIAN_POINT('Ctrl Pts',(2.36937600734381,-0.134002850878811,
-5.91422249313009));
#11735=CARTESIAN_POINT('Ctrl Pts',(2.37355925964272,-0.168020178416457,
-5.91196636331695));
#11736=CARTESIAN_POINT('Ctrl Pts',(2.37729923935332,-0.192193396399408,
-5.91039118992659));
#11737=CARTESIAN_POINT('Ctrl Pts',(2.40079692035164,-0.318001176972263,
-5.90225943617596));
#11738=CARTESIAN_POINT('Ctrl Pts',(2.43313902489403,-0.416819604865689,
-5.89605944901046));
#11739=CARTESIAN_POINT('Ctrl Pts',(2.48765961102549,-0.530269248192219,
-5.88805173051619));
#11740=CARTESIAN_POINT('Ctrl Pts',(2.49790247751019,-0.550116877253475,
-5.88661677915914));
#11741=CARTESIAN_POINT('Ctrl Pts',(2.51660560100441,-0.583960689153967,
-5.88410043890528));
#11742=CARTESIAN_POINT('Ctrl Pts',(2.52480471413348,-0.598094294283077,
-5.88302779575204));
#11743=CARTESIAN_POINT('Ctrl Pts',(2.53709281764408,-0.618296143640833,
-5.88146028177884));
#11744=CARTESIAN_POINT('Ctrl Pts',(2.54094873935566,-0.624504446131463,
-5.88097376278203));
#11745=CARTESIAN_POINT('Ctrl Pts',(2.54780566233151,-0.635318687087124,
-5.88011762402527));
#11746=CARTESIAN_POINT('Ctrl Pts',(2.55078162628431,-0.639940296155991,
-5.87974892570641));
#11747=CARTESIAN_POINT('Ctrl Pts',(2.55662808426741,-0.648881583288878,
-5.87903003201151));
#11748=CARTESIAN_POINT('Ctrl Pts',(2.55949497838933,-0.653203473072743,
-5.87867997564401));
#11749=CARTESIAN_POINT('Ctrl Pts',(2.56725086968374,-0.664729606458764,
-5.87773940284533));
#11750=CARTESIAN_POINT('Ctrl Pts',(2.57219128532318,-0.671898692357601,
-5.87714698042595));
#11751=CARTESIAN_POINT('Ctrl Pts',(2.5909084968569,-0.698425065503021,-5.87492668849393));
#11752=CARTESIAN_POINT('Ctrl Pts',(2.60518974233784,-0.717417701090581,
-5.87327993452043));
#11753=CARTESIAN_POINT('Ctrl Pts',(2.68302084173491,-0.814656754862096,
-5.86453738217128));
#11754=CARTESIAN_POINT('Ctrl Pts',(2.75584210404748,-0.884928640498914,
-5.857073789571));
#11755=CARTESIAN_POINT('Ctrl Pts',(2.86061040135281,-0.962842778902455,
-5.84755154736277));
#11756=CARTESIAN_POINT('Ctrl Pts',(2.88519171118066,-0.97971380636161,-5.84539549744997));
#11757=CARTESIAN_POINT('Ctrl Pts',(2.92001481048248,-1.00171814184796,-5.84247078212881));
#11758=CARTESIAN_POINT('Ctrl Pts',(2.9297296395284,-1.00766146832375,-5.8416682503467));
#11759=CARTESIAN_POINT('Ctrl Pts',(2.94460103162576,-1.01646561578382,-5.84046157248804));
#11760=CARTESIAN_POINT('Ctrl Pts',(2.94969512219012,-1.01943000458922,-5.84005205394333));
#11761=CARTESIAN_POINT('Ctrl Pts',(2.9591083372682,-1.02481362690101,-5.83930260876271));
#11762=CARTESIAN_POINT('Ctrl Pts',(2.96342084733076,-1.02724409387685,-5.83896204622149));
#11763=CARTESIAN_POINT('Ctrl Pts',(2.97051545957373,-1.03118378185554,-5.83840648308147));
#11764=CARTESIAN_POINT('Ctrl Pts',(2.97328849428612,-1.03270907629403,-5.83819050175509));
#11765=CARTESIAN_POINT('Ctrl Pts',(2.97880193514254,-1.03571283388441,-5.83776344437208));
#11766=CARTESIAN_POINT('Ctrl Pts',(2.98154210170897,-1.03719163257148,-5.83755235284934));
#11767=CARTESIAN_POINT('Ctrl Pts',(2.98767350633388,-1.04046926614404,-5.83708251675237));
#11768=CARTESIAN_POINT('Ctrl Pts',(2.99106777168128,-1.04226244017224,-5.83682412112084));
#11769=CARTESIAN_POINT('Ctrl Pts',(3.00283071737263,-1.04840337248369,-5.83593428939906));
#11770=CARTESIAN_POINT('Ctrl Pts',(3.0112430742722,-1.05266732875569,-5.8353077539383));
#11771=CARTESIAN_POINT('Ctrl Pts',(3.08887096324529,-1.09084942727537,-5.8296075090175));
#11772=CARTESIAN_POINT('Ctrl Pts',(3.16121893189687,-1.11800208080267,-5.82487561105016));
#11773=CARTESIAN_POINT('Ctrl Pts',(3.28881424901934,-1.15206908925458,-5.81670538909766));
#11774=CARTESIAN_POINT('Ctrl Pts',(3.3428424701339,-1.16251183834201,-5.81329723741568));
#11775=CARTESIAN_POINT('Ctrl Pts',(3.41764273791609,-1.17160449562992,-5.80848750862781));
#11776=CARTESIAN_POINT('Ctrl Pts',(3.4379460894029,-1.17353900279816,-5.80717339832075));
#11777=CARTESIAN_POINT('Ctrl Pts',(3.47349188199594,-1.1759964798411,-5.80485053102374));
#11778=CARTESIAN_POINT('Ctrl Pts',(3.48871354951401,-1.17675234184652,-5.80384875230846));
#11779=CARTESIAN_POINT('Ctrl Pts',(3.51105154830254,-1.17742737026895,-5.80236631673948));
#11780=CARTESIAN_POINT('Ctrl Pts',(3.51815971165065,-1.17757776213472,-5.80189277018669));
#11781=CARTESIAN_POINT('Ctrl Pts',(3.53073679420862,-1.17772995173204,-5.80105146650971));
#11782=CARTESIAN_POINT('Ctrl Pts',(3.53620523001797,-1.17775803291908,-5.80068453068911));
#11783=CARTESIAN_POINT('Ctrl Pts',(3.54766698721581,-1.17773706514276,-5.79991295324079));
#11784=CARTESIAN_POINT('Ctrl Pts',(3.55366012036343,-1.17768035193621,-5.79950808550401));
#11785=CARTESIAN_POINT('Ctrl Pts',(3.5694290271699,-1.17741074604027,-5.79843893338811));
#11786=CARTESIAN_POINT('Ctrl Pts',(3.57920286343207,-1.17712185290534,-5.79777232709906));
#11787=CARTESIAN_POINT('Ctrl Pts',(3.62164878129819,-1.17533801354753,-5.79485958774397));
#11788=CARTESIAN_POINT('Ctrl Pts',(3.65425141888492,-1.17260430804531,-5.79257589995079));
#11789=CARTESIAN_POINT('Ctrl Pts',(3.77690513087472,-1.15715590298647,-5.78380345109363));
#11790=CARTESIAN_POINT('Ctrl Pts',(3.86548866471428,-1.1353862014243,-5.7770655728495));
#11791=CARTESIAN_POINT('Ctrl Pts',(3.97776758578952,-1.09355815475573,-5.76833328612069));
#11792=CARTESIAN_POINT('Ctrl Pts',(4.004485597182,-1.08246826768167,-5.76624314554824));
#11793=CARTESIAN_POINT('Ctrl Pts',(4.04585689750954,-1.06348136172682,-5.76301293255282));
#11794=CARTESIAN_POINT('Ctrl Pts',(4.06079680188451,-1.05623870290635,-5.76184783550009));
#11795=CARTESIAN_POINT('Ctrl Pts',(4.0764432923149,-1.04824060315226,-5.76063280410153));
#11796=CARTESIAN_POINT('Ctrl Pts',(4.0773065526916,-1.04779797959445,-5.76056578435822));
#11797=CARTESIAN_POINT('Ctrl Pts',(4.07816926754817,-1.04735428871561,-5.76049882461148));
#11798=CARTESIAN_POINT('Ctrl Pts',(4.07816910321358,-1.04735437323224,-5.66222605418069));
#11799=CARTESIAN_POINT('Ctrl Pts',(4.05590441778445,-1.05880500950996,-5.66403345536945));
#11800=CARTESIAN_POINT('Ctrl Pts',(4.033270176812,-1.06954797620782,-5.66585731820949));
#11801=CARTESIAN_POINT('Ctrl Pts',(3.9573207630993,-1.10266827073946,-5.67191846171575));
#11802=CARTESIAN_POINT('Ctrl Pts',(3.90271247636352,-1.12184061798517,-5.67618723591131));
#11803=CARTESIAN_POINT('Ctrl Pts',(3.82711691893152,-1.1422798301042,-5.68184226915528));
#11804=CARTESIAN_POINT('Ctrl Pts',(3.80717965346055,-1.14711535848151,-5.68331001265983));
#11805=CARTESIAN_POINT('Ctrl Pts',(3.7743595768206,-1.1541730742003,-5.68567759216775));
#11806=CARTESIAN_POINT('Ctrl Pts',(3.76154856302646,-1.15670587834702,-5.68658978412911));
#11807=CARTESIAN_POINT('Ctrl Pts',(3.74406989137212,-1.15986039142249,-5.68781577392829));
#11808=CARTESIAN_POINT('Ctrl Pts',(3.73943729280115,-1.16066785618203,-5.68813894950106));
#11809=CARTESIAN_POINT('Ctrl Pts',(3.73167211651291,-1.16197345975913,-5.68867756801459));
#11810=CARTESIAN_POINT('Ctrl Pts',(3.7285421777667,-1.16248672254725,-5.68889383240835));
#11811=CARTESIAN_POINT('Ctrl Pts',(3.72258971076087,-1.16343816075113,-5.68930347999926));
#11812=CARTESIAN_POINT('Ctrl Pts',(3.7197676104416,-1.16387872118291,-5.68949699901895));
#11813=CARTESIAN_POINT('Ctrl Pts',(3.71305224277283,-1.16490205181255,-5.68995589237857));
#11814=CARTESIAN_POINT('Ctrl Pts',(3.70915757036099,-1.1654755822497,-5.6902207589026));
#11815=CARTESIAN_POINT('Ctrl Pts',(3.69535119074833,-1.16743803917434,-5.69115541536521));
#11816=CARTESIAN_POINT('Ctrl Pts',(3.68542440026647,-1.16872018740007,-5.69181963129424));
#11817=CARTESIAN_POINT('Ctrl Pts',(3.61187920507642,-1.17726761440479,-5.69669105897549));
#11818=CARTESIAN_POINT('Ctrl Pts',(3.54777056232801,-1.17946136770664,-5.70066699475069));
#11819=CARTESIAN_POINT('Ctrl Pts',(3.42224438139773,-1.17351549179823,-5.70844565012187));
#11820=CARTESIAN_POINT('Ctrl Pts',(3.36102169153983,-1.16577445977327,-5.71223871160024));
#11821=CARTESIAN_POINT('Ctrl Pts',(3.27775688639229,-1.14853123257754,-5.71763875963724));
#11822=CARTESIAN_POINT('Ctrl Pts',(3.25497425519768,-1.14309998583426,-5.71914116522909));
#11823=CARTESIAN_POINT('Ctrl Pts',(3.21601702606997,-1.1325760135616,-5.72176469560425));
#11824=CARTESIAN_POINT('Ctrl Pts',(3.19976229474584,-1.12780640457901,-5.72287599154865));
#11825=CARTESIAN_POINT('Ctrl Pts',(3.17655096827304,-1.12044820307637,-5.72448967257269));
#11826=CARTESIAN_POINT('Ctrl Pts',(3.16950666430863,-1.11814168796561,-5.72498298655269));
#11827=CARTESIAN_POINT('Ctrl Pts',(3.15726230291476,-1.11400414252061,-5.72584695276355));
#11828=CARTESIAN_POINT('Ctrl Pts',(3.15205240373679,-1.11220279019376,-5.72621663024624));
#11829=CARTESIAN_POINT('Ctrl Pts',(3.14199452048952,-1.10864597316496,-5.72693439884319));
#11830=CARTESIAN_POINT('Ctrl Pts',(3.13714503210403,-1.10689511410968,-5.72728233184394));
#11831=CARTESIAN_POINT('Ctrl Pts',(3.12428634094326,-1.10215694432326,-5.72820992393417));
#11832=CARTESIAN_POINT('Ctrl Pts',(3.11629802369937,-1.09911422918797,-5.72879139469081));
#11833=CARTESIAN_POINT('Ctrl Pts',(3.08725966083902,-1.08769014304142,-5.73092464958761));
#11834=CARTESIAN_POINT('Ctrl Pts',(3.06642070778634,-1.07878924663544,-5.73249345498974));
#11835=CARTESIAN_POINT('Ctrl Pts',(2.95345433061729,-1.02663545059916,-5.74121409764393));
#11836=CARTESIAN_POINT('Ctrl Pts',(2.86698592534885,-0.972185419718714,
-5.74874716505658));
#11837=CARTESIAN_POINT('Ctrl Pts',(2.76540078565253,-0.888112378900456,
-5.7583665023148));
#11838=CARTESIAN_POINT('Ctrl Pts',(2.7429355093011,-0.868019349789785,-5.76054682250989));
#11839=CARTESIAN_POINT('Ctrl Pts',(2.71301598321759,-0.83911814188063,-5.76350094255396));
#11840=CARTESIAN_POINT('Ctrl Pts',(2.70488423859892,-0.831030281523895,
-5.76430927323719));
#11841=CARTESIAN_POINT('Ctrl Pts',(2.69096671686843,-0.816777469859977,
-5.76570035168024));
#11842=CARTESIAN_POINT('Ctrl Pts',(2.68512688463055,-0.810666722720063,
-5.76628646766268));
#11843=CARTESIAN_POINT('Ctrl Pts',(2.67664930214213,-0.801602475234878,
-5.7671402171437));
#11844=CARTESIAN_POINT('Ctrl Pts',(2.67396000801465,-0.798697862807326,
-5.76741148428987));
#11845=CARTESIAN_POINT('Ctrl Pts',(2.66924276954727,-0.793551130123568,
-5.76788799702388));
#11846=CARTESIAN_POINT('Ctrl Pts',(2.6672087551954,-0.79131469768356,-5.76809368788746));
#11847=CARTESIAN_POINT('Ctrl Pts',(2.66280634073862,-0.786436567107738,
-5.76853935997601));
#11848=CARTESIAN_POINT('Ctrl Pts',(2.66044125314773,-0.783791985527263,
-5.76877909930313));
#11849=CARTESIAN_POINT('Ctrl Pts',(2.65394142832779,-0.776457614236689,
-5.76943896328464));
#11850=CARTESIAN_POINT('Ctrl Pts',(2.64983195567053,-0.771745443220508,
-5.76985729155267));
#11851=CARTESIAN_POINT('Ctrl Pts',(2.62775640454187,-0.746021577465351,
-5.77211213630108));
#11852=CARTESIAN_POINT('Ctrl Pts',(2.61049529189164,-0.724413175764943,
-5.7739030850614));
#11853=CARTESIAN_POINT('Ctrl Pts',(2.54453804874295,-0.635603930868825,
-5.78095332906597));
#11854=CARTESIAN_POINT('Ctrl Pts',(2.50224156354834,-0.563947579280367,
-5.78597648144959));
#11855=CARTESIAN_POINT('Ctrl Pts',(2.44534065814713,-0.439099542260725,
-5.7945514377408));
#11856=CARTESIAN_POINT('Ctrl Pts',(2.42629130910713,-0.388275199489886,
-5.7979956957979));
#11857=CARTESIAN_POINT('Ctrl Pts',(2.40770688448018,-0.325905601496133,
-5.80227263997611));
#11858=CARTESIAN_POINT('Ctrl Pts',(2.40474700643433,-0.315445138389542,
-5.80299143874695));
#11859=CARTESIAN_POINT('Ctrl Pts',(2.40031923231351,-0.298927508463371,
-5.80412948282503));
#11860=CARTESIAN_POINT('Ctrl Pts',(2.39875383935721,-0.292896929999704,
-5.80454560931671));
#11861=CARTESIAN_POINT('Ctrl Pts',(2.39591473307706,-0.281591323858041,
-5.80532703057016));
#11862=CARTESIAN_POINT('Ctrl Pts',(2.39462948027629,-0.276319342077268,
-5.80569194683368));
#11863=CARTESIAN_POINT('Ctrl Pts',(2.39183610346387,-0.264507022519579,
-5.80651084102657));
#11864=CARTESIAN_POINT('Ctrl Pts',(2.39034737474615,-0.257962338919741,
-5.80696542067858));
#11865=CARTESIAN_POINT('Ctrl Pts',(2.38670593283457,-0.241296591596315,
-5.80812535161508));
#11866=CARTESIAN_POINT('Ctrl Pts',(2.38463054984694,-0.23115940083819,-5.80883310712443));
#11867=CARTESIAN_POINT('Ctrl Pts',(2.36870487123071,-0.147794703097492,
-5.8146729711907));
#11868=CARTESIAN_POINT('Ctrl Pts',(2.36170273807556,-0.0734445351739944,
-5.82002094522557));
#11869=CARTESIAN_POINT('Ctrl Pts',(2.36184042799039,0.0801506629869638,
-5.83125281056311));
#11870=CARTESIAN_POINT('Ctrl Pts',(2.36987871761785,0.159040563076637,-5.83712062759711));
#11871=CARTESIAN_POINT('Ctrl Pts',(2.38837836564954,0.249277888215904,-5.84361948445117));
#11872=CARTESIAN_POINT('Ctrl Pts',(2.39120252526141,0.261980027144235,-5.84452883310714));
#11873=CARTESIAN_POINT('Ctrl Pts',(2.39536585718711,0.279342047056117,-5.84576195026205));
#11874=CARTESIAN_POINT('Ctrl Pts',(2.39652402375803,0.284043799293962,-5.84609488965759));
#11875=CARTESIAN_POINT('Ctrl Pts',(2.39841798137968,0.291533401966075,-5.84662350512072));
#11876=CARTESIAN_POINT('Ctrl Pts',(2.39913505269272,0.294325860926441,-5.846820210163));
#11877=CARTESIAN_POINT('Ctrl Pts',(2.40065571714905,0.300158724722065,-5.84723023708367));
#11878=CARTESIAN_POINT('Ctrl Pts',(2.40146124377929,0.303198583381686,-5.84744343888796));
#11879=CARTESIAN_POINT('Ctrl Pts',(2.40346673775005,0.310646218766213,-5.84796466282368));
#11880=CARTESIAN_POINT('Ctrl Pts',(2.4046802092756,0.315050371696231,-5.84827192525692));
#11881=CARTESIAN_POINT('Ctrl Pts',(2.40920476308002,0.331106324480908,-5.84938894917187));
#11882=CARTESIAN_POINT('Ctrl Pts',(2.41267005334852,0.342714388728082,-5.85019046800396));
#11883=CARTESIAN_POINT('Ctrl Pts',(2.42187751144078,0.371906635869094,-5.85219562012209));
#11884=CARTESIAN_POINT('Ctrl Pts',(2.42785610046585,0.389413299306522,-5.85338836885609));
#11885=CARTESIAN_POINT('Ctrl Pts',(2.45689613768073,0.468320250347978,-5.85875035692082));
#11886=CARTESIAN_POINT('Ctrl Pts',(2.48465021012575,0.527872297016709,-5.86276331676315));
#11887=CARTESIAN_POINT('Ctrl Pts',(2.55238885172492,0.646285944922952,-5.87121994260289));
#11888=CARTESIAN_POINT('Ctrl Pts',(2.5930266930545,0.704458511257287,-5.87565894743985));
#11889=CARTESIAN_POINT('Ctrl Pts',(2.64536381751722,0.766609716498963,-5.88099099172694));
#11890=CARTESIAN_POINT('Ctrl Pts',(2.65219366545694,0.774504801667363,-5.88168005157804));
#11891=CARTESIAN_POINT('Ctrl Pts',(2.66360419031718,0.787345949712134,-5.8828209760035));
#11892=CARTESIAN_POINT('Ctrl Pts',(2.66812407855202,0.792345433830036,-5.88327034809631));
#11893=CARTESIAN_POINT('Ctrl Pts',(2.67636144668496,0.801301117765885,-5.88408489483804));
#11894=CARTESIAN_POINT('Ctrl Pts',(2.68006386816501,0.805270959508957,-5.88444943225166));
#11895=CARTESIAN_POINT('Ctrl Pts',(2.6880605541363,0.813727263512018,-5.88523352005582));
#11896=CARTESIAN_POINT('Ctrl Pts',(2.69236310996546,0.818205622248709,-5.88565341747766));
#11897=CARTESIAN_POINT('Ctrl Pts',(2.70422893034798,0.830362352117846,-5.88680622327996));
#11898=CARTESIAN_POINT('Ctrl Pts',(2.7118623365081,0.837971103938437,-5.88754215018546));
#11899=CARTESIAN_POINT('Ctrl Pts',(2.75707937586495,0.88182150167839,-5.89186994696998));
#11900=CARTESIAN_POINT('Ctrl Pts',(2.7969299043815,0.915631465178649,-5.89556310449824));
#11901=CARTESIAN_POINT('Ctrl Pts',(2.90014188769413,0.992017827517853,-5.90483582406355));
#11902=CARTESIAN_POINT('Ctrl Pts',(2.96564810248908,1.03129705080707,-5.9104882905964));
#11903=CARTESIAN_POINT('Ctrl Pts',(3.04780609670735,1.07029473326181,-5.91708805263446));
#11904=CARTESIAN_POINT('Ctrl Pts',(3.06124366046387,1.0763666318341,-5.91815230514171));
#11905=CARTESIAN_POINT('Ctrl Pts',(3.09549191005506,1.09107399361051,-5.92082122346563));
#11906=CARTESIAN_POINT('Ctrl Pts',(3.1164441601943,1.09936816319868,-5.92241416415505));
#11907=CARTESIAN_POINT('Ctrl Pts',(3.14320756721701,1.10908411229172,-5.92438837180267));
#11908=CARTESIAN_POINT('Ctrl Pts',(3.14880752163197,1.11106924394302,-5.92479815364328));
#11909=CARTESIAN_POINT('Ctrl Pts',(3.15767584750484,1.11413764092582,-5.92544164240144));
#11910=CARTESIAN_POINT('Ctrl Pts',(3.16093426437226,1.11524906414737,-5.92567691680511));
#11911=CARTESIAN_POINT('Ctrl Pts',(3.16711107838899,1.11732574164928,-5.92612066512895));
#11912=CARTESIAN_POINT('Ctrl Pts',(3.17002835871406,1.11829385205943,-5.92632929172806));
#11913=CARTESIAN_POINT('Ctrl Pts',(3.17689843847846,1.12054389525013,-5.92681841097791));
#11914=CARTESIAN_POINT('Ctrl Pts',(3.18085427700204,1.12181634459729,-5.92709835617977));
#11915=CARTESIAN_POINT('Ctrl Pts',(3.19390963362582,1.12593966075054,-5.92801694034282));
#11916=CARTESIAN_POINT('Ctrl Pts',(3.20303732410554,1.12870104577624,-5.92865069601643));
#11917=CARTESIAN_POINT('Ctrl Pts',(3.25454283755589,1.14360255588783,-5.93218464190927));
#11918=CARTESIAN_POINT('Ctrl Pts',(3.29754717982951,1.15346813387787,-5.93497612372975));
#11919=CARTESIAN_POINT('Ctrl Pts',(3.36850400898774,1.16560158873795,-5.93947185000744));
#11920=CARTESIAN_POINT('Ctrl Pts',(3.39615908020165,1.16932509941993,-5.941197200551));
#11921=CARTESIAN_POINT('Ctrl Pts',(3.50385170993643,1.17994661414321,-5.94789086714254));
#11922=CARTESIAN_POINT('Ctrl Pts',(3.58436942354338,1.1796324027728,-5.95285927334266));
#11923=CARTESIAN_POINT('Ctrl Pts',(3.67958241869871,1.16949384898834,-5.95909945158123));
#11924=CARTESIAN_POINT('Ctrl Pts',(3.69490630658036,1.16755658304031,-5.96011448456682));
#11925=CARTESIAN_POINT('Ctrl Pts',(3.71718250921266,1.16429409650172,-5.96160772785424));
#11926=CARTESIAN_POINT('Ctrl Pts',(3.72416840961237,1.16320662749307,-5.96207856110625));
#11927=CARTESIAN_POINT('Ctrl Pts',(3.73654993867548,1.16116489387022,-5.96291776644867));
#11928=CARTESIAN_POINT('Ctrl Pts',(3.74194954116544,1.16023574172269,-5.96328534405909));
#11929=CARTESIAN_POINT('Ctrl Pts',(3.75320257220275,1.15821839929621,-5.96405482568101));
#11930=CARTESIAN_POINT('Ctrl Pts',(3.7590546122738,1.15712343455128,-5.96445693266082));
#11931=CARTESIAN_POINT('Ctrl Pts',(3.7743187940757,1.15414742027536,-5.96551098365056));
#11932=CARTESIAN_POINT('Ctrl Pts',(3.78371652530272,1.15219563059152,-5.96616513241124));
#11933=CARTESIAN_POINT('Ctrl Pts',(3.82675803935259,1.14270622793917,-5.96918579055234));
#11934=CARTESIAN_POINT('Ctrl Pts',(3.86008146848052,1.13380910050893,-5.97159463617168));
#11935=CARTESIAN_POINT('Ctrl Pts',(3.95727721363896,1.10323104992977,-5.97883453960332));
#11936=CARTESIAN_POINT('Ctrl Pts',(4.01972795658668,1.07751481677913,-5.98377480776373));
#11937=CARTESIAN_POINT('Ctrl Pts',(4.08678927887574,1.04290713118811,-5.98931248482588));
#11938=CARTESIAN_POINT('Ctrl Pts',(4.09391153456015,1.03913856710895,-5.98990356147036));
#11939=CARTESIAN_POINT('Ctrl Pts',(4.15011244382659,1.00865897608824,-5.99458904261567));
#11940=CARTESIAN_POINT('Ctrl Pts',(4.19727845647524,0.978555705884622,-5.99865502741021));
#11941=CARTESIAN_POINT('Ctrl Pts',(4.24729721532134,0.941374811239059,-6.00299203176129));
#11942=CARTESIAN_POINT('Ctrl Pts',(4.25242991902042,0.937493767429404,-6.00343734647252));
#11943=CARTESIAN_POINT('Ctrl Pts',(4.26065100879718,0.931170906272169,-6.0041507128686));
#11944=CARTESIAN_POINT('Ctrl Pts',(4.26375932641686,0.928755393972669,-6.00442045392978));
#11945=CARTESIAN_POINT('Ctrl Pts',(4.26925331145728,0.924441596151063,-6.00489718061023));
#11946=CARTESIAN_POINT('Ctrl Pts',(4.27164378230166,0.922549583568344,-6.00510458813698));
#11947=CARTESIAN_POINT('Ctrl Pts',(4.27682093511297,0.918419168113932,-6.00555372542975));
#11948=CARTESIAN_POINT('Ctrl Pts',(4.27960478858504,0.916177351033183,-6.00579521108816));
#11949=CARTESIAN_POINT('Ctrl Pts',(4.28745901458286,0.90979323942721,-6.00647659886485));
#11950=CARTESIAN_POINT('Ctrl Pts',(4.2925052098444,0.905621210585541,-6.00691446374079));
#11951=CARTESIAN_POINT('Ctrl Pts',(4.32616402126353,0.877317361924188,-6.00983770837115));
#11952=CARTESIAN_POINT('Ctrl Pts',(4.35365017138381,0.851872764363065,-6.01223797092243));
#11953=CARTESIAN_POINT('Ctrl Pts',(4.41676399519084,0.787596195246808,-6.01791612874001));
#11954=CARTESIAN_POINT('Ctrl Pts',(4.4510890804904,0.747600828657859,-6.02114961614977));
#11955=CARTESIAN_POINT('Ctrl Pts',(4.52638143105319,0.646942469589884,-6.02893706756474));
#11956=CARTESIAN_POINT('Ctrl Pts',(4.56459512533909,0.584507375386231,-6.03350763673975));
#11957=CARTESIAN_POINT('Ctrl Pts',(4.60138332518485,0.509557236070088,-6.03898648710132));
#11958=CARTESIAN_POINT('Ctrl Pts',(4.60586361685565,0.500113556196835,-6.03967640651002));
#11959=CARTESIAN_POINT('Ctrl Pts',(4.61302673722192,0.484480946207145,-6.04081846159462));
#11960=CARTESIAN_POINT('Ctrl Pts',(4.61578320737482,0.478326250733105,-6.04126809613255));
#11961=CARTESIAN_POINT('Ctrl Pts',(4.62066294234223,0.467174933498236,-6.04208292425452));
#11962=CARTESIAN_POINT('Ctrl Pts',(4.62280481904,0.462186623940911,-6.0424474786049));
#11963=CARTESIAN_POINT('Ctrl Pts',(4.62732173268691,0.451463087436911,-6.04323138738794));
#11964=CARTESIAN_POINT('Ctrl Pts',(4.62968605796868,0.445723555549147,-6.04365108733417));
#11965=CARTESIAN_POINT('Ctrl Pts',(4.63602608564814,0.429980532021151,-6.04480278948988));
#11966=CARTESIAN_POINT('Ctrl Pts',(4.63991010525876,0.419941006948005,-6.04553780054602));
#11967=CARTESIAN_POINT('Ctrl Pts',(4.66172987062527,0.361158501535252,-6.04984582608918));
#11968=CARTESIAN_POINT('Ctrl Pts',(4.67656069430446,0.311331854197686,-6.05351902030705));
#11969=CARTESIAN_POINT('Ctrl Pts',(4.70440071669947,0.188678151739639,-6.06259990435234));
#11970=CARTESIAN_POINT('Ctrl Pts',(4.71393687725998,0.11528430726658,-6.06807243452782));
#11971=CARTESIAN_POINT('Ctrl Pts',(4.71710910509289,0.0252881591905452,
-6.07461937195196));
#11972=CARTESIAN_POINT('Ctrl Pts',(4.71734563529417,0.00907752200102984,
-6.07579156722361));
#11973=CARTESIAN_POINT('Ctrl Pts',(4.71710481213331,-0.0306826391398403,
-6.07864231504494));
#11974=CARTESIAN_POINT('Ctrl Pts',(4.71625587545994,-0.0542243082636352,
-6.08030933238487));
#11975=CARTESIAN_POINT('Ctrl Pts',(4.71430359219265,-0.0837417753592146,
-6.08236105018067));
#11976=CARTESIAN_POINT('Ctrl Pts',(4.71385955155349,-0.0897540851022286,
-6.08277694316532));
#11977=CARTESIAN_POINT('Ctrl Pts',(4.71308787211326,-0.0992132425788758,
-6.08342782248112));
#11978=CARTESIAN_POINT('Ctrl Pts',(4.71279117487023,-0.102662405591984,
-6.08366443550864));
#11979=CARTESIAN_POINT('Ctrl Pts',(4.7122027868054,-0.109166543400187,-6.08410919525693));
#11980=CARTESIAN_POINT('Ctrl Pts',(4.71191436689844,-0.112221664211276,
-6.08431750593605));
#11981=CARTESIAN_POINT('Ctrl Pts',(4.71121086989207,-0.119374647054153,
-6.08480386463247));
#11982=CARTESIAN_POINT('Ctrl Pts',(4.7107862340634,-0.123471502678084,-6.08508138397478));
#11983=CARTESIAN_POINT('Ctrl Pts',(4.70932980611231,-0.136838817368064,
-6.08598372569516));
#11984=CARTESIAN_POINT('Ctrl Pts',(4.70820934469925,-0.146099539736795,
-6.08660389932088));
#11985=CARTESIAN_POINT('Ctrl Pts',(4.70142462970588,-0.197088081499661,
-6.08999597737722));
#11986=CARTESIAN_POINT('Ctrl Pts',(4.6936349970882,-0.238506708506432,-6.09266850379989));
#11987=CARTESIAN_POINT('Ctrl Pts',(4.68106826005522,-0.289962352409489,
-6.09598177255176));
#11988=CARTESIAN_POINT('Ctrl Pts',(4.67834877505836,-0.300465685335471,
-6.09665768602606));
#11989=CARTESIAN_POINT('Ctrl Pts',(4.65041839586667,-0.402507750322544,
-6.10323249202609));
#11990=CARTESIAN_POINT('Ctrl Pts',(4.61437356907952,-0.490709926578817,
-6.10901415270714));
#11991=CARTESIAN_POINT('Ctrl Pts',(4.55920521722374,-0.589636496441019,
-6.1163580264285));
#11992=CARTESIAN_POINT('Ctrl Pts',(4.54990507022347,-0.605434644556412,
-6.1175580596317));
#11993=CARTESIAN_POINT('Ctrl Pts',(4.53650506174603,-0.627028022809492,
-6.11923999862852));
#11994=CARTESIAN_POINT('Ctrl Pts',(4.53271552115075,-0.633013439868542,
-6.11971076099428));
#11995=CARTESIAN_POINT('Ctrl Pts',(4.52608253361021,-0.643283761225334,
-6.12052663031118));
#11996=CARTESIAN_POINT('Ctrl Pts',(4.5232645648998,-0.647584948203317,-6.12087079920097));
#11997=CARTESIAN_POINT('Ctrl Pts',(4.51736269007792,-0.656465811604456,
-6.1215866744195));
#11998=CARTESIAN_POINT('Ctrl Pts',(4.51427457170972,-0.661042523108681,
-6.12195853088882));
#11999=CARTESIAN_POINT('Ctrl Pts',(4.50693567913406,-0.671755799496713,
-6.12283601105967));
#12000=CARTESIAN_POINT('Ctrl Pts',(4.50265855611122,-0.677873937988855,
-6.12334261337593));
#12001=CARTESIAN_POINT('Ctrl Pts',(4.48830816062349,-0.697991208772863,
-6.12502696731538));
#12002=CARTESIAN_POINT('Ctrl Pts',(4.47798597202029,-0.711809163839903,
-6.12621409714304));
#12003=CARTESIAN_POINT('Ctrl Pts',(4.45259460187782,-0.744287017379406,
-6.12907918687214));
#12004=CARTESIAN_POINT('Ctrl Pts',(4.43725202505627,-0.762722424332887,
-6.13076716461647));
#12005=CARTESIAN_POINT('Ctrl Pts',(4.3786865913866,-0.828877042952145,-6.13705658888953));
#12006=CARTESIAN_POINT('Ctrl Pts',(4.33213858664354,-0.873494133910334,
-6.14177251505145));
#12007=CARTESIAN_POINT('Ctrl Pts',(4.23542319709147,-0.952072742278277,
-6.15091740595427));
#12008=CARTESIAN_POINT('Ctrl Pts',(4.1858107260038,-0.986424659151665,-6.15533038276007));
#12009=CARTESIAN_POINT('Ctrl Pts',(4.12512835546305,-1.02188907604602,-6.16025918078904));
#12010=CARTESIAN_POINT('Ctrl Pts',(4.1164094273622,-1.02683642879581,-6.16095662195275));
#12011=CARTESIAN_POINT('Ctrl Pts',(4.10417747106957,-1.03357217812863,-6.1619191413475));
#12012=CARTESIAN_POINT('Ctrl Pts',(4.10071732519429,-1.03545500960532,-6.16218966244169));
#12013=CARTESIAN_POINT('Ctrl Pts',(4.09473149177945,-1.03867336986333,-6.16265454515327));
#12014=CARTESIAN_POINT('Ctrl Pts',(4.09221029877305,-1.04001711944647,-6.16284940762528));
#12015=CARTESIAN_POINT('Ctrl Pts',(4.08688048340478,-1.04283295842484,-6.16325932263553));
#12016=CARTESIAN_POINT('Ctrl Pts',(4.0840707599462,-1.04430290317715,-6.1634742349395));
#12017=CARTESIAN_POINT('Ctrl Pts',(4.08022727770696,-1.04629394310005,-6.16376665336777));
#12018=CARTESIAN_POINT('Ctrl Pts',(4.07919866498243,-1.04682487363855,-6.1638447594958));
#12019=CARTESIAN_POINT('Ctrl Pts',(4.07816926754759,-1.04735428871591,-6.16392277459278));
#12020=CARTESIAN_POINT('Origin',(3.53951905042299,8.32667268468867E-16,
0.924367114736157));
#12021=CARTESIAN_POINT('',(4.0781692678987,-1.04735428853534,-6.76206729648848));
#12022=CARTESIAN_POINT('',(4.07816925191529,-1.04735429675555,-6.66223230003384));
#12023=CARTESIAN_POINT('',(4.07816926754759,-1.04735428871592,0.924367114736157));
#12024=CARTESIAN_POINT('Ctrl Pts',(4.0781692678987,-1.04735428853534,-6.76206729648848));
#12025=CARTESIAN_POINT('Ctrl Pts',(4.12294586906839,-1.02432585754318,-6.75891221404368));
#12026=CARTESIAN_POINT('Ctrl Pts',(4.16619577612126,-0.998451771647165,
-6.75570421536983));
#12027=CARTESIAN_POINT('Ctrl Pts',(4.21650939873315,-0.963791849091696,
-6.75168804733695));
#12028=CARTESIAN_POINT('Ctrl Pts',(4.22527931040189,-0.95757167534045,-6.75097700677152));
#12029=CARTESIAN_POINT('Ctrl Pts',(4.23897441162349,-0.947573620149851,
-6.74984844905781));
#12030=CARTESIAN_POINT('Ctrl Pts',(4.2439571426804,-0.94387527756948,-6.74943396220505));
#12031=CARTESIAN_POINT('Ctrl Pts',(4.25324476262864,-0.936867202031728,
-6.74865392619116));
#12032=CARTESIAN_POINT('Ctrl Pts',(4.25755645574725,-0.933566724648117,
-6.74828874172827));
#12033=CARTESIAN_POINT('Ctrl Pts',(4.2671759881112,-0.926097185242173,-6.74746701256643));
#12034=CARTESIAN_POINT('Ctrl Pts',(4.27247108641371,-0.921912102717862,
-6.74700984792915));
#12035=CARTESIAN_POINT('Ctrl Pts',(4.28588694809413,-0.911119981172702,
-6.74583895582923));
#12036=CARTESIAN_POINT('Ctrl Pts',(4.29395597890684,-0.9044498700557,-6.74512274566076));
#12037=CARTESIAN_POINT('Ctrl Pts',(4.35758061023219,-0.850411922128031,
-6.73937745305371));
#12038=CARTESIAN_POINT('Ctrl Pts',(4.40870126635017,-0.798087647356966,
-6.73414201789298));
#12039=CARTESIAN_POINT('Ctrl Pts',(4.48776191431729,-0.700498792080305,
-6.72496198139348));
#12040=CARTESIAN_POINT('Ctrl Pts',(4.51810399235955,-0.657445553258234,
-6.72107918119728));
#12041=CARTESIAN_POINT('Ctrl Pts',(4.56495733416495,-0.580496367214681,
-6.71453537548096));
#12042=CARTESIAN_POINT('Ctrl Pts',(4.58291176170722,-0.547569142183366,
-6.71184874296286));
#12043=CARTESIAN_POINT('Ctrl Pts',(4.60212436928633,-0.507944779302869,
-6.7087895550371));
#12044=CARTESIAN_POINT('Ctrl Pts',(4.60493284229168,-0.502027309524509,
-6.7083371273702));
#12045=CARTESIAN_POINT('Ctrl Pts',(4.60919777314104,-0.49284406669514,-6.7076421719171));
#12046=CARTESIAN_POINT('Ctrl Pts',(4.61068891838061,-0.489594688234796,
-6.70739764512554));
#12047=CARTESIAN_POINT('Ctrl Pts',(4.61342435445102,-0.483561534248623,
-6.70694623921899));
#12048=CARTESIAN_POINT('Ctrl Pts',(4.61467262886655,-0.480779723499948,
-6.70673913169493));
#12049=CARTESIAN_POINT('Ctrl Pts',(4.6175078359082,-0.474395128736488,-6.706266119389));
#12050=CARTESIAN_POINT('Ctrl Pts',(4.61908752028132,-0.470789209529827,
-6.70600064993203));
#12051=CARTESIAN_POINT('Ctrl Pts',(4.6232013752411,-0.461268989556435,-6.70530401006573));
#12052=CARTESIAN_POINT('Ctrl Pts',(4.62570525320708,-0.455341629173548,
-6.70487456987477));
#12053=CARTESIAN_POINT('Ctrl Pts',(4.64869035976942,-0.399660988058057,
-6.70087782824475));
#12054=CARTESIAN_POINT('Ctrl Pts',(4.66579104353472,-0.348572615305978,
-6.69748732430674));
#12055=CARTESIAN_POINT('Ctrl Pts',(4.68187099567671,-0.286754659145394,
-6.6935126710381));
#12056=CARTESIAN_POINT('Ctrl Pts',(4.68427794973705,-0.276989651486037,
-6.6928885682358));
#12057=CARTESIAN_POINT('Ctrl Pts',(4.70186607582313,-0.201485628112676,
-6.68808434664853));
#12058=CARTESIAN_POINT('Ctrl Pts',(4.71149729214537,-0.13458632785788,-6.68394369326068));
#12059=CARTESIAN_POINT('Ctrl Pts',(4.71665378599857,-0.04440392623186,-6.67820207065805));
#12060=CARTESIAN_POINT('Ctrl Pts',(4.71729392926832,-0.0215436977117833,
-6.67673391753122));
#12061=CARTESIAN_POINT('Ctrl Pts',(4.71724967130154,0.017955038036478,-6.67416473365664));
#12062=CARTESIAN_POINT('Ctrl Pts',(4.71687858043912,0.0345874428860701,
-6.67307297279306));
#12063=CARTESIAN_POINT('Ctrl Pts',(4.71583536023531,0.0585591735798976,
-6.67148258549858));
#12064=CARTESIAN_POINT('Ctrl Pts',(4.7154464293154,0.0659092786016217,-6.67099266275923));
#12065=CARTESIAN_POINT('Ctrl Pts',(4.71464623374949,0.0787494128198078,
-6.67013258806341));
#12066=CARTESIAN_POINT('Ctrl Pts',(4.7142653177287,0.0842411580578814,-6.66976338404987));
#12067=CARTESIAN_POINT('Ctrl Pts',(4.71345193211751,0.0948862163823833,
-6.66904502432509));
#12068=CARTESIAN_POINT('Ctrl Pts',(4.71302399302121,0.100039757154611,-6.66869601721195));
#12069=CARTESIAN_POINT('Ctrl Pts',(4.71179161219089,0.113782817097294,-6.66776193904133));
#12070=CARTESIAN_POINT('Ctrl Pts',(4.71092672101904,0.122366461682962,-6.66717500962747));
#12071=CARTESIAN_POINT('Ctrl Pts',(4.70738854419239,0.153993661534007,-6.66499895785164));
#12072=CARTESIAN_POINT('Ctrl Pts',(4.7041290633129,0.176964937351188,-6.66339191204045));
#12073=CARTESIAN_POINT('Ctrl Pts',(4.6830111624516,0.299628145184901,-6.65466181449661));
#12074=CARTESIAN_POINT('Ctrl Pts',(4.65302867038665,0.396788144129833,-6.64716430093981));
#12075=CARTESIAN_POINT('Ctrl Pts',(4.59855957454331,0.516165541995005,-6.63759317243328));
#12076=CARTESIAN_POINT('Ctrl Pts',(4.58507819413828,0.542954894142923,-6.63542399616074));
#12077=CARTESIAN_POINT('Ctrl Pts',(4.56236899977718,0.5840909832043,-6.6320874458712));
#12078=CARTESIAN_POINT('Ctrl Pts',(4.55382757857985,0.598800951631323,-6.63089319504041));
#12079=CARTESIAN_POINT('Ctrl Pts',(4.54226982419969,0.617748195805423,-6.62935832582027));
#12080=CARTESIAN_POINT('Ctrl Pts',(4.53954038234611,0.622156962455123,-6.62900142903356));
#12081=CARTESIAN_POINT('Ctrl Pts',(4.53503904824843,0.629321641736402,-6.6284220202326));
#12082=CARTESIAN_POINT('Ctrl Pts',(4.53328465282591,0.632088382250458,-6.62819841683938));
#12083=CARTESIAN_POINT('Ctrl Pts',(4.52984123477872,0.637468993913774,-6.62776389981318));
#12084=CARTESIAN_POINT('Ctrl Pts',(4.52815336676141,0.640083538228561,-6.62755291922081));
#12085=CARTESIAN_POINT('Ctrl Pts',(4.52396766556247,0.646511225999585,-6.62703455435523));
#12086=CARTESIAN_POINT('Ctrl Pts',(4.52145798528301,0.650316669868127,-6.6267279379496));
#12087=CARTESIAN_POINT('Ctrl Pts',(4.51411031837267,0.661318466055091,-6.62584199477558));
#12088=CARTESIAN_POINT('Ctrl Pts',(4.50921475402004,0.668476256990736,-6.62526623099818));
#12089=CARTESIAN_POINT('Ctrl Pts',(4.45923985469752,0.73983994907711,-6.61952512930229));
#12090=CARTESIAN_POINT('Ctrl Pts',(4.40792444146934,0.799453061407792,-6.61471497310608));
#12091=CARTESIAN_POINT('Ctrl Pts',(4.31189842067517,0.890754946157779,-6.60651656530318));
#12092=CARTESIAN_POINT('Ctrl Pts',(4.2702293474513,0.925243808395323,-6.60316360161088));
#12093=CARTESIAN_POINT('Ctrl Pts',(4.2099434283504,0.968521427195858,-6.59842486884806));
#12094=CARTESIAN_POINT('Ctrl Pts',(4.19324476206694,0.979870004192287,-6.59712358152529));
#12095=CARTESIAN_POINT('Ctrl Pts',(4.16354265234985,0.998958586717111,-6.59482135233132));
#12096=CARTESIAN_POINT('Ctrl Pts',(4.15066614736092,1.00688773247659,-6.59382721394972));
#12097=CARTESIAN_POINT('Ctrl Pts',(4.13153525485413,1.01816605391762,-6.59235397927314));
#12098=CARTESIAN_POINT('Ctrl Pts',(4.12539723719483,1.02171035340222,-6.59188186529944));
#12099=CARTESIAN_POINT('Ctrl Pts',(4.11447001498192,1.02788925676774,-6.59104218174043));
#12100=CARTESIAN_POINT('Ctrl Pts',(4.1096937173476,1.03054635184734,-6.59067542247206));
#12101=CARTESIAN_POINT('Ctrl Pts',(4.09963200215845,1.03605240924621,-6.5899032766969));
#12102=CARTESIAN_POINT('Ctrl Pts',(4.09434296012218,1.03889438362657,-6.5894976577528));
#12103=CARTESIAN_POINT('Ctrl Pts',(4.08034016452336,1.04628111296678,-6.58842434770627));
#12104=CARTESIAN_POINT('Ctrl Pts',(4.07159101124071,1.0507573759761,-6.58775430185985));
#12105=CARTESIAN_POINT('Ctrl Pts',(4.03310034540623,1.06984607512761,-6.58480828238663));
#12106=CARTESIAN_POINT('Ctrl Pts',(4.00280828435494,1.08330781952285,-6.58249369995613));
#12107=CARTESIAN_POINT('Ctrl Pts',(3.87750347885602,1.13277580274728,-6.57292938312651));
#12108=CARTESIAN_POINT('Ctrl Pts',(3.77859010214468,1.15769365587022,-6.56535491917215));
#12109=CARTESIAN_POINT('Ctrl Pts',(3.65628269370855,1.17214665872541,-6.55644810478756));
#12110=CARTESIAN_POINT('Ctrl Pts',(3.6347668743395,1.174090926378,-6.55490026791335));
#12111=CARTESIAN_POINT('Ctrl Pts',(3.59968418005628,1.17629029007599,-6.55241888923025));
#12112=CARTESIAN_POINT('Ctrl Pts',(3.58614546742989,1.17690471403828,-6.55147156906534));
#12113=CARTESIAN_POINT('Ctrl Pts',(3.56783069258954,1.17741932335509,-6.55020651238288));
#12114=CARTESIAN_POINT('Ctrl Pts',(3.56306204764912,1.17752432728116,-6.54987863483975));
#12115=CARTESIAN_POINT('Ctrl Pts',(3.55510717961657,1.17765114675324,-6.54933433922799));
#12116=CARTESIAN_POINT('Ctrl Pts',(3.55192131552593,1.1776890072353,-6.54911706366381));
#12117=CARTESIAN_POINT('Ctrl Pts',(3.5458902695692,1.17773620333583,-6.5487071410676));
#12118=CARTESIAN_POINT('Ctrl Pts',(3.54304514911707,1.17774815820159,-6.54851434771193));
#12119=CARTESIAN_POINT('Ctrl Pts',(3.53630889816459,1.17775205281308,-6.54805920848759));
#12120=CARTESIAN_POINT('Ctrl Pts',(3.5324177656834,1.17773501935053,-6.54779735067951));
#12121=CARTESIAN_POINT('Ctrl Pts',(3.51879198047609,1.17760783985833,-6.54688383948954));
#12122=CARTESIAN_POINT('Ctrl Pts',(3.50905835341731,1.17739627861934,-6.54623743631779));
#12123=CARTESIAN_POINT('Ctrl Pts',(3.42752961053978,1.17461247194562,-6.5408664805545));
#12124=CARTESIAN_POINT('Ctrl Pts',(3.35609549585743,1.16559632415304,-6.53643623612184));
#12125=CARTESIAN_POINT('Ctrl Pts',(3.22889658181621,1.1375493782972,-6.52837940305496));
#12126=CARTESIAN_POINT('Ctrl Pts',(3.17289044410174,1.12075319097083,-6.52476924843539));
#12127=CARTESIAN_POINT('Ctrl Pts',(3.09863830059703,1.09232107716451,-6.51970054991633));
#12128=CARTESIAN_POINT('Ctrl Pts',(3.0791213085877,1.08423936982468,-6.51834097168394));
#12129=CARTESIAN_POINT('Ctrl Pts',(3.04553384954998,1.06926087191269,-6.51594509405415));
#12130=CARTESIAN_POINT('Ctrl Pts',(3.03136387318905,1.06259986321686,-6.51491641233245));
#12131=CARTESIAN_POINT('Ctrl Pts',(3.01089022307675,1.05247245375225,-6.51340162254873));
#12132=CARTESIAN_POINT('Ctrl Pts',(3.00447845843092,1.04922746061217,-6.51292308451294));
#12133=CARTESIAN_POINT('Ctrl Pts',(2.99323121308099,1.04340532883207,-6.51207610616659));
#12134=CARTESIAN_POINT('Ctrl Pts',(2.98838322470096,1.0408527183706,-6.51170852554223));
#12135=CARTESIAN_POINT('Ctrl Pts',(2.97830145303762,1.03545418118627,-6.5109387818606));
#12136=CARTESIAN_POINT('Ctrl Pts',(2.97307111160399,1.03260219025089,-6.51053641406549));
#12137=CARTESIAN_POINT('Ctrl Pts',(2.95945825676147,1.02504484930612,-6.50948110177823));
#12138=CARTESIAN_POINT('Ctrl Pts',(2.95111146141057,1.02027641701927,-6.50882594338475));
#12139=CARTESIAN_POINT('Ctrl Pts',(2.91593388254755,0.999604615612054,-6.50602953355273));
#12140=CARTESIAN_POINT('Ctrl Pts',(2.88968428059032,0.98274223900862,-6.50385433175206));
#12141=CARTESIAN_POINT('Ctrl Pts',(2.79606961505231,0.917213840555172,-6.49575955666949));
#12142=CARTESIAN_POINT('Ctrl Pts',(2.73324224909032,0.862503727090912,-6.48963448534913));
#12143=CARTESIAN_POINT('Ctrl Pts',(2.64139842627212,0.763652168008503,-6.47975812700154));
#12144=CARTESIAN_POINT('Ctrl Pts',(2.60863848026168,0.723358789502896,-6.47599596749412));
#12145=CARTESIAN_POINT('Ctrl Pts',(2.57461891572294,0.675359998176562,-6.47190411238623));
#12146=CARTESIAN_POINT('Ctrl Pts',(2.57064893501322,0.669652224952945,-6.47142344757296));
#12147=CARTESIAN_POINT('Ctrl Pts',(2.56466630086488,0.660886205418549,-6.47069462164926));
#12148=CARTESIAN_POINT('Ctrl Pts',(2.56261705816145,0.657853295396841,-6.47044415185961));
#12149=CARTESIAN_POINT('Ctrl Pts',(2.55889062886374,0.65228231258221,-6.46998723979864));
#12150=CARTESIAN_POINT('Ctrl Pts',(2.55720912945023,0.649747286320787,-6.46978052222146));
#12151=CARTESIAN_POINT('Ctrl Pts',(2.55343426346913,0.644008154308815,-6.46931520251178));
#12152=CARTESIAN_POINT('Ctrl Pts',(2.55134668006022,0.640800341263827,-6.46905697927665));
#12153=CARTESIAN_POINT('Ctrl Pts',(2.54598982966767,0.632480489507565,-6.46839188563711));
#12154=CARTESIAN_POINT('Ctrl Pts',(2.54274431714432,0.627353183642247,-6.4679865022697));
#12155=CARTESIAN_POINT('Ctrl Pts',(2.52116884812424,0.592677808128442,-6.46527342525284));
#12156=CARTESIAN_POINT('Ctrl Pts',(2.50411366397944,0.562352482531343,-6.46303882045231));
#12157=CARTESIAN_POINT('Ctrl Pts',(2.47566575099091,0.506074137307548,-6.45905477299111));
#12158=CARTESIAN_POINT('Ctrl Pts',(2.46382022129255,0.480382165825438,-6.45729403121127));
#12159=CARTESIAN_POINT('Ctrl Pts',(2.41817938197563,0.371214106629763,-6.44995815463985));
#12160=CARTESIAN_POINT('Ctrl Pts',(2.39309226439797,0.284440647682221,-6.44444801447752));
#12161=CARTESIAN_POINT('Ctrl Pts',(2.37516021319155,0.178000693229838,-6.43744105101478));
#12162=CARTESIAN_POINT('Ctrl Pts',(2.372588483264,0.160277087697721,-6.43626744441922));
#12163=CARTESIAN_POINT('Ctrl Pts',(2.36950518607273,0.134981569568881,-6.43457949758076));
#12164=CARTESIAN_POINT('Ctrl Pts',(2.36866106878908,0.127452145011255,-6.43407544940521));
#12165=CARTESIAN_POINT('Ctrl Pts',(2.36732553725242,0.114403362164892,-6.43319888259013));
#12166=CARTESIAN_POINT('Ctrl Pts',(2.36680031194586,0.108887649588134,-6.43282742309709));
#12167=CARTESIAN_POINT('Ctrl Pts',(2.36586500703955,0.0982721889372516,
-6.43211063109108));
#12168=CARTESIAN_POINT('Ctrl Pts',(2.36544919904447,0.0931730611882645,
-6.43176548495266));
#12169=CARTESIAN_POINT('Ctrl Pts',(2.36444368903899,0.0797643618219554,
-6.43085560770614));
#12170=CARTESIAN_POINT('Ctrl Pts',(2.36390891320464,0.0714510842384667,
-6.43028919239542));
#12171=CARTESIAN_POINT('Ctrl Pts',(2.36232279813214,0.0419045591124454,
-6.42826751666083));
#12172=CARTESIAN_POINT('Ctrl Pts',(2.36175826511778,0.0206504180033991,
-6.42679745648869));
#12173=CARTESIAN_POINT('Ctrl Pts',(2.36178601530212,-0.0332627310663779,
-6.42302618903627));
#12174=CARTESIAN_POINT('Ctrl Pts',(2.36316104713104,-0.0659017181671396,
-6.42070333263085));
#12175=CARTESIAN_POINT('Ctrl Pts',(2.3701139953061,-0.148797490192785,-6.4147096206495));
#12176=CARTESIAN_POINT('Ctrl Pts',(2.37757443760778,-0.198829105981824,
-6.41100142558572));
#12177=CARTESIAN_POINT('Ctrl Pts',(2.38892298615492,-0.251465217744737,
-6.40705015076198));
#12178=CARTESIAN_POINT('Ctrl Pts',(2.38963557288157,-0.254703841678869,
-6.40680684376538));
#12179=CARTESIAN_POINT('Ctrl Pts',(2.39499021098422,-0.278559525092273,
-6.40501337354838));
#12180=CARTESIAN_POINT('Ctrl Pts',(2.40017285158668,-0.299051748802747,
-6.4034656674151));
#12181=CARTESIAN_POINT('Ctrl Pts',(2.41672368711429,-0.357795136622129,
-6.39902385038681));
#12182=CARTESIAN_POINT('Ctrl Pts',(2.42948874950418,-0.395626364350084,
-6.396156346492));
#12183=CARTESIAN_POINT('Ctrl Pts',(2.4464476069998,-0.438553242663619,-6.39294635308094));
#12184=CARTESIAN_POINT('Ctrl Pts',(2.4487904026558,-0.444348003529411,-6.39251399610978));
#12185=CARTESIAN_POINT('Ctrl Pts',(2.45266290994123,-0.453711209549035,
-6.39181727046263));
#12186=CARTESIAN_POINT('Ctrl Pts',(2.45416429175512,-0.457291133409122,
-6.39155133334197));
#12187=CARTESIAN_POINT('Ctrl Pts',(2.45687489219262,-0.463665785809996,
-6.39107867316813));
#12188=CARTESIAN_POINT('Ctrl Pts',(2.45807727400085,-0.46646330958374,-6.39087155685421));
#12189=CARTESIAN_POINT('Ctrl Pts',(2.46073116170004,-0.47257256271065,-6.39041994338628));
#12190=CARTESIAN_POINT('Ctrl Pts',(2.46218707494057,-0.475882287298432,
-6.39017571299449));
#12191=CARTESIAN_POINT('Ctrl Pts',(2.46640075707148,-0.485342793312489,
-6.3894787041054));
#12192=CARTESIAN_POINT('Ctrl Pts',(2.46919617326328,-0.491476797464264,
-6.38902811287098));
#12193=CARTESIAN_POINT('Ctrl Pts',(2.490228286078,-0.536597084265478,-6.38572111742289));
#12194=CARTESIAN_POINT('Ctrl Pts',(2.51053946217682,-0.574586324232129,
-6.38297757773909));
#12195=CARTESIAN_POINT('Ctrl Pts',(2.58258778816675,-0.693212795286867,
-6.37427492586448));
#12196=CARTESIAN_POINT('Ctrl Pts',(2.64207827258558,-0.768675366373853,
-6.36849427554628));
#12197=CARTESIAN_POINT('Ctrl Pts',(2.73018760142353,-0.856085553219501,
-6.36055546273));
#12198=CARTESIAN_POINT('Ctrl Pts',(2.75104123065136,-0.875329876603424,
-6.35871623235301));
#12199=CARTESIAN_POINT('Ctrl Pts',(2.77962509665173,-0.899857051898429,
-6.35623245344694));
#12200=CARTESIAN_POINT('Ctrl Pts',(2.78675349941669,-0.90582865481419,-6.3556159866354));
#12201=CARTESIAN_POINT('Ctrl Pts',(2.79851063216422,-0.915443209235069,
-6.3546035600282));
#12202=CARTESIAN_POINT('Ctrl Pts',(2.8030973890916,-0.919137029965733,-6.3542096417199));
#12203=CARTESIAN_POINT('Ctrl Pts',(2.81202325033869,-0.926215528558153,
-6.35344498986497));
#12204=CARTESIAN_POINT('Ctrl Pts',(2.81635876113683,-0.92960450661454,-6.35307443936028));
#12205=CARTESIAN_POINT('Ctrl Pts',(2.82653800918138,-0.937447107856184,
-6.3522063321698));
#12206=CARTESIAN_POINT('Ctrl Pts',(2.83239993454968,-0.941876635727669,
-6.35170785711019));
#12207=CARTESIAN_POINT('Ctrl Pts',(2.85160822394215,-0.956110877327952,
-6.35007885200092));
#12208=CARTESIAN_POINT('Ctrl Pts',(2.86511950189476,-0.965688622475829,
-6.34893977284582));
#12209=CARTESIAN_POINT('Ctrl Pts',(2.89764471465889,-0.987729253563438,
-6.34621215992179));
#12210=CARTESIAN_POINT('Ctrl Pts',(2.91682583919942,-0.99993239202549,-6.3446148452297));
#12211=CARTESIAN_POINT('Ctrl Pts',(2.99365118278365,-1.04574118241993,-6.33826062215976));
#12212=CARTESIAN_POINT('Ctrl Pts',(3.05374952649696,-1.07497558071424,-6.33337420040919));
#12213=CARTESIAN_POINT('Ctrl Pts',(3.17211340255953,-1.12059163457256,-6.32406524200008));
#12214=CARTESIAN_POINT('Ctrl Pts',(3.22981535992225,-1.13789173094266,-6.31966017815492));
#12215=CARTESIAN_POINT('Ctrl Pts',(3.29839122572907,-1.1528456256141,-6.31473820249754));
#12216=CARTESIAN_POINT('Ctrl Pts',(3.30821829082806,-1.15485741093623,-6.31404032895314));
#12217=CARTESIAN_POINT('Ctrl Pts',(3.32194048650467,-1.15748440969224,-6.31307728914153));
#12218=CARTESIAN_POINT('Ctrl Pts',(3.32581448173988,-1.15820591804602,-6.31280667312941));
#12219=CARTESIAN_POINT('Ctrl Pts',(3.33250390215438,-1.15941707608936,-6.31234165198646));
#12220=CARTESIAN_POINT('Ctrl Pts',(3.33531759190815,-1.1599159420946,-6.31214674552923));
#12221=CARTESIAN_POINT('Ctrl Pts',(3.34125767146775,-1.16094683128152,-6.31173676536307));
#12222=CARTESIAN_POINT('Ctrl Pts',(3.34438444515803,-1.16147647660685,-6.31152183178914));
#12223=CARTESIAN_POINT('Ctrl Pts',(3.35214903886939,-1.16275948397644,-6.31099017890119));
#12224=CARTESIAN_POINT('Ctrl Pts',(3.35678936272616,-1.16349774469293,-6.310674290318));
#12225=CARTESIAN_POINT('Ctrl Pts',(3.37431124288925,-1.16617800709058,-6.30948800825593));
#12226=CARTESIAN_POINT('Ctrl Pts',(3.38722086290756,-1.16793409941775,-6.3086272489041));
#12227=CARTESIAN_POINT('Ctrl Pts',(3.42045728511714,-1.1718947423068,-6.30643902679408));
#12228=CARTESIAN_POINT('Ctrl Pts',(3.44081773059848,-1.17378496306027,-6.30512514279939));
#12229=CARTESIAN_POINT('Ctrl Pts',(3.51895574897153,-1.17899136380083,-6.30014974112011));
#12230=CARTESIAN_POINT('Ctrl Pts',(3.57690171028414,-1.17857830810527,-6.29659662283391));
#12231=CARTESIAN_POINT('Ctrl Pts',(3.70982666257039,-1.16781366500642,-6.28833912627584));
#12232=CARTESIAN_POINT('Ctrl Pts',(3.78429717843459,-1.15450201305926,-6.28362472168193));
#12233=CARTESIAN_POINT('Ctrl Pts',(3.86698072823359,-1.13135840197258,-6.27798958768884));
#12234=CARTESIAN_POINT('Ctrl Pts',(3.87694700090374,-1.12842605038632,-6.2773038095413));
#12235=CARTESIAN_POINT('Ctrl Pts',(3.89329873998452,-1.12337892924114,-6.27616716589239));
#12236=CARTESIAN_POINT('Ctrl Pts',(3.89970733313321,-1.12134057505243,-6.27571875966038));
#12237=CARTESIAN_POINT('Ctrl Pts',(3.91125648179073,-1.1175579667008,-6.27490519380421));
#12238=CARTESIAN_POINT('Ctrl Pts',(3.91640313818159,-1.11583283224943,-6.27454066372616));
#12239=CARTESIAN_POINT('Ctrl Pts',(3.92742383943521,-1.1120538021081,-6.27375573405896));
#12240=CARTESIAN_POINT('Ctrl Pts',(3.93329387769254,-1.10998881389203,-6.27333498128008));
#12241=CARTESIAN_POINT('Ctrl Pts',(3.94933669339718,-1.10420192789361,-6.27217757825071));
#12242=CARTESIAN_POINT('Ctrl Pts',(3.95947470739659,-1.1003861279767,-6.27143786967141));
#12243=CARTESIAN_POINT('Ctrl Pts',(4.0065789668292,-1.08191102047812,-6.26796096808694));
#12244=CARTESIAN_POINT('Ctrl Pts',(4.04282830591753,-1.06553000843682,-6.26516801523436));
#12245=CARTESIAN_POINT('Ctrl Pts',(4.07816929763934,-1.04735427323984,-6.26232527378825));
#12246=CARTESIAN_POINT('',(2.36176890518371,-0.00054653709837472,-6.32657240471885));
#12247=CARTESIAN_POINT('Ctrl Pts',(4.07816926754759,-1.04735428871591,-6.16392277459278));
#12248=CARTESIAN_POINT('Ctrl Pts',(4.07502013789745,-1.04897387378667,-6.1641614381514));
#12249=CARTESIAN_POINT('Ctrl Pts',(4.07186366438915,-1.05057927613111,-6.16439924977879));
#12250=CARTESIAN_POINT('Ctrl Pts',(4.0570580046211,-1.05802566685627,-6.16550837055927));
#12251=CARTESIAN_POINT('Ctrl Pts',(4.04531909202946,-1.06368756380594,-6.16636942124603));
#12252=CARTESIAN_POINT('Ctrl Pts',(4.01492007998935,-1.07773247480256,-6.16855861305748));
#12253=CARTESIAN_POINT('Ctrl Pts',(3.99613067491405,-1.08582657441588,-6.16987315913917));
#12254=CARTESIAN_POINT('Ctrl Pts',(3.92342637088474,-1.11492484038397,-6.17484845673189));
#12255=CARTESIAN_POINT('Ctrl Pts',(3.86819965788022,-1.1324363532321,-6.17840090965472));
#12256=CARTESIAN_POINT('Ctrl Pts',(3.7384689278029,-1.16327636420832,-6.18665754403061));
#12257=CARTESIAN_POINT('Ctrl Pts',(3.66353338008815,-1.17363162470285,-6.19137176861899));
#12258=CARTESIAN_POINT('Ctrl Pts',(3.57774927867308,-1.17717518350043,-6.19700663723372));
#12259=CARTESIAN_POINT('Ctrl Pts',(3.56736567510591,-1.17746656738353,-6.1976923493616));
#12260=CARTESIAN_POINT('Ctrl Pts',(3.55025649072845,-1.17772024828522,-6.19882886956093));
#12261=CARTESIAN_POINT('Ctrl Pts',(3.54353253230921,-1.17776235491761,-6.19927721873989));
#12262=CARTESIAN_POINT('Ctrl Pts',(3.53138144657797,-1.17773439157945,-6.20009067093989));
#12263=CARTESIAN_POINT('Ctrl Pts',(3.52595442626198,-1.17768438768315,-6.2004551445162));
#12264=CARTESIAN_POINT('Ctrl Pts',(3.51430729473924,-1.17749655514891,-6.20123994056512));
#12265=CARTESIAN_POINT('Ctrl Pts',(3.50808756542951,-1.1773469451269,-6.20166061603618));
#12266=CARTESIAN_POINT('Ctrl Pts',(3.49104525481154,-1.17680186774773,-6.20281777272555));
#12267=CARTESIAN_POINT('Ctrl Pts',(3.48022671040027,-1.17630640125359,-6.20355731075585));
#12268=CARTESIAN_POINT('Ctrl Pts',(3.41619802949826,-1.17248850754873,-6.20796492500688));
#12269=CARTESIAN_POINT('Ctrl Pts',(3.3632639245627,-1.16570580990916,-6.21173883281912));
#12270=CARTESIAN_POINT('Ctrl Pts',(3.26388767797339,-1.14604826522759,-6.21906038791314));
#12271=CARTESIAN_POINT('Ctrl Pts',(3.21741347877128,-1.13386368021226,-6.22258574633196));
#12272=CARTESIAN_POINT('Ctrl Pts',(3.1171739077486,-1.10092131694876,-6.2303271628749));
#12273=CARTESIAN_POINT('Ctrl Pts',(3.06391587788669,-1.07898384278524,-6.23453235367495));
#12274=CARTESIAN_POINT('Ctrl Pts',(3.00353542697245,-1.04876900699087,-6.2392667417903));
#12275=CARTESIAN_POINT('Ctrl Pts',(2.99465789381907,-1.04418447178372,-6.23996182432005));
#12276=CARTESIAN_POINT('Ctrl Pts',(2.98236758599149,-1.03763807830931,-6.24092163763437));
#12277=CARTESIAN_POINT('Ctrl Pts',(2.97890497847574,-1.03577140302298,-6.24119177265377));
#12278=CARTESIAN_POINT('Ctrl Pts',(2.97294504273734,-1.03251978678107,-6.24165617245326));
#12279=CARTESIAN_POINT('Ctrl Pts',(2.97044330640134,-1.03114306198956,-6.24185093573545));
#12280=CARTESIAN_POINT('Ctrl Pts',(2.96522844310817,-1.0282485231014,-6.24225651899175));
#12281=CARTESIAN_POINT('Ctrl Pts',(2.96251627435219,-1.02672904104821,-6.24246722634055));
#12282=CARTESIAN_POINT('Ctrl Pts',(2.95585386489402,-1.02296171498635,-6.24298433774796));
#12283=CARTESIAN_POINT('Ctrl Pts',(2.95191050791039,-1.02070168099378,-6.2432899815758));
#12284=CARTESIAN_POINT('Ctrl Pts',(2.94340110036748,-1.01575907333391,-6.2439488309938));
#12285=CARTESIAN_POINT('Ctrl Pts',(2.93883983768375,-1.01306840405904,-6.24430154955885));
#12286=CARTESIAN_POINT('Ctrl Pts',(2.92591943657737,-1.00532877153501,-6.2452998697766));
#12287=CARTESIAN_POINT('Ctrl Pts',(2.91760452837382,-1.00020636171451,-6.24594137364636));
#12288=CARTESIAN_POINT('Ctrl Pts',(2.8179306268496,-0.937078510063803,-6.25363173075393));
#12289=CARTESIAN_POINT('Ctrl Pts',(2.73491309237749,-0.866845794405199,
-6.26008252479646));
#12290=CARTESIAN_POINT('Ctrl Pts',(2.63247693962192,-0.752603676590605,
-6.26973223623096));
#12291=CARTESIAN_POINT('Ctrl Pts',(2.60427004674549,-0.717249100912236,
-6.27262167856772));
#12292=CARTESIAN_POINT('Ctrl Pts',(2.5720154942144,-0.671673499634032,-6.27629178582774));
#12293=CARTESIAN_POINT('Ctrl Pts',(2.56598321513033,-0.662899982391096,
-6.27699583340061));
#12294=CARTESIAN_POINT('Ctrl Pts',(2.55660376281455,-0.648854050060129,
-6.27811976698117));
#12295=CARTESIAN_POINT('Ctrl Pts',(2.55317805315021,-0.643634582245182,
-6.27853672982177));
#12296=CARTESIAN_POINT('Ctrl Pts',(2.54685336424678,-0.633829102451121,
-6.27931890025064));
#12297=CARTESIAN_POINT('Ctrl Pts',(2.54394424947677,-0.629249799094225,
-6.27968372255175));
#12298=CARTESIAN_POINT('Ctrl Pts',(2.53751628278764,-0.618975228331711,
-6.28050133526381));
#12299=CARTESIAN_POINT('Ctrl Pts',(2.53401416656813,-0.613269765260091,
-6.2809547188123));
#12300=CARTESIAN_POINT('Ctrl Pts',(2.52380769317362,-0.596319455365579,
-6.28229999308776));
#12301=CARTESIAN_POINT('Ctrl Pts',(2.51724216183954,-0.58499264371845,-6.28319680468622));
#12302=CARTESIAN_POINT('Ctrl Pts',(2.47459868707184,-0.508513525002157,
-6.28924015643022));
#12303=CARTESIAN_POINT('Ctrl Pts',(2.44458810527291,-0.440186269604555,
-6.29459813975347));
#12304=CARTESIAN_POINT('Ctrl Pts',(2.40233468674374,-0.31230534810237,-6.30445551052623));
#12305=CARTESIAN_POINT('Ctrl Pts',(2.38785279992235,-0.253748219962056,
-6.30890480807214));
#12306=CARTESIAN_POINT('Ctrl Pts',(2.37391599007045,-0.170444927584836,
-6.31498108973219));
#12307=CARTESIAN_POINT('Ctrl Pts',(2.37065634078007,-0.146431277923936,
-6.31670307685991));
#12308=CARTESIAN_POINT('Ctrl Pts',(2.36736115857779,-0.114878645864958,
-6.31891342905543));
#12309=CARTESIAN_POINT('Ctrl Pts',(2.36665386830848,-0.107417403179678,
-6.31943229790962));
#12310=CARTESIAN_POINT('Ctrl Pts',(2.36569356785916,-0.0961425922919509,
-6.32021012063123));
#12311=CARTESIAN_POINT('Ctrl Pts',(2.36538783238512,-0.0923338802041197,
-6.3204717998406));
#12312=CARTESIAN_POINT('Ctrl Pts',(2.36488616062744,-0.0856783441053184,
-6.32092711679869));
#12313=CARTESIAN_POINT('Ctrl Pts',(2.36468202953945,-0.0828322363160884,
-6.32112119594855));
#12314=CARTESIAN_POINT('Ctrl Pts',(2.36429238112494,-0.0771080744679768,
-6.32151026492637));
#12315=CARTESIAN_POINT('Ctrl Pts',(2.36410709099576,-0.0742300846150639,
-6.3217052432612));
#12316=CARTESIAN_POINT('Ctrl Pts',(2.36371711101524,-0.0678047693212115,
-6.32213918163124));
#12317=CARTESIAN_POINT('Ctrl Pts',(2.363517897987,-0.0642571219988517,-6.32237784686789));
#12318=CARTESIAN_POINT('Ctrl Pts',(2.36292394846307,-0.0527497829958561,
-6.3231491442723));
#12319=CARTESIAN_POINT('Ctrl Pts',(2.36259393512665,-0.0447867705160469,
-6.32367845805451));
#12320=CARTESIAN_POINT('Ctrl Pts',(2.361966673931,-0.0247329843330736,-6.32500172323627));
#12321=CARTESIAN_POINT('Ctrl Pts',(2.36177477434794,-0.0126396599709577,
-6.32579080616873));
#12322=CARTESIAN_POINT('Ctrl Pts',(2.36176917656931,-0.000545103328149681,
-6.3265729688034));
#12323=CARTESIAN_POINT('Ctrl Pts',(2.36176917724781,-0.000546567323186017,
-6.32657287412589));
#12324=CARTESIAN_POINT('Ctrl Pts',(2.36171530663473,0.115534480745993,-6.33407991441413));
#12325=CARTESIAN_POINT('Ctrl Pts',(2.37882206593073,0.231003657072712,-6.34096235474007));
#12326=CARTESIAN_POINT('Ctrl Pts',(2.4225690790897,0.375108283706817,-6.35053505199396));
#12327=CARTESIAN_POINT('Ctrl Pts',(2.43402570898826,0.407636583637145,-6.35275989632741));
#12328=CARTESIAN_POINT('Ctrl Pts',(2.4504739962544,0.448517614569015,-6.35566381326407));
#12329=CARTESIAN_POINT('Ctrl Pts',(2.45416514963681,0.45737739523965,-6.3562997502674));
#12330=CARTESIAN_POINT('Ctrl Pts',(2.46032068289413,0.47165812891405,-6.35733601523052));
#12331=CARTESIAN_POINT('Ctrl Pts',(2.46271866441086,0.477107360591116,-6.35773411071914));
#12332=CARTESIAN_POINT('Ctrl Pts',(2.46740263227201,0.487536119556301,-6.35850126305974));
#12333=CARTESIAN_POINT('Ctrl Pts',(2.46968225968352,0.492518346237845,-6.35887009660498));
#12334=CARTESIAN_POINT('Ctrl Pts',(2.47498299868598,0.503892889987843,-6.35971761078906));
#12335=CARTESIAN_POINT('Ctrl Pts',(2.47802705005049,0.510274219808296,-6.36019706385215));
#12336=CARTESIAN_POINT('Ctrl Pts',(2.4879037618546,0.530508174631676,-6.3617302850166));
#12337=CARTESIAN_POINT('Ctrl Pts',(2.49495131712421,0.544253479370657,-6.3627913776444));
#12338=CARTESIAN_POINT('Ctrl Pts',(2.5402995277526,0.628571939037131,-6.36942590602651));
#12339=CARTESIAN_POINT('Ctrl Pts',(2.58545749323482,0.695201083181851,-6.37524264991213));
#12340=CARTESIAN_POINT('Ctrl Pts',(2.66651818748641,0.791878135940975,-6.38449679129754));
#12341=CARTESIAN_POINT('Ctrl Pts',(2.69803786179309,0.825294592956751,-6.3878737559664));
#12342=CARTESIAN_POINT('Ctrl Pts',(2.74670532572128,0.871195998023929,-6.39270801840454));
#12343=CARTESIAN_POINT('Ctrl Pts',(2.7623660740988,0.885194569736173,-6.39421180341642));
#12344=CARTESIAN_POINT('Ctrl Pts',(2.78527100251953,0.904591710158034,-6.39632950736209));
#12345=CARTESIAN_POINT('Ctrl Pts',(2.792215177414,0.910336867578443,-6.39696124695351));
#12346=CARTESIAN_POINT('Ctrl Pts',(2.80312101522292,0.919150744606068,-6.39793666402185));
#12347=CARTESIAN_POINT('Ctrl Pts',(2.8070373148256,0.922274724105697,-6.39828364584724));
#12348=CARTESIAN_POINT('Ctrl Pts',(2.81431192422147,0.928002014933254,-6.39892193742269));
#12349=CARTESIAN_POINT('Ctrl Pts',(2.81766460111428,0.930612309732869,-6.39921369493215));
#12350=CARTESIAN_POINT('Ctrl Pts',(2.82346167656667,0.935075562273203,-6.39971392487481));
#12351=CARTESIAN_POINT('Ctrl Pts',(2.82589930564568,0.93693720732448,-6.39992298851146));
#12352=CARTESIAN_POINT('Ctrl Pts',(2.83063821674679,0.940527143910821,-6.4003269066802));
#12353=CARTESIAN_POINT('Ctrl Pts',(2.83293859276156,0.942256547915393,-6.40052184232947));
#12354=CARTESIAN_POINT('Ctrl Pts',(2.83846767274727,0.946381631088716,-6.40098772851276));
#12355=CARTESIAN_POINT('Ctrl Pts',(2.84170237659095,0.948769264203232,-6.4012581346757));
#12356=CARTESIAN_POINT('Ctrl Pts',(2.85165873670115,0.956039891179337,-6.40208407748998));
#12357=CARTESIAN_POINT('Ctrl Pts',(2.85842005590125,0.960868489329611,-6.40263614518901));
#12358=CARTESIAN_POINT('Ctrl Pts',(2.93276678021822,1.0127840964013,-6.40861779516577));
#12359=CARTESIAN_POINT('Ctrl Pts',(3.00507296977708,1.05273521884625,-6.4136520290829));
#12360=CARTESIAN_POINT('Ctrl Pts',(3.12858205517243,1.10494261304925,-6.42195271818642));
#12361=CARTESIAN_POINT('Ctrl Pts',(3.17746823006922,1.12191176245831,-6.42516744887105));
#12362=CARTESIAN_POINT('Ctrl Pts',(3.24626538962809,1.14082597568257,-6.42972779049516));
#12363=CARTESIAN_POINT('Ctrl Pts',(3.26534963038493,1.14556216770455,-6.43099614802907));
#12364=CARTESIAN_POINT('Ctrl Pts',(3.29900656622579,1.15302571457568,-6.4332452534537));
#12365=CARTESIAN_POINT('Ctrl Pts',(3.31352911292379,1.15595980457719,-6.43421963514288));
#12366=CARTESIAN_POINT('Ctrl Pts',(3.33501843609346,1.15988102066785,-6.43566900905131));
#12367=CARTESIAN_POINT('Ctrl Pts',(3.341945272507,1.16108099720014,-6.43613734425711));
#12368=CARTESIAN_POINT('Ctrl Pts',(3.35426797719213,1.16310226899619,-6.4369727251645));
#12369=CARTESIAN_POINT('Ctrl Pts',(3.3596596379837,1.16394821118643,-6.43733898916408));
#12370=CARTESIAN_POINT('Ctrl Pts',(3.37102273126913,1.16565022304492,-6.43811257552093));
#12371=CARTESIAN_POINT('Ctrl Pts',(3.37699523480088,1.16649794645077,-6.43852014703686));
#12372=CARTESIAN_POINT('Ctrl Pts',(3.39284485414717,1.16862351975635,-6.43960444865519));
#12373=CARTESIAN_POINT('Ctrl Pts',(3.40273193735257,1.16982200608203,-6.44028362177657));
#12374=CARTESIAN_POINT('Ctrl Pts',(3.44694685704018,1.17461344074678,-6.44333404853311));
#12375=CARTESIAN_POINT('Ctrl Pts',(3.48140444965084,1.17682140500423,-6.44574740149083));
#12376=CARTESIAN_POINT('Ctrl Pts',(3.61599202629003,1.17952028646134,-6.45531886249316));
#12377=CARTESIAN_POINT('Ctrl Pts',(3.71592127437108,1.16875744456909,-6.46278229060058));
#12378=CARTESIAN_POINT('Ctrl Pts',(3.83417232556991,1.14049842416938,-6.47157384106521));
#12379=CARTESIAN_POINT('Ctrl Pts',(3.85494173261071,1.13492988848359,-6.47311427078975));
#12380=CARTESIAN_POINT('Ctrl Pts',(3.88849226778399,1.12494228824751,-6.47558513499365));
#12381=CARTESIAN_POINT('Ctrl Pts',(3.90136976960366,1.12086643018572,-6.4765292143405));
#12382=CARTESIAN_POINT('Ctrl Pts',(3.91869067024776,1.11505454241571,-6.47779064581055));
#12383=CARTESIAN_POINT('Ctrl Pts',(3.92319722941423,1.11351192484223,-6.47811806772425));
#12384=CARTESIAN_POINT('Ctrl Pts',(3.93070078377988,1.11089245825476,-6.47866179151212));
#12385=CARTESIAN_POINT('Ctrl Pts',(3.93370295023513,1.10983073311865,-6.47887894750128));
#12386=CARTESIAN_POINT('Ctrl Pts',(3.93937972909166,1.10779718251264,-6.47928878301345));
#12387=CARTESIAN_POINT('Ctrl Pts',(3.942055180102,1.10682782069727,-6.47948160792783));
#12388=CARTESIAN_POINT('Ctrl Pts',(3.94838365694887,1.10450892318519,-6.47993699121781));
#12389=CARTESIAN_POINT('Ctrl Pts',(3.95203358289088,1.10315093683375,-6.48019906004639));
#12390=CARTESIAN_POINT('Ctrl Pts',(3.9648034783201,1.09832754612606,-6.48111416961166));
#12391=CARTESIAN_POINT('Ctrl Pts',(3.97388736391617,1.09476683661903,-6.48176193553076));
#12392=CARTESIAN_POINT('Ctrl Pts',(4.04922328174113,1.06415122726164,-6.48711568660296));
#12393=CARTESIAN_POINT('Ctrl Pts',(4.11293638203291,1.03121853666367,-6.49152981841795));
#12394=CARTESIAN_POINT('Ctrl Pts',(4.22264297488093,0.961180400018604,-6.49958067380963));
#12395=CARTESIAN_POINT('Ctrl Pts',(4.26959081906515,0.92602408902228,-6.50320146259553));
#12396=CARTESIAN_POINT('Ctrl Pts',(4.32967112981816,0.873614567741719,-6.50828371032867));
#12397=CARTESIAN_POINT('Ctrl Pts',(4.34523677994508,0.859279687926859,-6.50964557705863));
#12398=CARTESIAN_POINT('Ctrl Pts',(4.37164880867881,0.833607159183514,-6.51204509365738));
#12399=CARTESIAN_POINT('Ctrl Pts',(4.38267062407157,0.822457425464716,-6.51307509232735));
#12400=CARTESIAN_POINT('Ctrl Pts',(4.39841723920085,0.805878804813921,-6.51459142030952));
#12401=CARTESIAN_POINT('Ctrl Pts',(4.40332034525348,0.800621050155294,-6.51507015636227));
#12402=CARTESIAN_POINT('Ctrl Pts',(4.41187460089195,0.791277999215493,-6.51591731338677));
#12403=CARTESIAN_POINT('Ctrl Pts',(4.41554598760184,0.787211459573994,-6.51628487284406));
#12404=CARTESIAN_POINT('Ctrl Pts',(4.4231481624079,0.77867201796701,-6.51705440082348));
#12405=CARTESIAN_POINT('Ctrl Pts',(4.42707365940531,0.774194635050932,-6.51745657287766));
#12406=CARTESIAN_POINT('Ctrl Pts',(4.43724041894056,0.762419579027643,-6.51851098425855));
#12407=CARTESIAN_POINT('Ctrl Pts',(4.443426573987,0.755075128284217,-6.51916543111938));
#12408=CARTESIAN_POINT('Ctrl Pts',(4.46926795172895,0.723622520857745,-6.52195526744885));
#12409=CARTESIAN_POINT('Ctrl Pts',(4.48805223818473,0.698818326629725,-6.52412441199115));
#12410=CARTESIAN_POINT('Ctrl Pts',(4.56519469614052,0.588104637046068,-6.53368238066644));
#12411=CARTESIAN_POINT('Ctrl Pts',(4.61302577514608,0.495434471449038,-6.5414259457628));
#12412=CARTESIAN_POINT('Ctrl Pts',(4.6554252126742,0.377254909202711,-6.5505078137947));
#12413=CARTESIAN_POINT('Ctrl Pts',(4.66220009675545,0.35658829616128,-6.5520663503187));
#12414=CARTESIAN_POINT('Ctrl Pts',(4.67228065187524,0.32269427835323,-6.55456282921598));
#12415=CARTESIAN_POINT('Ctrl Pts',(4.67593566408856,0.309576748256058,-6.5555147459365));
#12416=CARTESIAN_POINT('Ctrl Pts',(4.68056496445609,0.291774076878011,-6.55678486590864));
#12417=CARTESIAN_POINT('Ctrl Pts',(4.68173924546384,0.28714267862063,-6.55711331252978));
#12418=CARTESIAN_POINT('Ctrl Pts',(4.68364988690451,0.27940982619535,-6.55765827041756));
#12419=CARTESIAN_POINT('Ctrl Pts',(4.68440188776263,0.276312343988887,-6.55787564371449));
#12420=CARTESIAN_POINT('Ctrl Pts',(4.68580086701504,0.27044619243034,-6.55828553519333));
#12421=CARTESIAN_POINT('Ctrl Pts',(4.6864504087604,0.267678175705502,-6.55847820103284));
#12422=CARTESIAN_POINT('Ctrl Pts',(4.68796364454089,0.26112289369182,-6.55893277067281));
#12423=CARTESIAN_POINT('Ctrl Pts',(4.68881864493384,0.257333624866884,-6.55919418915567));
#12424=CARTESIAN_POINT('Ctrl Pts',(4.69176545543255,0.243965987942151,-6.56011190202533));
#12425=CARTESIAN_POINT('Ctrl Pts',(4.6937564683154,0.234365483014759,-6.56076285283522));
#12426=CARTESIAN_POINT('Ctrl Pts',(4.70918494119134,0.154998574411806,-6.56608568560102));
#12427=CARTESIAN_POINT('Ctrl Pts',(4.71640577698327,0.0841623742297525,
-6.57047008952881));
#12428=CARTESIAN_POINT('Ctrl Pts',(4.71785165203879,-0.0458290387227297,
-6.57851129554207));
#12429=CARTESIAN_POINT('Ctrl Pts',(4.71408332509042,-0.104719280449985,
-6.58215306769525));
#12430=CARTESIAN_POINT('Ctrl Pts',(4.70298425418913,-0.184104733424839,
-6.58726211292166));
#12431=CARTESIAN_POINT('Ctrl Pts',(4.69947654534109,-0.205047220625451,
-6.58862855706507));
#12432=CARTESIAN_POINT('Ctrl Pts',(4.69239019521921,-0.241309477263978,
-6.59103540804927));
#12433=CARTESIAN_POINT('Ctrl Pts',(4.68906706402577,-0.256673853135453,
-6.59206809745574));
#12434=CARTESIAN_POINT('Ctrl Pts',(4.68377569653301,-0.278968785689635,
-6.5935876572805));
#12435=CARTESIAN_POINT('Ctrl Pts',(4.6820497073416,-0.285955503031096,-6.59406688760917));
#12436=CARTESIAN_POINT('Ctrl Pts',(4.67889692076402,-0.298233396502753,
-6.59491460918908));
#12437=CARTESIAN_POINT('Ctrl Pts',(4.67749701009548,-0.303531302804515,
-6.59528223511535));
#12438=CARTESIAN_POINT('Ctrl Pts',(4.67449974632466,-0.314562073954441,
-6.59605159448137));
#12439=CARTESIAN_POINT('Ctrl Pts',(4.67289581355544,-0.320292973682849,
-6.59645352939703));
#12440=CARTESIAN_POINT('Ctrl Pts',(4.66859483546785,-0.335223568166869,
-6.59750662742625));
#12441=CARTESIAN_POINT('Ctrl Pts',(4.66582881910959,-0.344402765041082,
-6.59815998793711));
#12442=CARTESIAN_POINT('Ctrl Pts',(4.65365848927878,-0.383075250196805,
-6.60093845193831));
#12443=CARTESIAN_POINT('Ctrl Pts',(4.64320611574455,-0.412223110009007,
-6.6030969666943));
#12444=CARTESIAN_POINT('Ctrl Pts',(4.60051707690937,-0.517957341431438,
-6.61117231157706));
#12445=CARTESIAN_POINT('Ctrl Pts',(4.5613549439675,-0.591476687592265,-6.61729559025054));
#12446=CARTESIAN_POINT('Ctrl Pts',(4.4855554575964,-0.703441735428664,-6.62719319371163));
#12447=CARTESIAN_POINT('Ctrl Pts',(4.45347712905797,-0.744645613169313,
-6.63097701400828));
#12448=CARTESIAN_POINT('Ctrl Pts',(4.4141403374804,-0.788784548749866,-6.63508921453577));
#12449=CARTESIAN_POINT('Ctrl Pts',(4.40946568440461,-0.793937226733229,
-6.63557019747927));
#12450=CARTESIAN_POINT('Ctrl Pts',(4.40226179869619,-0.801737746749021,
-6.63629938053248));
#12451=CARTESIAN_POINT('Ctrl Pts',(4.39976552033298,-0.80441561159858,-6.63654989308485));
#12452=CARTESIAN_POINT('Ctrl Pts',(4.39517249770622,-0.809296911723115,
-6.63700681164602));
#12453=CARTESIAN_POINT('Ctrl Pts',(4.3930796968975,-0.811503873317242,-6.63721349352151));
#12454=CARTESIAN_POINT('Ctrl Pts',(4.38833551473673,-0.816468189299387,
-6.63767864080093));
#12455=CARTESIAN_POINT('Ctrl Pts',(4.38567923454699,-0.819220750508467,
-6.63793672817168));
#12456=CARTESIAN_POINT('Ctrl Pts',(4.3787787185151,-0.826302016088787,-6.63860130412161));
#12457=CARTESIAN_POINT('Ctrl Pts',(4.37451432475022,-0.830611044921556,
-6.63900630920203));
#12458=CARTESIAN_POINT('Ctrl Pts',(4.34565856595261,-0.859322008509864,
-6.64171055390627));
#12459=CARTESIAN_POINT('Ctrl Pts',(4.3200315506661,-0.882664134852977,-6.64393724589545));
#12460=CARTESIAN_POINT('Ctrl Pts',(4.2717270343421,-0.922910097270403,-6.6479100790801));
#12461=CARTESIAN_POINT('Ctrl Pts',(4.24940087593044,-0.940191200882933,
-6.64966740446288));
#12462=CARTESIAN_POINT('Ctrl Pts',(4.18750710597177,-0.984635972691225,
-6.654391835549));
#12463=CARTESIAN_POINT('Ctrl Pts',(4.14686698557342,-1.01021033045519,-6.6573419860796));
#12464=CARTESIAN_POINT('Ctrl Pts',(4.09596916778885,-1.03805549725572,-6.66097008034091));
#12465=CARTESIAN_POINT('Ctrl Pts',(4.08709787329504,-1.04276234184578,-6.66160001813117));
#12466=CARTESIAN_POINT('Ctrl Pts',(4.07816925191529,-1.04735429675555,-6.66223230003384));
#12467=CARTESIAN_POINT('Origin',(3.53951905042299,8.32667268468867E-16,
0.924367114736157));
#12468=CARTESIAN_POINT('',(4.07816926754786,-1.04735428871577,-7.26048212650804));
#12469=CARTESIAN_POINT('',(4.0781692089456,-1.04735431885469,-7.16215973101906));
#12470=CARTESIAN_POINT('',(4.07816926754759,-1.04735428871592,0.924367114736157));
#12471=CARTESIAN_POINT('',(2.36176955567229,0.00102997123974061,-6.92455466901993));
#12472=CARTESIAN_POINT('Ctrl Pts',(4.07816926754783,-1.04735428871579,-7.26048212650804));
#12473=CARTESIAN_POINT('Ctrl Pts',(4.0791210384006,-1.04686479668619,-7.26040895432542));
#12474=CARTESIAN_POINT('Ctrl Pts',(4.08007214743775,-1.0463740045061,-7.26033586072063));
#12475=CARTESIAN_POINT('Ctrl Pts',(4.08372394638214,-1.04448329195444,-7.26005532686991));
#12476=CARTESIAN_POINT('Ctrl Pts',(4.08641986423175,-1.04307421425932,-7.25984846229205));
#12477=CARTESIAN_POINT('Ctrl Pts',(4.09234881626624,-1.03994601750304,-7.25939404491509));
#12478=CARTESIAN_POINT('Ctrl Pts',(4.09557930866954,-1.03822225916838,-7.25914678372801));
#12479=CARTESIAN_POINT('Ctrl Pts',(4.10492562876973,-1.03317901863033,-7.25843224090554));
#12480=CARTESIAN_POINT('Ctrl Pts',(4.11102027058487,-1.02982029719037,-7.25796732132046));
#12481=CARTESIAN_POINT('Ctrl Pts',(4.16258002015432,-1.00080730824881,-7.2540398349102));
#12482=CARTESIAN_POINT('Ctrl Pts',(4.20632906893002,-0.972206821970832,
-7.25074380492524));
#12483=CARTESIAN_POINT('Ctrl Pts',(4.31449867956874,-0.890743150276272,
-7.24230877133553));
#12484=CARTESIAN_POINT('Ctrl Pts',(4.37546338937657,-0.833794612940169,
-7.23724602807653));
#12485=CARTESIAN_POINT('Ctrl Pts',(4.45008209734152,-0.747608828442086,
-7.22997481502585));
#12486=CARTESIAN_POINT('Ctrl Pts',(4.46932267187858,-0.723539212705974,
-7.22798191619663));
#12487=CARTESIAN_POINT('Ctrl Pts',(4.49327538620863,-0.691039458935407,
-7.22532121204929));
#12488=CARTESIAN_POINT('Ctrl Pts',(4.49885993192031,-0.683265501877888,
-7.2246869698913));
#12489=CARTESIAN_POINT('Ctrl Pts',(4.50776034052246,-0.670551452851053,
-7.22365274462778));
#12490=CARTESIAN_POINT('Ctrl Pts',(4.51113468905718,-0.665652683716904,
-7.22325497685624));
#12491=CARTESIAN_POINT('Ctrl Pts',(4.51754704970258,-0.656190783863797,
-7.22248796033129));
#12492=CARTESIAN_POINT('Ctrl Pts',(4.52059060355455,-0.651631581567085,
-7.22211893133012));
#12493=CARTESIAN_POINT('Ctrl Pts',(4.52756107757768,-0.641030373930713,
-7.22126204035052));
#12494=CARTESIAN_POINT('Ctrl Pts',(4.53146456088762,-0.634973297076931,
-7.22077333133698));
#12495=CARTESIAN_POINT('Ctrl Pts',(4.54373056030214,-0.615550863422892,
-7.21920879819117));
#12496=CARTESIAN_POINT('Ctrl Pts',(4.55188009666416,-0.6020537288065,-7.2181253392048));
#12497=CARTESIAN_POINT('Ctrl Pts',(4.57040407276885,-0.569934558620777,
-7.21555456661155));
#12498=CARTESIAN_POINT('Ctrl Pts',(4.58054845669689,-0.551186908442242,
-7.21405977016025));
#12499=CARTESIAN_POINT('Ctrl Pts',(4.61698809842442,-0.479245130209868,
-7.20834463453967));
#12500=CARTESIAN_POINT('Ctrl Pts',(4.63975718209956,-0.424370209527562,
-7.20402195141923));
#12501=CARTESIAN_POINT('Ctrl Pts',(4.68031292177284,-0.301081408911668,
-7.19450082427979));
#12502=CARTESIAN_POINT('Ctrl Pts',(4.69628223715173,-0.23229590519864,-7.18930747221862));
#12503=CARTESIAN_POINT('Ctrl Pts',(4.70736193492338,-0.152756788635022,
-7.18367885848958));
#12504=CARTESIAN_POINT('Ctrl Pts',(4.70859595856498,-0.143006426131493,
-7.18299538101601));
#12505=CARTESIAN_POINT('Ctrl Pts',(4.71014773044312,-0.129378031055884,
-7.1820501629168));
#12506=CARTESIAN_POINT('Ctrl Pts',(4.71056849564459,-0.125512466811791,
-7.18178319216913));
#12507=CARTESIAN_POINT('Ctrl Pts',(4.71126390343153,-0.118815624456901,
-7.18132272118901));
#12508=CARTESIAN_POINT('Ctrl Pts',(4.71154744425036,-0.115985333850374,
-7.1811287417708));
#12509=CARTESIAN_POINT('Ctrl Pts',(4.71212691884321,-0.10998184297856,-7.18071865482951));
#12510=CARTESIAN_POINT('Ctrl Pts',(4.71242023242729,-0.106808410875968,
-7.18050269838268));
#12511=CARTESIAN_POINT('Ctrl Pts',(4.71312072562801,-0.0988785091499942,
-7.17996500435443));
#12512=CARTESIAN_POINT('Ctrl Pts',(4.71351187940819,-0.0941206197330737,
-7.17964413933385));
#12513=CARTESIAN_POINT('Ctrl Pts',(4.71490461659455,-0.0758175651574341,
-7.17841607212677));
#12514=CARTESIAN_POINT('Ctrl Pts',(4.71570084347704,-0.0622572163110699,
-7.17751940029991));
#12515=CARTESIAN_POINT('Ctrl Pts',(4.71715802779972,-0.0270365754443105,
-7.17521758072504));
#12516=CARTESIAN_POINT('Ctrl Pts',(4.71745617129102,-0.00536577729133605,
-7.17382785174512));
#12517=CARTESIAN_POINT('Ctrl Pts',(4.71573566097996,0.118920575617957,-7.16594793532118));
#12518=CARTESIAN_POINT('Ctrl Pts',(4.7009090513346,0.220914048676916,-7.1597954908354));
#12519=CARTESIAN_POINT('Ctrl Pts',(4.66431207532299,0.350672797991655,-7.15120964144321));
#12520=CARTESIAN_POINT('Ctrl Pts',(4.65431106422306,0.381273179406102,-7.14913014551336));
#12521=CARTESIAN_POINT('Ctrl Pts',(4.63967459309447,0.420532210610792,-7.14636981466399));
#12522=CARTESIAN_POINT('Ctrl Pts',(4.63616623923376,0.429598058892855,-7.14572585942135));
#12523=CARTESIAN_POINT('Ctrl Pts',(4.63031871311958,0.444169933965177,-7.14467971145538));
#12524=CARTESIAN_POINT('Ctrl Pts',(4.62804906182708,0.449703509457974,-7.14427983136713));
#12525=CARTESIAN_POINT('Ctrl Pts',(4.62362239022782,0.460266176901633,-7.14351139261523));
#12526=CARTESIAN_POINT('Ctrl Pts',(4.62147226990143,0.465298005693713,-7.14314307315783));
#12527=CARTESIAN_POINT('Ctrl Pts',(4.61643773921654,0.476856494180382,-7.14229171841119));
#12528=CARTESIAN_POINT('Ctrl Pts',(4.61352894725653,0.483372233315901,-7.14180787135677));
#12529=CARTESIAN_POINT('Ctrl Pts',(4.60416435443203,0.503847170335354,-7.14027477490588));
#12530=CARTESIAN_POINT('Ctrl Pts',(4.5974944618875,0.517706079155251,-7.13921831706065));
#12531=CARTESIAN_POINT('Ctrl Pts',(4.58124366558678,0.549846119485413,-7.13672284330316));
#12532=CARTESIAN_POINT('Ctrl Pts',(4.57145005041813,0.568013425182072,-7.13527692622006));
#12533=CARTESIAN_POINT('Ctrl Pts',(4.53327934984958,0.63457225533011,-7.12984584248786));
#12534=CARTESIAN_POINT('Ctrl Pts',(4.50193633311551,0.681170461710787,-7.12576922185289));
#12535=CARTESIAN_POINT('Ctrl Pts',(4.4210017810568,0.784702493667794,-7.11613628728554));
#12536=CARTESIAN_POINT('Ctrl Pts',(4.36901626240151,0.839467732045456,-7.11056922925221));
#12537=CARTESIAN_POINT('Ctrl Pts',(4.30494733946576,0.895156807276934,-7.10462289367839));
#12538=CARTESIAN_POINT('Ctrl Pts',(4.29766696994318,0.901331194321186,-7.10395929873762));
#12539=CARTESIAN_POINT('Ctrl Pts',(4.28733913469973,0.909876405250098,-7.10303570768108));
#12540=CARTESIAN_POINT('Ctrl Pts',(4.28435409219315,0.912321606057675,-7.10277081078597));
#12541=CARTESIAN_POINT('Ctrl Pts',(4.27893459410847,0.916716664978687,-7.10229364718935));
#12542=CARTESIAN_POINT('Ctrl Pts',(4.27650431216894,0.918671603386434,-7.1020810283009));
#12543=CARTESIAN_POINT('Ctrl Pts',(4.27151367795629,0.922653559735491,-7.10164722793083));
#12544=CARTESIAN_POINT('Ctrl Pts',(4.26895261695194,0.924679619495199,-7.10142611262159));
#12545=CARTESIAN_POINT('Ctrl Pts',(4.26234095325326,0.929865555141514,-7.10085902767194));
#12546=CARTESIAN_POINT('Ctrl Pts',(4.25827799028721,0.933009669095838,-7.10051413941098));
#12547=CARTESIAN_POINT('Ctrl Pts',(4.24102359068131,0.946182340578814,-7.09906397122429));
#12548=CARTESIAN_POINT('Ctrl Pts',(4.22764112376203,0.955959058714413,-7.09797470867935));
#12549=CARTESIAN_POINT('Ctrl Pts',(4.1904146663823,0.981968279526118,-7.09502693918456));
#12550=CARTESIAN_POINT('Ctrl Pts',(4.16617292585347,0.997613130239746,-7.09319681941355));
#12551=CARTESIAN_POINT('Ctrl Pts',(4.06396078936841,1.05837992662433,-7.08573714744645));
#12552=CARTESIAN_POINT('Ctrl Pts',(3.98151966398361,1.09537351101818,-7.08029034884683));
#12553=CARTESIAN_POINT('Ctrl Pts',(3.86374415862517,1.1327377199476,-7.0724330627609));
#12554=CARTESIAN_POINT('Ctrl Pts',(3.83140697363367,1.14149804262041,-7.07027151766898));
#12555=CARTESIAN_POINT('Ctrl Pts',(3.7891187116076,1.1510397069154,-7.06741640472314));
#12556=CARTESIAN_POINT('Ctrl Pts',(3.77946813094281,1.15309012085085,-7.06676300706239));
#12557=CARTESIAN_POINT('Ctrl Pts',(3.76389662643314,1.15619458442182,-7.06570526355605));
#12558=CARTESIAN_POINT('Ctrl Pts',(3.75799126644132,1.1573249769293,-7.06530332651568));
#12559=CARTESIAN_POINT('Ctrl Pts',(3.74670380254696,1.15939613203936,-7.06453342886018));
#12560=CARTESIAN_POINT('Ctrl Pts',(3.74132328686276,1.16034475951355,-7.06416572599855));
#12561=CARTESIAN_POINT('Ctrl Pts',(3.72896423821972,1.16243519633773,-7.06331939722583));
#12562=CARTESIAN_POINT('Ctrl Pts',(3.7219816897657,1.16355165176923,-7.06283999164924));
#12563=CARTESIAN_POINT('Ctrl Pts',(3.70012532011317,1.16684474223184,-7.06133524645699));
#12564=CARTESIAN_POINT('Ctrl Pts',(3.68522011240307,1.16879946555535,-7.06030307214294));
#12565=CARTESIAN_POINT('Ctrl Pts',(3.65037241594901,1.1726926020889,-7.05787485732478));
#12566=CARTESIAN_POINT('Ctrl Pts',(3.63041024933091,1.17440841101419,-7.0564724128042));
#12567=CARTESIAN_POINT('Ctrl Pts',(3.55717262922423,1.17882503985399,-7.05128454953918));
#12568=CARTESIAN_POINT('Ctrl Pts',(3.50377923600831,1.17841489720657,-7.04741645188211));
#12569=CARTESIAN_POINT('Ctrl Pts',(3.37128271906969,1.16838321756274,-7.03768549736953));
#12570=CARTESIAN_POINT('Ctrl Pts',(3.29276967058799,1.15435673735584,-7.03179312721365));
#12571=CARTESIAN_POINT('Ctrl Pts',(3.20799161631081,1.13015868902606,-7.02562057644877));
#12572=CARTESIAN_POINT('Ctrl Pts',(3.19974327642594,1.12770631634214,-7.02502226540288));
#12573=CARTESIAN_POINT('Ctrl Pts',(3.18718404317643,1.12382192790666,-7.02411543887595));
#12574=CARTESIAN_POINT('Ctrl Pts',(3.18285352568081,1.12245507176932,-7.02380352383687));
#12575=CARTESIAN_POINT('Ctrl Pts',(3.17557192389653,1.12011035848703,-7.02328046749271));
#12576=CARTESIAN_POINT('Ctrl Pts',(3.17261663866611,1.11914581140252,-7.02306857708582));
#12577=CARTESIAN_POINT('Ctrl Pts',(3.16654985692893,1.1171391184539,-7.02263445641438));
#12578=CARTESIAN_POINT('Ctrl Pts',(3.16343884642749,1.11609565455025,-7.02241230380538));
#12579=CARTESIAN_POINT('Ctrl Pts',(3.15540058745813,1.11336211637116,-7.02183940157568));
#12580=CARTESIAN_POINT('Ctrl Pts',(3.15048005177301,1.11165230886274,-7.02148977618183));
#12581=CARTESIAN_POINT('Ctrl Pts',(3.12964028181421,1.10425550228127,-7.0200129248423));
#12582=CARTESIAN_POINT('Ctrl Pts',(3.11383222540537,1.0982584478319,-7.01890235942144));
#12583=CARTESIAN_POINT('Ctrl Pts',(3.07047355563768,1.08073263222544,-7.01586891152624));
#12584=CARTESIAN_POINT('Ctrl Pts',(3.04322286992921,1.06849288819651,-7.01397664954022));
#12585=CARTESIAN_POINT('Ctrl Pts',(2.92067289526724,1.00774758908265,-7.00540645995481));
#12586=CARTESIAN_POINT('Ctrl Pts',(2.83179755056081,0.947447136530567,-6.99896834281064));
#12587=CARTESIAN_POINT('Ctrl Pts',(2.73802478613671,0.863173903915375,-6.99080402974186));
#12588=CARTESIAN_POINT('Ctrl Pts',(2.72408796947361,0.850020193533559,-6.98955063881296));
#12589=CARTESIAN_POINT('Ctrl Pts',(2.70479918924047,0.830904180454798,-6.98775394633782));
#12590=CARTESIAN_POINT('Ctrl Pts',(2.69917714512367,0.825217838336029,-6.98722247997151));
#12591=CARTESIAN_POINT('Ctrl Pts',(2.6897436626013,0.815480095705618,-6.98631708987481));
#12592=CARTESIAN_POINT('Ctrl Pts',(2.68590217489836,0.811458085335159,-6.98594447207879));
#12593=CARTESIAN_POINT('Ctrl Pts',(2.67819411719149,0.803272498089551,-6.98518871210472));
#12594=CARTESIAN_POINT('Ctrl Pts',(2.67432890548019,0.799107851257122,-6.98480552677368));
#12595=CARTESIAN_POINT('Ctrl Pts',(2.66540850215684,0.789355803408201,-6.98391121726921));
#12596=CARTESIAN_POINT('Ctrl Pts',(2.66037654132012,0.783747586331053,-6.98339914477914));
#12597=CARTESIAN_POINT('Ctrl Pts',(2.64222170240549,0.763118832124705,-6.98152333159484));
#12598=CARTESIAN_POINT('Ctrl Pts',(2.62942778510317,0.747814607760834,-6.98014637455723));
#12599=CARTESIAN_POINT('Ctrl Pts',(2.59874059627809,0.709151862477085,-6.97670125298433));
#12600=CARTESIAN_POINT('Ctrl Pts',(2.58132305717579,0.685434650845956,-6.97461647779052));
#12601=CARTESIAN_POINT('Ctrl Pts',(2.53484419726017,0.616906754337731,-6.96867491154743));
#12602=CARTESIAN_POINT('Ctrl Pts',(2.50791691668799,0.570737906001056,-6.96476271389434));
#12603=CARTESIAN_POINT('Ctrl Pts',(2.45676075446857,0.467497000174545,-6.95630659854012));
#12604=CARTESIAN_POINT('Ctrl Pts',(2.4337093016752,0.410006441491091,-6.95177275174832));
#12605=CARTESIAN_POINT('Ctrl Pts',(2.412293817439,0.341406839854758,-6.94673332944894));
#12606=CARTESIAN_POINT('Ctrl Pts',(2.40943139879548,0.331809090270396,-6.94603654360019));
#12607=CARTESIAN_POINT('Ctrl Pts',(2.40561440271821,0.31838784525321,-6.9450747514714));
#12608=CARTESIAN_POINT('Ctrl Pts',(2.40455614928163,0.314594634788478,-6.94480431328668));
#12609=CARTESIAN_POINT('Ctrl Pts',(2.40276302248338,0.308040512244304,-6.94433951461768));
#12610=CARTESIAN_POINT('Ctrl Pts',(2.4020191409051,0.305282132676973,-6.94414465389109));
#12611=CARTESIAN_POINT('Ctrl Pts',(2.40047052317772,0.299455466884699,-6.94373467133754));
#12612=CARTESIAN_POINT('Ctrl Pts',(2.39966813213276,0.296386586367043,-6.94351969017118));
#12613=CARTESIAN_POINT('Ctrl Pts',(2.39770710240917,0.288760536575892,-6.94298775343229));
#12614=CARTESIAN_POINT('Ctrl Pts',(2.39656332223055,0.284199537950749,-6.94267163054727));
#12615=CARTESIAN_POINT('Ctrl Pts',(2.39415621230736,0.274351200446754,-6.94199314472811));
#12616=CARTESIAN_POINT('Ctrl Pts',(2.3929021048578,0.269061693552751,-6.94163127155982));
#12617=CARTESIAN_POINT('Ctrl Pts',(2.38941377332809,0.253881329908542,-6.94059949593436));
#12618=CARTESIAN_POINT('Ctrl Pts',(2.38727054037059,0.243969802280411,-6.93993403143119));
#12619=CARTESIAN_POINT('Ctrl Pts',(2.3697068138731,0.157343976556934,-6.934179407255));
#12620=CARTESIAN_POINT('Ctrl Pts',(2.36183797518918,0.0792913967190124,
-6.92940337711709));
#12621=CARTESIAN_POINT('Ctrl Pts',(2.36176950122289,0.00103046541328306,
-6.92455479479514));
#12622=CARTESIAN_POINT('Ctrl Pts',(2.36176950078553,0.00102996541417458,
-6.92455476381816));
#12623=CARTESIAN_POINT('Ctrl Pts',(2.36170919468074,-0.067929134354621,
-6.92028246753168));
#12624=CARTESIAN_POINT('Ctrl Pts',(2.36770518372916,-0.1367539347171,-6.915970531133));
#12625=CARTESIAN_POINT('Ctrl Pts',(2.38139014680442,-0.214309562451292,
-6.91082537945449));
#12626=CARTESIAN_POINT('Ctrl Pts',(2.38321387131569,-0.223940772383019,
-6.91018151456286));
#12627=CARTESIAN_POINT('Ctrl Pts',(2.38643756776599,-0.239874597967229,
-6.90910753605252));
#12628=CARTESIAN_POINT('Ctrl Pts',(2.38776954649811,-0.246190588509361,
-6.90867952474163));
#12629=CARTESIAN_POINT('Ctrl Pts',(2.39026544663821,-0.25756188507796,-6.90790462094745));
#12630=CARTESIAN_POINT('Ctrl Pts',(2.3914109839286,-0.262621089513881,-6.9075583114395));
#12631=CARTESIAN_POINT('Ctrl Pts',(2.39382185310142,-0.272951236309381,
-6.90684794636779));
#12632=CARTESIAN_POINT('Ctrl Pts',(2.39509022643722,-0.278221333662394,
-6.90648380227523));
#12633=CARTESIAN_POINT('Ctrl Pts',(2.39791732375754,-0.289621417142105,
-6.90569223386097));
#12634=CARTESIAN_POINT('Ctrl Pts',(2.39948913248429,-0.295747951984234,
-6.90526440286357));
#12635=CARTESIAN_POINT('Ctrl Pts',(2.40393089073505,-0.312499138139667,
-6.90408779205807));
#12636=CARTESIAN_POINT('Ctrl Pts',(2.40690047373151,-0.323096464302741,
-6.90333585776163));
#12637=CARTESIAN_POINT('Ctrl Pts',(2.42482907262387,-0.383789859677081,
-6.89898436493865));
#12638=CARTESIAN_POINT('Ctrl Pts',(2.4429600617432,-0.432880355212411,-6.8952835756504));
#12639=CARTESIAN_POINT('Ctrl Pts',(2.4838735253723,-0.524414922717426,-6.88803953382313));
#12640=CARTESIAN_POINT('Ctrl Pts',(2.50611729994515,-0.566991061716404,
-6.88451543417852));
#12641=CARTESIAN_POINT('Ctrl Pts',(2.56116444011136,-0.658296552316439,
-6.87669277199488));
#12642=CARTESIAN_POINT('Ctrl Pts',(2.59514384381577,-0.706179144703532,
-6.87240518397654));
#12643=CARTESIAN_POINT('Ctrl Pts',(2.63871565185895,-0.758776422832698,
-6.86762062593331));
#12644=CARTESIAN_POINT('Ctrl Pts',(2.64497122427565,-0.76614138671602,-6.86694892914909));
#12645=CARTESIAN_POINT('Ctrl Pts',(2.65410555721875,-0.776631212399946,
-6.86599072269893));
#12646=CARTESIAN_POINT('Ctrl Pts',(2.65691149273527,-0.779818565141312,
-6.86569936452814));
#12647=CARTESIAN_POINT('Ctrl Pts',(2.66178738811554,-0.785297220839857,
-6.86519830526048));
#12648=CARTESIAN_POINT('Ctrl Pts',(2.6638492132091,-0.787595666053827,-6.86498802206589));
#12649=CARTESIAN_POINT('Ctrl Pts',(2.66820043557348,-0.792408035160965,
-6.86454761792684));
#12650=CARTESIAN_POINT('Ctrl Pts',(2.67049169991478,-0.794920176859078,
-6.86431763847893));
#12651=CARTESIAN_POINT('Ctrl Pts',(2.67668437976571,-0.801651053360571,
-6.86370111310438));
#12652=CARTESIAN_POINT('Ctrl Pts',(2.68060590459111,-0.805851283730036,
-6.86331603163618));
#12653=CARTESIAN_POINT('Ctrl Pts',(2.69859871933711,-0.824842298223499,
-6.86157235238685));
#12654=CARTESIAN_POINT('Ctrl Pts',(2.71302329995988,-0.839295368444953,
-6.86023816056863));
#12655=CARTESIAN_POINT('Ctrl Pts',(2.78597322101274,-0.908683528060233,
-6.85375137573298));
#12656=CARTESIAN_POINT('Ctrl Pts',(2.8496366286983,-0.957915354664559,-6.84887499095558));
#12657=CARTESIAN_POINT('Ctrl Pts',(2.95440713323276,-1.02303224210467,-6.8412091100522));
#12658=CARTESIAN_POINT('Ctrl Pts',(2.99221324381584,-1.04374653801709,-6.8385081516993));
#12659=CARTESIAN_POINT('Ctrl Pts',(3.04690171233199,-1.06992121100906,-6.83461753571593));
#12660=CARTESIAN_POINT('Ctrl Pts',(3.06290328524702,-1.07714465325082,-6.83348127574796));
#12661=CARTESIAN_POINT('Ctrl Pts',(3.09143455460048,-1.08926402428989,-6.83145454376817));
#12662=CARTESIAN_POINT('Ctrl Pts',(3.10389805971806,-1.09430807292105,-6.83056895845158));
#12663=CARTESIAN_POINT('Ctrl Pts',(3.12257297279339,-1.10149632303885,-6.82924034775368));
#12664=CARTESIAN_POINT('Ctrl Pts',(3.12872067800373,-1.10380382116081,-6.82880271045113));
#12665=CARTESIAN_POINT('Ctrl Pts',(3.14000647019486,-1.10793252248344,-6.82799866813231));
#12666=CARTESIAN_POINT('Ctrl Pts',(3.14513855047203,-1.10976970389853,-6.82763279955168));
#12667=CARTESIAN_POINT('Ctrl Pts',(3.15600984688852,-1.1135764768967,-6.8268571828388));
#12668=CARTESIAN_POINT('Ctrl Pts',(3.16175188380064,-1.11553746890858,-6.82644716597567));
#12669=CARTESIAN_POINT('Ctrl Pts',(3.17710907756102,-1.12065001472731,-6.82534950274754));
#12670=CARTESIAN_POINT('Ctrl Pts',(3.18674994830207,-1.12372211576038,-6.82465930570032));
#12671=CARTESIAN_POINT('Ctrl Pts',(3.2306282311633,-1.13708380167775,-6.82151218747376));
#12672=CARTESIAN_POINT('Ctrl Pts',(3.26528047917392,-1.14593448819666,-6.81900995488147));
#12673=CARTESIAN_POINT('Ctrl Pts',(3.38624125856184,-1.17102886747839,-6.81021398054998));
#12674=CARTESIAN_POINT('Ctrl Pts',(3.47392299217035,-1.1791932018851,-6.8037069410587));
#12675=CARTESIAN_POINT('Ctrl Pts',(3.60371246515373,-1.17675037546062,-6.79424928101347));
#12676=CARTESIAN_POINT('Ctrl Pts',(3.64567538323102,-1.17370945192453,-6.79122406196703));
#12677=CARTESIAN_POINT('Ctrl Pts',(3.6940468309022,-1.16758779123739,-6.78783531294426));
#12678=CARTESIAN_POINT('Ctrl Pts',(3.70069650445169,-1.16668844117385,-6.78737165789985));
#12679=CARTESIAN_POINT('Ctrl Pts',(3.7109106955437,-1.16521800227792,-6.78666321539333));
#12680=CARTESIAN_POINT('Ctrl Pts',(3.71448074850584,-1.16468729448425,-6.78641630807778));
#12681=CARTESIAN_POINT('Ctrl Pts',(3.72105872643431,-1.16367851399729,-6.78596274375536));
#12682=CARTESIAN_POINT('Ctrl Pts',(3.72406723659236,-1.16320518622926,-6.78575583940993));
#12683=CARTESIAN_POINT('Ctrl Pts',(3.7309147060906,-1.16210064126571,-6.78528611865612));
#12684=CARTESIAN_POINT('Ctrl Pts',(3.73475239962943,-1.16146206906641,-6.78502371378005));
#12685=CARTESIAN_POINT('Ctrl Pts',(3.74477504862178,-1.15974327189991,-6.78434047062667));
#12686=CARTESIAN_POINT('Ctrl Pts',(3.75095475131992,-1.15863256907437,-6.78392125720717));
#12687=CARTESIAN_POINT('Ctrl Pts',(3.79708553285239,-1.14995991974874,-6.78080526553379));
#12688=CARTESIAN_POINT('Ctrl Pts',(3.83663459613673,-1.14038214217488,-6.77820869735128));
#12689=CARTESIAN_POINT('Ctrl Pts',(3.94425947164555,-1.10833675414791,-6.7711557365467));
#12690=CARTESIAN_POINT('Ctrl Pts',(4.01089912620436,-1.08167765371538,-6.76679557453375));
#12691=CARTESIAN_POINT('Ctrl Pts',(4.07586091965954,-1.0485390526759,-6.76222984462527));
#12692=CARTESIAN_POINT('Ctrl Pts',(4.07701560047057,-1.04794761518503,-6.76214858706782));
#12693=CARTESIAN_POINT('Ctrl Pts',(4.0781692678987,-1.04735428853534,-6.76206729648848));
#12694=CARTESIAN_POINT('Ctrl Pts',(4.07816925191529,-1.04735429675555,-6.66223230003384));
#12695=CARTESIAN_POINT('Ctrl Pts',(4.03969408049091,-1.06714192631356,-6.66495692610531));
#12696=CARTESIAN_POINT('Ctrl Pts',(4.00015451341866,-1.0847961500492,-6.66772673241389));
#12697=CARTESIAN_POINT('Ctrl Pts',(3.94961087810461,-1.10410010970873,-6.67128271102149));
#12698=CARTESIAN_POINT('Ctrl Pts',(3.93944078089483,-1.10782442476969,-6.67199887128965));
#12699=CARTESIAN_POINT('Ctrl Pts',(3.92334981969789,-1.11346652953801,-6.67313367573815));
#12700=CARTESIAN_POINT('Ctrl Pts',(3.91746247746872,-1.11547861265525,-6.67354923123327));
#12701=CARTESIAN_POINT('Ctrl Pts',(3.90641021242486,-1.11915834125073,-6.67433014449681));
#12702=CARTESIAN_POINT('Ctrl Pts',(3.9012491479838,-1.12083712125192,-6.67469512841656));
#12703=CARTESIAN_POINT('Ctrl Pts',(3.8896683945488,-1.12451576686303,-6.67551491441929));
#12704=CARTESIAN_POINT('Ctrl Pts',(3.88324285425023,-1.12649643432913,-6.6759703241808));
#12705=CARTESIAN_POINT('Ctrl Pts',(3.86684900013226,-1.13139650577913,-6.67713381126026));
#12706=CARTESIAN_POINT('Ctrl Pts',(3.85685855264548,-1.13423920652473,-6.67784431832386));
#12707=CARTESIAN_POINT('Ctrl Pts',(3.77397218326361,-1.15664307375816,-6.68375271513853));
#12708=CARTESIAN_POINT('Ctrl Pts',(3.69940161201151,-1.16928403529077,-6.68917232137838));
#12709=CARTESIAN_POINT('Ctrl Pts',(3.56647119885207,-1.17886067955666,-6.69892168937668));
#12710=CARTESIAN_POINT('Ctrl Pts',(3.50856621911921,-1.17876252662703,-6.70319260695171));
#12711=CARTESIAN_POINT('Ctrl Pts',(3.430476630254,-1.17287014583568,-6.70884754199157));
#12712=CARTESIAN_POINT('Ctrl Pts',(3.41009381814368,-1.17079624066649,-6.71031328272101));
#12713=CARTESIAN_POINT('Ctrl Pts',(3.3768353038047,-1.16653299596295,-6.7126780057569));
#12714=CARTESIAN_POINT('Ctrl Pts',(3.36392403236121,-1.16465945968854,-6.71358930928048));
#12715=CARTESIAN_POINT('Ctrl Pts',(3.34640590602214,-1.1618194659259,-6.71481430947922));
#12716=CARTESIAN_POINT('Ctrl Pts',(3.34177035121634,-1.16103945315861,-6.71513736493399));
#12717=CARTESIAN_POINT('Ctrl Pts',(3.33401534805295,-1.15968674565955,-6.7156758392496));
#12718=CARTESIAN_POINT('Ctrl Pts',(3.330893357844,-1.15912917352665,-6.71589207864268));
#12719=CARTESIAN_POINT('Ctrl Pts',(3.32496359592468,-1.15804541331727,-6.71630172199128));
#12720=CARTESIAN_POINT('Ctrl Pts',(3.32215543508724,-1.15752161169072,-6.71649526149435));
#12721=CARTESIAN_POINT('Ctrl Pts',(3.31548077415606,-1.15625145174104,-6.71695425751133));
#12722=CARTESIAN_POINT('Ctrl Pts',(3.31161602595741,-1.155495902818,-6.7172192056744));
#12723=CARTESIAN_POINT('Ctrl Pts',(3.29793503437833,-1.15274999179229,-6.7181544379576));
#12724=CARTESIAN_POINT('Ctrl Pts',(3.28814013888731,-1.15065374441439,-6.71881913911782));
#12725=CARTESIAN_POINT('Ctrl Pts',(3.21947976052878,-1.13504081276552,-6.72345183954457));
#12726=CARTESIAN_POINT('Ctrl Pts',(3.16169609695336,-1.1171367409232,-6.72721468055645));
#12727=CARTESIAN_POINT('Ctrl Pts',(3.0558610259697,-1.07518610689265,-6.7342672712723));
#12728=CARTESIAN_POINT('Ctrl Pts',(3.00758619799352,-1.05213946569287,-6.73755358868724));
#12729=CARTESIAN_POINT('Ctrl Pts',(2.92123351878949,-1.00344747065451,-6.74378862857377));
#12730=CARTESIAN_POINT('Ctrl Pts',(2.88276793149337,-0.978703761563427,
-6.7467114903992));
#12731=CARTESIAN_POINT('Ctrl Pts',(2.83741459217629,-0.945649557057543,
-6.75040308936541));
#12732=CARTESIAN_POINT('Ctrl Pts',(2.82907137834889,-0.939397598930528,
-6.7510929208828));
#12733=CARTESIAN_POINT('Ctrl Pts',(2.81595303325433,-0.92929269168857,-6.75219538589434));
#12734=CARTESIAN_POINT('Ctrl Pts',(2.81112298626219,-0.925511674339759,
-6.75260522442358));
#12735=CARTESIAN_POINT('Ctrl Pts',(2.80206687151045,-0.918307639487769,
-6.75338122221944));
#12736=CARTESIAN_POINT('Ctrl Pts',(2.79783453391576,-0.914892733165022,
-6.75374705493866));
#12737=CARTESIAN_POINT('Ctrl Pts',(2.78832200767073,-0.907108063804068,
-6.75457659830966));
#12738=CARTESIAN_POINT('Ctrl Pts',(2.7830560466221,-0.902721306331306,-6.75504098096405));
#12739=CARTESIAN_POINT('Ctrl Pts',(2.76723079188693,-0.889302524766589,
-6.75645249151779));
#12740=CARTESIAN_POINT('Ctrl Pts',(2.75679308935315,-0.880129635948533,
-6.75740529730052));
#12741=CARTESIAN_POINT('Ctrl Pts',(2.67239925143129,-0.803273702268906,
-6.76529445937801));
#12742=CARTESIAN_POINT('Ctrl Pts',(2.60721341766611,-0.72659719171487,-6.77263362982777));
#12743=CARTESIAN_POINT('Ctrl Pts',(2.54760172196587,-0.63504080914287,-6.7806444360294));
#12744=CARTESIAN_POINT('Ctrl Pts',(2.54275563879319,-0.627406980593619,
-6.78130681115992));
#12745=CARTESIAN_POINT('Ctrl Pts',(2.51416970121923,-0.581209487116651,
-6.78527972789266));
#12746=CARTESIAN_POINT('Ctrl Pts',(2.49257972503752,-0.541354463291943,
-6.78856125460678));
#12747=CARTESIAN_POINT('Ctrl Pts',(2.46923364269699,-0.491607065996209,
-6.79240971705387));
#12748=CARTESIAN_POINT('Ctrl Pts',(2.46523764919929,-0.482812434938268,
-6.79308098821138));
#12749=CARTESIAN_POINT('Ctrl Pts',(2.45966922551096,-0.470145577907281,
-6.79403387539043));
#12750=CARTESIAN_POINT('Ctrl Pts',(2.45800862003142,-0.466312876813195,
-6.79432038729489));
#12751=CARTESIAN_POINT('Ctrl Pts',(2.45516024036512,-0.459641708385756,
-6.79481585096563));
#12752=CARTESIAN_POINT('Ctrl Pts',(2.45396314725701,-0.456807301865322,
-6.79502534908458));
#12753=CARTESIAN_POINT('Ctrl Pts',(2.45145430405074,-0.45080145079258,-6.79546708942839));
#12754=CARTESIAN_POINT('Ctrl Pts',(2.45014529747735,-0.447628939508743,
-6.79569917014659));
#12755=CARTESIAN_POINT('Ctrl Pts',(2.4466266519131,-0.438994287205734,-6.79632752076504));
#12756=CARTESIAN_POINT('Ctrl Pts',(2.44444406783868,-0.433521124072911,
-6.79672222760861));
#12757=CARTESIAN_POINT('Ctrl Pts',(2.4343161268973,-0.407559158618024,-6.79857869023566));
#12758=CARTESIAN_POINT('Ctrl Pts',(2.42690358519853,-0.386865538044714,
-6.80001203097592));
#12759=CARTESIAN_POINT('Ctrl Pts',(2.41324450231184,-0.345085114794105,
-6.80283692026412));
#12760=CARTESIAN_POINT('Ctrl Pts',(2.40700078244525,-0.324007038712493,
-6.80422790288981));
#12761=CARTESIAN_POINT('Ctrl Pts',(2.38504935955152,-0.241486362180716,
-6.80958467523989));
#12762=CARTESIAN_POINT('Ctrl Pts',(2.37372360218986,-0.178989729123073,
-6.81345784811891));
#12763=CARTESIAN_POINT('Ctrl Pts',(2.36369347475816,-0.0775462282988194,
-6.81981413563133));
#12764=CARTESIAN_POINT('Ctrl Pts',(2.36178645437343,-0.0390484374729072,
-6.82224090627389));
#12765=CARTESIAN_POINT('Ctrl Pts',(2.3617584524301,0.0233528855997684,-6.82625508664994));
#12766=CARTESIAN_POINT('Ctrl Pts',(2.3624741030455,0.0472276289898454,-6.82780978548872));
#12767=CARTESIAN_POINT('Ctrl Pts',(2.36444120900201,0.0797697700894638,
-6.82996265995066));
#12768=CARTESIAN_POINT('Ctrl Pts',(2.36506422404484,0.088470354637313,-6.83054154617317));
#12769=CARTESIAN_POINT('Ctrl Pts',(2.36621188892993,0.10233421586873,-6.83146955726326));
#12770=CARTESIAN_POINT('Ctrl Pts',(2.36667412925588,0.107502448255194,-6.83181674632096));
#12771=CARTESIAN_POINT('Ctrl Pts',(2.36769610319958,0.11813648966522,-6.83253375246205));
#12772=CARTESIAN_POINT('Ctrl Pts',(2.36825996220806,0.123601765149962,-6.83290368905072));
#12773=CARTESIAN_POINT('Ctrl Pts',(2.36966153568733,0.136314658528128,-6.83376765044031));
#12774=CARTESIAN_POINT('Ctrl Pts',(2.37052838903993,0.143558769729832,-6.83426256783966));
#12775=CARTESIAN_POINT('Ctrl Pts',(2.37354584110022,0.166932044275687,-6.83586813280142));
#12776=CARTESIAN_POINT('Ctrl Pts',(2.3759633270335,0.183024219701473,-6.83698699192357));
#12777=CARTESIAN_POINT('Ctrl Pts',(2.38246764859101,0.220953666794613,-6.83965737353814));
#12778=CARTESIAN_POINT('Ctrl Pts',(2.38684038647574,0.242734952476235,-6.84121719054443));
#12779=CARTESIAN_POINT('Ctrl Pts',(2.41664227400825,0.37210790352346,-6.85064031129608));
#12780=CARTESIAN_POINT('Ctrl Pts',(2.45649638177561,0.475786202878335,-6.85892347298615));
#12781=CARTESIAN_POINT('Ctrl Pts',(2.52185312925952,0.593316987607398,-6.86857015164366));
#12782=CARTESIAN_POINT('Ctrl Pts',(2.53413294163859,0.613895704616208,-6.87026668762828));
#12783=CARTESIAN_POINT('Ctrl Pts',(2.5502586990682,0.639136071292022,-6.87234428553934));
#12784=CARTESIAN_POINT('Ctrl Pts',(2.55352301263909,0.64416052165229,-6.87275768961468));
#12785=CARTESIAN_POINT('Ctrl Pts',(2.5587482993456,0.65207052099037,-6.87340797241401));
#12786=CARTESIAN_POINT('Ctrl Pts',(2.56068393865322,0.654972560705993,-6.87364643346443));
#12787=CARTESIAN_POINT('Ctrl Pts',(2.56417156785656,0.660151454470522,-6.87407171460712));
#12788=CARTESIAN_POINT('Ctrl Pts',(2.56571864891025,0.662431455184437,-6.87425884400697));
#12789=CARTESIAN_POINT('Ctrl Pts',(2.56947155445387,0.667920715522432,-6.87470915837135));
#12790=CARTESIAN_POINT('Ctrl Pts',(2.57168531122946,0.671124489960972,-6.87497181124606));
#12791=CARTESIAN_POINT('Ctrl Pts',(2.57856179719177,0.680971431693616,-6.87577875659032));
#12792=CARTESIAN_POINT('Ctrl Pts',(2.58327745414761,0.687577596972359,-6.87631965809008));
#12793=CARTESIAN_POINT('Ctrl Pts',(2.594474469119,0.702925465070551,-6.8775765737132));
#12794=CARTESIAN_POINT('Ctrl Pts',(2.6010095271337,0.711627264318275,-6.87828940948526));
#12795=CARTESIAN_POINT('Ctrl Pts',(2.6246683207623,0.74223737859779,-6.88080259418332));
#12796=CARTESIAN_POINT('Ctrl Pts',(2.64244709400461,0.763629688795714,-6.88256956757008));
#12797=CARTESIAN_POINT('Ctrl Pts',(2.71624717849137,0.846290733441035,-6.88953014948902));
#12798=CARTESIAN_POINT('Ctrl Pts',(2.77791685332837,0.902190278146503,-6.89456020945228));
#12799=CARTESIAN_POINT('Ctrl Pts',(2.8779799133711,0.975260739708032,-6.90238144938915));
#12800=CARTESIAN_POINT('Ctrl Pts',(2.91223774222761,0.99763978986436,-6.90500497567985));
#12801=CARTESIAN_POINT('Ctrl Pts',(2.95665397386629,1.02346145575756,-6.90838408444585));
#12802=CARTESIAN_POINT('Ctrl Pts',(2.96579034400363,1.02861091220321,-6.90907794112124));
#12803=CARTESIAN_POINT('Ctrl Pts',(2.98038922446982,1.0365841455794,-6.91018535130848));
#12804=CARTESIAN_POINT('Ctrl Pts',(2.98580732021764,1.03948841770918,-6.9105960657593));
#12805=CARTESIAN_POINT('Ctrl Pts',(2.99557789382863,1.0446276933287,-6.91133633763614));
#12806=CARTESIAN_POINT('Ctrl Pts',(2.999922062018,1.0468782586212,-6.91166534227625));
#12807=CARTESIAN_POINT('Ctrl Pts',(3.01013540744032,1.05208898392355,-6.91243860675864));
#12808=CARTESIAN_POINT('Ctrl Pts',(3.01601554545276,1.05502717917947,-6.91288361435874));
#12809=CARTESIAN_POINT('Ctrl Pts',(3.03314434600629,1.06340766834748,-6.91417956492516));
#12810=CARTESIAN_POINT('Ctrl Pts',(3.04445512022817,1.06872021340993,-6.91503489968446));
#12811=CARTESIAN_POINT('Ctrl Pts',(3.07026111078137,1.08034343267464,-6.91698610640284));
#12812=CARTESIAN_POINT('Ctrl Pts',(3.0848029204116,1.08654412999859,-6.91808544202488));
#12813=CARTESIAN_POINT('Ctrl Pts',(3.13347979615136,1.106151872226,-6.92176556801476));
#12814=CARTESIAN_POINT('Ctrl Pts',(3.16811338083593,1.11825633481821,-6.92438515878998));
#12815=CARTESIAN_POINT('Ctrl Pts',(3.27713711834445,1.15073639310091,-6.9326184293187));
#12816=CARTESIAN_POINT('Ctrl Pts',(3.35300009215083,1.16543915224477,-6.93834205555534));
#12817=CARTESIAN_POINT('Ctrl Pts',(3.46160203977756,1.17560504884084,-6.94623244178478));
#12818=CARTESIAN_POINT('Ctrl Pts',(3.49356229339287,1.17728784614667,-6.94851554194323));
#12819=CARTESIAN_POINT('Ctrl Pts',(3.53205527235309,1.17774429433506,-6.95119004652786));
#12820=CARTESIAN_POINT('Ctrl Pts',(3.53855693738647,1.17776755344958,-6.95163919166778));
#12821=CARTESIAN_POINT('Ctrl Pts',(3.54866271551492,1.17772002000042,-6.95233294898447));
#12822=CARTESIAN_POINT('Ctrl Pts',(3.55226675154519,1.17768652412811,-6.95257950139132));
#12823=CARTESIAN_POINT('Ctrl Pts',(3.55891582329761,1.17759420117772,-6.95303270350876));
#12824=CARTESIAN_POINT('Ctrl Pts',(3.56196078344325,1.17754010820978,-6.95323959798634));
#12825=CARTESIAN_POINT('Ctrl Pts',(3.56890033084387,1.17738990092643,-6.95370965989493));
#12826=CARTESIAN_POINT('Ctrl Pts',(3.57279467737905,1.17728627452348,-6.95397241289479));
#12827=CARTESIAN_POINT('Ctrl Pts',(3.58480836779236,1.17690693688837,-6.95477997857616));
#12828=CARTESIAN_POINT('Ctrl Pts',(3.59292563546801,1.17656653277554,-6.95532139276072));
#12829=CARTESIAN_POINT('Ctrl Pts',(3.61191920870908,1.17557304421458,-6.95657969502754));
#12830=CARTESIAN_POINT('Ctrl Pts',(3.62279142004709,1.17485296792975,-6.95729339513135));
#12831=CARTESIAN_POINT('Ctrl Pts',(3.66142100468109,1.17175553079635,-6.95981077564493));
#12832=CARTESIAN_POINT('Ctrl Pts',(3.68910375097065,1.16854428311075,-6.96158096037175));
#12833=CARTESIAN_POINT('Ctrl Pts',(3.79898141687525,1.151828962299,-6.96856178832686));
#12834=CARTESIAN_POINT('Ctrl Pts',(3.87975351181944,1.13060683134617,-6.97360820901913));
#12835=CARTESIAN_POINT('Ctrl Pts',(3.99554955308146,1.0866360613769,-6.98142920784409));
#12836=CARTESIAN_POINT('Ctrl Pts',(4.03271244296891,1.07028103207164,-6.9840330768067));
#12837=CARTESIAN_POINT('Ctrl Pts',(4.07830420868544,1.04733717994058,-6.98739015706453));
#12838=CARTESIAN_POINT('Ctrl Pts',(4.08759038698651,1.04250775236297,-6.98808266737241));
#12839=CARTESIAN_POINT('Ctrl Pts',(4.10222241145279,1.03464859994552,-6.98918842348921));
#12840=CARTESIAN_POINT('Ctrl Pts',(4.10761118408278,1.03169962835317,-6.98959884501701));
#12841=CARTESIAN_POINT('Ctrl Pts',(4.11725047536827,1.026326169348,-6.99033886629625));
#12842=CARTESIAN_POINT('Ctrl Pts',(4.1215094498028,1.02391707625673,-6.99066791565676));
#12843=CARTESIAN_POINT('Ctrl Pts',(4.13145976732477,1.01820653131191,-6.99144164850299));
#12844=CARTESIAN_POINT('Ctrl Pts',(4.13713865422664,1.01488381544195,-6.99188708269975));
#12845=CARTESIAN_POINT('Ctrl Pts',(4.15354724550633,1.00509767556964,-6.99318552368948));
#12846=CARTESIAN_POINT('Ctrl Pts',(4.16420176897901,0.998510611830281,-6.99404294828922));
#12847=CARTESIAN_POINT('Ctrl Pts',(4.1881008433109,0.983202997381192,-6.99599966527891));
#12848=CARTESIAN_POINT('Ctrl Pts',(4.20127817750515,0.974382518504581,-6.99710244965141));
#12849=CARTESIAN_POINT('Ctrl Pts',(4.24446813913542,0.944192296356771,-7.00079823258044));
#12850=CARTESIAN_POINT('Ctrl Pts',(4.27365368339299,0.921682269978761,-7.0034303986974));
#12851=CARTESIAN_POINT('Ctrl Pts',(4.3666215747848,0.842758117476609,-7.0122580986104));
#12852=CARTESIAN_POINT('Ctrl Pts',(4.4253428181045,0.78080430182532,-7.01859655327805));
#12853=CARTESIAN_POINT('Ctrl Pts',(4.49173489557294,0.69352905887114,-7.02646820873037));
#12854=CARTESIAN_POINT('Ctrl Pts',(4.50598314550552,0.673531681459298,-7.02820756241506));
#12855=CARTESIAN_POINT('Ctrl Pts',(4.52294516082613,0.648077620395582,-7.03032959292079));
#12856=CARTESIAN_POINT('Ctrl Pts',(4.52625468912475,0.643027448770807,-7.03074623642977));
#12857=CARTESIAN_POINT('Ctrl Pts',(4.53142055666271,0.635010792467661,-7.03140046871349));
#12858=CARTESIAN_POINT('Ctrl Pts',(4.53330270842835,0.632061188902619,-7.03163967101463));
#12859=CARTESIAN_POINT('Ctrl Pts',(4.53664249492721,0.626775462534022,-7.03206556867885));
#12860=CARTESIAN_POINT('Ctrl Pts',(4.53810507870295,0.624442622155051,-7.03225257927809));
#12861=CARTESIAN_POINT('Ctrl Pts',(4.54160793173517,0.618811744674869,-7.03270170007058));
#12862=CARTESIAN_POINT('Ctrl Pts',(4.54364010875641,0.615508734854622,-7.03296328610699));
#12863=CARTESIAN_POINT('Ctrl Pts',(4.54983152899528,0.605333203400713,-7.03376363905737));
#12864=CARTESIAN_POINT('Ctrl Pts',(4.55393691031919,0.598427945324766,-7.03429909447342));
#12865=CARTESIAN_POINT('Ctrl Pts',(4.56336416527044,0.58219545329873,-7.03554129993238));
#12866=CARTESIAN_POINT('Ctrl Pts',(4.56862984534281,0.572836237231097,-7.03624497275124));
#12867=CARTESIAN_POINT('Ctrl Pts',(4.58680310738221,0.53947546330884,-7.03871387024338));
#12868=CARTESIAN_POINT('Ctrl Pts',(4.59900565958248,0.515098048178396,-7.04044697458996));
#12869=CARTESIAN_POINT('Ctrl Pts',(4.64375868190631,0.417359329041283,-7.04720422796433));
#12870=CARTESIAN_POINT('Ctrl Pts',(4.66962187985426,0.341177737989694,-7.0520714402714));
#12871=CARTESIAN_POINT('Ctrl Pts',(4.69738058053782,0.219988313203584,-7.05989752168927));
#12872=CARTESIAN_POINT('Ctrl Pts',(4.70480147631856,0.176506033451226,-7.06271819697244));
#12873=CARTESIAN_POINT('Ctrl Pts',(4.71095973806301,0.122203362351113,-7.0663110198783));
#12874=CARTESIAN_POINT('Ctrl Pts',(4.7120099783872,0.11167792246834,-7.06701054922194));
#12875=CARTESIAN_POINT('Ctrl Pts',(4.71345306976491,0.0949355685228497,
-7.06812888491756));
#12876=CARTESIAN_POINT('Ctrl Pts',(4.71393863073535,0.0887270579131143,
-7.06854481798648));
#12877=CARTESIAN_POINT('Ctrl Pts',(4.71475512596359,0.0771017389255085,
-7.06932606683925));
#12878=CARTESIAN_POINT('Ctrl Pts',(4.71509790381717,0.0716859062987276,
-7.0696910056985));
#12879=CARTESIAN_POINT('Ctrl Pts',(4.71578111806654,0.0595626924295782,
-7.0705102004321));
#12880=CARTESIAN_POINT('Ctrl Pts',(4.71610163264545,0.0528544235359496,
-7.0709650600379));
#12881=CARTESIAN_POINT('Ctrl Pts',(4.71688184619523,0.0329559973079337,
-7.07231912300433));
#12882=CARTESIAN_POINT('Ctrl Pts',(4.71717720794089,0.0197608227562213,
-7.0732233445949));
#12883=CARTESIAN_POINT('Ctrl Pts',(4.71772531631624,-0.0785835143482757,
-7.08001209986993));
#12884=CARTESIAN_POINT('Ctrl Pts',(4.70896457929958,-0.16351529553302,-7.08617926684367));
#12885=CARTESIAN_POINT('Ctrl Pts',(4.67647328173662,-0.315159851093711,
-7.09755692516775));
#12886=CARTESIAN_POINT('Ctrl Pts',(4.65574570538109,-0.382139350420601,
-7.10271206375049));
#12887=CARTESIAN_POINT('Ctrl Pts',(4.62546688419015,-0.455970112022877,
-7.10830532817737));
#12888=CARTESIAN_POINT('Ctrl Pts',(4.62162824007426,-0.465006621511712,
-7.10898814851061));
#12889=CARTESIAN_POINT('Ctrl Pts',(4.6161054547918,-0.477568866689485,-7.10993387306767));
#12890=CARTESIAN_POINT('Ctrl Pts',(4.61451621964331,-0.481135527432326,
-7.11020198279427));
#12891=CARTESIAN_POINT('Ctrl Pts',(4.61173710184475,-0.487290082821082,
-7.11066385324795));
#12892=CARTESIAN_POINT('Ctrl Pts',(4.61055552751744,-0.489881658958593,
-7.11085810016822));
#12893=CARTESIAN_POINT('Ctrl Pts',(4.60803437035533,-0.495358651147113,
-7.11126807298457));
#12894=CARTESIAN_POINT('Ctrl Pts',(4.6066924752041,-0.4982429769944,-7.11148365144671));
#12895=CARTESIAN_POINT('Ctrl Pts',(4.60331869858652,-0.505418553060139,
-7.11201924163671));
#12896=CARTESIAN_POINT('Ctrl Pts',(4.60127249679907,-0.509703076545849,
-7.11233839510334));
#12897=CARTESIAN_POINT('Ctrl Pts',(4.59335598893426,-0.526024828496433,
-7.11355216653634));
#12898=CARTESIAN_POINT('Ctrl Pts',(4.58730617461557,-0.537974528177732,
-7.11443656459233));
#12899=CARTESIAN_POINT('Ctrl Pts',(4.57113500721997,-0.568607931362771,
-7.11669939343489));
#12900=CARTESIAN_POINT('Ctrl Pts',(4.56070926585022,-0.587126149222905,
-7.11806305040252));
#12901=CARTESIAN_POINT('Ctrl Pts',(4.52564812402616,-0.645639374330876,
-7.12239065165006));
#12902=CARTESIAN_POINT('Ctrl Pts',(4.49911919740118,-0.684447799843941,
-7.12529115394666));
#12903=CARTESIAN_POINT('Ctrl Pts',(4.42208324700518,-0.78382395189669,-7.13306862470912));
#12904=CARTESIAN_POINT('Ctrl Pts',(4.36770706680266,-0.841072046630359,
-7.13794684798209));
#12905=CARTESIAN_POINT('Ctrl Pts',(4.29629525084763,-0.902565557050582,
-7.1440881164435));
#12906=CARTESIAN_POINT('Ctrl Pts',(4.28436468504494,-0.912436160314251,
-7.14510563663329));
#12907=CARTESIAN_POINT('Ctrl Pts',(4.2667028192457,-0.926471215205673,-7.14660186467681));
#12908=CARTESIAN_POINT('Ctrl Pts',(4.26112273061399,-0.930823974402834,
-7.1470731528378));
#12909=CARTESIAN_POINT('Ctrl Pts',(4.25115276647287,-0.938457536113191,
-7.14791288009413));
#12910=CARTESIAN_POINT('Ctrl Pts',(4.24677854591947,-0.941758513211628,
-7.14828052128374));
#12911=CARTESIAN_POINT('Ctrl Pts',(4.23760693701277,-0.948579871057561,
-7.14904984236514));
#12912=CARTESIAN_POINT('Ctrl Pts',(4.23280559823294,-0.952094653679381,
-7.14945172326379));
#12913=CARTESIAN_POINT('Ctrl Pts',(4.22020251971272,-0.96117475787509,-7.15050452211094));
#12914=CARTESIAN_POINT('Ctrl Pts',(4.21235925589059,-0.966681410308054,
-7.15115763514999));
#12915=CARTESIAN_POINT('Ctrl Pts',(4.17613138693082,-0.991462023976714,
-7.15416566124351));
#12916=CARTESIAN_POINT('Ctrl Pts',(4.14698278190948,-1.00958388109635,-7.15656247583159));
#12917=CARTESIAN_POINT('Ctrl Pts',(4.10424251179752,-1.03363422219343,-7.16004652232032));
#12918=CARTESIAN_POINT('Ctrl Pts',(4.09126744113973,-1.04061795015813,-7.16110026873543));
#12919=CARTESIAN_POINT('Ctrl Pts',(4.0781692089456,-1.04735431885469,-7.16215973101906));
#12920=CARTESIAN_POINT('Origin',(3.53951905042299,8.32667268468867E-16,
0.924367114736157));
#12921=CARTESIAN_POINT('',(4.07816960641416,-1.04735411443809,-7.76226461992607));
#12922=CARTESIAN_POINT('',(4.07816926754758,-1.04735428871592,-7.66392024962001));
#12923=CARTESIAN_POINT('',(4.07816926754759,-1.04735428871592,0.924367114736157));
#12924=CARTESIAN_POINT('Ctrl Pts',(4.07816960641408,-1.04735411443813,-7.76226461992608));
#12925=CARTESIAN_POINT('Ctrl Pts',(4.14556688893452,-1.01269192788493,-7.75682161009484));
#12926=CARTESIAN_POINT('Ctrl Pts',(4.20950448577251,-0.971582581204844,
-7.75120889432629));
#12927=CARTESIAN_POINT('Ctrl Pts',(4.29235791872549,-0.906205453315994,
-7.7435124974742));
#12928=CARTESIAN_POINT('Ctrl Pts',(4.31494024023408,-0.886959356333163,
-7.74136708228466));
#12929=CARTESIAN_POINT('Ctrl Pts',(4.34512879996207,-0.859195473604848,
-7.73845527776039));
#12930=CARTESIAN_POINT('Ctrl Pts',(4.35337322174209,-0.85139023921627,-7.73765531120893));
#12931=CARTESIAN_POINT('Ctrl Pts',(4.36750977062185,-0.83761372868248,-7.73627714661413));
#12932=CARTESIAN_POINT('Ctrl Pts',(4.37345324343183,-0.831696557019306,
-7.73569566060694));
#12933=CARTESIAN_POINT('Ctrl Pts',(4.38209990431143,-0.822902266345793,
-7.73484732040817));
#12934=CARTESIAN_POINT('Ctrl Pts',(4.38485248793398,-0.820074396539185,
-7.73457689649046));
#12935=CARTESIAN_POINT('Ctrl Pts',(4.38970713354745,-0.815036555907846,
-7.7340993984581));
#12936=CARTESIAN_POINT('Ctrl Pts',(4.39181488219016,-0.812832196743304,
-7.73389189753237));
#12937=CARTESIAN_POINT('Ctrl Pts',(4.3963701542494,-0.808030928655589,-7.73344305606354));
#12938=CARTESIAN_POINT('Ctrl Pts',(4.39881445139993,-0.805431071227729,
-7.73320195612856));
#12939=CARTESIAN_POINT('Ctrl Pts',(4.40556957504016,-0.798180283170265,
-7.7325347899299));
#12940=CARTESIAN_POINT('Ctrl Pts',(4.40985478988405,-0.793505501344605,
-7.73211058469992));
#12941=CARTESIAN_POINT('Ctrl Pts',(4.43356395906844,-0.767217800467252,
-7.72975649443369));
#12942=CARTESIAN_POINT('Ctrl Pts',(4.45222236381671,-0.744924445941719,
-7.72787705318411));
#12943=CARTESIAN_POINT('Ctrl Pts',(4.53468386509084,-0.638641745695555,
-7.71931978289575));
#12944=CARTESIAN_POINT('Ctrl Pts',(4.58784769191558,-0.547015653763979,
-7.71301198460183));
#12945=CARTESIAN_POINT('Ctrl Pts',(4.63643928222183,-0.429345949587526,
-7.70490609887472));
#12946=CARTESIAN_POINT('Ctrl Pts',(4.64421094666931,-0.408934795361378,
-7.70350188756853));
#12947=CARTESIAN_POINT('Ctrl Pts',(4.65670621506438,-0.373156647211704,
-7.70103459210921));
#12948=CARTESIAN_POINT('Ctrl Pts',(4.66169104429829,-0.35788688164406,-7.69997978330874));
#12949=CARTESIAN_POINT('Ctrl Pts',(4.66847301687645,-0.33557517637653,-7.69843363712351));
#12950=CARTESIAN_POINT('Ctrl Pts',(4.67051986224482,-0.328610585780765,
-7.69795032981678));
#12951=CARTESIAN_POINT('Ctrl Pts',(4.67400126517393,-0.316346805770901,
-7.69709788943068));
#12952=CARTESIAN_POINT('Ctrl Pts',(4.67546341213067,-0.311055626011664,
-7.69672965287915));
#12953=CARTESIAN_POINT('Ctrl Pts',(4.67842674805309,-0.300032377602288,
-7.69596146357307));
#12954=CARTESIAN_POINT('Ctrl Pts',(4.67992177291725,-0.294298827124975,
-7.69556132559128));
#12955=CARTESIAN_POINT('Ctrl Pts',(4.68369246471328,-0.27937761272359,-7.69451836812927));
#12956=CARTESIAN_POINT('Ctrl Pts',(4.68590071255792,-0.270173514823771,
-7.69387342952474));
#12957=CARTESIAN_POINT('Ctrl Pts',(4.69459483236595,-0.231908560928371,
-7.69118494549031));
#12958=CARTESIAN_POINT('Ctrl Pts',(4.70008791690094,-0.202635820551755,
-7.68911065875982));
#12959=CARTESIAN_POINT('Ctrl Pts',(4.72096561249892,-0.0622027350810218,
-7.67906958150976));
#12960=CARTESIAN_POINT('Ctrl Pts',(4.72151870365948,0.0505470770343604,
-7.67066829831299));
#12961=CARTESIAN_POINT('Ctrl Pts',(4.70251539861179,0.187682554051796,-7.66071514207197));
#12962=CARTESIAN_POINT('Ctrl Pts',(4.69803931440612,0.213579701841117,-7.65885146117777));
#12963=CARTESIAN_POINT('Ctrl Pts',(4.69148657916122,0.245156184020468,-7.65661514843368));
#12964=CARTESIAN_POINT('Ctrl Pts',(4.69022836973812,0.250995633504863,-7.65620312203101));
#12965=CARTESIAN_POINT('Ctrl Pts',(4.68817342071676,0.260192434492154,-7.65555689540233));
#12966=CARTESIAN_POINT('Ctrl Pts',(4.68740628344853,0.263556192095195,-7.65532110619441));
#12967=CARTESIAN_POINT('Ctrl Pts',(4.68592805367901,0.269909057829779,-7.65487693049772));
#12968=CARTESIAN_POINT('Ctrl Pts',(4.68522005173237,0.272898732269683,-7.65466838725027));
#12969=CARTESIAN_POINT('Ctrl Pts',(4.68354671871649,0.279843401665547,-7.65418504824056));
#12970=CARTESIAN_POINT('Ctrl Pts',(4.6825725709175,0.283796204686188,-7.65391075220427));
#12971=CARTESIAN_POINT('Ctrl Pts',(4.67930457805331,0.296766904017365,-7.65301311455201));
#12972=CARTESIAN_POINT('Ctrl Pts',(4.67692428956788,0.305762946693021,-7.65239442003223));
#12973=CARTESIAN_POINT('Ctrl Pts',(4.65250890940407,0.393804922296951,-7.64636902511804));
#12974=CARTESIAN_POINT('Ctrl Pts',(4.62237270312612,0.470383641490296,-7.64135285622537));
#12975=CARTESIAN_POINT('Ctrl Pts',(4.55015983196625,0.609301078279215,-7.63166113997555));
#12976=CARTESIAN_POINT('Ctrl Pts',(4.50962003393686,0.671970707722357,-7.62701651962438));
#12977=CARTESIAN_POINT('Ctrl Pts',(4.45539595190987,0.740562445376185,-7.62129362756211));
#12978=CARTESIAN_POINT('Ctrl Pts',(4.44718649577451,0.750601772713224,-7.62043872537782));
#12979=CARTESIAN_POINT('Ctrl Pts',(4.4345060383587,0.765596399152738,-7.61913414032792));
#12980=CARTESIAN_POINT('Ctrl Pts',(4.43015576195676,0.77065284010654,-7.61868930563029));
#12981=CARTESIAN_POINT('Ctrl Pts',(4.42219024726662,0.779753836696831,-7.61787953296758));
#12982=CARTESIAN_POINT('Ctrl Pts',(4.41858954630701,0.783810914165555,-7.61751519731575));
#12983=CARTESIAN_POINT('Ctrl Pts',(4.41077109874536,0.792498682785925,-7.61672765773584));
#12984=CARTESIAN_POINT('Ctrl Pts',(4.40654419752674,0.797120872638972,-7.61630407910134));
#12985=CARTESIAN_POINT('Ctrl Pts',(4.39497423766218,0.809571920341705,-7.61515039278713));
#12986=CARTESIAN_POINT('Ctrl Pts',(4.38756084819705,0.817334305891291,-7.61441733018609));
#12987=CARTESIAN_POINT('Ctrl Pts',(4.34734595271497,0.858306196982865,-7.61047206654441));
#12988=CARTESIAN_POINT('Ctrl Pts',(4.3127021477042,0.889640785273998,-7.6071801280333));
#12989=CARTESIAN_POINT('Ctrl Pts',(4.21524262469063,0.967789587261133,-7.59819413757494));
#12990=CARTESIAN_POINT('Ctrl Pts',(4.1494648353104,1.0105363052994,-7.59239258528162));
#12991=CARTESIAN_POINT('Ctrl Pts',(4.04493593915915,1.06451921182557,-7.58383579205721));
#12992=CARTESIAN_POINT('Ctrl Pts',(4.00903992169192,1.08083219033206,-7.58100676178135));
#12993=CARTESIAN_POINT('Ctrl Pts',(3.96623188831529,1.09774999937062,-7.577808417719));
#12994=CARTESIAN_POINT('Ctrl Pts',(3.96005322310931,1.10013177475018,-7.57735096065689));
#12995=CARTESIAN_POINT('Ctrl Pts',(3.95049372172519,1.10372450057733,-7.57664996040968));
#12996=CARTESIAN_POINT('Ctrl Pts',(3.94712700566097,1.10497226631243,-7.57640436445649));
#12997=CARTESIAN_POINT('Ctrl Pts',(3.94089232620351,1.10725057799854,-7.57595199754452));
#12998=CARTESIAN_POINT('Ctrl Pts',(3.93802607329534,1.10828538836894,-7.57574498964887));
#12999=CARTESIAN_POINT('Ctrl Pts',(3.9314678314928,1.11062439470798,-7.5752734931914));
#13000=CARTESIAN_POINT('Ctrl Pts',(3.927773329516,1.11192131420009,-7.57500942905415));
#13001=CARTESIAN_POINT('Ctrl Pts',(3.91805844771433,1.11527730648662,-7.57431894286253));
#13002=CARTESIAN_POINT('Ctrl Pts',(3.91202763390589,1.11730609292246,-7.57389420224471));
#13003=CARTESIAN_POINT('Ctrl Pts',(3.86192002569974,1.13371164791394,-7.57039511874947));
#13004=CARTESIAN_POINT('Ctrl Pts',(3.81704039864237,1.14552497512976,-7.56745157925536));
#13005=CARTESIAN_POINT('Ctrl Pts',(3.71741807104378,1.16554645724494,-7.56109875264762));
#13006=CARTESIAN_POINT('Ctrl Pts',(3.66256090604426,1.17260715137597,-7.55771426052089));
#13007=CARTESIAN_POINT('Ctrl Pts',(3.55145784837768,1.17902230863197,-7.55078820078201));
#13008=CARTESIAN_POINT('Ctrl Pts',(3.49535288270694,1.17825480126588,-7.54725328098998));
#13009=CARTESIAN_POINT('Ctrl Pts',(3.42515159458367,1.17227261902852,-7.54265367479405));
#13010=CARTESIAN_POINT('Ctrl Pts',(3.41080757898879,1.17078449593913,-7.54170480659726));
#13011=CARTESIAN_POINT('Ctrl Pts',(3.38959066704497,1.16818873714807,-7.54028620263621));
#13012=CARTESIAN_POINT('Ctrl Pts',(3.38269408681089,1.16728290189347,-7.53982271421798));
#13013=CARTESIAN_POINT('Ctrl Pts',(3.37040931943457,1.16555851848352,-7.53899269576496));
#13014=CARTESIAN_POINT('Ctrl Pts',(3.36501798355633,1.16476355415321,-7.53862691011797));
#13015=CARTESIAN_POINT('Ctrl Pts',(3.35362916747868,1.16300340239256,-7.53785090376922));
#13016=CARTESIAN_POINT('Ctrl Pts',(3.34763326671612,1.16202917613298,-7.53744041047483));
#13017=CARTESIAN_POINT('Ctrl Pts',(3.33163964535706,1.15930334075905,-7.53634010672077));
#13018=CARTESIAN_POINT('Ctrl Pts',(3.32165676842966,1.15746883234305,-7.53564772395708));
#13019=CARTESIAN_POINT('Ctrl Pts',(3.27596070484942,1.14845937836228,-7.53245180078064));
#13020=CARTESIAN_POINT('Ctrl Pts',(3.24057212085304,1.13975970599746,-7.52990108477408));
#13021=CARTESIAN_POINT('Ctrl Pts',(3.12211405006214,1.10474229777203,-7.52110011411212));
#13022=CARTESIAN_POINT('Ctrl Pts',(3.0415842270428,1.07085959932035,-7.51464409387036));
#13023=CARTESIAN_POINT('Ctrl Pts',(2.94066112215654,1.01453236404436,-7.5062237636216));
#13024=CARTESIAN_POINT('Ctrl Pts',(2.91629388640277,0.999748642053308,-7.50416536506393));
#13025=CARTESIAN_POINT('Ctrl Pts',(2.87875349053625,0.975066160459048,-7.50097804434586));
#13026=CARTESIAN_POINT('Ctrl Pts',(2.86521121123606,0.965750562022281,-7.49982482722649));
#13027=CARTESIAN_POINT('Ctrl Pts',(2.84770921187083,0.953163388533873,-7.49833428488007));
#13028=CARTESIAN_POINT('Ctrl Pts',(2.84357033802254,0.950145615199158,-7.49798179332134));
#13029=CARTESIAN_POINT('Ctrl Pts',(2.83682787805081,0.945161795954031,-7.49740772525638));
#13030=CARTESIAN_POINT('Ctrl Pts',(2.83421259342468,0.943211803698645,-7.49718509412854));
#13031=CARTESIAN_POINT('Ctrl Pts',(2.82911093237284,0.939374850850652,-7.49675093831355));
#13032=CARTESIAN_POINT('Ctrl Pts',(2.82662390715178,0.937488837088095,-7.49653935625221));
#13033=CARTESIAN_POINT('Ctrl Pts',(2.82107232016178,0.933243973189096,-7.49606713477346));
#13034=CARTESIAN_POINT('Ctrl Pts',(2.81801179095989,0.930879849017439,-7.49580685619984));
#13035=CARTESIAN_POINT('Ctrl Pts',(2.80739828943548,0.922597595576172,-7.49490420832118));
#13036=CARTESIAN_POINT('Ctrl Pts',(2.79990579484172,0.916602083041674,-7.49426692723583));
#13037=CARTESIAN_POINT('Ctrl Pts',(2.73473396053334,0.863131884636884,-7.48871467942003));
#13038=CARTESIAN_POINT('Ctrl Pts',(2.68161143822556,0.810353882608565,-7.4841193203172));
#13039=CARTESIAN_POINT('Ctrl Pts',(2.58219490917316,0.690762617566794,-7.47449950292365));
#13040=CARTESIAN_POINT('Ctrl Pts',(2.53708382043786,0.623493270004544,-7.46948785952424));
#13041=CARTESIAN_POINT('Ctrl Pts',(2.49304658496915,0.540521511846388,-7.46334177058802));
#13042=CARTESIAN_POINT('Ctrl Pts',(2.48707455503482,0.528799288291251,-7.46247473973934));
#13043=CARTESIAN_POINT('Ctrl Pts',(2.47835580874302,0.510952673090671,-7.46115539102211));
#13044=CARTESIAN_POINT('Ctrl Pts',(2.47546289825003,0.504900546175978,-7.46070809240338));
#13045=CARTESIAN_POINT('Ctrl Pts',(2.4703233806384,0.493908021405485,-7.45989570768715));
#13046=CARTESIAN_POINT('Ctrl Pts',(2.46805890613414,0.488976146055614,-7.45953124269526));
#13047=CARTESIAN_POINT('Ctrl Pts',(2.46326615766888,0.478344697240547,-7.45874552669394));
#13048=CARTESIAN_POINT('Ctrl Pts',(2.46074890777709,0.472640365706225,-7.45832391593644));
#13049=CARTESIAN_POINT('Ctrl Pts',(2.45407147222019,0.457177376545754,-7.45718080115945));
#13050=CARTESIAN_POINT('Ctrl Pts',(2.44999773135078,0.447382253977575,-7.45645643231889));
#13051=CARTESIAN_POINT('Ctrl Pts',(2.42950247694841,0.396161552753347,-7.45266618120069));
#13052=CARTESIAN_POINT('Ctrl Pts',(2.41531137661965,0.353888396322722,-7.44952797532048));
#13053=CARTESIAN_POINT('Ctrl Pts',(2.38405264448443,0.239681402833478,-7.44102609144474));
#13054=CARTESIAN_POINT('Ctrl Pts',(2.37130027080308,0.166772635025084,-7.43556544492163));
#13055=CARTESIAN_POINT('Ctrl Pts',(2.36298973644776,0.0620364063141323,
-7.42789490259095));
#13056=CARTESIAN_POINT('Ctrl Pts',(2.36175857158196,0.0308262828120917,
-7.42563304031908));
#13057=CARTESIAN_POINT('Ctrl Pts',(2.36177491127275,-0.0175518500710472,
-7.42219527426652));
#13058=CARTESIAN_POINT('Ctrl Pts',(2.3621554818096,-0.0347048538431212,
-7.42098975325048));
#13059=CARTESIAN_POINT('Ctrl Pts',(2.36314819822653,-0.0572345130445356,
-7.41942898196717));
#13060=CARTESIAN_POINT('Ctrl Pts',(2.36342273796347,-0.0626229830538355,
-7.41905739414851));
#13061=CARTESIAN_POINT('Ctrl Pts',(2.36392615809165,-0.0713263799025043,
-7.41846016669743));
#13062=CARTESIAN_POINT('Ctrl Pts',(2.36413204959821,-0.0746424809090667,
-7.41823330994137));
#13063=CARTESIAN_POINT('Ctrl Pts',(2.36455857239887,-0.081072063061075,
-7.41779486145195));
#13064=CARTESIAN_POINT('Ctrl Pts',(2.36477755038012,-0.0841855846151045,
-7.41758318788287));
#13065=CARTESIAN_POINT('Ctrl Pts',(2.3653381693077,-0.0917281502064954,
-7.41707189533858));
#13066=CARTESIAN_POINT('Ctrl Pts',(2.3656925002255,-0.0961562621719395,
-7.41677296861253));
#13067=CARTESIAN_POINT('Ctrl Pts',(2.3670347256975,-0.11181537776369,-7.4157199435097));
#13068=CARTESIAN_POINT('Ctrl Pts',(2.36815885684629,-0.123034508608218,
-7.41497290254353));
#13069=CARTESIAN_POINT('Ctrl Pts',(2.37135628342574,-0.150904988387344,
-7.41313170964893));
#13070=CARTESIAN_POINT('Ctrl Pts',(2.37362466863601,-0.167531834464555,
-7.41204630573908));
#13071=CARTESIAN_POINT('Ctrl Pts',(2.38513347139392,-0.240250300839454,
-7.40733432865442));
#13072=CARTESIAN_POINT('Ctrl Pts',(2.39807300964722,-0.295682575766201,
-7.40383180037847));
#13073=CARTESIAN_POINT('Ctrl Pts',(2.43758343936905,-0.42264185021791,-7.39560658305977));
#13074=CARTESIAN_POINT('Ctrl Pts',(2.46718873488503,-0.492944241335636,
-7.39088332970528));
#13075=CARTESIAN_POINT('Ctrl Pts',(2.5107463763192,-0.573552821775649,-7.38491289294547));
#13076=CARTESIAN_POINT('Ctrl Pts',(2.51839536227356,-0.587062544660563,
-7.38389276839869));
#13077=CARTESIAN_POINT('Ctrl Pts',(2.52992074156787,-0.606511758666798,
-7.382393372298));
#13078=CARTESIAN_POINT('Ctrl Pts',(2.53358749158466,-0.612574039532877,
-7.38192156487214));
#13079=CARTESIAN_POINT('Ctrl Pts',(2.54018795301456,-0.623267575890443,
-7.38108119440569));
#13080=CARTESIAN_POINT('Ctrl Pts',(2.54309974828614,-0.627912164240503,
-7.38071343288301));
#13081=CARTESIAN_POINT('Ctrl Pts',(2.54923839092688,-0.63755365117648,-7.37994414556265));
#13082=CARTESIAN_POINT('Ctrl Pts',(2.55247087385164,-0.642546759069216,
-7.37954242060587));
#13083=CARTESIAN_POINT('Ctrl Pts',(2.5610026075107,-0.655509132505916,-7.37849066869931));
#13084=CARTESIAN_POINT('Ctrl Pts',(2.56636132769273,-0.663438534579768,
-7.37783845531848));
#13085=CARTESIAN_POINT('Ctrl Pts',(2.59128342030557,-0.699364544516707,
-7.37484205455371));
#13086=CARTESIAN_POINT('Ctrl Pts',(2.61196048694143,-0.726564710922545,
-7.37245636668347));
#13087=CARTESIAN_POINT('Ctrl Pts',(2.676135566738,-0.803774249584545,-7.36532512157706));
#13088=CARTESIAN_POINT('Ctrl Pts',(2.72270194348722,-0.851053525663398,
-7.36047455959067));
#13089=CARTESIAN_POINT('Ctrl Pts',(2.81915164222707,-0.933735967846705,
-7.35115138795128));
#13090=CARTESIAN_POINT('Ctrl Pts',(2.86831396420381,-0.969678949547176,
-7.3466963901952));
#13091=CARTESIAN_POINT('Ctrl Pts',(2.92854601322085,-1.00692954776905,-7.34173031180666));
#13092=CARTESIAN_POINT('Ctrl Pts',(2.93712241950821,-1.01208373267619,-7.34103419675094));
#13093=CARTESIAN_POINT('Ctrl Pts',(2.94916336320602,-1.01911271225521,-7.34007317421425));
#13094=CARTESIAN_POINT('Ctrl Pts',(2.95257290143136,-1.02108020106437,-7.33980284581708));
#13095=CARTESIAN_POINT('Ctrl Pts',(2.95847352604694,-1.02444586023953,-7.33933818447485));
#13096=CARTESIAN_POINT('Ctrl Pts',(2.96095992581449,-1.02585211494429,-7.33914335195661));
#13097=CARTESIAN_POINT('Ctrl Pts',(2.96621850301783,-1.02880105427373,-7.33873336778936));
#13098=CARTESIAN_POINT('Ctrl Pts',(2.9689918426367,-1.03034160963548,-7.33851835712587));
#13099=CARTESIAN_POINT('Ctrl Pts',(2.97589300031738,-1.03413870848479,-7.33798624460505));
#13100=CARTESIAN_POINT('Ctrl Pts',(2.98002823316944,-1.03638179259591,-7.33766997664737));
#13101=CARTESIAN_POINT('Ctrl Pts',(2.99570141204313,-1.04476228211655,-7.33648055482144));
#13102=CARTESIAN_POINT('Ctrl Pts',(3.00732830167183,-1.05073255008836,-7.33561710094718));
#13103=CARTESIAN_POINT('Ctrl Pts',(3.03747289894531,-1.06558264308977,-7.33342042466545));
#13104=CARTESIAN_POINT('Ctrl Pts',(3.05612833523825,-1.07417420566003,-7.33210091350839));
#13105=CARTESIAN_POINT('Ctrl Pts',(3.12808628594222,-1.10505902904771,-7.32712667699415));
#13106=CARTESIAN_POINT('Ctrl Pts',(3.18278021541193,-1.12390861700971,-7.32357945695171));
#13107=CARTESIAN_POINT('Ctrl Pts',(3.31157466755809,-1.15794101315003,-7.31533086677878));
#13108=CARTESIAN_POINT('Ctrl Pts',(3.38618237176527,-1.17015883026993,-7.31061934435885));
#13109=CARTESIAN_POINT('Ctrl Pts',(3.47180595062898,-1.1758477448179,-7.30498743434305));
#13110=CARTESIAN_POINT('Ctrl Pts',(3.48217994915853,-1.17639925159406,-7.30430166016472));
#13111=CARTESIAN_POINT('Ctrl Pts',(3.49927920361848,-1.17708157826402,-7.30316502173826));
#13112=CARTESIAN_POINT('Ctrl Pts',(3.50600083752436,-1.17729215295732,-7.3027166167198));
#13113=CARTESIAN_POINT('Ctrl Pts',(3.51815048893182,-1.17756864402106,-7.30190305216002));
#13114=CARTESIAN_POINT('Ctrl Pts',(3.52357789664097,-1.17765462030809,-7.30153852215557));
#13115=CARTESIAN_POINT('Ctrl Pts',(3.53522806363121,-1.17775862201109,-7.30075359163784));
#13116=CARTESIAN_POINT('Ctrl Pts',(3.54145073621434,-1.17776485357393,-7.3003328379277));
#13117=CARTESIAN_POINT('Ctrl Pts',(3.55850502094474,-1.17764677740409,-7.29917542968816));
#13118=CARTESIAN_POINT('Ctrl Pts',(3.56933510123431,-1.17742234942754,-7.29843571678396));
#13119=CARTESIAN_POINT('Ctrl Pts',(3.63347263269487,-1.17520780571752,-7.29402578887434));
#13120=CARTESIAN_POINT('Ctrl Pts',(3.68659052806748,-1.16974748147788,-7.29024961513138));
#13121=CARTESIAN_POINT('Ctrl Pts',(3.78641748207615,-1.15257824430726,-7.2829285458542));
#13122=CARTESIAN_POINT('Ctrl Pts',(3.83314291179909,-1.14156911274191,-7.27940612396363));
#13123=CARTESIAN_POINT('Ctrl Pts',(3.90607884860877,-1.11960926775308,-7.27381761678875));
#13124=CARTESIAN_POINT('Ctrl Pts',(3.93279312957075,-1.11050735745112,-7.27175135618686));
#13125=CARTESIAN_POINT('Ctrl Pts',(3.99152812727448,-1.08810993835968,-7.2671937460092));
#13126=CARTESIAN_POINT('Ctrl Pts',(4.02334381197907,-1.07434144438989,-7.26471485313204));
#13127=CARTESIAN_POINT('Ctrl Pts',(4.05996151990547,-1.0565374849183,-7.26188482376515));
#13128=CARTESIAN_POINT('Ctrl Pts',(4.06539366050339,-1.05384425766796,-7.26146562114232));
#13129=CARTESIAN_POINT('Ctrl Pts',(4.07326404666124,-1.04986615046214,-7.26085942367658));
#13130=CARTESIAN_POINT('Ctrl Pts',(4.075718850527,-1.0486145286122,-7.26067051467021));
#13131=CARTESIAN_POINT('Ctrl Pts',(4.07816926754783,-1.04735428871579,-7.26048212650804));
#13132=CARTESIAN_POINT('',(2.36176959049357,0.00105055091081243,-7.32538762190826));
#13133=CARTESIAN_POINT('Ctrl Pts',(4.0781692089456,-1.04735431885469,-7.16215973101906));
#13134=CARTESIAN_POINT('Ctrl Pts',(4.03189278705024,-1.07115409849092,-7.165902840997));
#13135=CARTESIAN_POINT('Ctrl Pts',(3.98407925293551,-1.09186616169668,-7.16972076716216));
#13136=CARTESIAN_POINT('Ctrl Pts',(3.87851241723449,-1.12950442731467,-7.17794547881627));
#13137=CARTESIAN_POINT('Ctrl Pts',(3.82052010221274,-1.14531070155958,-7.18234059192762));
#13138=CARTESIAN_POINT('Ctrl Pts',(3.75171322921099,-1.15852036697102,-7.18725395155754));
#13139=CARTESIAN_POINT('Ctrl Pts',(3.7418317223724,-1.16028677905324,-7.18795233897041));
#13140=CARTESIAN_POINT('Ctrl Pts',(3.72804002897374,-1.16257061613521,-7.18891594365121));
#13141=CARTESIAN_POINT('Ctrl Pts',(3.72414833940331,-1.16319500670419,-7.18918661931587));
#13142=CARTESIAN_POINT('Ctrl Pts',(3.71742991545244,-1.16423835687664,-7.18965169543354));
#13143=CARTESIAN_POINT('Ctrl Pts',(3.71460468655344,-1.16466658232457,-7.18984659768361));
#13144=CARTESIAN_POINT('Ctrl Pts',(3.7086416525481,-1.16554822248687,-7.19025651077819));
#13145=CARTESIAN_POINT('Ctrl Pts',(3.70550352445459,-1.16599925742052,-7.19047138184478));
#13146=CARTESIAN_POINT('Ctrl Pts',(3.69771303154502,-1.16708687592374,-7.19100277904636));
#13147=CARTESIAN_POINT('Ctrl Pts',(3.69305854551136,-1.16770832699178,-7.19131847589845));
#13148=CARTESIAN_POINT('Ctrl Pts',(3.67549554654422,-1.16994644914826,-7.19250338905063));
#13149=CARTESIAN_POINT('Ctrl Pts',(3.66256370115544,-1.17137711680587,-7.19336299894246));
#13150=CARTESIAN_POINT('Ctrl Pts',(3.62929399595669,-1.17450070512467,-7.19554767394808));
#13151=CARTESIAN_POINT('Ctrl Pts',(3.60893046682664,-1.17587992628015,-7.19685921455894));
#13152=CARTESIAN_POINT('Ctrl Pts',(3.53068438219167,-1.17913956742849,-7.20183513682557));
#13153=CARTESIAN_POINT('Ctrl Pts',(3.47272613017931,-1.17727978250984,-7.20539074087249));
#13154=CARTESIAN_POINT('Ctrl Pts',(3.34005273553033,-1.16318935857027,-7.21365188002389));
#13155=CARTESIAN_POINT('Ctrl Pts',(3.26591996851086,-1.14801464601014,-7.21836738543932));
#13156=CARTESIAN_POINT('Ctrl Pts',(3.18382284931931,-1.1228015053018,-7.22400382123348));
#13157=CARTESIAN_POINT('Ctrl Pts',(3.17393206868165,-1.11962009421629,-7.22468967317676));
#13158=CARTESIAN_POINT('Ctrl Pts',(3.15771100241562,-1.11416466427672,-7.22582637733591));
#13159=CARTESIAN_POINT('Ctrl Pts',(3.15135567252948,-1.11196648940518,-7.22627476926045));
#13160=CARTESIAN_POINT('Ctrl Pts',(3.13990583621995,-1.10789611302313,-7.22708826712923));
#13161=CARTESIAN_POINT('Ctrl Pts',(3.13480474936594,-1.10604287939175,-7.22745274330312));
#13162=CARTESIAN_POINT('Ctrl Pts',(3.12963152328319,-1.10412285813431,-7.22782450567117));
#13163=CARTESIAN_POINT('Ctrl Pts',(3.12954632443391,-1.10409122571667,-7.22783062888601));
#13164=CARTESIAN_POINT('Ctrl Pts',(3.12934456579987,-1.1040162906975,-7.2278451306125));
#13165=CARTESIAN_POINT('Ctrl Pts',(3.1292280092276,-1.10397297950452,-7.22785350940733));
#13166=CARTESIAN_POINT('Ctrl Pts',(3.12900184752818,-1.10388889943817,-7.22786976942748));
#13167=CARTESIAN_POINT('Ctrl Pts',(3.12889224160648,-1.10384813269604,-7.22787765058237));
#13168=CARTESIAN_POINT('Ctrl Pts',(3.12867952544058,-1.1037689791426,-7.2278929477204));
#13169=CARTESIAN_POINT('Ctrl Pts',(3.12857641449611,-1.10373059420437,-7.22790036364171));
#13170=CARTESIAN_POINT('Ctrl Pts',(3.12837626508327,-1.10365605298337,-7.22791476042095));
#13171=CARTESIAN_POINT('Ctrl Pts',(3.12827922599752,-1.10361989834827,-7.22792174122452));
#13172=CARTESIAN_POINT('Ctrl Pts',(3.12809082732742,-1.10354967683723,-7.22793529574844));
#13173=CARTESIAN_POINT('Ctrl Pts',(3.12799946720125,-1.10351561141296,-7.22794186942074));
#13174=CARTESIAN_POINT('Ctrl Pts',(3.12782206150752,-1.10344943710745,-7.22795463568569));
#13175=CARTESIAN_POINT('Ctrl Pts',(3.1277360154572,-1.10341732950375,-7.22796082823634));
#13176=CARTESIAN_POINT('Ctrl Pts',(3.12756889889575,-1.10335494862061,-7.22797285643134));
#13177=CARTESIAN_POINT('Ctrl Pts',(3.12748782796089,-1.10332467646893,-7.22797869203847));
#13178=CARTESIAN_POINT('Ctrl Pts',(3.12733034659614,-1.10326585263539,-7.22799002882429));
#13179=CARTESIAN_POINT('Ctrl Pts',(3.12725393579239,-1.1032373019493,-7.2279955299701));
#13180=CARTESIAN_POINT('Ctrl Pts',(3.12710548182472,-1.103181814957,-7.22800621874234));
#13181=CARTESIAN_POINT('Ctrl Pts',(3.12703343832857,-1.10315487953001,-7.22801140633984));
#13182=CARTESIAN_POINT('Ctrl Pts',(3.12689344658147,-1.10310252416426,-7.2280214874744));
#13183=CARTESIAN_POINT('Ctrl Pts',(3.12682549803937,-1.10307710500405,-7.22802638098567));
#13184=CARTESIAN_POINT('Ctrl Pts',(3.12669344271404,-1.10302768995398,-7.22803589206598));
#13185=CARTESIAN_POINT('Ctrl Pts',(3.12662933567708,-1.1030036947547,-7.22804050961189));
#13186=CARTESIAN_POINT('Ctrl Pts',(3.12650472736896,-1.10295704160498,-7.22804948563811));
#13187=CARTESIAN_POINT('Ctrl Pts',(3.12644422586398,-1.10293438426287,-7.22805384409857));
#13188=CARTESIAN_POINT('Ctrl Pts',(3.12632660874939,-1.10289032653477,-7.22806231768533));
#13189=CARTESIAN_POINT('Ctrl Pts',(3.12626949293543,-1.10286892668916,-7.22806643279382));
#13190=CARTESIAN_POINT('Ctrl Pts',(3.12615844224776,-1.10282730897758,-7.22807443434771));
#13191=CARTESIAN_POINT('Ctrl Pts',(3.12610450719502,-1.10280709159188,-7.22807832077715));
#13192=CARTESIAN_POINT('Ctrl Pts',(3.12599962686868,-1.10276776875449,-7.2280858786627));
#13193=CARTESIAN_POINT('Ctrl Pts',(3.12594868143424,-1.10274866372848,-7.22808955010477));
#13194=CARTESIAN_POINT('Ctrl Pts',(3.12584960193837,-1.10271150013656,-7.22809669079727));
#13195=CARTESIAN_POINT('Ctrl Pts',(3.12580146773137,-1.10269344194785,-7.22810016003541));
#13196=CARTESIAN_POINT('Ctrl Pts',(3.12570784407525,-1.10265831079342,-7.22810690826171));
#13197=CARTESIAN_POINT('Ctrl Pts',(3.12566235450039,-1.10264123816444,-7.22811018723868));
#13198=CARTESIAN_POINT('Ctrl Pts',(3.12557386441292,-1.10260802082552,-7.22811656610591));
#13199=CARTESIAN_POINT('Ctrl Pts',(3.12553086379293,-1.10259187641686,-7.22811966598589));
#13200=CARTESIAN_POINT('Ctrl Pts',(3.12544720606644,-1.10256046187832,-7.22812569709862));
#13201=CARTESIAN_POINT('Ctrl Pts',(3.12540654885501,-1.10254519201314,-7.22812862832288));
#13202=CARTESIAN_POINT('Ctrl Pts',(3.12532744174252,-1.10251547630215,-7.22813433189665));
#13203=CARTESIAN_POINT('Ctrl Pts',(3.125288991759,-1.10250103069625,-7.22813710423782));
#13204=CARTESIAN_POINT('Ctrl Pts',(3.12521417163555,-1.10247291641225,-7.228142499194));
#13205=CARTESIAN_POINT('Ctrl Pts',(3.12517780141175,-1.10245924794408,-7.22814512180231));
#13206=CARTESIAN_POINT('Ctrl Pts',(3.12510702140893,-1.10243264377458,-7.22815022586499));
#13207=CARTESIAN_POINT('Ctrl Pts',(3.12507261155463,-1.10241970826029,-7.2281527073134));
#13208=CARTESIAN_POINT('Ctrl Pts',(3.11889598244139,-1.1000974307304,-7.22859814908234));
#13209=CARTESIAN_POINT('Ctrl Pts',(3.11277328018497,-1.09773683867651,-7.22904279728506));
#13210=CARTESIAN_POINT('Ctrl Pts',(3.09417800232924,-1.09038839598744,-7.23040288465889));
#13211=CARTESIAN_POINT('Ctrl Pts',(3.08177111956379,-1.08523836512921,-7.23132366536547));
#13212=CARTESIAN_POINT('Ctrl Pts',(3.0533827131784,-1.07288107754954,-7.2334622600049));
#13213=CARTESIAN_POINT('Ctrl Pts',(3.03746893453555,-1.06552708577844,-7.23468474647203));
#13214=CARTESIAN_POINT('Ctrl Pts',(2.98311807810975,-1.03892286713517,-7.23894323940753));
#13215=CARTESIAN_POINT('Ctrl Pts',(2.94557760240269,-1.01792713896474,-7.24203281457939));
#13216=CARTESIAN_POINT('Ctrl Pts',(2.84281118088179,-0.952828748158203,
-7.25088773410883));
#13217=CARTESIAN_POINT('Ctrl Pts',(2.78073700149172,-0.904176119073045,
-7.25673434805639));
#13218=CARTESIAN_POINT('Ctrl Pts',(2.70817999179209,-0.834535718238671,
-7.26392979663895));
#13219=CARTESIAN_POINT('Ctrl Pts',(2.69280760370369,-0.818934899488915,
-7.26547700626055));
#13220=CARTESIAN_POINT('Ctrl Pts',(2.67386610554319,-0.798607959978751,
-7.26740314335034));
#13221=CARTESIAN_POINT('Ctrl Pts',(2.66988637399968,-0.794272438414205,
-7.26780898769877));
#13222=CARTESIAN_POINT('Ctrl Pts',(2.66363852330199,-0.787362770106394,
-7.26844771183));
#13223=CARTESIAN_POINT('Ctrl Pts',(2.6613489314276,-0.784808302965292,-7.26868212141593));
#13224=CARTESIAN_POINT('Ctrl Pts',(2.65702659302985,-0.779943328058985,
-7.26912523605247));
#13225=CARTESIAN_POINT('Ctrl Pts',(2.65499175622809,-0.777634874722648,
-7.26933408643254));
#13226=CARTESIAN_POINT('Ctrl Pts',(2.65021416581738,-0.772171844661248,
-7.26982507869239));
#13227=CARTESIAN_POINT('Ctrl Pts',(2.64747912575672,-0.769010604350966,
-7.27010666044162));
#13228=CARTESIAN_POINT('Ctrl Pts',(2.6387274723152,-0.758785666865766,-7.27100955505673));
#13229=CARTESIAN_POINT('Ctrl Pts',(2.63277730435533,-0.751665201079264,
-7.27162632253638));
#13230=CARTESIAN_POINT('Ctrl Pts',(2.58552534371156,-0.693741840681457,
-7.2765548998223));
#13231=CARTESIAN_POINT('Ctrl Pts',(2.54843557126951,-0.639638675217191,
-7.28061942503178));
#13232=CARTESIAN_POINT('Ctrl Pts',(2.49345074093151,-0.543064549221617,
-7.28749797029545));
#13233=CARTESIAN_POINT('Ctrl Pts',(2.47319423423252,-0.502124718753124,
-7.29031099425505));
#13234=CARTESIAN_POINT('Ctrl Pts',(2.43636275694106,-0.415339709853604,
-7.29622383666118));
#13235=CARTESIAN_POINT('Ctrl Pts',(2.42015456135697,-0.369436279673885,
-7.29932508744073));
#13236=CARTESIAN_POINT('Ctrl Pts',(2.40386173285749,-0.312241895559978,
-7.30323258168735));
#13237=CARTESIAN_POINT('Ctrl Pts',(2.40103634525039,-0.301777503336854,
-7.30394910241728));
#13238=CARTESIAN_POINT('Ctrl Pts',(2.39680104595856,-0.285184410987463,
-7.30508848591029));
#13239=CARTESIAN_POINT('Ctrl Pts',(2.39529505447766,-0.27908068818422,-7.30550828587332));
#13240=CARTESIAN_POINT('Ctrl Pts',(2.39258140445568,-0.267691045082041,
-7.30629304079023));
#13241=CARTESIAN_POINT('Ctrl Pts',(2.39136123629985,-0.262408253565323,
-7.30665758760299));
#13242=CARTESIAN_POINT('Ctrl Pts',(2.38904289480896,-0.252045022624808,
-7.30737388973229));
#13243=CARTESIAN_POINT('Ctrl Pts',(2.3879417898328,-0.246965360854379,-7.30772554289584));
#13244=CARTESIAN_POINT('Ctrl Pts',(2.38554040392649,-0.235521834293679,
-7.30851905507155));
#13245=CARTESIAN_POINT('Ctrl Pts',(2.38425908114074,-0.229154208867454,
-7.30896150021165));
#13246=CARTESIAN_POINT('Ctrl Pts',(2.38115766622933,-0.213053982500291,
-7.31008260582606));
#13247=CARTESIAN_POINT('Ctrl Pts',(2.37940754428838,-0.203308580360016,
-7.31076341986982));
#13248=CARTESIAN_POINT('Ctrl Pts',(2.36706479407936,-0.129221253194858,
-7.31595686887277));
#13249=CARTESIAN_POINT('Ctrl Pts',(2.36171133875935,-0.0641335218267783,
-7.32063005701069));
#13250=CARTESIAN_POINT('Ctrl Pts',(2.36176951954998,0.00105120331072818,
-7.32538754544545));
#13251=CARTESIAN_POINT('Ctrl Pts',(2.36176951897595,0.00105055998136013,
-7.32538749849224));
#13252=CARTESIAN_POINT('Ctrl Pts',(2.36184243587445,0.0827953861394267,
-7.33135362058476));
#13253=CARTESIAN_POINT('Ctrl Pts',(2.37042547558946,0.164315098730552,-7.33742953962348));
#13254=CARTESIAN_POINT('Ctrl Pts',(2.38948890391776,0.254221795642659,-7.34393441290863));
#13255=CARTESIAN_POINT('Ctrl Pts',(2.39172231424939,0.264122561087035,-7.34464772615235));
#13256=CARTESIAN_POINT('Ctrl Pts',(2.39534885736636,0.279283395544758,-7.34573413890476));
#13257=CARTESIAN_POINT('Ctrl Pts',(2.39665086308174,0.284564500223568,-7.34611147720832));
#13258=CARTESIAN_POINT('Ctrl Pts',(2.39914707353257,0.294395898268841,-7.34681164566584));
#13259=CARTESIAN_POINT('Ctrl Pts',(2.40033203985735,0.298948402640113,-7.3471349434781));
#13260=CARTESIAN_POINT('Ctrl Pts',(2.40236167494422,0.306558685530069,-7.3476737087491));
#13261=CARTESIAN_POINT('Ctrl Pts',(2.40319146806741,0.309620333042458,-7.34788999859804));
#13262=CARTESIAN_POINT('Ctrl Pts',(2.40479184859045,0.315432078538282,-7.34829965056871));
#13263=CARTESIAN_POINT('Ctrl Pts',(2.40556008301194,0.318182776749839,-7.3484931487926));
#13264=CARTESIAN_POINT('Ctrl Pts',(2.40741068161247,0.324717093114046,-7.34895193787748));
#13265=CARTESIAN_POINT('Ctrl Pts',(2.4085020274289,0.328498164516393,-7.34921672146595));
#13266=CARTESIAN_POINT('Ctrl Pts',(2.41243382993525,0.341868374897534,-7.35015079328584));
#13267=CARTESIAN_POINT('Ctrl Pts',(2.41537754522886,0.351427051522242,-7.35081451658718));
#13268=CARTESIAN_POINT('Ctrl Pts',(2.43718135149746,0.419148071552181,-7.35549551203285));
#13269=CARTESIAN_POINT('Ctrl Pts',(2.46042628962904,0.47580906762492,-7.35930230538704));
#13270=CARTESIAN_POINT('Ctrl Pts',(2.50974391247105,0.573581496989081,-7.36608482172921));
#13271=CARTESIAN_POINT('Ctrl Pts',(2.53415507307774,0.615366299254801,-7.36906087915854));
#13272=CARTESIAN_POINT('Ctrl Pts',(2.5874105310899,0.694856085767757,-7.37505996221279));
#13273=CARTESIAN_POINT('Ctrl Pts',(2.61610060199798,0.732552522774052,-7.37807526913517));
#13274=CARTESIAN_POINT('Ctrl Pts',(2.65452626388713,0.777185089491855,-7.3819373798523));
#13275=CARTESIAN_POINT('Ctrl Pts',(2.66220270022906,0.785840252081935,-7.38270091629134));
#13276=CARTESIAN_POINT('Ctrl Pts',(2.67361826217614,0.798335507435076,-7.38382565087836));
#13277=CARTESIAN_POINT('Ctrl Pts',(2.67725824097824,0.802265574746541,-7.38418273850289));
#13278=CARTESIAN_POINT('Ctrl Pts',(2.68467733332273,0.810167115032765,-7.38490755162201));
#13279=CARTESIAN_POINT('Ctrl Pts',(2.68845761549258,0.814137302804437,-7.38527532129913));
#13280=CARTESIAN_POINT('Ctrl Pts',(2.69639413052852,0.822356833620065,-7.38604432634151));
#13281=CARTESIAN_POINT('Ctrl Pts',(2.70055508116586,0.826601384226098,-7.3864457588098));
#13282=CARTESIAN_POINT('Ctrl Pts',(2.71148723228862,0.83758560221194,-7.38749607367599));
#13283=CARTESIAN_POINT('Ctrl Pts',(2.7183085103172,0.844274583515395,-7.38814713204762));
#13284=CARTESIAN_POINT('Ctrl Pts',(2.74734697110669,0.872064969480325,-7.39090150189392));
#13285=CARTESIAN_POINT('Ctrl Pts',(2.77030007837068,0.892376484648271,-7.39303750174718));
#13286=CARTESIAN_POINT('Ctrl Pts',(2.88013590131762,0.982183056159513,-7.40308156844346));
#13287=CARTESIAN_POINT('Ctrl Pts',(2.97577712964786,1.04002794298598,-7.41140986004234));
#13288=CARTESIAN_POINT('Ctrl Pts',(3.10217961238231,1.09385298051383,-7.42128595344743));
#13289=CARTESIAN_POINT('Ctrl Pts',(3.12659832350609,1.10330269731129,-7.42314259493292));
#13290=CARTESIAN_POINT('Ctrl Pts',(3.15696084240543,1.11390307356102,-7.42537276390583));
#13291=CARTESIAN_POINT('Ctrl Pts',(3.16262307306998,1.11583164762738,-7.42578536431569));
#13292=CARTESIAN_POINT('Ctrl Pts',(3.17157548421258,1.11880494616473,-7.42643226240809));
#13293=CARTESIAN_POINT('Ctrl Pts',(3.17485588956654,1.11987845562197,-7.42666815477586));
#13294=CARTESIAN_POINT('Ctrl Pts',(3.18106425277223,1.12187996416063,-7.42711236553682));
#13295=CARTESIAN_POINT('Ctrl Pts',(3.18399109949272,1.12281092454739,-7.42732084183016));
#13296=CARTESIAN_POINT('Ctrl Pts',(3.19080166391844,1.1249479025798,-7.4278038177268));
#13297=CARTESIAN_POINT('Ctrl Pts',(3.19468802725204,1.12614526854072,-7.42807781966024));
#13298=CARTESIAN_POINT('Ctrl Pts',(3.20746497842382,1.13000942817179,-7.42897362701713));
#13299=CARTESIAN_POINT('Ctrl Pts',(3.21638116451142,1.13259133599541,-7.42959081085674));
#13300=CARTESIAN_POINT('Ctrl Pts',(3.30461931651397,1.15701604834792,-7.4356292015358));
#13301=CARTESIAN_POINT('Ctrl Pts',(3.38600528911636,1.17059883606947,-7.44065760695193));
#13302=CARTESIAN_POINT('Ctrl Pts',(3.51974568914811,1.17871783523835,-7.44895191517728));
#13303=CARTESIAN_POINT('Ctrl Pts',(3.5714860429165,1.1784499308291,-7.45216626088356));
#13304=CARTESIAN_POINT('Ctrl Pts',(3.64264827103797,1.17339077961384,-7.45672610473294));
#13305=CARTESIAN_POINT('Ctrl Pts',(3.66221938496886,1.17150591989179,-7.45799436912116));
#13306=CARTESIAN_POINT('Ctrl Pts',(3.69643933009624,1.16734337435549,-7.46024332415843));
#13307=CARTESIAN_POINT('Ctrl Pts',(3.71110966822755,1.16527728710072,-7.46121764982164));
#13308=CARTESIAN_POINT('Ctrl Pts',(3.7326780250518,1.16182360605822,-7.46266695613577));
#13309=CARTESIAN_POINT('Ctrl Pts',(3.73960921142448,1.16064999244261,-7.46313528068593));
#13310=CARTESIAN_POINT('Ctrl Pts',(3.75190200106858,1.15845514817542,-7.46397064963821));
#13311=CARTESIAN_POINT('Ctrl Pts',(3.75726783860394,1.15745855718234,-7.46433691241976));
#13312=CARTESIAN_POINT('Ctrl Pts',(3.76854971247594,1.15528196079142,-7.46511050347151));
#13313=CARTESIAN_POINT('Ctrl Pts',(3.77446398089755,1.15409372686963,-7.4655180809496));
#13314=CARTESIAN_POINT('Ctrl Pts',(3.79011800887891,1.15082336639973,-7.46660241557859));
#13315=CARTESIAN_POINT('Ctrl Pts',(3.79984075402518,1.14866307449062,-7.46728161601366));
#13316=CARTESIAN_POINT('Ctrl Pts',(3.84313430712023,1.13846581172964,-7.4703323530194));
#13317=CARTESIAN_POINT('Ctrl Pts',(3.87636647093499,1.12907928138577,-7.47274599948933));
#13318=CARTESIAN_POINT('Ctrl Pts',(4.00417984980738,1.08683286897286,-7.48231748144728));
#13319=CARTESIAN_POINT('Ctrl Pts',(4.09482696600384,1.04342893878017,-7.48978057988738));
#13320=CARTESIAN_POINT('Ctrl Pts',(4.1969291888781,0.977429846577178,-7.49857178806097));
#13321=CARTESIAN_POINT('Ctrl Pts',(4.21466129290306,0.965266936998673,-7.50011219556277));
#13322=CARTESIAN_POINT('Ctrl Pts',(4.24297525080469,0.944683454289842,-7.50258302830171));
#13323=CARTESIAN_POINT('Ctrl Pts',(4.2537621954935,0.936554442277191,-7.50352709800399));
#13324=CARTESIAN_POINT('Ctrl Pts',(4.2681615103941,0.925309632067565,-7.5047885187767));
#13325=CARTESIAN_POINT('Ctrl Pts',(4.27189780453866,0.922355198471373,-7.50511593942487));
#13326=CARTESIAN_POINT('Ctrl Pts',(4.27810189143184,0.917387916457647,-7.50565966168908));
#13327=CARTESIAN_POINT('Ctrl Pts',(4.28057959369621,0.915387608734789,-7.50587681741037));
#13328=CARTESIAN_POINT('Ctrl Pts',(4.28525603837566,0.911580772474331,-7.50628665285588));
#13329=CARTESIAN_POINT('Ctrl Pts',(4.28745639145432,0.909776288037184,-7.50647947796868));
#13330=CARTESIAN_POINT('Ctrl Pts',(4.29265243748205,0.905483478180304,-7.50693486227134));
#13331=CARTESIAN_POINT('Ctrl Pts',(4.29564239483926,0.902988215348579,-7.50719693190891));
#13332=CARTESIAN_POINT('Ctrl Pts',(4.30607926643327,0.894189957352579,-7.50811204707535));
#13333=CARTESIAN_POINT('Ctrl Pts',(4.31346043548588,0.887809096722862,-7.50875981770221));
#13334=CARTESIAN_POINT('Ctrl Pts',(4.37431224652546,0.833868285022994,-7.51411346174223));
#13335=CARTESIAN_POINT('Ctrl Pts',(4.42343279309649,0.781610747760335,-7.51852749624356));
#13336=CARTESIAN_POINT('Ctrl Pts',(4.5035778386305,0.679055847571457,-7.52657831834167));
#13337=CARTESIAN_POINT('Ctrl Pts',(4.53615057322714,0.630278622722896,-7.53019917419818));
#13338=CARTESIAN_POINT('Ctrl Pts',(4.57536544014826,0.560860934983936,-7.53528150761178));
#13339=CARTESIAN_POINT('Ctrl Pts',(4.58527339946112,0.54216279213002,-7.53664338901217));
#13340=CARTESIAN_POINT('Ctrl Pts',(4.60163643890632,0.509163517637524,-7.53904292912152));
#13341=CARTESIAN_POINT('Ctrl Pts',(4.60831949937232,0.494981209105619,-7.54007293641988));
#13342=CARTESIAN_POINT('Ctrl Pts',(4.61765134721941,0.474107052982491,-7.54158927476668));
#13343=CARTESIAN_POINT('Ctrl Pts',(4.62052523363759,0.467517245781826,-7.54206801240573));
#13344=CARTESIAN_POINT('Ctrl Pts',(4.62548259047749,0.455859921671493,-7.54291517124143));
#13345=CARTESIAN_POINT('Ctrl Pts',(4.62759138696171,0.450803357623126,-7.54328273091139));
#13346=CARTESIAN_POINT('Ctrl Pts',(4.63191835474615,0.440220716113297,-7.54405225834637));
#13347=CARTESIAN_POINT('Ctrl Pts',(4.63413004550781,0.434692174044824,-7.54445442963685));
#13348=CARTESIAN_POINT('Ctrl Pts',(4.63979860265615,0.420204921372195,-7.54550883678833));
#13349=CARTESIAN_POINT('Ctrl Pts',(4.6431879363808,0.411220439311926,-7.54616328015078));
#13350=CARTESIAN_POINT('Ctrl Pts',(4.65708892325133,0.37296128711295,-7.54895307983373));
#13351=CARTESIAN_POINT('Ctrl Pts',(4.66654768156233,0.343320108195707,-7.55112219011722));
#13352=CARTESIAN_POINT('Ctrl Pts',(4.70244830288698,0.213244596650607,-7.56068015706712));
#13353=CARTESIAN_POINT('Ctrl Pts',(4.71671304202461,0.109938252689443,-7.56842376183125));
#13354=CARTESIAN_POINT('Ctrl Pts',(4.71736622886991,-0.0156158618247626,
-7.57750567089768));
#13355=CARTESIAN_POINT('Ctrl Pts',(4.716877212013,-0.0373591426470613,-7.57906420987694));
#13356=CARTESIAN_POINT('Ctrl Pts',(4.71510343489739,-0.0726759822207703,
-7.58156069224452));
#13357=CARTESIAN_POINT('Ctrl Pts',(4.714184670166,-0.0862621879796819,-7.58251261002496));
#13358=CARTESIAN_POINT('Ctrl Pts',(4.7126254698977,-0.104590718879772,-7.58378273117153));
#13359=CARTESIAN_POINT('Ctrl Pts',(4.71219151337433,-0.10934892088687,-7.58411117793075));
#13360=CARTESIAN_POINT('Ctrl Pts',(4.71141979816182,-0.117276849438524,
-7.5846561359849));
#13361=CARTESIAN_POINT('Ctrl Pts',(4.71109811025182,-0.120448035470747,
-7.58487350931117));
#13362=CARTESIAN_POINT('Ctrl Pts',(4.71046512540397,-0.126445385579752,
-7.58528340079781));
#13363=CARTESIAN_POINT('Ctrl Pts',(4.71015646290111,-0.129271787298657,
-7.58547606661611));
#13364=CARTESIAN_POINT('Ctrl Pts',(4.70940188344247,-0.135957009251804,
-7.58593063614728));
#13365=CARTESIAN_POINT('Ctrl Pts',(4.70894710163209,-0.13981482562664,-7.58619205454313));
#13366=CARTESIAN_POINT('Ctrl Pts',(4.70727727039615,-0.153401175759362,
-7.58710976702059));
#13367=CARTESIAN_POINT('Ctrl Pts',(4.70595980233641,-0.163117039810494,
-7.58776071753037));
#13368=CARTESIAN_POINT('Ctrl Pts',(4.69409596646019,-0.243094686519461,
-7.5930835628376));
#13369=CARTESIAN_POINT('Ctrl Pts',(4.67733126855029,-0.312296423694265,
-7.59746797797777));
#13370=CARTESIAN_POINT('Ctrl Pts',(4.63543425501089,-0.435359471362672,
-7.60550918761953));
#13371=CARTESIAN_POINT('Ctrl Pts',(4.61228242720532,-0.489638728645046,
-7.60915095186344));
#13372=CARTESIAN_POINT('Ctrl Pts',(4.5753970519282,-0.560805312091225,-7.61425998699209));
#13373=CARTESIAN_POINT('Ctrl Pts',(4.56511975651704,-0.579386695731533,
-7.61562642941479));
#13374=CARTESIAN_POINT('Ctrl Pts',(4.54636948148894,-0.611223649158535,
-7.61803327764238));
#13375=CARTESIAN_POINT('Ctrl Pts',(4.53812260221285,-0.624606314666664,
-7.61906596603792));
#13376=CARTESIAN_POINT('Ctrl Pts',(4.5257132296598,-0.64386947151939,-7.62058552464857));
#13377=CARTESIAN_POINT('Ctrl Pts',(4.52176048484166,-0.649883540476997,
-7.62106475479168));
#13378=CARTESIAN_POINT('Ctrl Pts',(4.51470139804205,-0.660412355350961,
-7.62191247615958));
#13379=CARTESIAN_POINT('Ctrl Pts',(4.51161817041951,-0.664942395535229,
-7.62228010206081));
#13380=CARTESIAN_POINT('Ctrl Pts',(4.50512077440949,-0.674346935256228,
-7.62304946148975));
#13381=CARTESIAN_POINT('Ctrl Pts',(4.50170105535977,-0.679217391996296,
-7.62345139649413));
#13382=CARTESIAN_POINT('Ctrl Pts',(4.49267641491328,-0.691865599419147,
-7.62450449501469));
#13383=CARTESIAN_POINT('Ctrl Pts',(4.48701327534066,-0.699601067371228,
-7.62515785593197));
#13384=CARTESIAN_POINT('Ctrl Pts',(4.46266664202129,-0.73201903260682,-7.62793632418563));
#13385=CARTESIAN_POINT('Ctrl Pts',(4.44310978148363,-0.756027000026072,
-7.6300948429159));
#13386=CARTESIAN_POINT('Ctrl Pts',(4.36766627637729,-0.841527648912774,
-7.63817018883987));
#13387=CARTESIAN_POINT('Ctrl Pts',(4.30626961959595,-0.897823380166583,
-7.64429346404369));
#13388=CARTESIAN_POINT('Ctrl Pts',(4.19752946974113,-0.9781806811457,-7.65419106255317));
#13389=CARTESIAN_POINT('Ctrl Pts',(4.1535672243875,-1.00636042093365,-7.65797488144446));
#13390=CARTESIAN_POINT('Ctrl Pts',(4.10178348345933,-1.03489234583026,-7.66208708064864));
#13391=CARTESIAN_POINT('Ctrl Pts',(4.0956605067869,-1.0381956205251,-7.66256806356824));
#13392=CARTESIAN_POINT('Ctrl Pts',(4.08627127854972,-1.04315409470419,-7.66329724659285));
#13393=CARTESIAN_POINT('Ctrl Pts',(4.08302611141962,-1.04484857267568,-7.66354775914025));
#13394=CARTESIAN_POINT('Ctrl Pts',(4.07923865954719,-1.04680378662507,-7.66383833136182));
#13395=CARTESIAN_POINT('Ctrl Pts',(4.07870406858489,-1.04707924263269,-7.66387930335525));
#13396=CARTESIAN_POINT('Ctrl Pts',(4.07816926754758,-1.04735428871592,-7.66392024962001));
#13397=CARTESIAN_POINT('Origin',(3.53951905042299,8.32667268468867E-16,
0.924367114736157));
#13398=CARTESIAN_POINT('',(4.07816941731682,-1.04735421169017,-8.2621380879065));
#13399=CARTESIAN_POINT('',(4.0781691572555,-1.0473543454387,-8.16230176652656));
#13400=CARTESIAN_POINT('',(4.07816926754759,-1.04735428871592,0.924367114736157));
#13401=CARTESIAN_POINT('',(2.36176950623101,-0.000671540642540941,-7.92526768877284));
#13402=CARTESIAN_POINT('Ctrl Pts',(4.07816941731679,-1.04735421169019,-8.2621380879065));
#13403=CARTESIAN_POINT('Ctrl Pts',(4.09787021646655,-1.03722216412531,-8.26074508697215));
#13404=CARTESIAN_POINT('Ctrl Pts',(4.11729263674474,-1.02653040785042,-8.25934001281429));
#13405=CARTESIAN_POINT('Ctrl Pts',(4.15925528987737,-1.00186036158223,-8.25621923947244));
#13406=CARTESIAN_POINT('Ctrl Pts',(4.18163663589062,-0.987664937537115,
-8.25449844096451));
#13407=CARTESIAN_POINT('Ctrl Pts',(4.21101323274282,-0.967611987992991,
-8.25215165275585));
#13408=CARTESIAN_POINT('Ctrl Pts',(4.21844791336526,-0.962409989382561,
-8.25154987201976));
#13409=CARTESIAN_POINT('Ctrl Pts',(4.23056803536388,-0.953719285308015,
-8.25055542681309));
#13410=CARTESIAN_POINT('Ctrl Pts',(4.23528903781803,-0.950280641344982,
-8.25016466424955));
#13411=CARTESIAN_POINT('Ctrl Pts',(4.24442501643088,-0.943521677708989,
-8.24940169185106));
#13412=CARTESIAN_POINT('Ctrl Pts',(4.24884259995885,-0.940205125230167,
-8.24902963348167));
#13413=CARTESIAN_POINT('Ctrl Pts',(4.25918530220381,-0.932325840442442,
-8.24815103840464));
#13414=CARTESIAN_POINT('Ctrl Pts',(4.26509055981882,-0.927737552864946,
-8.24764351655232));
#13415=CARTESIAN_POINT('Ctrl Pts',(4.28452728992103,-0.912336449667722,
-8.24595312015627));
#13416=CARTESIAN_POINT('Ctrl Pts',(4.29786335948661,-0.901281824969567,
-8.24476077574491));
#13417=CARTESIAN_POINT('Ctrl Pts',(4.32917328033652,-0.874141216498856,
-8.24188072854002));
#13418=CARTESIAN_POINT('Ctrl Pts',(4.34690567509686,-0.857789816166167,
-8.24018286891336));
#13419=CARTESIAN_POINT('Ctrl Pts',(4.41057444698654,-0.795355415259501,
-8.23383374641222));
#13420=CARTESIAN_POINT('Ctrl Pts',(4.45316769001884,-0.746037725967231,
-8.22906555558485));
#13421=CARTESIAN_POINT('Ctrl Pts',(4.4929673045481,-0.691402906601309,-8.22410538503906));
#13422=CARTESIAN_POINT('Ctrl Pts',(4.49446062887,-0.689338911076299,-8.22391845959956));
#13423=CARTESIAN_POINT('Ctrl Pts',(4.51123550305327,-0.665994431249304,
-8.22180954230394));
#13424=CARTESIAN_POINT('Ctrl Pts',(4.52581001751704,-0.64421397816899,-8.21989101172835));
#13425=CARTESIAN_POINT('Ctrl Pts',(4.54703476143244,-0.610084333994029,
-8.2169742089834));
#13426=CARTESIAN_POINT('Ctrl Pts',(4.55421115809595,-0.598072532699133,
-8.21596398108153));
#13427=CARTESIAN_POINT('Ctrl Pts',(4.57273307190567,-0.565777214057839,
-8.21329574267617));
#13428=CARTESIAN_POINT('Ctrl Pts',(4.58369592508163,-0.545279651801057,
-8.2116513246021));
#13429=CARTESIAN_POINT('Ctrl Pts',(4.59671901417798,-0.519094725044495,
-8.20962316698562));
#13430=CARTESIAN_POINT('Ctrl Pts',(4.59935112062951,-0.513699409882844,
-8.20920906439331));
#13431=CARTESIAN_POINT('Ctrl Pts',(4.60343368236609,-0.505165978886334,
-8.20856032695725));
#13432=CARTESIAN_POINT('Ctrl Pts',(4.60491172633417,-0.502041290312482,
-8.2083240830048));
#13433=CARTESIAN_POINT('Ctrl Pts',(4.60767681181786,-0.496128500068766,
-8.2078795633681));
#13434=CARTESIAN_POINT('Ctrl Pts',(4.60896669700945,-0.493341892863146,
-8.20767112709396));
#13435=CARTESIAN_POINT('Ctrl Pts',(4.61196606337652,-0.486795158866127,
-8.20718386526916));
#13436=CARTESIAN_POINT('Ctrl Pts',(4.61366668204815,-0.483031043566971,
-8.20690557419312));
#13437=CARTESIAN_POINT('Ctrl Pts',(4.61916902760897,-0.47067949178062,-8.20599823306855));
#13438=CARTESIAN_POINT('Ctrl Pts',(4.62288796597554,-0.462055260417316,
-8.20537390274077));
#13439=CARTESIAN_POINT('Ctrl Pts',(4.64294164298617,-0.413977066192752,
-8.20193920370032));
#13440=CARTESIAN_POINT('Ctrl Pts',(4.65722622700692,-0.373697611893329,
-8.19923096705546));
#13441=CARTESIAN_POINT('Ctrl Pts',(4.67693768935054,-0.306767431839981,
-8.1948687038696));
#13442=CARTESIAN_POINT('Ctrl Pts',(4.68368616563274,-0.280551408272435,
-8.1931934384416));
#13443=CARTESIAN_POINT('Ctrl Pts',(4.70740820313345,-0.173200991391785,
-8.1863922214657));
#13444=CARTESIAN_POINT('Ctrl Pts',(4.71669733160403,-0.0906249788242832,
-8.18127545668112));
#13445=CARTESIAN_POINT('Ctrl Pts',(4.71733465130768,0.00607210071476501,
-8.17497260465963));
#13446=CARTESIAN_POINT('Ctrl Pts',(4.71718206071303,0.0199064941922861,
-8.17406405520422));
#13447=CARTESIAN_POINT('Ctrl Pts',(4.71658679466932,0.0406800681975707,
-8.17268803815387));
#13448=CARTESIAN_POINT('Ctrl Pts',(4.7163263134372,0.0476235736809692,-8.17222613817922));
#13449=CARTESIAN_POINT('Ctrl Pts',(4.71576774865549,0.059667051544863,-8.17142136979478));
#13450=CARTESIAN_POINT('Ctrl Pts',(4.7154978924116,0.0647681938443807,-8.17107937850627));
#13451=CARTESIAN_POINT('Ctrl Pts',(4.71486582255102,0.0754041951773591,
-8.17036389758792));
#13452=CARTESIAN_POINT('Ctrl Pts',(4.71449767778961,0.0809385620458983,
-8.16999023309416));
#13453=CARTESIAN_POINT('Ctrl Pts',(4.71353168187364,0.0940602300973112,
-8.16910094754776));
#13454=CARTESIAN_POINT('Ctrl Pts',(4.71289935663556,0.101644665258518,-8.16858427303211));
#13455=CARTESIAN_POINT('Ctrl Pts',(4.71051362700583,0.127259257566909,-8.16683003091132));
#13456=CARTESIAN_POINT('Ctrl Pts',(4.70841784309341,0.145254144319727,-8.16558198331525));
#13457=CARTESIAN_POINT('Ctrl Pts',(4.69797423765539,0.219897833869709,-8.16033683817268));
#13458=CARTESIAN_POINT('Ctrl Pts',(4.68591705833291,0.275941005798534,-8.15622925892115));
#13459=CARTESIAN_POINT('Ctrl Pts',(4.65124613749381,0.394380512588343,-8.14723060275528));
#13460=CARTESIAN_POINT('Ctrl Pts',(4.62733914904783,0.456202370662872,-8.14233132241669));
#13461=CARTESIAN_POINT('Ctrl Pts',(4.58531584570611,0.542487404669705,-8.1354028620356));
#13462=CARTESIAN_POINT('Ctrl Pts',(4.57125063138831,0.568782738265171,-8.13327973969102));
#13463=CARTESIAN_POINT('Ctrl Pts',(4.5529786859207,0.600029490407156,-8.13076583666157));
#13464=CARTESIAN_POINT('Ctrl Pts',(4.5497110809275,0.605514564812551,-8.13032490205492));
#13465=CARTESIAN_POINT('Ctrl Pts',(4.54454276796691,0.614031914759355,-8.12964108833851));
#13466=CARTESIAN_POINT('Ctrl Pts',(4.54267263049038,0.617082458691369,-8.12939635403739));
#13467=CARTESIAN_POINT('Ctrl Pts',(4.53918332728128,0.622716380763,-8.12894476272226));
#13468=CARTESIAN_POINT('Ctrl Pts',(4.53756803697222,0.625301989516149,-8.12873767564058));
#13469=CARTESIAN_POINT('Ctrl Pts',(4.5338461826726,0.631208429122032,-8.12826496249736));
#13470=CARTESIAN_POINT('Ctrl Pts',(4.53173301154942,0.634525006115584,-8.12799976961665));
#13471=CARTESIAN_POINT('Ctrl Pts',(4.52510067518684,0.644820164778107,-8.12717712876888));
#13472=CARTESIAN_POINT('Ctrl Pts',(4.52052408291728,0.651761704785397,-8.12662326431956));
#13473=CARTESIAN_POINT('Ctrl Pts',(4.50959642653452,0.667960295516328,-8.12533121790871));
#13474=CARTESIAN_POINT('Ctrl Pts',(4.50318566832801,0.677176300338191,-8.12459646287379));
#13475=CARTESIAN_POINT('Ctrl Pts',(4.47965573977095,0.709991529513571,-8.12197599025489));
#13476=CARTESIAN_POINT('Ctrl Pts',(4.46179255421233,0.733046239508686,-8.12012678473544));
#13477=CARTESIAN_POINT('Ctrl Pts',(4.38267794540693,0.827677232508278,-8.11239186556977));
#13478=CARTESIAN_POINT('Ctrl Pts',(4.31381708871012,0.892428961517595,-8.10670250495221));
#13479=CARTESIAN_POINT('Ctrl Pts',(4.21404835231191,0.965913324493517,-8.09878935867756));
#13480=CARTESIAN_POINT('Ctrl Pts',(4.18946207780677,0.982625136534703,-8.09686488413498));
#13481=CARTESIAN_POINT('Ctrl Pts',(4.15625276492076,1.00340623377441,-8.09428243244944));
#13482=CARTESIAN_POINT('Ctrl Pts',(4.14817390793684,1.00832722883727,-8.09365550825484));
#13483=CARTESIAN_POINT('Ctrl Pts',(4.13494073765065,1.01617083752472,-8.09263026103577));
#13484=CARTESIAN_POINT('Ctrl Pts',(4.12982199816092,1.01915287586252,-8.09223408111743));
#13485=CARTESIAN_POINT('Ctrl Pts',(4.11991668644993,1.02482378287332,-8.09146807789496));
#13486=CARTESIAN_POINT('Ctrl Pts',(4.11513337252015,1.02751805448563,-8.09109845941313));
#13487=CARTESIAN_POINT('Ctrl Pts',(4.10397935484342,1.0336983914267,-8.09023713035922));
#13488=CARTESIAN_POINT('Ctrl Pts',(4.09759495359104,1.03715914011266,-8.08974454451684));
#13489=CARTESIAN_POINT('Ctrl Pts',(4.07697376475947,1.0480915990565,-8.08815463417633));
#13490=CARTESIAN_POINT('Ctrl Pts',(4.06261636887136,1.05533062173797,-8.08704932136377));
#13491=CARTESIAN_POINT('Ctrl Pts',(4.02839318888358,1.07171604991502,-8.08441720446404));
#13492=CARTESIAN_POINT('Ctrl Pts',(4.00841250153652,1.08060725582464,-8.08288242384131));
#13493=CARTESIAN_POINT('Ctrl Pts',(3.89033799969225,1.12925785405858,-8.07382352804963));
#13494=CARTESIAN_POINT('Ctrl Pts',(3.78749306257316,1.15620092709752,-8.06591575437205));
#13495=CARTESIAN_POINT('Ctrl Pts',(3.65399016608896,1.17252468732886,-8.05621716720229));
#13496=CARTESIAN_POINT('Ctrl Pts',(3.62539875270154,1.17496500395357,-8.05417630264844));
#13497=CARTESIAN_POINT('Ctrl Pts',(3.59043539084954,1.17666583411506,-8.05174571652767));
#13498=CARTESIAN_POINT('Ctrl Pts',(3.58412394903756,1.17692198820975,-8.05130954715574));
#13499=CARTESIAN_POINT('Ctrl Pts',(3.574249754385,1.17724319220592,-8.0506315236999));
#13500=CARTESIAN_POINT('Ctrl Pts',(3.57068836230364,1.17734286859734,-8.05038786295831));
#13501=CARTESIAN_POINT('Ctrl Pts',(3.56407672093481,1.17749789370034,-8.04993722490762));
#13502=CARTESIAN_POINT('Ctrl Pts',(3.5610267183482,1.17755755247908,-8.04973002613013));
#13503=CARTESIAN_POINT('Ctrl Pts',(3.55402248454749,1.17766733428773,-8.04925573862796));
#13504=CARTESIAN_POINT('Ctrl Pts',(3.55006820246112,1.17770939385604,-8.04898909433009));
#13505=CARTESIAN_POINT('Ctrl Pts',(3.53768450464758,1.17777873588606,-8.04815732900005));
#13506=CARTESIAN_POINT('Ctrl Pts',(3.52925473588557,1.17773544148328,-8.04759590619492));
#13507=CARTESIAN_POINT('Ctrl Pts',(3.45128289249397,1.17649772056819,-8.04244112333659));
#13508=CARTESIAN_POINT('Ctrl Pts',(3.38196370783951,1.16923549712724,-8.03813430385383));
#13509=CARTESIAN_POINT('Ctrl Pts',(3.2306501769793,1.13967216950146,-8.02859508682647));
#13510=CARTESIAN_POINT('Ctrl Pts',(3.14961756253098,1.1145525457017,-8.0233788516996));
#13511=CARTESIAN_POINT('Ctrl Pts',(3.05930782627813,1.07549189626892,-8.01696511213609));
#13512=CARTESIAN_POINT('Ctrl Pts',(3.0467350499965,1.06978948491779,-8.01605847737323));
#13513=CARTESIAN_POINT('Ctrl Pts',(3.02799590737272,1.06088986949967,-8.01468487936058));
#13514=CARTESIAN_POINT('Ctrl Pts',(3.02175255572325,1.05785684032362,-8.01422345592586));
#13515=CARTESIAN_POINT('Ctrl Pts',(3.01096323863144,1.05249697973298,-8.01341928456777));
#13516=CARTESIAN_POINT('Ctrl Pts',(3.00640487540771,1.05019541682962,-8.01307741052808));
#13517=CARTESIAN_POINT('Ctrl Pts',(2.99702371536533,1.0453819598403,-8.01236935998165));
#13518=CARTESIAN_POINT('Ctrl Pts',(2.99220306726012,1.04286616753549,-8.01200305458771));
#13519=CARTESIAN_POINT('Ctrl Pts',(2.98088294371363,1.03685833125116,-8.01113695637178));
#13520=CARTESIAN_POINT('Ctrl Pts',(2.97439858270958,1.03333844963125,-8.01063619906663));
#13521=CARTESIAN_POINT('Ctrl Pts',(2.96071676443277,1.02574430249559,-8.00956954865645));
#13522=CARTESIAN_POINT('Ctrl Pts',(2.95352832332996,1.0216546980689,-8.0090031338202));
#13523=CARTESIAN_POINT('Ctrl Pts',(2.93405081734917,1.01030048393135,-8.00745172348554));
#13524=CARTESIAN_POINT('Ctrl Pts',(2.92185014566977,1.00288780164954,-8.00646156960118));
#13525=CARTESIAN_POINT('Ctrl Pts',(2.88317667090131,0.978417801883694,-8.00326279267926));
#13526=CARTESIAN_POINT('Ctrl Pts',(2.85725382311953,0.960520995304603,-8.00102578860465));
#13527=CARTESIAN_POINT('Ctrl Pts',(2.7904468856044,0.910328395448378,-7.99501370419639));
#13528=CARTESIAN_POINT('Ctrl Pts',(2.75093575032511,0.876323348329264,-7.99119351040912));
#13529=CARTESIAN_POINT('Ctrl Pts',(2.67128798005187,0.79801339596437,-7.98299678873544));
#13530=CARTESIAN_POINT('Ctrl Pts',(2.63200077614562,0.753035574767279,-7.9786309147343));
#13531=CARTESIAN_POINT('Ctrl Pts',(2.59026036599144,0.697211792060864,-7.97374251517666));
#13532=CARTESIAN_POINT('Ctrl Pts',(2.58433744388942,0.689075067245759,-7.97304228689874));
#13533=CARTESIAN_POINT('Ctrl Pts',(2.57623802634225,0.677643197491073,-7.97207653876398));
#13534=CARTESIAN_POINT('Ctrl Pts',(2.57397290368347,0.67441179860419,-7.9718055305378));
#13535=CARTESIAN_POINT('Ctrl Pts',(2.57009478155914,0.668819723883629,-7.97134001853496));
#13536=CARTESIAN_POINT('Ctrl Pts',(2.56847407562655,0.666464472785826,-7.97114501103933));
#13537=CARTESIAN_POINT('Ctrl Pts',(2.56507464085285,0.661485602260752,-7.97073503515564));
#13538=CARTESIAN_POINT('Ctrl Pts',(2.56329789826379,0.658860661934902,-7.97052020574611));
#13539=CARTESIAN_POINT('Ctrl Pts',(2.55891811024194,0.652333397869032,-7.96998917513778));
#13540=CARTESIAN_POINT('Ctrl Pts',(2.55632770460325,0.64842258228734,-7.96967380038315));
#13541=CARTESIAN_POINT('Ctrl Pts',(2.54666273304519,0.633639989371951,-7.96849175906524));
#13542=CARTESIAN_POINT('Ctrl Pts',(2.53974425220579,0.622666596284655,-7.96763463804521));
#13543=CARTESIAN_POINT('Ctrl Pts',(2.52245579714508,0.594214060390553,-7.9654578137858));
#13544=CARTESIAN_POINT('Ctrl Pts',(2.51235406731231,0.576576279199561,-7.96415151182035));
#13545=CARTESIAN_POINT('Ctrl Pts',(2.45467807658373,0.469541350189625,-7.95642501541004));
#13546=CARTESIAN_POINT('Ctrl Pts',(2.41833834277047,0.374573445293031,-7.95035414576092));
#13547=CARTESIAN_POINT('Ctrl Pts',(2.38650237053188,0.242567533977751,-7.94173392020738));
#13548=CARTESIAN_POINT('Ctrl Pts',(2.37988961134717,0.208676039467854,-7.93950971701043));
#13549=CARTESIAN_POINT('Ctrl Pts',(2.37324383318611,0.16432865133715,-7.93655937948593));
#13550=CARTESIAN_POINT('Ctrl Pts',(2.37184731709931,0.154092504908083,-7.93587571436136));
#13551=CARTESIAN_POINT('Ctrl Pts',(2.36983897146936,0.137771389640783,-7.93478078549251));
#13552=CARTESIAN_POINT('Ctrl Pts',(2.36913954485042,0.131697583349774,-7.93437224945119));
#13553=CARTESIAN_POINT('Ctrl Pts',(2.36791902205137,0.120319733217702,-7.93360483805153));
#13554=CARTESIAN_POINT('Ctrl Pts',(2.3673865737766,0.115017043402438,-7.93324632528428));
#13555=CARTESIAN_POINT('Ctrl Pts',(2.36640123908301,0.104485446871551,-7.9325325108268));
#13556=CARTESIAN_POINT('Ctrl Pts',(2.36594727951419,0.0992567623689709,
-7.93217725115629));
#13557=CARTESIAN_POINT('Ctrl Pts',(2.364995855742,0.0873773763892674,-7.93136807229652));
#13558=CARTESIAN_POINT('Ctrl Pts',(2.36451990884689,0.0807251811422267,
-7.93091349850281));
#13559=CARTESIAN_POINT('Ctrl Pts',(2.36253235015777,0.0491843186856213,
-7.92875104626062));
#13560=CARTESIAN_POINT('Ctrl Pts',(2.36175499908727,0.0242577447497806,
-7.92702086516518));
#13561=CARTESIAN_POINT('Ctrl Pts',(2.36176924264068,-0.000672880918024107,
-7.92526805329864));
#13562=CARTESIAN_POINT('Ctrl Pts',(2.36176924189409,-0.000671572882392571,
-7.92526814526343));
#13563=CARTESIAN_POINT('Ctrl Pts',(2.36182874002516,-0.105014547877794,
-7.91793204682712));
#13564=CARTESIAN_POINT('Ctrl Pts',(2.37575537529407,-0.208883089305192,
-7.91018050052472));
#13565=CARTESIAN_POINT('Ctrl Pts',(2.41340834476088,-0.347111401056375,
-7.89976355597196));
#13566=CARTESIAN_POINT('Ctrl Pts',(2.42550200525097,-0.384159261872818,
-7.8969683755995));
#13567=CARTESIAN_POINT('Ctrl Pts',(2.44176920881263,-0.426712988878862,
-7.8938030358703));
#13568=CARTESIAN_POINT('Ctrl Pts',(2.4441796374853,-0.432862871050662,-7.8933467320813));
#13569=CARTESIAN_POINT('Ctrl Pts',(2.44797872648623,-0.442320754302456,
-7.89264711749572));
#13570=CARTESIAN_POINT('Ctrl Pts',(2.4493309278344,-0.445643115841913,-7.89240176631258));
#13571=CARTESIAN_POINT('Ctrl Pts',(2.45186011309046,-0.451776922058735,
-7.89194962064927));
#13572=CARTESIAN_POINT('Ctrl Pts',(2.45303282899958,-0.454589971599706,
-7.89174259118068));
#13573=CARTESIAN_POINT('Ctrl Pts',(2.45573897904796,-0.461011049293892,
-7.89127075322823));
#13574=CARTESIAN_POINT('Ctrl Pts',(2.45727951827934,-0.464615999352169,
-7.89100637163265));
#13575=CARTESIAN_POINT('Ctrl Pts',(2.46137393663102,-0.47406630868873,-7.89031449689183));
#13576=CARTESIAN_POINT('Ctrl Pts',(2.46395739465777,-0.479898823181687,
-7.88988869613323));
#13577=CARTESIAN_POINT('Ctrl Pts',(2.48611061912444,-0.528835159126472,
-7.88632395785479));
#13578=CARTESIAN_POINT('Ctrl Pts',(2.50821792777159,-0.57074957711135,-7.88332144604226));
#13579=CARTESIAN_POINT('Ctrl Pts',(2.57323889122626,-0.677843567369104,
-7.87549415025452));
#13580=CARTESIAN_POINT('Ctrl Pts',(2.62019810293726,-0.740282602905352,
-7.87075387472766));
#13581=CARTESIAN_POINT('Ctrl Pts',(2.69082968639269,-0.817016525230019,
-7.86416012938778));
#13582=CARTESIAN_POINT('Ctrl Pts',(2.70932318569956,-0.835801604992794,
-7.86247595689157));
#13583=CARTESIAN_POINT('Ctrl Pts',(2.73759518937276,-0.862654597433883,
-7.85994709854885));
#13584=CARTESIAN_POINT('Ctrl Pts',(2.74689935110735,-0.871211126312293,
-7.85912180446637));
#13585=CARTESIAN_POINT('Ctrl Pts',(2.76202758228735,-0.884680784060638,
-7.85778950911532));
#13586=CARTESIAN_POINT('Ctrl Pts',(2.76776489478522,-0.889690166035058,
-7.85728638991197));
#13587=CARTESIAN_POINT('Ctrl Pts',(2.77873227542358,-0.899080131374576,
-7.85632837347067));
#13588=CARTESIAN_POINT('Ctrl Pts',(2.78395262365634,-0.903471621642111,
-7.85587393868121));
#13589=CARTESIAN_POINT('Ctrl Pts',(2.78925201976461,-0.907851556189349,
-7.85541409511517));
#13590=CARTESIAN_POINT('Ctrl Pts',(2.78929330427405,-0.907885672969693,
-7.85541051283117));
#13591=CARTESIAN_POINT('Ctrl Pts',(2.79338483398073,-0.911266370301086,
-7.85505549697381));
#13592=CARTESIAN_POINT('Ctrl Pts',(2.79745736820196,-0.914585766804777,
-7.85470298948713));
#13593=CARTESIAN_POINT('Ctrl Pts',(2.80561374538718,-0.921143435526385,
-7.85399862218538));
#13594=CARTESIAN_POINT('Ctrl Pts',(2.80969714516943,-0.924382069644818,
-7.85364678771651));
#13595=CARTESIAN_POINT('Ctrl Pts',(2.82076433139421,-0.933040655363849,
-7.85269526920025));
#13596=CARTESIAN_POINT('Ctrl Pts',(2.82778775143206,-0.938409165203609,
-7.85209359799435));
#13597=CARTESIAN_POINT('Ctrl Pts',(2.85468645697024,-0.958494114878888,
-7.84979698753703));
#13598=CARTESIAN_POINT('Ctrl Pts',(2.8749618558444,-0.97266141392418,-7.84808144234096));
#13599=CARTESIAN_POINT('Ctrl Pts',(2.97861622030849,-1.0403348019763,-7.83938123253326));
#13600=CARTESIAN_POINT('Ctrl Pts',(3.06805822498817,-1.08380212983403,-7.83204773736348));
#13601=CARTESIAN_POINT('Ctrl Pts',(3.19039147666707,-1.12521655850216,-7.82262609199434));
#13602=CARTESIAN_POINT('Ctrl Pts',(3.21928441327302,-1.133777926907,-7.820446164179));
#13603=CARTESIAN_POINT('Ctrl Pts',(3.25958702226249,-1.14405621165389,-7.81749248755068));
#13604=CARTESIAN_POINT('Ctrl Pts',(3.27073969054687,-1.14672761948898,-7.81668422016562));
#13605=CARTESIAN_POINT('Ctrl Pts',(3.29017712253898,-1.15108431347198,-7.81529322201355));
#13606=CARTESIAN_POINT('Ctrl Pts',(3.29844415787695,-1.15284404849337,-7.81470712391008));
#13607=CARTESIAN_POINT('Ctrl Pts',(3.31061024995569,-1.15529714548863,-7.81385337024948));
#13608=CARTESIAN_POINT('Ctrl Pts',(3.31449478024017,-1.15606003835501,-7.81358208149238));
#13609=CARTESIAN_POINT('Ctrl Pts',(3.32135285214677,-1.15737103549866,-7.81310551690047));
#13610=CARTESIAN_POINT('Ctrl Pts',(3.32432474192281,-1.15792729228806,-7.81289979581226));
#13611=CARTESIAN_POINT('Ctrl Pts',(3.33078937516846,-1.15911154675628,-7.81245403910711));
#13612=CARTESIAN_POINT('Ctrl Pts',(3.33428283308934,-1.15973520731395,-7.81221424560107));
#13613=CARTESIAN_POINT('Ctrl Pts',(3.3439409058313,-1.16141438221933,-7.81155418695836));
#13614=CARTESIAN_POINT('Ctrl Pts',(3.35011130037759,-1.16243661604988,-7.8111357195743));
#13615=CARTESIAN_POINT('Ctrl Pts',(3.38362026596937,-1.16771405678282,-7.80887926711422));
#13616=CARTESIAN_POINT('Ctrl Pts',(3.41109654103612,-1.17105443329986,-7.80708692359229));
#13617=CARTESIAN_POINT('Ctrl Pts',(3.54509038932417,-1.18257073763232,-7.79851598864044));
#13618=CARTESIAN_POINT('Ctrl Pts',(3.65226583812479,-1.17719832191472,-7.79213408930033));
#13619=CARTESIAN_POINT('Ctrl Pts',(3.77881925169055,-1.15339151023154,-7.78393636740898));
#13620=CARTESIAN_POINT('Ctrl Pts',(3.80026544549824,-1.14873312464606,-7.78252558185132));
#13621=CARTESIAN_POINT('Ctrl Pts',(3.8372201260119,-1.13961792888321,-7.78004778766584));
#13622=CARTESIAN_POINT('Ctrl Pts',(3.85279060425364,-1.13543641260057,-7.77898915379222));
#13623=CARTESIAN_POINT('Ctrl Pts',(3.87525051983323,-1.12890756559048,-7.77743842223813));
#13624=CARTESIAN_POINT('Ctrl Pts',(3.88221220231322,-1.12681378713968,-7.77695442311493));
#13625=CARTESIAN_POINT('Ctrl Pts',(3.89439745562673,-1.12302561497784,-7.77610118739983));
#13626=CARTESIAN_POINT('Ctrl Pts',(3.89962944288688,-1.12135887113613,-7.77573285269488));
#13627=CARTESIAN_POINT('Ctrl Pts',(3.90979105090446,-1.1180432579845,-7.77501351975038));
#13628=CARTESIAN_POINT('Ctrl Pts',(3.91472179510634,-1.11639821746324,-7.77466265328197));
#13629=CARTESIAN_POINT('Ctrl Pts',(3.92793970869251,-1.11189087761117,-7.77371708494631));
#13630=CARTESIAN_POINT('Ctrl Pts',(3.93620593906893,-1.10896863646193,-7.77312044018602));
#13631=CARTESIAN_POINT('Ctrl Pts',(3.96716186367784,-1.09763484365831,-7.77086558654179));
#13632=CARTESIAN_POINT('Ctrl Pts',(3.98962178057065,-1.08861747623762,-7.76918772356668));
#13633=CARTESIAN_POINT('Ctrl Pts',(4.03425479370724,-1.06908051436565,-7.76576585230553));
#13634=CARTESIAN_POINT('Ctrl Pts',(4.05639274468124,-1.05855387822235,-7.76402332099047));
#13635=CARTESIAN_POINT('Ctrl Pts',(4.07816960641408,-1.04735411443813,-7.76226461992608));
#13636=CARTESIAN_POINT('Ctrl Pts',(4.07816926754758,-1.04735428871592,-7.66392024962001));
#13637=CARTESIAN_POINT('Ctrl Pts',(4.07599933067676,-1.04847027876743,-7.66408638768524));
#13638=CARTESIAN_POINT('Ctrl Pts',(4.07382593516263,-1.0495795204847,-7.6642520981632));
#13639=CARTESIAN_POINT('Ctrl Pts',(4.06823659364625,-1.05241030673236,-7.66467650685746));
#13640=CARTESIAN_POINT('Ctrl Pts',(4.0648156862231,-1.0541219757116,-7.66493459423372));
#13641=CARTESIAN_POINT('Ctrl Pts',(4.0559518984867,-1.05850315338341,-7.66559917020746));
#13642=CARTESIAN_POINT('Ctrl Pts',(4.0504965571681,-1.06114739960968,-7.666004175306));
#13643=CARTESIAN_POINT('Ctrl Pts',(4.01373074194367,-1.07861879499067,-7.66870842048069));
#13644=CARTESIAN_POINT('Ctrl Pts',(3.9817963483123,-1.09210188638138,-7.67093511289324));
#13645=CARTESIAN_POINT('Ctrl Pts',(3.92285150753164,-1.11397837109124,-7.67490795160055));
#13646=CARTESIAN_POINT('Ctrl Pts',(3.89604682207342,-1.12284444738343,-7.6766652819446));
#13647=CARTESIAN_POINT('Ctrl Pts',(3.8228898202535,-1.14415800566199,-7.68138972842663));
#13648=CARTESIAN_POINT('Ctrl Pts',(3.77605503881949,-1.15474982941892,-7.68433988936288));
#13649=CARTESIAN_POINT('Ctrl Pts',(3.67607140816564,-1.17102187003846,-7.690674660315));
#13650=CARTESIAN_POINT('Ctrl Pts',(3.62292282389914,-1.17600233552378,-7.69406459648467));
#13651=CARTESIAN_POINT('Ctrl Pts',(3.55879719845989,-1.17764201358477,-7.69828058026507));
#13652=CARTESIAN_POINT('Ctrl Pts',(3.54796738261376,-1.17776949020798,-7.69899673981775));
#13653=CARTESIAN_POINT('Ctrl Pts',(3.53091596820103,-1.17773501212722,-7.70013154338773));
#13654=CARTESIAN_POINT('Ctrl Pts',(3.52469460032593,-1.17767313164058,-7.70054709872797));
#13655=CARTESIAN_POINT('Ctrl Pts',(3.51304772995083,-1.17746498323356,-7.70132801185411));
#13656=CARTESIAN_POINT('Ctrl Pts',(3.50762216039025,-1.17733049916599,-7.7016929957926));
#13657=CARTESIAN_POINT('Ctrl Pts',(3.4954772805074,-1.17694545143863,-7.70251278203914));
#13658=CARTESIAN_POINT('Ctrl Pts',(3.48875884144225,-1.17667483660613,-7.70296819202734));
#13659=CARTESIAN_POINT('Ctrl Pts',(3.4716687161671,-1.17583981971684,-7.70413168007832));
#13660=CARTESIAN_POINT('Ctrl Pts',(3.46130168433332,-1.17519572036113,-7.70484218789373));
#13661=CARTESIAN_POINT('Ctrl Pts',(3.37566400039517,-1.16873693410163,-7.71075196532745));
#13662=CARTESIAN_POINT('Ctrl Pts',(3.30111759441655,-1.15583535098057,-7.71617307756693));
#13663=CARTESIAN_POINT('Ctrl Pts',(3.17252192617881,-1.12060544461102,-7.72592684272138));
#13664=CARTESIAN_POINT('Ctrl Pts',(3.11791510789142,-1.10122378340417,-7.73020067207606));
#13665=CARTESIAN_POINT('Ctrl Pts',(3.04624034787487,-1.06966781603221,-7.73585547351368));
#13666=CARTESIAN_POINT('Ctrl Pts',(3.02774391662478,-1.06094270653197,-7.73731849390011));
#13667=CARTESIAN_POINT('Ctrl Pts',(2.99784897382991,-1.04587681761694,-7.73967933610442));
#13668=CARTESIAN_POINT('Ctrl Pts',(2.98631239963288,-1.03982076639324,-7.74058943201842));
#13669=CARTESIAN_POINT('Ctrl Pts',(2.97075501624351,-1.03132177780032,-7.74181308691415));
#13670=CARTESIAN_POINT('Ctrl Pts',(2.96664534557664,-1.02904463271438,-7.74213597893885));
#13671=CARTESIAN_POINT('Ctrl Pts',(2.95978504394658,-1.02518954268339,-7.74267425708184));
#13672=CARTESIAN_POINT('Ctrl Pts',(2.95702699479534,-1.02362499119719,-7.74289046247985));
#13673=CARTESIAN_POINT('Ctrl Pts',(2.95179596606035,-1.0206296100506,-7.74330010015454));
#13674=CARTESIAN_POINT('Ctrl Pts',(2.94932182895659,-1.01920089531999,-7.74349366760424));
#13675=CARTESIAN_POINT('Ctrl Pts',(2.94344852930459,-1.01578074208898,-7.74395280360183));
#13676=CARTESIAN_POINT('Ctrl Pts',(2.94005408435178,-1.01378120800476,-7.7442178630693));
#13677=CARTESIAN_POINT('Ctrl Pts',(2.9280566471667,-1.00663266061807,-7.74515388091924));
#13678=CARTESIAN_POINT('Ctrl Pts',(2.91950914964193,-1.0013906946412,-7.74581924411855));
#13679=CARTESIAN_POINT('Ctrl Pts',(2.86043178839065,-0.964113560823456,
-7.75041510479541));
#13680=CARTESIAN_POINT('Ctrl Pts',(2.81233372185633,-0.928373744823914,
-7.75414444405375));
#13681=CARTESIAN_POINT('Ctrl Pts',(2.71660604837684,-0.845217537616965,
-7.76200080480283));
#13682=CARTESIAN_POINT('Ctrl Pts',(2.66989610621342,-0.797078309952863,
-7.76611179794526));
#13683=CARTESIAN_POINT('Ctrl Pts',(2.60579444269048,-0.718633012873777,
-7.77255201164657));
#13684=CARTESIAN_POINT('Ctrl Pts',(2.58523450023074,-0.691097460731915,
-7.77476919362937));
#13685=CARTESIAN_POINT('Ctrl Pts',(2.56051406242008,-0.654779508937179,
-7.77766441192508));
#13686=CARTESIAN_POINT('Ctrl Pts',(2.55521672100893,-0.646788904696646,
-7.7782996400518));
#13687=CARTESIAN_POINT('Ctrl Pts',(2.54679012290392,-0.633734767313471,
-7.7793350350392));
#13688=CARTESIAN_POINT('Ctrl Pts',(2.54360059546308,-0.628710511846509,
-7.7797329764866));
#13689=CARTESIAN_POINT('Ctrl Pts',(2.53754760353215,-0.619013981839423,
-7.78050002719979));
#13690=CARTESIAN_POINT('Ctrl Pts',(2.53467839516187,-0.614345461357498,
-7.78086891458866));
#13691=CARTESIAN_POINT('Ctrl Pts',(2.52817943998174,-0.603603606680172,
-7.78171682991672));
#13692=CARTESIAN_POINT('Ctrl Pts',(2.52457166297125,-0.597517295623453,
-7.78219663276089));
#13693=CARTESIAN_POINT('Ctrl Pts',(2.51324888297684,-0.57801734272091,-7.78373213218779));
#13694=CARTESIAN_POINT('Ctrl Pts',(2.50574357027402,-0.564484474773569,
-7.78479518406623));
#13695=CARTESIAN_POINT('Ctrl Pts',(2.46146197049144,-0.480793522645426,
-7.79135685972649));
#13696=CARTESIAN_POINT('Ctrl Pts',(2.43158085101455,-0.407232425315046,
-7.79709156562835));
#13697=CARTESIAN_POINT('Ctrl Pts',(2.39398850534059,-0.278966808632871,
-7.80689404753544));
#13698=CARTESIAN_POINT('Ctrl Pts',(2.38231188412581,-0.225687427177136,
-7.81090641336049));
#13699=CARTESIAN_POINT('Ctrl Pts',(2.37197344526455,-0.155567315329824,
-7.81599157449511));
#13700=CARTESIAN_POINT('Ctrl Pts',(2.3699206223463,-0.139296458171391,-7.81715778788155));
#13701=CARTESIAN_POINT('Ctrl Pts',(2.36705077574876,-0.111964492097584,
-7.8190884161107));
#13702=CARTESIAN_POINT('Ctrl Pts',(2.36604899329987,-0.100925466978323,
-7.81986044562139));
#13703=CARTESIAN_POINT('Ctrl Pts',(2.36486648113425,-0.0854743775618568,
-7.82092877814227));
#13704=CARTESIAN_POINT('Ctrl Pts',(2.36455452284292,-0.0810733510683677,
-7.82123168941661));
#13705=CARTESIAN_POINT('Ctrl Pts',(2.36406449451421,-0.0735619093196238,
-7.8217461985763));
#13706=CARTESIAN_POINT('Ctrl Pts',(2.36387402275671,-0.0704523764723134,
-7.82195846468412));
#13707=CARTESIAN_POINT('Ctrl Pts',(2.36352888200818,-0.0644260593539233,
-7.82236839152458));
#13708=CARTESIAN_POINT('Ctrl Pts',(2.36337272274075,-0.0615094275918239,
-7.82256613781282));
#13709=CARTESIAN_POINT('Ctrl Pts',(2.36297689330821,-0.0535627928466335,
-7.82310321623733));
#13710=CARTESIAN_POINT('Ctrl Pts',(2.36275862647741,-0.0485317129067095,
-7.82344139072724));
#13711=CARTESIAN_POINT('Ctrl Pts',(2.36204278491587,-0.0291634094983746,
-7.82473666981689));
#13712=CARTESIAN_POINT('Ctrl Pts',(2.36177488286253,-0.0148182653979148,
-7.8256821052238));
#13713=CARTESIAN_POINT('Ctrl Pts',(2.36175953056197,0.0235664998942394,
-7.82818322953387));
#13714=CARTESIAN_POINT('Ctrl Pts',(2.36248581951748,0.0476002929455243,
-7.82971921949145));
#13715=CARTESIAN_POINT('Ctrl Pts',(2.36721770908896,0.125295133830403,-7.83463471318658));
#13716=CARTESIAN_POINT('Ctrl Pts',(2.37416376763856,0.178708983497501,-7.83793899574084));
#13717=CARTESIAN_POINT('Ctrl Pts',(2.39924636467484,0.303847515676125,-7.8458443064072));
#13718=CARTESIAN_POINT('Ctrl Pts',(2.42052633574254,0.374697597684427,-7.85046048557332));
#13719=CARTESIAN_POINT('Ctrl Pts',(2.45221963643209,0.452751468272571,-7.85598885609869));
#13720=CARTESIAN_POINT('Ctrl Pts',(2.45627278956272,0.462365044837467,-7.8566775111369));
#13721=CARTESIAN_POINT('Ctrl Pts',(2.46315287194618,0.4780965498791,-7.85781790304939));
#13722=CARTESIAN_POINT('Ctrl Pts',(2.46590560098539,0.484246444690515,-7.85826715151437));
#13723=CARTESIAN_POINT('Ctrl Pts',(2.47097103731202,0.495307654249576,-7.85908156578698));
#13724=CARTESIAN_POINT('Ctrl Pts',(2.47326523502905,0.500227276499942,-7.85944609530074));
#13725=CARTESIAN_POINT('Ctrl Pts',(2.47825746934426,0.510742110613748,-7.86023026781283));
#13726=CARTESIAN_POINT('Ctrl Pts',(2.48096591681059,0.516332168081663,-7.86065025855924));
#13727=CARTESIAN_POINT('Ctrl Pts',(2.48849712075084,0.531567736380428,-7.86180358602152));
#13728=CARTESIAN_POINT('Ctrl Pts',(2.49340823500583,0.541168646053145,-7.86253994584183));
#13729=CARTESIAN_POINT('Ctrl Pts',(2.52292407524643,0.596966702556771,-7.86687715304661));
#13730=CARTESIAN_POINT('Ctrl Pts',(2.55045113486666,0.641543335113617,-7.87057981786423));
#13731=CARTESIAN_POINT('Ctrl Pts',(2.62580475670246,0.747135358210077,-7.87994864816813));
#13732=CARTESIAN_POINT('Ctrl Pts',(2.67685913574037,0.805544453025278,-7.88569208628232));
#13733=CARTESIAN_POINT('Ctrl Pts',(2.75847135023436,0.882187427319258,-7.89380896596216));
#13734=CARTESIAN_POINT('Ctrl Pts',(2.7847038771568,0.90473460964183,-7.89628223371594));
#13735=CARTESIAN_POINT('Ctrl Pts',(2.81665755169725,0.929840325062126,-7.89910667328438));
#13736=CARTESIAN_POINT('Ctrl Pts',(2.82145101250359,0.933547038574874,-7.89952561743558));
#13737=CARTESIAN_POINT('Ctrl Pts',(2.82931621212083,0.939532658226551,-7.90020502900419));
#13738=CARTESIAN_POINT('Ctrl Pts',(2.83237074928425,0.941833832818596,-7.90046694398928));
#13739=CARTESIAN_POINT('Ctrl Pts',(2.83787460027423,0.945938358664749,-7.90093532457074));
#13740=CARTESIAN_POINT('Ctrl Pts',(2.84031973216837,0.947747132313531,-7.90114215336278));
#13741=CARTESIAN_POINT('Ctrl Pts',(2.84572405890346,0.951712655999637,-7.90159653939135));
#13742=CARTESIAN_POINT('Ctrl Pts',(2.84868631857519,0.953865088661074,-7.90184380475498));
#13743=CARTESIAN_POINT('Ctrl Pts',(2.85730859327204,0.960068957483658,-7.90255848385646));
#13744=CARTESIAN_POINT('Ctrl Pts',(2.86299466400094,0.96408416195213,-7.90302353375881));
#13745=CARTESIAN_POINT('Ctrl Pts',(2.91174891292745,0.997868088427713,-7.90696117643822));
#13746=CARTESIAN_POINT('Ctrl Pts',(2.95672821372755,1.02478894607964,-7.91026625506025));
#13747=CARTESIAN_POINT('Ctrl Pts',(3.07778011709415,1.08668269577411,-7.91873437274206));
#13748=CARTESIAN_POINT('Ctrl Pts',(3.15604029988409,1.11670307393626,-7.92382090397586));
#13749=CARTESIAN_POINT('Ctrl Pts',(3.26615393099711,1.14598778583277,-7.93109212874473));
#13750=CARTESIAN_POINT('Ctrl Pts',(3.29577775326035,1.15265191106773,-7.9330566735109));
#13751=CARTESIAN_POINT('Ctrl Pts',(3.33498931899542,1.15989368099631,-7.93568483420892));
#13752=CARTESIAN_POINT('Ctrl Pts',(3.34437498356216,1.16150959817997,-7.93631593813377));
#13753=CARTESIAN_POINT('Ctrl Pts',(3.35964207183885,1.16394784572987,-7.93734627241968));
#13754=CARTESIAN_POINT('Ctrl Pts',(3.36551205663904,1.16483985119583,-7.93774331825712));
#13755=CARTESIAN_POINT('Ctrl Pts',(3.37681647861515,1.16647032199944,-7.93850978710612));
#13756=CARTESIAN_POINT('Ctrl Pts',(3.3822498335401,1.16721528890515,-7.93887899660334));
#13757=CARTESIAN_POINT('Ctrl Pts',(3.39485552970633,1.1688540406299,-7.93973756413188));
#13758=CARTESIAN_POINT('Ctrl Pts',(3.4020312274163,1.16971979423164,-7.94022778046154));
#13759=CARTESIAN_POINT('Ctrl Pts',(3.42500715009868,1.17227752349685,-7.94180239726834));
#13760=CARTESIAN_POINT('Ctrl Pts',(3.44083325407097,1.17371573999058,-7.94289457308637));
#13761=CARTESIAN_POINT('Ctrl Pts',(3.4781640898054,1.17634789247088,-7.94548982727891));
#13762=CARTESIAN_POINT('Ctrl Pts',(3.49968146617711,1.17727297668321,-7.94700058425828));
#13763=CARTESIAN_POINT('Ctrl Pts',(3.58163396158158,1.17854707806411,-7.9528113677481));
#13764=CARTESIAN_POINT('Ctrl Pts',(3.64203331349611,1.17483455253705,-7.95721757077947));
#13765=CARTESIAN_POINT('Ctrl Pts',(3.77007661815412,1.15701335510924,-7.96670291533719));
#13766=CARTESIAN_POINT('Ctrl Pts',(3.83732106760747,1.14155700509463,-7.9717730964071));
#13767=CARTESIAN_POINT('Ctrl Pts',(3.91221756712543,1.11726817856383,-7.97729251785475));
#13768=CARTESIAN_POINT('Ctrl Pts',(3.92156258616551,1.11410731971923,-7.97797866728605));
#13769=CARTESIAN_POINT('Ctrl Pts',(3.93455737876684,1.10952921977917,-7.9789282201923));
#13770=CARTESIAN_POINT('Ctrl Pts',(3.93824116220082,1.10821074217709,-7.97919688277755));
#13771=CARTESIAN_POINT('Ctrl Pts',(3.94459701224662,1.10590009981054,-7.97965944301357));
#13772=CARTESIAN_POINT('Ctrl Pts',(3.94727214522463,1.1049165579523,-7.97985383021229));
#13773=CARTESIAN_POINT('Ctrl Pts',(3.95292321249396,1.10281556289205,-7.98026378504648));
#13774=CARTESIAN_POINT('Ctrl Pts',(3.95589824469661,1.10169575383819,-7.98047920691228));
#13775=CARTESIAN_POINT('Ctrl Pts',(3.96329475408134,1.09887744957494,-7.98101387400011));
#13776=CARTESIAN_POINT('Ctrl Pts',(3.96771064635915,1.09716427907276,-7.98133226735685));
#13777=CARTESIAN_POINT('Ctrl Pts',(3.98449314698845,1.09053665509096,-7.98253963907799));
#13778=CARTESIAN_POINT('Ctrl Pts',(3.99678703457802,1.08543916003456,-7.98341853533375));
#13779=CARTESIAN_POINT('Ctrl Pts',(4.02830534967419,1.07173992397506,-7.98566393577523));
#13780=CARTESIAN_POINT('Ctrl Pts',(4.04739077121115,1.0628287411521,-7.98701595004106));
#13781=CARTESIAN_POINT('Ctrl Pts',(4.10750138849634,1.03277320498155,-7.99128104343455));
#13782=CARTESIAN_POINT('Ctrl Pts',(4.14752851994361,1.00972738002557,-7.99413271592813));
#13783=CARTESIAN_POINT('Ctrl Pts',(4.25290974355454,0.94050926715765,-8.00193140006753));
#13784=CARTESIAN_POINT('Ctrl Pts',(4.31506883090708,0.889946346859065,-8.00687724209208));
#13785=CARTESIAN_POINT('Ctrl Pts',(4.38256396026648,0.822562594487059,-8.01309271023972));
#13786=CARTESIAN_POINT('Ctrl Pts',(4.39328537825723,0.811428963784638,-8.01410843621434));
#13787=CARTESIAN_POINT('Ctrl Pts',(4.40858845543719,0.794898386246554,-8.01560251117703));
#13788=CARTESIAN_POINT('Ctrl Pts',(4.41334576605828,0.789665715719755,-8.0160734712462));
#13789=CARTESIAN_POINT('Ctrl Pts',(4.4217048081552,0.780303385651714,-8.01691282204701));
#13790=CARTESIAN_POINT('Ctrl Pts',(4.42532541798199,0.776190802746072,-8.01728041734379));
#13791=CARTESIAN_POINT('Ctrl Pts',(4.43281933305807,0.76755788195842,-8.01804985402368));
#13792=CARTESIAN_POINT('Ctrl Pts',(4.43668731889776,0.76303315321934,-8.01845189782744));
#13793=CARTESIAN_POINT('Ctrl Pts',(4.44669937561324,0.751139777104453,-8.01950559893049));
#13794=CARTESIAN_POINT('Ctrl Pts',(4.45278789644545,0.743725159317698,-8.02015945827958));
#13795=CARTESIAN_POINT('Ctrl Pts',(4.48030824730135,0.709363241103852,-8.02317657984523));
#13796=CARTESIAN_POINT('Ctrl Pts',(4.50064059136776,0.6815610655869,-8.02558205634847));
#13797=CARTESIAN_POINT('Ctrl Pts',(4.55700565228999,0.59694100733188,-8.03280607622727));
#13798=CARTESIAN_POINT('Ctrl Pts',(4.58942083239077,0.53788655892917,-8.03773320938785));
#13799=CARTESIAN_POINT('Ctrl Pts',(4.64067044636245,0.422014935357697,-8.04703071292563));
#13800=CARTESIAN_POINT('Ctrl Pts',(4.66057277854912,0.365883808944387,-8.05138389697688));
#13801=CARTESIAN_POINT('Ctrl Pts',(4.67877465897564,0.298817754867696,-8.05625697026201));
#13802=CARTESIAN_POINT('Ctrl Pts',(4.68127492668306,0.289117498343914,-8.05695388311472));
#13803=CARTESIAN_POINT('Ctrl Pts',(4.684585386014,0.275560622657904,-8.05791579648316));
#13804=CARTESIAN_POINT('Ctrl Pts',(4.68550036337036,0.271730383196766,-8.05818623119838));
#13805=CARTESIAN_POINT('Ctrl Pts',(4.68704589542861,0.26511386703647,-8.05865100584461));
#13806=CARTESIAN_POINT('Ctrl Pts',(4.68768554875982,0.262329782991995,-8.05884584610375));
#13807=CARTESIAN_POINT('Ctrl Pts',(4.68901394454091,0.256450010983176,-8.05925576227636));
#13808=CARTESIAN_POINT('Ctrl Pts',(4.68970032442039,0.253353818048499,-8.05947069770028));
#13809=CARTESIAN_POINT('Ctrl Pts',(4.69137297357451,0.245661751955655,-8.06000247890595));
#13810=CARTESIAN_POINT('Ctrl Pts',(4.69234426483084,0.241062613330397,-8.06031849275867));
#13811=CARTESIAN_POINT('Ctrl Pts',(4.69590685177904,0.223679366779489,-8.06150602657403));
#13812=CARTESIAN_POINT('Ctrl Pts',(4.69831335624334,0.21085776671871,-8.06236788525131));
#13813=CARTESIAN_POINT('Ctrl Pts',(4.70394966352988,0.17780856618879,-8.0645596114501));
#13814=CARTESIAN_POINT('Ctrl Pts',(4.70686583482621,0.157531341017235,-8.06587584425933));
#13815=CARTESIAN_POINT('Ctrl Pts',(4.71598751525121,0.0797549411841474,
-8.07085079217485));
#13816=CARTESIAN_POINT('Ctrl Pts',(4.71848471588639,0.0219011894639412,
-8.07440147699045));
#13817=CARTESIAN_POINT('Ctrl Pts',(4.71442086586518,-0.111339375009466,
-8.08265544155528));
#13818=CARTESIAN_POINT('Ctrl Pts',(4.70487551711657,-0.186367459087978,
-8.08736880221026));
#13819=CARTESIAN_POINT('Ctrl Pts',(4.68592773817508,-0.270092730762107,
-8.09300270423713));
#13820=CARTESIAN_POINT('Ctrl Pts',(4.68350106420552,-0.280192975495403,
-8.09368841499957));
#13821=CARTESIAN_POINT('Ctrl Pts',(4.67928400458495,-0.296776220448255,
-8.09482493340234));
#13822=CARTESIAN_POINT('Ctrl Pts',(4.67757108937437,-0.303278468161848,
-8.09527328216385));
#13823=CARTESIAN_POINT('Ctrl Pts',(4.6743751683658,-0.315001760738158,-8.09608673391792));
#13824=CARTESIAN_POINT('Ctrl Pts',(4.67291156205078,-0.32022793538717,-8.09645120746891));
#13825=CARTESIAN_POINT('Ctrl Pts',(4.66969272935793,-0.331423031053153,
-8.09723600381042));
#13826=CARTESIAN_POINT('Ctrl Pts',(4.66792622881616,-0.337388510854894,
-8.09765667960181));
#13827=CARTESIAN_POINT('Ctrl Pts',(4.66295547830574,-0.353698936619533,
-8.09881383808323));
#13828=CARTESIAN_POINT('Ctrl Pts',(4.65965574201968,-0.364013906078497,
-8.09955337760108));
#13829=CARTESIAN_POINT('Ctrl Pts',(4.63927153071905,-0.424831620805284,
-8.10396102536625));
#13830=CARTESIAN_POINT('Ctrl Pts',(4.61891845833394,-0.474165448162224,
-8.10773496713708));
#13831=CARTESIAN_POINT('Ctrl Pts',(4.57403179429686,-0.56496106664072,-8.11505531157072));
#13832=CARTESIAN_POINT('Ctrl Pts',(4.55015814282189,-0.606634827725838,
-8.11857938297091));
#13833=CARTESIAN_POINT('Ctrl Pts',(4.50830751646034,-0.670329060104568,
-8.12417104878833));
#13834=CARTESIAN_POINT('Ctrl Pts',(4.49196037929793,-0.693359755237035,
-8.12623879928793));
#13835=CARTESIAN_POINT('Ctrl Pts',(4.45374840689439,-0.743289761903298,
-8.13079737101257));
#13836=CARTESIAN_POINT('Ctrl Pts',(4.43149023323762,-0.769859007028095,
-8.13327577408438));
#13837=CARTESIAN_POINT('Ctrl Pts',(4.40399676309858,-0.799881300427521,
-8.13610527621456));
#13838=CARTESIAN_POINT('Ctrl Pts',(4.39986813103883,-0.804320380095369,
-8.13652441753216));
#13839=CARTESIAN_POINT('Ctrl Pts',(4.39307871316497,-0.811508223019384,
-8.13720408363009));
#13840=CARTESIAN_POINT('Ctrl Pts',(4.39043854757939,-0.814276184280567,
-8.13746605772801));
#13841=CARTESIAN_POINT('Ctrl Pts',(4.38567496250284,-0.81922187805559,-8.13793450010119));
#13842=CARTESIAN_POINT('Ctrl Pts',(4.38355655686312,-0.82140428620393,-8.13814133201844));
#13843=CARTESIAN_POINT('Ctrl Pts',(4.37886965662658,-0.826195512214695,
-8.13859567281474));
#13844=CARTESIAN_POINT('Ctrl Pts',(4.37629744082877,-0.828800573599379,
-8.13884289021091));
#13845=CARTESIAN_POINT('Ctrl Pts',(4.36880199642375,-0.836321264907127,
-8.13955729033005));
#13846=CARTESIAN_POINT('Ctrl Pts',(4.36384720477366,-0.841205422225085,
-8.14002211204946));
#13847=CARTESIAN_POINT('Ctrl Pts',(4.3213771798022,-0.882334385032535,-8.14394688501801));
#13848=CARTESIAN_POINT('Ctrl Pts',(4.28153026818175,-0.916098748325419,
-8.14724055042111));
#13849=CARTESIAN_POINT('Ctrl Pts',(4.18853051777139,-0.98483881953171,-8.15444442903269));
#13850=CARTESIAN_POINT('Ctrl Pts',(4.13455216629061,-1.01835679177162,-8.15832338762119));
#13851=CARTESIAN_POINT('Ctrl Pts',(4.07816915725551,-1.04735434543869,-8.16230176652656));
#13852=CARTESIAN_POINT('Origin',(3.53951905042299,8.32667268468867E-16,
0.924367114736157));
#13853=CARTESIAN_POINT('',(4.07816926754758,-1.04735428871592,-8.76047541727166));
#13854=CARTESIAN_POINT('',(4.0781691574206,-1.04735434535379,-8.66209739867239));
#13855=CARTESIAN_POINT('',(4.07816926754759,-1.04735428871592,0.924367114736157));
#13856=CARTESIAN_POINT('Ctrl Pts',(4.07816926754756,-1.04735428871593,-8.76047541727166));
#13857=CARTESIAN_POINT('Ctrl Pts',(4.07894167719801,-1.04695704145165,-8.76041663737559));
#13858=CARTESIAN_POINT('Ctrl Pts',(4.07971365089275,-1.04655893792941,-8.76035790996024));
#13859=CARTESIAN_POINT('Ctrl Pts',(4.08398913035627,-1.04434810052881,-8.76003275863783));
#13860=CARTESIAN_POINT('Ctrl Pts',(4.08748401095802,-1.0425185975108,-8.759767356016));
#13861=CARTESIAN_POINT('Ctrl Pts',(4.09985431291982,-1.03596358879242,-8.75882908017515));
#13862=CARTESIAN_POINT('Ctrl Pts',(4.10867863906273,-1.0311418635942,-8.75816183669268));
#13863=CARTESIAN_POINT('Ctrl Pts',(4.1694784759547,-0.996901684785136,-8.75357135667992));
#13864=CARTESIAN_POINT('Ctrl Pts',(4.21921901049277,-0.963676110532028,
-8.74984838855954));
#13865=CARTESIAN_POINT('Ctrl Pts',(4.31895738292415,-0.885471935464067,
-8.74199558192822));
#13866=CARTESIAN_POINT('Ctrl Pts',(4.36805845418722,-0.839706212042074,
-8.73788191574333));
#13867=CARTESIAN_POINT('Ctrl Pts',(4.43605213722485,-0.76452887931233,-8.73143801305769));
#13868=CARTESIAN_POINT('Ctrl Pts',(4.457974851502,-0.738047814722179,-8.72921998365108));
#13869=CARTESIAN_POINT('Ctrl Pts',(4.48449317042756,-0.703001369460029,
-8.72632374268465));
#13870=CARTESIAN_POINT('Ctrl Pts',(4.49018542063203,-0.695284442914425,
-8.72568837469458));
#13871=CARTESIAN_POINT('Ctrl Pts',(4.49925722358364,-0.682666192611757,
-8.72465276782382));
#13872=CARTESIAN_POINT('Ctrl Pts',(4.50269503310349,-0.677807137572368,
-8.72425475547095));
#13873=CARTESIAN_POINT('Ctrl Pts',(4.5092272003606,-0.6684244183521,-8.72348757848482));
#13874=CARTESIAN_POINT('Ctrl Pts',(4.51232711057117,-0.663904793983033,
-8.72311863587933));
#13875=CARTESIAN_POINT('Ctrl Pts',(4.51935687410455,-0.653500553125249,
-8.72227060757938));
#13876=CARTESIAN_POINT('Ctrl Pts',(4.52326543196141,-0.647601873592266,
-8.72179074686709));
#13877=CARTESIAN_POINT('Ctrl Pts',(4.53555170613786,-0.628691885618473,
-8.72025511476989));
#13878=CARTESIAN_POINT('Ctrl Pts',(4.54372594391739,-0.615550983984805,
-8.71919198728));
#13879=CARTESIAN_POINT('Ctrl Pts',(4.59213721494029,-0.534193211276483,
-8.71263113727757));
#13880=CARTESIAN_POINT('Ctrl Pts',(4.62566054368773,-0.462233565168181,
-8.70689742218396));
#13881=CARTESIAN_POINT('Ctrl Pts',(4.66163295506535,-0.358978655410027,
-8.69887849644065));
#13882=CARTESIAN_POINT('Ctrl Pts',(4.67046026857206,-0.330117072024171,
-8.69666078823665));
#13883=CARTESIAN_POINT('Ctrl Pts',(4.68916829934652,-0.259334424213223,
-8.69131246159671));
#13884=CARTESIAN_POINT('Ctrl Pts',(4.69787857338737,-0.217144464822941,
-8.68819929075556));
#13885=CARTESIAN_POINT('Ctrl Pts',(4.7056571047478,-0.165245198072979,-8.6845260584898));
#13886=CARTESIAN_POINT('Ctrl Pts',(4.70694250689332,-0.155905177983892,
-8.68387115598234));
#13887=CARTESIAN_POINT('Ctrl Pts',(4.70863041020275,-0.142445791302384,
-8.68293718217323));
#13888=CARTESIAN_POINT('Ctrl Pts',(4.70912353458231,-0.13833845077449,-8.68265347108429));
#13889=CARTESIAN_POINT('Ctrl Pts',(4.70994507827246,-0.131177017952631,
-8.68216117263583));
#13890=CARTESIAN_POINT('Ctrl Pts',(4.71028320604943,-0.1281241175152,-8.68195205983454));
#13891=CARTESIAN_POINT('Ctrl Pts',(4.71097610655518,-0.12163614907077,-8.68150928370947));
#13892=CARTESIAN_POINT('Ctrl Pts',(4.71132771837084,-0.11820081901649,-8.68127579450919));
#13893=CARTESIAN_POINT('Ctrl Pts',(4.71224767154721,-0.108804847567738,
-8.68063967238852));
#13894=CARTESIAN_POINT('Ctrl Pts',(4.71278568541892,-0.102841239845358,
-8.68023866821042));
#13895=CARTESIAN_POINT('Ctrl Pts',(4.71517480988392,-0.0738936653030591,
-8.67830433912641));
#13896=CARTESIAN_POINT('Ctrl Pts',(4.71639629805474,-0.0508610995218777,
-8.6768023856533));
#13897=CARTESIAN_POINT('Ctrl Pts',(4.71745525039126,-0.0060202718215907,
-8.67392477403572));
#13898=CARTESIAN_POINT('Ctrl Pts',(4.71736502113479,0.0157763560118024,
-8.67254728714376));
#13899=CARTESIAN_POINT('Ctrl Pts',(4.7148086565318,0.095896599358694,-8.66752294070916));
#13900=CARTESIAN_POINT('Ctrl Pts',(4.70861320325548,0.154016299215415,-8.66395071123672));
#13901=CARTESIAN_POINT('Ctrl Pts',(4.6880366002948,0.266769587040108,-8.65681838791266));
#13902=CARTESIAN_POINT('Ctrl Pts',(4.67398969918011,0.321300173780052,-8.65327149184867));
#13903=CARTESIAN_POINT('Ctrl Pts',(4.65150784642783,0.388309994217652,-8.64865740279191));
#13904=CARTESIAN_POINT('Ctrl Pts',(4.64666167768181,0.401919030822529,-8.6477069097239));
#13905=CARTESIAN_POINT('Ctrl Pts',(4.63911134223433,0.421948224718169,-8.64628634151834));
#13906=CARTESIAN_POINT('Ctrl Pts',(4.63659843747045,0.428439409467722,-8.64582253941805));
#13907=CARTESIAN_POINT('Ctrl Pts',(4.63201559574652,0.439972800833869,-8.64499217235558));
#13908=CARTESIAN_POINT('Ctrl Pts',(4.62996790100747,0.445023673047537,-8.64462635417326));
#13909=CARTESIAN_POINT('Ctrl Pts',(4.62556499293986,0.455671087806128,-8.643850502281));
#13910=CARTESIAN_POINT('Ctrl Pts',(4.62320141649993,0.461263977124023,-8.64344019750508));
#13911=CARTESIAN_POINT('Ctrl Pts',(4.61677645067952,0.476145275539295,-8.64234093869668));
#13912=CARTESIAN_POINT('Ctrl Pts',(4.61263828065911,0.485399769653717,-8.64164942092564));
#13913=CARTESIAN_POINT('Ctrl Pts',(4.5931399703854,0.527536911875695,-8.6384636009424));
#13914=CARTESIAN_POINT('Ctrl Pts',(4.57638593150609,0.559748891316038,-8.63592248768897));
#13915=CARTESIAN_POINT('Ctrl Pts',(4.51438768266219,0.666585653805986,-8.62712293548962));
#13916=CARTESIAN_POINT('Ctrl Pts',(4.46235688783584,0.736934511634343,-8.62065725483451));
#13917=CARTESIAN_POINT('Ctrl Pts',(4.38366152179544,0.821785405833363,-8.61222595943785));
#13918=CARTESIAN_POINT('Ctrl Pts',(4.36352192276271,0.84197817567143,-8.610166217067));
#13919=CARTESIAN_POINT('Ctrl Pts',(4.33064279840472,0.872633135757097,-8.60697707828644));
#13920=CARTESIAN_POINT('Ctrl Pts',(4.31838329929547,0.88359262320473,-8.60582335619578));
#13921=CARTESIAN_POINT('Ctrl Pts',(4.30200769432815,0.89762596551128,-8.6043322671962));
#13922=CARTESIAN_POINT('Ctrl Pts',(4.29809600262463,0.900934135244649,-8.60397972049204));
#13923=CARTESIAN_POINT('Ctrl Pts',(4.29165809790856,0.906307099519065,-8.60340558557649));
#13924=CARTESIAN_POINT('Ctrl Pts',(4.28914472176671,0.908387064479045,-8.60318294228608));
#13925=CARTESIAN_POINT('Ctrl Pts',(4.28420992744763,0.912436464380075,-8.6027487822397));
#13926=CARTESIAN_POINT('Ctrl Pts',(4.28178927734339,0.914406755466843,-8.60253720798839));
#13927=CARTESIAN_POINT('Ctrl Pts',(4.27635221284621,0.91879644372195,-8.60206502421522));
#13928=CARTESIAN_POINT('Ctrl Pts',(4.273331630036,0.921210678016675,-8.601804775349));
#13929=CARTESIAN_POINT('Ctrl Pts',(4.26277643591755,0.929562174448172,-8.6009023308121));
#13930=CARTESIAN_POINT('Ctrl Pts',(4.25518097830398,0.935422418612936,-8.60026522035512));
#13931=CARTESIAN_POINT('Ctrl Pts',(4.18779171641593,0.986114964937178,-8.59471113198653));
#13932=CARTESIAN_POINT('Ctrl Pts',(4.12391952051061,1.02526068021109,-8.59011404178723));
#13933=CARTESIAN_POINT('Ctrl Pts',(3.98419860014707,1.09356227255585,-8.58049395013948));
#13934=CARTESIAN_POINT('Ctrl Pts',(3.90819144645325,1.12147079937742,-8.57548379790194));
#13935=CARTESIAN_POINT('Ctrl Pts',(3.81718319798797,1.1446268999476,-8.56933940746492));
#13936=CARTESIAN_POINT('Ctrl Pts',(3.80438129615286,1.14765678108192,-8.56847239334271));
#13937=CARTESIAN_POINT('Ctrl Pts',(3.78497916224747,1.1519068505908,-8.56715306498016));
#13938=CARTESIAN_POINT('Ctrl Pts',(3.77841456375193,1.15328616982992,-8.56670576975186));
#13939=CARTESIAN_POINT('Ctrl Pts',(3.76651837175313,1.15567980945034,-8.56589338864939));
#13940=CARTESIAN_POINT('Ctrl Pts',(3.76119083263706,1.15671350521278,-8.56552892385501));
#13941=CARTESIAN_POINT('Ctrl Pts',(3.7497274030358,1.15885563704338,-8.56474320543117));
#13942=CARTESIAN_POINT('Ctrl Pts',(3.74358949686853,1.15995223579348,-8.56432159203344));
#13943=CARTESIAN_POINT('Ctrl Pts',(3.72698567308032,1.1627828118813,-8.56317846307211));
#13944=CARTESIAN_POINT('Ctrl Pts',(3.71650477115154,1.16442416846699,-8.56245408256723));
#13945=CARTESIAN_POINT('Ctrl Pts',(3.66188692833145,1.17222314980592,-8.55866363262338));
#13946=CARTESIAN_POINT('Ctrl Pts',(3.61745397904909,1.17601287359168,-8.55552523033936));
#13947=CARTESIAN_POINT('Ctrl Pts',(3.49311547712419,1.17954029340672,-8.54659387911479));
#13948=CARTESIAN_POINT('Ctrl Pts',(3.41329264872653,1.1736838088619,-8.54067565904613));
#13949=CARTESIAN_POINT('Ctrl Pts',(3.30793374917549,1.15507632667367,-8.53289016369807));
#13950=CARTESIAN_POINT('Ctrl Pts',(3.28135107368906,1.1494270584444,-8.53093017990873));
#13951=CARTESIAN_POINT('Ctrl Pts',(3.24458715709001,1.14027412442777,-8.52824472074925));
#13952=CARTESIAN_POINT('Ctrl Pts',(3.23422374128349,1.13754327076715,-8.52749057441487));
#13953=CARTESIAN_POINT('Ctrl Pts',(3.21617134511942,1.13252181223845,-8.52618354332796));
#13954=CARTESIAN_POINT('Ctrl Pts',(3.2084659351522,1.13029342977862,-8.52562779253115));
#13955=CARTESIAN_POINT('Ctrl Pts',(3.19707144198659,1.12687165243393,-8.52480974476516));
#13956=CARTESIAN_POINT('Ctrl Pts',(3.1933647098405,1.12573853943016,-8.52454422298092));
#13957=CARTESIAN_POINT('Ctrl Pts',(3.187034327676,1.12376917767997,-8.52409186432015));
#13958=CARTESIAN_POINT('Ctrl Pts',(3.18440794368603,1.12294200514727,-8.52390451583051));
#13959=CARTESIAN_POINT('Ctrl Pts',(3.17844858026903,1.12104212087132,-8.52348017499062));
#13960=CARTESIAN_POINT('Ctrl Pts',(3.17511746500235,1.11996375232857,-8.52324351250845));
#13961=CARTESIAN_POINT('Ctrl Pts',(3.16604682836266,1.1169825976276,-8.52260040581994));
#13962=CARTESIAN_POINT('Ctrl Pts',(3.1603169758199,1.11505040895927,-8.52219561238292));
#13963=CARTESIAN_POINT('Ctrl Pts',(3.13130028363809,1.10501602206794,-8.52015186246492));
#13964=CARTESIAN_POINT('Ctrl Pts',(3.10825526564424,1.09622749524947,-8.51854895746084));
#13965=CARTESIAN_POINT('Ctrl Pts',(2.98417627878229,1.04438893918088,-8.50994256029602));
#13966=CARTESIAN_POINT('Ctrl Pts',(2.88926500168818,0.98809287574705,-8.50339777767256));
#13967=CARTESIAN_POINT('Ctrl Pts',(2.77743761387999,0.898578455106839,-8.49428234908546));
#13968=CARTESIAN_POINT('Ctrl Pts',(2.75225641022963,0.87660057569829,-8.49212413958846));
#13969=CARTESIAN_POINT('Ctrl Pts',(2.72115792865735,0.847036266523619,-8.48929586229167));
#13970=CARTESIAN_POINT('Ctrl Pts',(2.71435048905148,0.840405972757504,-8.48866612744616));
#13971=CARTESIAN_POINT('Ctrl Pts',(2.70342410021016,0.829503165820822,-8.48763743252494));
#13972=CARTESIAN_POINT('Ctrl Pts',(2.69925581182815,0.825280531434257,-8.48724064318669));
#13973=CARTESIAN_POINT('Ctrl Pts',(2.69129480770916,0.817092895909135,-8.48647425703022));
#13974=CARTESIAN_POINT('Ctrl Pts',(2.68749753550389,0.813132524770494,-8.48610487079755));
#13975=CARTESIAN_POINT('Ctrl Pts',(2.67883843410771,0.803974249263913,-8.48525358057556));
#13976=CARTESIAN_POINT('Ctrl Pts',(2.67399581296909,0.798758560742342,-8.48477088140782));
#13977=CARTESIAN_POINT('Ctrl Pts',(2.65901443198015,0.782326829947111,-8.4832564831037));
#13978=CARTESIAN_POINT('Ctrl Pts',(2.6490445273262,0.770959622067727,-8.48221787510914));
#13979=CARTESIAN_POINT('Ctrl Pts',(2.58514172435429,0.695207147980153,-8.47535155363096));
#13980=CARTESIAN_POINT('Ctrl Pts',(2.53801879968694,0.625412982214548,-8.46925464976282));
#13981=CARTESIAN_POINT('Ctrl Pts',(2.46585157925222,0.48914858571782,-8.45793991106179));
#13982=CARTESIAN_POINT('Ctrl Pts',(2.43859409938251,0.424257483959232,-8.45277110510551));
#13983=CARTESIAN_POINT('Ctrl Pts',(2.41473183721581,0.349312718931294,-8.44727950744019));
#13984=CARTESIAN_POINT('Ctrl Pts',(2.41226849366853,0.341279713674368,-8.44669693316973));
#13985=CARTESIAN_POINT('Ctrl Pts',(2.40877390108438,0.329432945656863,-8.44584731520043));
#13986=CARTESIAN_POINT('Ctrl Pts',(2.407675601022,0.325639471846193,-8.44557668684376));
#13987=CARTESIAN_POINT('Ctrl Pts',(2.40577041564792,0.318932957741597,-8.44510084680316));
#13988=CARTESIAN_POINT('Ctrl Pts',(2.40495563961301,0.316022255524059,-8.444895194759));
#13989=CARTESIAN_POINT('Ctrl Pts',(2.4032069318705,0.309681239384391,-8.4444490787412));
#13990=CARTESIAN_POINT('Ctrl Pts',(2.40227732066876,0.306249815900599,-8.44420886049168));
#13991=CARTESIAN_POINT('Ctrl Pts',(2.39974793001022,0.296742861274635,-8.44354649343665));
#13992=CARTESIAN_POINT('Ctrl Pts',(2.39818117580525,0.2906585503752,-8.44312616282846));
#13993=CARTESIAN_POINT('Ctrl Pts',(2.38987335001104,0.257292698606628,-8.44083915609968));
#13994=CARTESIAN_POINT('Ctrl Pts',(2.38406108336921,0.22978673756206,-8.43901959458475));
#13995=CARTESIAN_POINT('Ctrl Pts',(2.36767240847776,0.135695832573901,-8.43293643656744));
#13996=CARTESIAN_POINT('Ctrl Pts',(2.36182733505878,0.0684204361754785,
-8.42881828362204));
#13997=CARTESIAN_POINT('Ctrl Pts',(2.36171109837723,-0.0670221457747454,
-8.42041453648346));
#13998=CARTESIAN_POINT('Ctrl Pts',(2.36754740706567,-0.134922850805612,
-8.41614138650875));
#13999=CARTESIAN_POINT('Ctrl Pts',(2.3809958634023,-0.212197045817843,-8.41099392244342));
#14000=CARTESIAN_POINT('Ctrl Pts',(2.3829178310719,-0.222434640364436,-8.41030634553304));
#14001=CARTESIAN_POINT('Ctrl Pts',(2.38630535142021,-0.239245825696107,
-8.40916733531976));
#14002=CARTESIAN_POINT('Ctrl Pts',(2.38769197391493,-0.24583487007222,-8.40871837931082));
#14003=CARTESIAN_POINT('Ctrl Pts',(2.39029846120642,-0.257714126105459,
-8.40790422563686));
#14004=CARTESIAN_POINT('Ctrl Pts',(2.39149855791437,-0.263008518053009,
-8.4075396617061));
#14005=CARTESIAN_POINT('Ctrl Pts',(2.39415135534913,-0.274347501794364,
-8.40675511489876));
#14006=CARTESIAN_POINT('Ctrl Pts',(2.39561539294219,-0.280389244629929,
-8.40633478205096));
#14007=CARTESIAN_POINT('Ctrl Pts',(2.39975462755282,-0.296898721168346,
-8.40517972785861));
#14008=CARTESIAN_POINT('Ctrl Pts',(2.40252608536289,-0.307341461882251,
-8.40444196888563));
#14009=CARTESIAN_POINT('Ctrl Pts',(2.41966980699661,-0.368530042638528,
-8.4000756464045));
#14010=CARTESIAN_POINT('Ctrl Pts',(2.43729204199588,-0.418295250520235,
-8.39634362246878));
#14011=CARTESIAN_POINT('Ctrl Pts',(2.49035572886478,-0.541240797259785,
-8.3866695571447));
#14012=CARTESIAN_POINT('Ctrl Pts',(2.53014233362705,-0.612244117505038,
-8.38063578176255));
#14013=CARTESIAN_POINT('Ctrl Pts',(2.59461113326625,-0.703695712638651,
-8.37255123801458));
#14014=CARTESIAN_POINT('Ctrl Pts',(2.61328700866883,-0.728102463512583,
-8.37036139090804));
#14015=CARTESIAN_POINT('Ctrl Pts',(2.63700500402221,-0.756706591717967,
-8.36778032532398));
#14016=CARTESIAN_POINT('Ctrl Pts',(2.64115299219315,-0.761626483244267,
-8.36733584751317));
#14017=CARTESIAN_POINT('Ctrl Pts',(2.64767734312063,-0.769237489966658,
-8.36664773123736));
#14018=CARTESIAN_POINT('Ctrl Pts',(2.6500259606934,-0.771952065249593,-8.36640220114627));
#14019=CARTESIAN_POINT('Ctrl Pts',(2.65439144341123,-0.776951394168435,
-8.36594989383805));
#14020=CARTESIAN_POINT('Ctrl Pts',(2.65640476233692,-0.779239054548447,
-8.36574288020811));
#14021=CARTESIAN_POINT('Ctrl Pts',(2.66102602661373,-0.784449112625628,
-8.36527129217798));
#14022=CARTESIAN_POINT('Ctrl Pts',(2.66363968859208,-0.787366336468796,
-8.36500714286347));
#14023=CARTESIAN_POINT('Ctrl Pts',(2.67179126022163,-0.796373846062074,
-8.36419102470067));
#14024=CARTESIAN_POINT('Ctrl Pts',(2.677378643775,-0.80241931006212,-8.36364255849445));
#14025=CARTESIAN_POINT('Ctrl Pts',(2.69063554465881,-0.816464731761108,
-8.36236517798217));
#14026=CARTESIAN_POINT('Ctrl Pts',(2.69835561024227,-0.824416127297166,
-8.36163958540622));
#14027=CARTESIAN_POINT('Ctrl Pts',(2.72638653046604,-0.852483230938626,
-8.35906425502588));
#14028=CARTESIAN_POINT('Ctrl Pts',(2.74731709514597,-0.871968143662895,
-8.35724969201277));
#14029=CARTESIAN_POINT('Ctrl Pts',(2.83533745573989,-0.948120508046633,
-8.34994587666708));
#14030=CARTESIAN_POINT('Ctrl Pts',(2.907951967483,-0.997961797715426,-8.34463263717578));
#14031=CARTESIAN_POINT('Ctrl Pts',(3.01689772192598,-1.05604615518521,-8.33680003673317));
#14032=CARTESIAN_POINT('Ctrl Pts',(3.04910569725687,-1.07138270307079,-8.33450297401191));
#14033=CARTESIAN_POINT('Ctrl Pts',(3.09127361683347,-1.08916174804517,-8.33149066566375));
#14034=CARTESIAN_POINT('Ctrl Pts',(3.10063973184961,-1.09296944853439,-8.33082134756185));
#14035=CARTESIAN_POINT('Ctrl Pts',(3.11570172974273,-1.09886793412042,-8.32974404639008));
#14036=CARTESIAN_POINT('Ctrl Pts',(3.12136689846352,-1.10103616354446,-8.32933863782942));
#14037=CARTESIAN_POINT('Ctrl Pts',(3.13215460473117,-1.10506967581051,-8.32856613133437));
#14038=CARTESIAN_POINT('Ctrl Pts',(3.13727385261059,-1.1069433495594,-8.32819932169251));
#14039=CARTESIAN_POINT('Ctrl Pts',(3.14896871985422,-1.1111318994336,-8.32736075399843));
#14040=CARTESIAN_POINT('Ctrl Pts',(3.15555220320492,-1.11342405006773,-8.32688826609158));
#14041=CARTESIAN_POINT('Ctrl Pts',(3.17589154265965,-1.12030369213053,-8.32542700848202));
#14042=CARTESIAN_POINT('Ctrl Pts',(3.1897116327207,-1.12469554325453,-8.32443195761117));
#14043=CARTESIAN_POINT('Ctrl Pts',(3.25794026328678,-1.14499858195926,-8.31950681014561));
#14044=CARTESIAN_POINT('Ctrl Pts',(3.31336010578011,-1.1572202988964,-8.31546182403757));
#14045=CARTESIAN_POINT('Ctrl Pts',(3.43094931057503,-1.17438153781219,-8.30682270724011));
#14046=CARTESIAN_POINT('Ctrl Pts',(3.4930733968492,-1.17847438861881,-8.30222594957249));
#14047=CARTESIAN_POINT('Ctrl Pts',(3.57404026514595,-1.17739427150161,-8.29633632062212));
#14048=CARTESIAN_POINT('Ctrl Pts',(3.59284352033292,-1.17669262992757,-8.29497626222724));
#14049=CARTESIAN_POINT('Ctrl Pts',(3.63349208578982,-1.17419938823439,-8.29206246582409));
#14050=CARTESIAN_POINT('Ctrl Pts',(3.65532159167139,-1.17224786397305,-8.29051419852507));
#14051=CARTESIAN_POINT('Ctrl Pts',(3.68293202746475,-1.16900061372482,-8.28858690779628));
#14052=CARTESIAN_POINT('Ctrl Pts',(3.6887734443652,-1.16826916691848,-8.28818093185543));
#14053=CARTESIAN_POINT('Ctrl Pts',(3.69801046151917,-1.1670421188928,-8.28754202573396));
#14054=CARTESIAN_POINT('Ctrl Pts',(3.70140970609501,-1.16657543734981,-8.28730756464445));
#14055=CARTESIAN_POINT('Ctrl Pts',(3.70785420220928,-1.16566196287278,-8.28686436896848));
#14056=CARTESIAN_POINT('Ctrl Pts',(3.71089971888508,-1.16521809190991,-8.28665548889017));
#14057=CARTESIAN_POINT('Ctrl Pts',(3.71807784491507,-1.16414315916352,-8.2861644455726));
#14058=CARTESIAN_POINT('Ctrl Pts',(3.72220888347381,-1.16350202593281,-8.28588284246284));
#14059=CARTESIAN_POINT('Ctrl Pts',(3.73589114198609,-1.16130388427055,-8.28495319087635));
#14060=CARTESIAN_POINT('Ctrl Pts',(3.7454268831382,-1.15965110669471,-8.28431018833489));
#14061=CARTESIAN_POINT('Ctrl Pts',(3.79963017956614,-1.14956664198542,-8.28067765834852));
#14062=CARTESIAN_POINT('Ctrl Pts',(3.84380533166667,-1.1386711839365,-8.27780356820473));
#14063=CARTESIAN_POINT('Ctrl Pts',(3.8911227553943,-1.12404909828158,-8.27471382251194));
#14064=CARTESIAN_POINT('Ctrl Pts',(3.89499492655824,-1.12283054932074,-8.27446089984202));
#14065=CARTESIAN_POINT('Ctrl Pts',(3.96060868788209,-1.10180885897501,-8.27017273092163));
#14066=CARTESIAN_POINT('Ctrl Pts',(4.02057866627441,-1.07697292027265,-8.2662102054588));
#14067=CARTESIAN_POINT('Ctrl Pts',(4.07816941731679,-1.04735421169019,-8.2621380879065));
#14068=CARTESIAN_POINT('',(2.36176920301685,-0.00059952881750885,-8.32476442050443));
#14069=CARTESIAN_POINT('Ctrl Pts',(4.07816915725551,-1.04735434543869,-8.16230176652656));
#14070=CARTESIAN_POINT('Ctrl Pts',(4.06073549734461,-1.05632040627034,-8.16353188364908));
#14071=CARTESIAN_POINT('Ctrl Pts',(4.04307190617316,-1.06485430475583,-8.16477093535508));
#14072=CARTESIAN_POINT('Ctrl Pts',(3.99701977505773,-1.08570004337058,-8.16799473780531));
#14073=CARTESIAN_POINT('Ctrl Pts',(3.96835626301873,-1.09733763424601,-8.16999526366853));
#14074=CARTESIAN_POINT('Ctrl Pts',(3.93025510188608,-1.11108606666217,-8.17266465525085));
#14075=CARTESIAN_POINT('Ctrl Pts',(3.92120121171684,-1.1142287145254,-8.17329967124867));
#14076=CARTESIAN_POINT('Ctrl Pts',(3.90646535603871,-1.11914292169965,-8.17433480590633));
#14077=CARTESIAN_POINT('Ctrl Pts',(3.90080642365143,-1.12098256103426,-8.17473270126296));
#14078=CARTESIAN_POINT('Ctrl Pts',(3.88990968634928,-1.12443385523869,-8.17549972165527));
#14079=CARTESIAN_POINT('Ctrl Pts',(3.88467408494917,-1.12605199389359,-8.1758686252423));
#14080=CARTESIAN_POINT('Ctrl Pts',(3.87253551839709,-1.12971098483687,-8.17672486506758));
#14081=CARTESIAN_POINT('Ctrl Pts',(3.86562481522897,-1.13172518898455,-8.17721304479307));
#14082=CARTESIAN_POINT('Ctrl Pts',(3.84355771358168,-1.13793800079285,-8.17877438232976));
#14083=CARTESIAN_POINT('Ctrl Pts',(3.82833603164517,-1.1418962791287,-8.17985513208896));
#14084=CARTESIAN_POINT('Ctrl Pts',(3.79237505212377,-1.15048263902049,-8.18241838030266));
#14085=CARTESIAN_POINT('Ctrl Pts',(3.77158128612784,-1.15485647691928,-8.18390830313411));
#14086=CARTESIAN_POINT('Ctrl Pts',(3.69263205179868,-1.16924469347928,-8.18959480980407));
#14087=CARTESIAN_POINT('Ctrl Pts',(3.6338755575999,-1.17544552741947,-8.19389261342827));
#14088=CARTESIAN_POINT('Ctrl Pts',(3.50399101501144,-1.1793500889145,-8.20342455683792));
#14089=CARTESIAN_POINT('Ctrl Pts',(3.43301989923687,-1.17506961604388,-8.20865490359785));
#14090=CARTESIAN_POINT('Ctrl Pts',(3.35319778904565,-1.16295957410807,-8.21431328507573));
#14091=CARTESIAN_POINT('Ctrl Pts',(3.3435531050952,-1.16137330225034,-8.21499301095464));
#14092=CARTESIAN_POINT('Ctrl Pts',(3.33009151782234,-1.15898678139177,-8.21593517475724));
#14093=CARTESIAN_POINT('Ctrl Pts',(3.32625746309614,-1.1582874199884,-8.21620276858639));
#14094=CARTESIAN_POINT('Ctrl Pts',(3.31962932290604,-1.1570443690027,-8.21666399584115));
#14095=CARTESIAN_POINT('Ctrl Pts',(3.31683363599089,-1.15650956362117,-8.21685811233292));
#14096=CARTESIAN_POINT('Ctrl Pts',(3.31091535024887,-1.15535515962905,-8.21726810454076));
#14097=CARTESIAN_POINT('Ctrl Pts',(3.30779326886099,-1.15473302510711,-8.21748383126231));
#14098=CARTESIAN_POINT('Ctrl Pts',(3.3000105146125,-1.15314932666193,-8.21802029289698));
#14099=CARTESIAN_POINT('Ctrl Pts',(3.29535301415351,-1.15217214728251,-8.21834016350221));
#14100=CARTESIAN_POINT('Ctrl Pts',(3.27753271886894,-1.1483204004705,-8.21956000107659));
#14101=CARTESIAN_POINT('Ctrl Pts',(3.26441308816788,-1.14524815112546,-8.22044961659397));
#14102=CARTESIAN_POINT('Ctrl Pts',(3.23057450747311,-1.13670900744828,-8.22272901672618));
#14103=CARTESIAN_POINT('Ctrl Pts',(3.20994624849184,-1.13090051643412,-8.22410375475496));
#14104=CARTESIAN_POINT('Ctrl Pts',(3.0949110140873,-1.09509358266368,-8.23174479328571));
#14105=CARTESIAN_POINT('Ctrl Pts',(3.0044250515071,-1.05384189374142,-8.23769211062487));
#14106=CARTESIAN_POINT('Ctrl Pts',(2.88999386488484,-0.983092326946821,
-8.24622934224479));
#14107=CARTESIAN_POINT('Ctrl Pts',(2.86068165635078,-0.963085097966447,
-8.2485150974589));
#14108=CARTESIAN_POINT('Ctrl Pts',(2.82427440828986,-0.935746422877154,
-8.25151234904213));
#14109=CARTESIAN_POINT('Ctrl Pts',(2.81630787696671,-0.929603062779868,
-8.25217838736915));
#14110=CARTESIAN_POINT('Ctrl Pts',(2.80367460499541,-0.91960027709676,-8.25325161890292));
#14111=CARTESIAN_POINT('Ctrl Pts',(2.79895711802928,-0.915805514003791,
-8.25365627182413));
#14112=CARTESIAN_POINT('Ctrl Pts',(2.79022993678891,-0.908673812405774,
-8.2544122689703));
#14113=CARTESIAN_POINT('Ctrl Pts',(2.78621273183558,-0.905346266374552,
-8.2547632326959));
#14114=CARTESIAN_POINT('Ctrl Pts',(2.7821519465749,-0.901936882440655,-8.25512107657468));
#14115=CARTESIAN_POINT('Ctrl Pts',(2.78208607966513,-0.901881569113669,
-8.25512688171452));
#14116=CARTESIAN_POINT('Ctrl Pts',(2.78196023573616,-0.901775865127666,
-8.25513797447173));
#14117=CARTESIAN_POINT('Ctrl Pts',(2.78190025768347,-0.901725475698881,
-8.25514326203924));
#14118=CARTESIAN_POINT('Ctrl Pts',(2.781785524688,-0.901629065410631,-8.25515337802556));
#14119=CARTESIAN_POINT('Ctrl Pts',(2.78173076890668,-0.9015830455441,-8.25515820640423));
#14120=CARTESIAN_POINT('Ctrl Pts',(2.78162590926246,-0.901494899246168,
-8.25516745404972));
#14121=CARTESIAN_POINT('Ctrl Pts',(2.78157580471779,-0.901452773624273,
-8.25517187328376));
#14122=CARTESIAN_POINT('Ctrl Pts',(2.78147975527106,-0.901372005949661,
-8.25518034578901));
#14123=CARTESIAN_POINT('Ctrl Pts',(2.78143380980148,-0.901333364552745,
-8.25518439903413));
#14124=CARTESIAN_POINT('Ctrl Pts',(2.78134565179312,-0.901259209746639,
-8.25519217698409));
#14125=CARTESIAN_POINT('Ctrl Pts',(2.78130343879901,-0.901223696888161,
-8.25519590166635));
#14126=CARTESIAN_POINT('Ctrl Pts',(2.77603242535316,-0.89678867736647,-8.25566103439582));
#14127=CARTESIAN_POINT('Ctrl Pts',(2.77084210881456,-0.89234383202169,-8.25612427268104));
#14128=CARTESIAN_POINT('Ctrl Pts',(2.75996749929069,-0.882865834528284,
-8.25710609299208));
#14129=CARTESIAN_POINT('Ctrl Pts',(2.7542926265547,-0.877822397316013,-8.25762508446563));
#14130=CARTESIAN_POINT('Ctrl Pts',(2.73934452115733,-0.864276611912959,
-8.25901011484282));
#14131=CARTESIAN_POINT('Ctrl Pts',(2.73015830159822,-0.855680136748306,
-8.25988000738303));
#14132=CARTESIAN_POINT('Ctrl Pts',(2.70228727702932,-0.828748017138927,
-8.26257842807472));
#14133=CARTESIAN_POINT('Ctrl Pts',(2.68407570317796,-0.809936308071678,
-8.2644262723009));
#14134=CARTESIAN_POINT('Ctrl Pts',(2.63525212525014,-0.756018914141172,
-8.2696217206456));
#14135=CARTESIAN_POINT('Ctrl Pts',(2.60607407402053,-0.719682643910868,
-8.27301345992998));
#14136=CARTESIAN_POINT('Ctrl Pts',(2.53580503111774,-0.620688669606909,
-8.28191310786105));
#14137=CARTESIAN_POINT('Ctrl Pts',(2.49839701114971,-0.555664500011472,
-8.28744250732238));
#14138=CARTESIAN_POINT('Ctrl Pts',(2.46344431126419,-0.478800661341516,
-8.29335778435933));
#14139=CARTESIAN_POINT('Ctrl Pts',(2.45958349030215,-0.470027784455235,
-8.29402412159409));
#14140=CARTESIAN_POINT('Ctrl Pts',(2.45431653133051,-0.457652152582669,
-8.29495085444575));
#14141=CARTESIAN_POINT('Ctrl Pts',(2.45282050633424,-0.454088400576892,
-8.29521619395022));
#14142=CARTESIAN_POINT('Ctrl Pts',(2.45014844907429,-0.447634327873626,
-8.29569389492909));
#14143=CARTESIAN_POINT('Ctrl Pts',(2.44896631070694,-0.444746580955021,
-8.29590661129576));
#14144=CARTESIAN_POINT('Ctrl Pts',(2.44657173926473,-0.438830126501377,
-8.29634029331725));
#14145=CARTESIAN_POINT('Ctrl Pts',(2.44536039133525,-0.435801026035407,
-8.29656119482868));
#14146=CARTESIAN_POINT('Ctrl Pts',(2.44227879460698,-0.428001330697253,
-8.29712718375281));
#14147=CARTESIAN_POINT('Ctrl Pts',(2.44042703988587,-0.423223431332281,
-8.29747119748459));
#14148=CARTESIAN_POINT('Ctrl Pts',(2.4327599354013,-0.403051021945426,-8.29891291664065));
#14149=CARTESIAN_POINT('Ctrl Pts',(2.42723606091783,-0.387546749506852,
-8.29999483466165));
#14150=CARTESIAN_POINT('Ctrl Pts',(2.41302343835898,-0.344844384244739,
-8.30291682181446));
#14151=CARTESIAN_POINT('Ctrl Pts',(2.40499540442107,-0.31743713828913,-8.3047291022613));
#14152=CARTESIAN_POINT('Ctrl Pts',(2.37397794645469,-0.195241175366891,
-8.31264077386489));
#14153=CARTESIAN_POINT('Ctrl Pts',(2.36181884170173,-0.0981126955574954,
-8.3185224645049));
#14154=CARTESIAN_POINT('Ctrl Pts',(2.36176920301685,-0.00059952881750885,
-8.32476442050443));
#14155=CARTESIAN_POINT('Ctrl Pts',(2.36176920232564,-0.000598169433328872,
-8.32476450752056));
#14156=CARTESIAN_POINT('Ctrl Pts',(2.36176078348145,0.0159778906434922,
-8.32582556508734));
#14157=CARTESIAN_POINT('Ctrl Pts',(2.36210231053494,0.0325518147491741,
-8.32689511243933));
#14158=CARTESIAN_POINT('Ctrl Pts',(2.3632880888756,0.0609627629056844,-8.32874710217912));
#14159=CARTESIAN_POINT('Ctrl Pts',(2.3639616363581,0.0728044195543848,-8.32952454898454));
#14160=CARTESIAN_POINT('Ctrl Pts',(2.36529272230237,0.0912797575822726,
-8.33074720652455));
#14161=CARTESIAN_POINT('Ctrl Pts',(2.36582794586177,0.097921661903201,-8.33118871079188));
#14162=CARTESIAN_POINT('Ctrl Pts',(2.36688523479258,0.109783963946712,-8.33198090684105));
#14163=CARTESIAN_POINT('Ctrl Pts',(2.36738587832962,0.115006128882268,-8.33233093345332));
#14164=CARTESIAN_POINT('Ctrl Pts',(2.36846555335454,0.125527633098669,-8.33303882149122));
#14165=CARTESIAN_POINT('Ctrl Pts',(2.3690457082434,0.130826730141698,-8.33339670969349));
#14166=CARTESIAN_POINT('Ctrl Pts',(2.37036882146246,0.142197836632974,-8.33416770460845));
#14167=CARTESIAN_POINT('Ctrl Pts',(2.37112315013313,0.14826833907374,-8.33458115498868));
#14168=CARTESIAN_POINT('Ctrl Pts',(2.37328079151084,0.164591850499612,-8.33569804832022));
#14169=CARTESIAN_POINT('Ctrl Pts',(2.37477197897301,0.174832495547505,-8.33640420175529));
#14170=CARTESIAN_POINT('Ctrl Pts',(2.38235476865716,0.222493200376698,-8.33971711464745));
#14171=CARTESIAN_POINT('Ctrl Pts',(2.39011539350623,0.259621034503504,-8.34237513906323));
#14172=CARTESIAN_POINT('Ctrl Pts',(2.41357854808535,0.349881821637091,-8.3490306541492));
#14173=CARTESIAN_POINT('Ctrl Pts',(2.43126392072715,0.402403845014105,-8.35307584541218));
#14174=CARTESIAN_POINT('Ctrl Pts',(2.47186594605988,0.499722039360119,-8.36081419854414));
#14175=CARTESIAN_POINT('Ctrl Pts',(2.49408918139198,0.544685400994504,-8.36449572639096));
#14176=CARTESIAN_POINT('Ctrl Pts',(2.52692639280436,0.601661214198898,-8.36920738648013));
#14177=CARTESIAN_POINT('Ctrl Pts',(2.53501305265763,0.615067360084952,-8.37031937416484));
#14178=CARTESIAN_POINT('Ctrl Pts',(2.54907675903647,0.637364700071641,-8.37216983659112));
#14179=CARTESIAN_POINT('Ctrl Pts',(2.55491200851504,0.646342545901904,-8.37291518236059));
#14180=CARTESIAN_POINT('Ctrl Pts',(2.56329036313399,0.65885624575479,-8.37395312550783));
#14181=CARTESIAN_POINT('Ctrl Pts',(2.56573167118435,0.662459164024132,-8.37425185477075));
#14182=CARTESIAN_POINT('Ctrl Pts',(2.56994873913427,0.668609088486464,-8.37476145765566));
#14183=CARTESIAN_POINT('Ctrl Pts',(2.57171468728923,0.671162735380082,-8.37497296830299));
#14184=CARTESIAN_POINT('Ctrl Pts',(2.57517103568886,0.676118774457328,-8.37538324279247));
#14185=CARTESIAN_POINT('Ctrl Pts',(2.57686033829371,0.678521845731866,-8.37558208073538));
#14186=CARTESIAN_POINT('Ctrl Pts',(2.58151871724492,0.685096079024294,-8.37612586870096));
#14187=CARTESIAN_POINT('Ctrl Pts',(2.58450607370395,0.689254301800044,-8.37646961026985));
#14188=CARTESIAN_POINT('Ctrl Pts',(2.59633102872468,0.705489452312067,-8.37781145673959));
#14189=CARTESIAN_POINT('Ctrl Pts',(2.60537179489746,0.717417568419994,-8.37879680066266));
#14190=CARTESIAN_POINT('Ctrl Pts',(2.6625211180006,0.789905837487637,-8.38480389256936));
#14191=CARTESIAN_POINT('Ctrl Pts',(2.71627609625787,0.845783958635265,-8.38952749019953));
#14192=CARTESIAN_POINT('Ctrl Pts',(2.81283353155703,0.928159282717652,-8.397389559084));
#14193=CARTESIAN_POINT('Ctrl Pts',(2.85252957276116,0.957912519213582,-8.40047769743529));
#14194=CARTESIAN_POINT('Ctrl Pts',(2.91000815473591,0.995579411105192,-8.40487403231615));
#14195=CARTESIAN_POINT('Ctrl Pts',(2.92629051023476,1.00569032416323,-8.40611129291946));
#14196=CARTESIAN_POINT('Ctrl Pts',(2.95154890788124,1.02053362371434,-8.40802356147196));
#14197=CARTESIAN_POINT('Ctrl Pts',(2.96035185823942,1.02555502974522,-8.40868873019762));
#14198=CARTESIAN_POINT('Ctrl Pts',(2.97498524871428,1.03365375908587,-8.40979301758771));
#14199=CARTESIAN_POINT('Ctrl Pts',(2.98077878926827,1.03679690615021,-8.41022985052777));
#14200=CARTESIAN_POINT('Ctrl Pts',(2.99204867994407,1.04278922172803,-8.41107907659921));
#14201=CARTESIAN_POINT('Ctrl Pts',(2.99752165794217,1.04564429497018,-8.41149124859477));
#14202=CARTESIAN_POINT('Ctrl Pts',(3.0031273065338,1.04851274432564,-8.41191324272441));
#14203=CARTESIAN_POINT('Ctrl Pts',(3.00323788122554,1.04856930409486,-8.41192156673778));
#14204=CARTESIAN_POINT('Ctrl Pts',(3.00342760145061,1.04866630952776,-8.41193584867706));
#14205=CARTESIAN_POINT('Ctrl Pts',(3.00350674264168,1.04870676373657,-8.41194180630864));
#14206=CARTESIAN_POINT('Ctrl Pts',(3.00369151720069,1.04880118764809,-8.4119557157843));
#14207=CARTESIAN_POINT('Ctrl Pts',(3.00379715412595,1.04885515034204,-8.41196366786963));
#14208=CARTESIAN_POINT('Ctrl Pts',(3.00404358363176,1.04898098741264,-8.41198221833064));
#14209=CARTESIAN_POINT('Ctrl Pts',(3.00418438250648,1.0490528493909,-8.41199281713353));
#14210=CARTESIAN_POINT('Ctrl Pts',(3.00451246163604,1.04922021361064,-8.41201751343464));
#14211=CARTESIAN_POINT('Ctrl Pts',(3.00469975295649,1.0493156940368,-8.41203161168472));
#14212=CARTESIAN_POINT('Ctrl Pts',(3.00974093748187,1.05188397105003,-8.41241107909415));
#14213=CARTESIAN_POINT('Ctrl Pts',(3.01461183209274,1.05432307569324,-8.41277760506912));
#14214=CARTESIAN_POINT('Ctrl Pts',(3.02572890960923,1.05979382811957,-8.413613958701));
#14215=CARTESIAN_POINT('Ctrl Pts',(3.03198528345281,1.06280418644835,-8.41408450255825));
#14216=CARTESIAN_POINT('Ctrl Pts',(3.05125910350334,1.07186911251431,-8.4155339070149));
#14217=CARTESIAN_POINT('Ctrl Pts',(3.06436052435261,1.07774093068685,-8.41651890293448));
#14218=CARTESIAN_POINT('Ctrl Pts',(3.16623233261341,1.12117943555923,-8.4241792865517));
#14219=CARTESIAN_POINT('Ctrl Pts',(3.25918932323782,1.14795222313181,-8.43122245127678));
#14220=CARTESIAN_POINT('Ctrl Pts',(3.39652600960279,1.16981726679668,-8.44142450440444));
#14221=CARTESIAN_POINT('Ctrl Pts',(3.43904440882171,1.17423368633329,-8.44454845461538));
#14222=CARTESIAN_POINT('Ctrl Pts',(3.4959612390448,1.17703072899519,-8.44862038899891));
#14223=CARTESIAN_POINT('Ctrl Pts',(3.51022364871473,1.17747205426027,-8.44963145722491));
#14224=CARTESIAN_POINT('Ctrl Pts',(3.53447613724297,1.17778153594492,-8.45133129499277));
#14225=CARTESIAN_POINT('Ctrl Pts',(3.54446269446469,1.1777819638142,-8.45202564480724));
#14226=CARTESIAN_POINT('Ctrl Pts',(3.5586809796072,1.17760171540678,-8.45300514502328));
#14227=CARTESIAN_POINT('Ctrl Pts',(3.56291326864206,1.17752524032596,-8.45329556270668));
#14228=CARTESIAN_POINT('Ctrl Pts',(3.57022945136861,1.17735357986424,-8.45379551098007));
#14229=CARTESIAN_POINT('Ctrl Pts',(3.57331352286744,1.177269092133,-8.4540056168586));
#14230=CARTESIAN_POINT('Ctrl Pts',(3.57980093206327,1.17706585560554,-8.45444619224068));
#14231=CARTESIAN_POINT('Ctrl Pts',(3.58320411657049,1.176944465197,-8.45467651666644));
#14232=CARTESIAN_POINT('Ctrl Pts',(3.59237350454669,1.1765775697008,-8.45529506806198));
#14233=CARTESIAN_POINT('Ctrl Pts',(3.59813860016192,1.17630443449146,-8.45568181359106));
#14234=CARTESIAN_POINT('Ctrl Pts',(3.62455042772362,1.17485845080363,-8.457444685568));
#14235=CARTESIAN_POINT('Ctrl Pts',(3.64516743184313,1.17318423927814,-8.45879574553957));
#14236=CARTESIAN_POINT('Ctrl Pts',(3.75004831213089,1.16187971710014,-8.46558934874178));
#14237=CARTESIAN_POINT('Ctrl Pts',(3.83314476718577,1.14371053453635,-8.47072471942511));
#14238=CARTESIAN_POINT('Ctrl Pts',(3.96546579235455,1.0993903585392,-8.47941622617269));
#14239=CARTESIAN_POINT('Ctrl Pts',(4.01607619473185,1.07841644012371,-8.4828718505141));
#14240=CARTESIAN_POINT('Ctrl Pts',(4.07779586716481,1.04764318308853,-8.48737551929737));
#14241=CARTESIAN_POINT('Ctrl Pts',(4.09043308348804,1.0410532504195,-8.4883134819999));
#14242=CARTESIAN_POINT('Ctrl Pts',(4.10902642607274,1.03092402098117,-8.48971885375018));
#14243=CARTESIAN_POINT('Ctrl Pts',(4.11507624026926,1.02755871157946,-8.49018018622034));
#14244=CARTESIAN_POINT('Ctrl Pts',(4.12583100290101,1.02145142224118,-8.49100776511676));
#14245=CARTESIAN_POINT('Ctrl Pts',(4.13054730392122,1.0187297558649,-8.49137328327114));
#14246=CARTESIAN_POINT('Ctrl Pts',(4.14049969022332,1.01289409384736,-8.49215022197749));
#14247=CARTESIAN_POINT('Ctrl Pts',(4.14573081111337,1.00977199087759,-8.49256192531093));
#14248=CARTESIAN_POINT('Ctrl Pts',(4.15968315294684,1.0012972866936,-8.49366912193411));
#14249=CARTESIAN_POINT('Ctrl Pts',(4.1683590635553,0.995871476056532,-8.49436724494464));
#14250=CARTESIAN_POINT('Ctrl Pts',(4.20852813092419,0.970016016376495,-8.49764576156005));
#14251=CARTESIAN_POINT('Ctrl Pts',(4.23910055237191,0.94820325248831,-8.50027644314178));
#14252=CARTESIAN_POINT('Ctrl Pts',(4.34468730792228,0.864980202184821,-8.509865916935));
#14253=CARTESIAN_POINT('Ctrl Pts',(4.41309969317005,0.795826513084492,-8.51708911224113));
#14254=CARTESIAN_POINT('Ctrl Pts',(4.48524465052383,0.70224679447951,-8.52563080566304));
#14255=CARTESIAN_POINT('Ctrl Pts',(4.49777338669352,0.685051974154603,-8.52715445888678));
#14256=CARTESIAN_POINT('Ctrl Pts',(4.51742671607161,0.656484041974723,-8.5296015499679));
#14257=CARTESIAN_POINT('Ctrl Pts',(4.52483458296233,0.645312357990113,-8.53053833038903));
#14258=CARTESIAN_POINT('Ctrl Pts',(4.53460721584136,0.630013620454196,-8.53179166238889));
#14259=CARTESIAN_POINT('Ctrl Pts',(4.5371397517018,0.6259956527282,-8.53211812333897));
#14260=CARTESIAN_POINT('Ctrl Pts',(4.54132805893828,0.619260764496889,-8.53266069052015));
#14261=CARTESIAN_POINT('Ctrl Pts',(4.54299722813137,0.616552294285877,-8.53287764345538));
#14262=CARTESIAN_POINT('Ctrl Pts',(4.54613975814134,0.611406512883597,-8.53328743014268));
#14263=CARTESIAN_POINT('Ctrl Pts',(4.54761528325948,0.608970573167416,-8.53348040714606));
#14264=CARTESIAN_POINT('Ctrl Pts',(4.55109230512926,0.603183099193891,-8.53393656499734));
#14265=CARTESIAN_POINT('Ctrl Pts',(4.55308601929775,0.599826892922202,-8.53419925227035));
#14266=CARTESIAN_POINT('Ctrl Pts',(4.56003193179556,0.588000667300395,-8.53511865226972));
#14267=CARTESIAN_POINT('Ctrl Pts',(4.56489510715683,0.579478458143812,-8.53577002527697));
#14268=CARTESIAN_POINT('Ctrl Pts',(4.60361959657166,0.509603489367829,-8.541028813743));
#14269=CARTESIAN_POINT('Ctrl Pts',(4.63205456827286,0.445392584374849,-8.54535691824139));
#14270=CARTESIAN_POINT('Ctrl Pts',(4.67379162317286,0.322602367426191,-8.55337926701765));
#14271=CARTESIAN_POINT('Ctrl Pts',(4.68865901741366,0.264807918989477,-8.55705994800979));
#14272=CARTESIAN_POINT('Ctrl Pts',(4.70282844640128,0.185102235443723,-8.56221864047418));
#14273=CARTESIAN_POINT('Ctrl Pts',(4.70599483514099,0.163968747254171,-8.56359350718065));
#14274=CARTESIAN_POINT('Ctrl Pts',(4.71049919872604,0.127082840863855,-8.56601384679704));
#14275=CARTESIAN_POINT('Ctrl Pts',(4.71209815794922,0.111367653997609,-8.56705147957901));
#14276=CARTESIAN_POINT('Ctrl Pts',(4.71396599474155,0.0884388505797337,
-8.56857697513455));
#14277=CARTESIAN_POINT('Ctrl Pts',(4.71448542527577,0.0812469655499764,
-8.56905711141265));
#14278=CARTESIAN_POINT('Ctrl Pts',(4.71528343765786,0.0685800088011585,
-8.56990586882487));
#14279=CARTESIAN_POINT('Ctrl Pts',(4.71558989610086,0.0631068626366261,
-8.5702736176451));
#14280=CARTESIAN_POINT('Ctrl Pts',(4.71614903908379,0.0516940467651455,
-8.57104267325166));
#14281=CARTESIAN_POINT('Ctrl Pts',(4.71639498017566,0.0457542175321624,
-8.57144417776944));
#14282=CARTESIAN_POINT('Ctrl Pts',(4.71691904845266,0.0302600167263839,
-8.5724948917667));
#14283=CARTESIAN_POINT('Ctrl Pts',(4.71712584639623,0.0207038332566813,
-8.57314628028743));
#14284=CARTESIAN_POINT('Ctrl Pts',(4.71750672063379,-0.0195381573761509,
-8.57590410907704));
#14285=CARTESIAN_POINT('Ctrl Pts',(4.71659779669541,-0.050219693612534,
-8.5780433410594));
#14286=CARTESIAN_POINT('Ctrl Pts',(4.70733399068953,-0.184884185073918,
-8.58759982283007));
#14287=CARTESIAN_POINT('Ctrl Pts',(4.68638390766865,-0.287522454895993,
-8.59537806441465));
#14288=CARTESIAN_POINT('Ctrl Pts',(4.64506917273959,-0.406605480060373,
-8.60449579594782));
#14289=CARTESIAN_POINT('Ctrl Pts',(4.63736336424964,-0.42697431729419,-8.60605646720677));
#14290=CARTESIAN_POINT('Ctrl Pts',(4.62392295508212,-0.459727057020625,
-8.60855596303928));
#14291=CARTESIAN_POINT('Ctrl Pts',(4.61853036117598,-0.472245091705853,
-8.60950880102283));
#14292=CARTESIAN_POINT('Ctrl Pts',(4.61095454229709,-0.489023407460298,
-8.61077994173423));
#14293=CARTESIAN_POINT('Ctrl Pts',(4.60896113534847,-0.493367545810233,
-8.6111085083254));
#14294=CARTESIAN_POINT('Ctrl Pts',(4.6055941985544,-0.500588656288921,-8.61165361075));
#14295=CARTESIAN_POINT('Ctrl Pts',(4.60423535414794,-0.503472360276474,
-8.61187100954129));
#14296=CARTESIAN_POINT('Ctrl Pts',(4.60164255535387,-0.508917286714236,
-8.61228090783311));
#14297=CARTESIAN_POINT('Ctrl Pts',(4.60041101058886,-0.511479612238486,
-8.61247355525552));
#14298=CARTESIAN_POINT('Ctrl Pts',(4.59747529028392,-0.517531387488772,
-8.61292803045502));
#14299=CARTESIAN_POINT('Ctrl Pts',(4.59576309756903,-0.521016944470832,
-8.61318937340532));
#14300=CARTESIAN_POINT('Ctrl Pts',(4.5896708982446,-0.533265536182916,-8.61410651738165));
#14301=CARTESIAN_POINT('Ctrl Pts',(4.58519868258256,-0.541982617598227,
-8.61475698364283));
#14302=CARTESIAN_POINT('Ctrl Pts',(4.54727226219442,-0.613689952245968,
-8.62009747764822));
#14303=CARTESIAN_POINT('Ctrl Pts',(4.50826355218086,-0.673586541315487,
-8.62449772361319));
#14304=CARTESIAN_POINT('Ctrl Pts',(4.42768005500991,-0.77570327773717,-8.63254402284896));
#14305=CARTESIAN_POINT('Ctrl Pts',(4.38789514166113,-0.819025576961739,
-8.63617457326418));
#14306=CARTESIAN_POINT('Ctrl Pts',(4.32958614886297,-0.873692251181874,
-8.64126928940964));
#14307=CARTESIAN_POINT('Ctrl Pts',(4.31373830148116,-0.887766095862214,
-8.64263328865554));
#14308=CARTESIAN_POINT('Ctrl Pts',(4.28550665895609,-0.91150640607757,-8.64503622250764));
#14309=CARTESIAN_POINT('Ctrl Pts',(4.27329295323843,-0.921367061625402,
-8.6460674750963));
#14310=CARTESIAN_POINT('Ctrl Pts',(4.25520064786482,-0.935385828702654,
-8.64758530924305));
#14311=CARTESIAN_POINT('Ctrl Pts',(4.2494748769335,-0.939739069115081,-8.64806427573587));
#14312=CARTESIAN_POINT('Ctrl Pts',(4.23931779162323,-0.947315578756129,
-8.6489116959137));
#14313=CARTESIAN_POINT('Ctrl Pts',(4.23490314428115,-0.950560910315168,
-8.64927928630794));
#14314=CARTESIAN_POINT('Ctrl Pts',(4.22564520798168,-0.957267672088207,
-8.65004873541952));
#14315=CARTESIAN_POINT('Ctrl Pts',(4.22079800950673,-0.960723413776496,
-8.65045079670912));
#14316=CARTESIAN_POINT('Ctrl Pts',(4.20807001540218,-0.969652894894793,
-8.65150459465732));
#14317=CARTESIAN_POINT('Ctrl Pts',(4.20014829255068,-0.975067240938383,
-8.65215853411324));
#14318=CARTESIAN_POINT('Ctrl Pts',(4.16632706798313,-0.997582057101962,
-8.65494305709908));
#14319=CARTESIAN_POINT('Ctrl Pts',(4.13982523641633,-1.01375067267504,-8.65710723485515));
#14320=CARTESIAN_POINT('Ctrl Pts',(4.10129953939983,-1.03521427371071,-8.66023075645344));
#14321=CARTESIAN_POINT('Ctrl Pts',(4.08978158170309,-1.0413821224762,-8.66116176426806));
#14322=CARTESIAN_POINT('Ctrl Pts',(4.07816915742063,-1.04735434535377,-8.66209739867239));
#14323=CARTESIAN_POINT('Origin',(3.53951905042299,8.32667268468867E-16,
0.924367114736157));
#14324=CARTESIAN_POINT('',(4.07816930022569,-1.0473542719097,-9.26219992867132));
#14325=CARTESIAN_POINT('',(4.07816926754755,-1.04735428871594,-9.16390755708093));
#14326=CARTESIAN_POINT('',(4.07816926754759,-1.04735428871592,0.924367114736157));
#14327=CARTESIAN_POINT('',(2.36176880457028,-0.000312140290006209,-8.92337267760163));
#14328=CARTESIAN_POINT('Ctrl Pts',(4.07816930022569,-1.0473542719097,-9.26219992867132));
#14329=CARTESIAN_POINT('Ctrl Pts',(4.08963334306672,-1.04145835903123,-9.26127063730459));
#14330=CARTESIAN_POINT('Ctrl Pts',(4.1010020975504,-1.03537344480409,-9.26033685088515));
#14331=CARTESIAN_POINT('Ctrl Pts',(4.16522820456332,-0.999628076415812,
-9.25499407938348));
#14332=CARTESIAN_POINT('Ctrl Pts',(4.21582958212587,-0.966111787617561,
-9.25051465419603));
#14333=CARTESIAN_POINT('Ctrl Pts',(4.29570019777826,-0.903846834707519,
-9.24314029442522));
#14334=CARTESIAN_POINT('Ctrl Pts',(4.3264615069074,-0.87719515088128,-9.24021534012738));
#14335=CARTESIAN_POINT('Ctrl Pts',(4.36031091982148,-0.844650927099082,
-9.23694933981284));
#14336=CARTESIAN_POINT('Ctrl Pts',(4.36480211480201,-0.840263261988187,
-9.23651499506486));
#14337=CARTESIAN_POINT('Ctrl Pts',(4.37201908160375,-0.833098970981894,
-9.23581571117833));
#14338=CARTESIAN_POINT('Ctrl Pts',(4.37476648882677,-0.830344455691755,
-9.23554918530032));
#14339=CARTESIAN_POINT('Ctrl Pts',(4.37964025009225,-0.825409418096969,
-9.23507589663737));
#14340=CARTESIAN_POINT('Ctrl Pts',(4.38177184379941,-0.823234213558013,
-9.23486873617146));
#14341=CARTESIAN_POINT('Ctrl Pts',(4.3864111418626,-0.818463117163704,-9.23441751402385));
#14342=CARTESIAN_POINT('Ctrl Pts',(4.38891536393468,-0.815863954448002,
-9.23417371553508));
#14343=CARTESIAN_POINT('Ctrl Pts',(4.39604087317134,-0.808399932866357,
-9.23347918874594));
#14344=CARTESIAN_POINT('Ctrl Pts',(4.40063268022099,-0.803506942148487,
-9.23303062349273));
#14345=CARTESIAN_POINT('Ctrl Pts',(4.43368499966977,-0.767677881049802,
-9.2297920926314));
#14346=CARTESIAN_POINT('Ctrl Pts',(4.46051640196867,-0.735273280729588,
-9.22710973787847));
#14347=CARTESIAN_POINT('Ctrl Pts',(4.53757918975904,-0.631346531393782,
-9.21899012150749));
#14348=CARTESIAN_POINT('Ctrl Pts',(4.58163335796371,-0.555626474272578,
-9.21370441083827));
#14349=CARTESIAN_POINT('Ctrl Pts',(4.63152725662795,-0.442631127956828,
-9.20587193656605));
#14350=CARTESIAN_POINT('Ctrl Pts',(4.64460819991752,-0.408878725878092,
-9.20354193730801));
#14351=CARTESIAN_POINT('Ctrl Pts',(4.65933517862198,-0.364978717601283,
-9.20049408875856));
#14352=CARTESIAN_POINT('Ctrl Pts',(4.66243208574637,-0.355336361622174,
-9.19982366696854));
#14353=CARTESIAN_POINT('Ctrl Pts',(4.66718554213982,-0.339853183258862,
-9.19874501033467));
#14354=CARTESIAN_POINT('Ctrl Pts',(4.66892199164482,-0.334037268492338,
-9.19833936166919));
#14355=CARTESIAN_POINT('Ctrl Pts',(4.67213232569506,-0.322973590811261,
-9.19756666953539));
#14356=CARTESIAN_POINT('Ctrl Pts',(4.67361489002397,-0.317728495057857,
-9.19719991644738));
#14357=CARTESIAN_POINT('Ctrl Pts',(4.67690874478701,-0.305758482561444,
-9.19636185880566));
#14358=CARTESIAN_POINT('Ctrl Pts',(4.67869688507542,-0.299027463514963,
-9.19588982767392));
#14359=CARTESIAN_POINT('Ctrl Pts',(4.6840151654805,-0.278267795252604,-9.19443141043853));
#14360=CARTESIAN_POINT('Ctrl Pts',(4.68734651148602,-0.264190103164261,
-9.19343877846734));
#14361=CARTESIAN_POINT('Ctrl Pts',(4.70239420986669,-0.194931884615751,
-9.18853546129311));
#14362=CARTESIAN_POINT('Ctrl Pts',(4.71039341590205,-0.139027482799525,
-9.18451105362411));
#14363=CARTESIAN_POINT('Ctrl Pts',(4.71858583218342,-0.022747468196687,
-9.17603826664869));
#14364=CARTESIAN_POINT('Ctrl Pts',(4.71820837928671,0.0375109533950848,
-9.17159145904167));
#14365=CARTESIAN_POINT('Ctrl Pts',(4.70982465616552,0.138459987042075,-9.16421327406482));
#14366=CARTESIAN_POINT('Ctrl Pts',(4.70427615462658,0.179242910641523,-9.16125432621756));
#14367=CARTESIAN_POINT('Ctrl Pts',(4.69543002744637,0.225841801929512,-9.15795512584361));
#14368=CARTESIAN_POINT('Ctrl Pts',(4.6942061132978,0.232018312735089,-9.15751952514883));
#14369=CARTESIAN_POINT('Ctrl Pts',(4.69214483700591,0.24200007238953,-9.15681862455754));
#14370=CARTESIAN_POINT('Ctrl Pts',(4.69133804372864,0.245811404715399,-9.15655172633476));
#14371=CARTESIAN_POINT('Ctrl Pts',(4.6898667778766,0.252595419317296,-9.15607803813025));
#14372=CARTESIAN_POINT('Ctrl Pts',(4.68920967077125,0.255569595437543,-9.15587084768446));
#14373=CARTESIAN_POINT('Ctrl Pts',(4.68774960209091,0.262058504494397,-9.15541986490099));
#14374=CARTESIAN_POINT('Ctrl Pts',(4.68694203740685,0.265572117087249,-9.15517633353269));
#14375=CARTESIAN_POINT('Ctrl Pts',(4.68458969482365,0.275595805334758,-9.15448334423797));
#14376=CARTESIAN_POINT('Ctrl Pts',(4.6830055284955,0.282096629209457,-9.15403603439235));
#14377=CARTESIAN_POINT('Ctrl Pts',(4.67121284352306,0.32875705178178,-9.15083840015818));
#14378=CARTESIAN_POINT('Ctrl Pts',(4.65894538874058,0.36837145359408,-9.14819261039131));
#14379=CARTESIAN_POINT('Ctrl Pts',(4.61536088769029,0.486637140151741,-9.1402783699292));
#14380=CARTESIAN_POINT('Ctrl Pts',(4.57764197956753,0.562630195292374,-9.13515435698543));
#14381=CARTESIAN_POINT('Ctrl Pts',(4.51106281395198,0.666878027597784,-9.12733329502117));
#14382=CARTESIAN_POINT('Ctrl Pts',(4.48839341349544,0.698756425904325,-9.12482164501113));
#14383=CARTESIAN_POINT('Ctrl Pts',(4.45776177492426,0.737585817886362,-9.12156794623588));
#14384=CARTESIAN_POINT('Ctrl Pts',(4.45123381713147,0.745639800961582,-9.12088191730762));
#14385=CARTESIAN_POINT('Ctrl Pts',(4.44068336071585,0.758310902967337,-9.11978408369215));
#14386=CARTESIAN_POINT('Ctrl Pts',(4.43672960966522,0.762984763740334,-9.11937503229437));
#14387=CARTESIAN_POINT('Ctrl Pts',(4.42954794135272,0.771341439396519,-9.11863610890818));
#14388=CARTESIAN_POINT('Ctrl Pts',(4.42633313032989,0.775035372907749,-9.11830677570351));
#14389=CARTESIAN_POINT('Ctrl Pts',(4.41872399066602,0.783669220839258,-9.11753056446599));
#14390=CARTESIAN_POINT('Ctrl Pts',(4.41431095395292,0.78859235164709,-9.11708292067995));
#14391=CARTESIAN_POINT('Ctrl Pts',(4.40131462950385,0.802847556905981,-9.11577174995042));
#14392=CARTESIAN_POINT('Ctrl Pts',(4.39262204055105,0.812078251290364,-9.11490367186589));
#14393=CARTESIAN_POINT('Ctrl Pts',(4.3725553530735,0.832709352064227,-9.11291885955465));
#14394=CARTESIAN_POINT('Ctrl Pts',(4.36109324951042,0.844020224018436,-9.11179848748276));
#14395=CARTESIAN_POINT('Ctrl Pts',(4.32202449301362,0.881023456425117,-9.10802254504472));
#14396=CARTESIAN_POINT('Ctrl Pts',(4.29341853456765,0.905622545049296,-9.10532590165063));
#14397=CARTESIAN_POINT('Ctrl Pts',(4.19873448746549,0.979445226994026,-9.09662732168164));
#14398=CARTESIAN_POINT('Ctrl Pts',(4.12865545500534,1.02313031586584,-9.09049984960047));
#14399=CARTESIAN_POINT('Ctrl Pts',(4.03142391945597,1.07041510186476,-9.08272768367678));
#14400=CARTESIAN_POINT('Ctrl Pts',(4.00788805977255,1.08092071459722,-9.08089969833643));
#14401=CARTESIAN_POINT('Ctrl Pts',(3.97835066881136,1.09295901750643,-9.07868626043227));
#14402=CARTESIAN_POINT('Ctrl Pts',(3.97265864685262,1.09522723546081,-9.0782633591093));
#14403=CARTESIAN_POINT('Ctrl Pts',(3.9636693543853,1.09872834224854,-9.07760147925565));
#14404=CARTESIAN_POINT('Ctrl Pts',(3.96038391356208,1.09999100823811,-9.07736082638668));
#14405=CARTESIAN_POINT('Ctrl Pts',(3.95452091590766,1.10221417149019,-9.07693366324458));
#14406=CARTESIAN_POINT('Ctrl Pts',(3.95194565856286,1.10318036663616,-9.07674682639839));
#14407=CARTESIAN_POINT('Ctrl Pts',(3.94575839536678,1.10547703413972,-9.07629980351597));
#14408=CARTESIAN_POINT('Ctrl Pts',(3.94214322633311,1.10679883105043,-9.0760401272873));
#14409=CARTESIAN_POINT('Ctrl Pts',(3.93110419472364,1.11077373401279,-9.07525162115299));
#14410=CARTESIAN_POINT('Ctrl Pts',(3.92365993440262,1.11337011048949,-9.07472596184706));
#14411=CARTESIAN_POINT('Ctrl Pts',(3.90625970466304,1.11924358376448,-9.07351015179051));
#14412=CARTESIAN_POINT('Ctrl Pts',(3.89628480994533,1.12246296901949,-9.07282290104905));
#14413=CARTESIAN_POINT('Ctrl Pts',(3.86116177180829,1.13328335453121,-9.07043260088062));
#14414=CARTESIAN_POINT('Ctrl Pts',(3.83580215638392,1.14017617431293,-9.0687595007412));
#14415=CARTESIAN_POINT('Ctrl Pts',(3.73437495640479,1.16413119829472,-9.06219971522339));
#14416=CARTESIAN_POINT('Ctrl Pts',(3.6569262098942,1.17447290519373,-9.05746845855324));
#14417=CARTESIAN_POINT('Ctrl Pts',(3.53156931604559,1.17867981538654,-9.04959495586625));
#14418=CARTESIAN_POINT('Ctrl Pts',(3.48406947340453,1.1774013087679,-9.04656497099992));
#14419=CARTESIAN_POINT('Ctrl Pts',(3.42604321405689,1.17232011891981,-9.0427372482447));
#14420=CARTESIAN_POINT('Ctrl Pts',(3.41532006689647,1.17123260993621,-9.04202468907453));
#14421=CARTESIAN_POINT('Ctrl Pts',(3.39838136732172,1.16927951085471,-9.04089017243358));
#14422=CARTESIAN_POINT('Ctrl Pts',(3.39215504153234,1.16851113234425,-9.04047123282275));
#14423=CARTESIAN_POINT('Ctrl Pts',(3.38055783923645,1.16698578082427,-9.03968720548648));
#14424=CARTESIAN_POINT('Ctrl Pts',(3.37518545506005,1.16624137598451,-9.03932251860125));
#14425=CARTESIAN_POINT('Ctrl Pts',(3.36323066364055,1.16450065979171,-9.03850759904843));
#14426=CARTESIAN_POINT('Ctrl Pts',(3.35665121845978,1.1634855971851,-9.03805679208694));
#14427=CARTESIAN_POINT('Ctrl Pts',(3.3373448740235,1.16033925122396,-9.03672699418806));
#14428=CARTESIAN_POINT('Ctrl Pts',(3.32464433158858,1.15805457893625,-9.03584325233268));
#14429=CARTESIAN_POINT('Ctrl Pts',(3.23423826910566,1.14025326364087,-9.02948614802173));
#14430=CARTESIAN_POINT('Ctrl Pts',(3.1582500251045,1.11714074226845,-9.02377049920137));
#14431=CARTESIAN_POINT('Ctrl Pts',(3.01422070215346,1.05691564585518,-9.01233051479835));
#14432=CARTESIAN_POINT('Ctrl Pts',(2.94634207959322,1.02036857650566,-9.00664242673716));
#14433=CARTESIAN_POINT('Ctrl Pts',(2.87467016283542,0.972193495537268,-9.00059461486867));
#14434=CARTESIAN_POINT('Ctrl Pts',(2.86689622447771,0.966831311097906,-8.99993823704848));
#14435=CARTESIAN_POINT('Ctrl Pts',(2.85605205373321,0.959157275726047,-8.99902298535755));
#14436=CARTESIAN_POINT('Ctrl Pts',(2.85292759994875,0.956923192484188,-8.99875932279186));
#14437=CARTESIAN_POINT('Ctrl Pts',(2.84728970449266,0.952850089783382,-8.99828371742789));
#14438=CARTESIAN_POINT('Ctrl Pts',(2.84477252497009,0.951016312772162,-8.99807142961469));
#14439=CARTESIAN_POINT('Ctrl Pts',(2.83968959327961,0.947282421592249,-8.99764292220031));
#14440=CARTESIAN_POINT('Ctrl Pts',(2.83712425097242,0.94538182850305,-8.99742673704875));
#14441=CARTESIAN_POINT('Ctrl Pts',(2.83071938564329,0.940596173958933,-8.99688710575142));
#14442=CARTESIAN_POINT('Ctrl Pts',(2.82688967760883,0.937697982421469,-8.99656454525431));
#14443=CARTESIAN_POINT('Ctrl Pts',(2.81846895712306,0.931244083643993,-8.9958552705697));
#14444=CARTESIAN_POINT('Ctrl Pts',(2.81388626687212,0.92767766332118,-8.99546925057171));
#14445=CARTESIAN_POINT('Ctrl Pts',(2.80058346694731,0.917166034860543,-8.99434801501589));
#14446=CARTESIAN_POINT('Ctrl Pts',(2.79193511747921,0.910130548343248,-8.99361821525855));
#14447=CARTESIAN_POINT('Ctrl Pts',(2.76127234382075,0.884454160107922,-8.99102220184978));
#14448=CARTESIAN_POINT('Ctrl Pts',(2.73984326759052,0.865127720320402,-8.98919177269108));
#14449=CARTESIAN_POINT('Ctrl Pts',(2.65448340844706,0.782258625648962,-8.98172854256945));
#14450=CARTESIAN_POINT('Ctrl Pts',(2.5972423842953,0.712272274297962,-8.97627865820013));
#14451=CARTESIAN_POINT('Ctrl Pts',(2.53047149259053,0.608306034599382,-8.96842090093681));
#14452=CARTESIAN_POINT('Ctrl Pts',(2.51360955787103,0.57941573864605,-8.96626259963272));
#14453=CARTESIAN_POINT('Ctrl Pts',(2.49339641322563,0.541128213777162,-8.96341113527916));
#14454=CARTESIAN_POINT('Ctrl Pts',(2.48890217169691,0.53234996030533,-8.9627580081856));
#14455=CARTESIAN_POINT('Ctrl Pts',(2.48184658109268,0.518131402611675,-8.96170059706348));
#14456=CARTESIAN_POINT('Ctrl Pts',(2.47921567050628,0.512725992147499,-8.96129871906388));
#14457=CARTESIAN_POINT('Ctrl Pts',(2.47427286168787,0.502369856149128,-8.96052886436018));
#14458=CARTESIAN_POINT('Ctrl Pts',(2.47195380031458,0.497422707581607,-8.9601611448831));
#14459=CARTESIAN_POINT('Ctrl Pts',(2.46671179418306,0.486034650087646,-8.95931467700909));
#14460=CARTESIAN_POINT('Ctrl Pts',(2.46381230526263,0.47958324070721,-8.9588351480557));
#14461=CARTESIAN_POINT('Ctrl Pts',(2.45492885865795,0.459331504189362,-8.95732961954061));
#14462=CARTESIAN_POINT('Ctrl Pts',(2.44915125745764,0.445442874693758,-8.95629677508804));
#14463=CARTESIAN_POINT('Ctrl Pts',(2.43629641795002,0.412791587659935,-8.95386670986936));
#14464=CARTESIAN_POINT('Ctrl Pts',(2.4294294010271,0.393951722943571,-8.95246307168722));
#14465=CARTESIAN_POINT('Ctrl Pts',(2.40604235155459,0.324312519831071,-8.9472686394524));
#14466=CARTESIAN_POINT('Ctrl Pts',(2.39250378116479,0.272585558554468,-8.9433949359844));
#14467=CARTESIAN_POINT('Ctrl Pts',(2.36869852434421,0.147462386188431,-8.93406709201026));
#14468=CARTESIAN_POINT('Ctrl Pts',(2.36174956856233,0.0736584921003024,
-8.92859389040902));
#14469=CARTESIAN_POINT('Ctrl Pts',(2.36176909144411,-0.000310846004542871,
-8.92337227123527));
#14470=CARTESIAN_POINT('Ctrl Pts',(2.36176909177713,-0.000312105247537074,
-8.92337218234323));
#14471=CARTESIAN_POINT('Ctrl Pts',(2.36177231614068,-0.0124794560323217,
-8.92251326923424));
#14472=CARTESIAN_POINT('Ctrl Pts',(2.36196409229702,-0.0246466945384356,
-8.92166180223257));
#14473=CARTESIAN_POINT('Ctrl Pts',(2.36247050361707,-0.0408418590511107,
-8.92054020408476));
#14474=CARTESIAN_POINT('Ctrl Pts',(2.362617316509,-0.0448736989792606,-8.92026194889334));
#14475=CARTESIAN_POINT('Ctrl Pts',(2.36291075130765,-0.0519342519770015,
-8.91977645943059));
#14476=CARTESIAN_POINT('Ctrl Pts',(2.36304835584035,-0.0549632730162014,
-8.91956875898379));
#14477=CARTESIAN_POINT('Ctrl Pts',(2.36334290853361,-0.0609380626644507,
-8.91916025015191));
#14478=CARTESIAN_POINT('Ctrl Pts',(2.36349922911758,-0.0638838392538005,
-8.91895941147573));
#14479=CARTESIAN_POINT('Ctrl Pts',(2.36386097653497,-0.0702487557989056,
-8.91852672076499));
#14480=CARTESIAN_POINT('Ctrl Pts',(2.36407025187672,-0.0736676125520782,
-8.91829508170281));
#14481=CARTESIAN_POINT('Ctrl Pts',(2.36467799633847,-0.0829331121346435,
-8.91766930113932));
#14482=CARTESIAN_POINT('Ctrl Pts',(2.36510519782933,-0.0887778677943178,
-8.91727670077202));
#14483=CARTESIAN_POINT('Ctrl Pts',(2.36731058186096,-0.11614008789068,-8.91544778385838));
#14484=CARTESIAN_POINT('Ctrl Pts',(2.36963672974143,-0.137610721060054,
-8.91403886236286));
#14485=CARTESIAN_POINT('Ctrl Pts',(2.38133402428916,-0.22345833706628,-8.90846743496257));
#14486=CARTESIAN_POINT('Ctrl Pts',(2.39544112017721,-0.287077292534596,
-8.90447455344316));
#14487=CARTESIAN_POINT('Ctrl Pts',(2.43703807823093,-0.421058881289123,
-8.89579171533054));
#14488=CARTESIAN_POINT('Ctrl Pts',(2.4661742525164,-0.4905953086895,-8.89110400683701));
#14489=CARTESIAN_POINT('Ctrl Pts',(2.50793363757105,-0.568417288364759,
-8.8853247761715));
#14490=CARTESIAN_POINT('Ctrl Pts',(2.51431974038685,-0.579856042604948,
-8.88446131719707));
#14491=CARTESIAN_POINT('Ctrl Pts',(2.52425670568453,-0.596977623060411,
-8.88314631488429));
#14492=CARTESIAN_POINT('Ctrl Pts',(2.52766757932933,-0.602740830219868,
-8.88269974011925));
#14493=CARTESIAN_POINT('Ctrl Pts',(2.53393074493679,-0.613120433271041,
-8.88188812492872));
#14494=CARTESIAN_POINT('Ctrl Pts',(2.5367661625282,-0.617746833225735,-8.88152370008984));
#14495=CARTESIAN_POINT('Ctrl Pts',(2.54293252729267,-0.627653840240728,
-8.88073745886427));
#14496=CARTESIAN_POINT('Ctrl Pts',(2.54627368435401,-0.632927864330125,
-8.88031527838795));
#14497=CARTESIAN_POINT('Ctrl Pts',(2.55542440021407,-0.647121385776659,
-8.87916910557777));
#14498=CARTESIAN_POINT('Ctrl Pts',(2.56131308989063,-0.655988913307658,
-8.87844222248564));
#14499=CARTESIAN_POINT('Ctrl Pts',(2.59280065046521,-0.702037783473917,
-8.8746093584544));
#14500=CARTESIAN_POINT('Ctrl Pts',(2.62039827712374,-0.737800020886741,
-8.87142906096169));
#14501=CARTESIAN_POINT('Ctrl Pts',(2.72094054186407,-0.853667504362611,
-8.86040848353568));
#14502=CARTESIAN_POINT('Ctrl Pts',(2.80283439872371,-0.925263300356887,
-8.85227333757289));
#14503=CARTESIAN_POINT('Ctrl Pts',(2.90152362503403,-0.990026502614511,
-8.84392696276257));
#14504=CARTESIAN_POINT('Ctrl Pts',(2.90976392173099,-0.995288466050037,
-8.84324040757507));
#14505=CARTESIAN_POINT('Ctrl Pts',(2.92257112261698,-1.00324394137235,-8.84219027383643));
#14506=CARTESIAN_POINT('Ctrl Pts',(2.92709209135357,-1.00601012611928,-8.84182277416599));
#14507=CARTESIAN_POINT('Ctrl Pts',(2.93552925982405,-1.01109450750296,-8.84114307391586));
#14508=CARTESIAN_POINT('Ctrl Pts',(2.93944050101716,-1.01342069571614,-8.8408304082343));
#14509=CARTESIAN_POINT('Ctrl Pts',(2.94604676579269,-1.01729807712049,-8.84030649511363));
#14510=CARTESIAN_POINT('Ctrl Pts',(2.94873459662084,-1.01886135475544,-8.84009449452714));
#14511=CARTESIAN_POINT('Ctrl Pts',(2.9539029945154,-1.02184003325973,-8.83968910540955));
#14512=CARTESIAN_POINT('Ctrl Pts',(2.95638256253205,-1.02325708179407,-8.83949560891932));
#14513=CARTESIAN_POINT('Ctrl Pts',(2.96228996236755,-1.02660465558767,-8.83903690863292));
#14514=CARTESIAN_POINT('Ctrl Pts',(2.96572238797495,-1.02852706830489,-8.83877221143111));
#14515=CARTESIAN_POINT('Ctrl Pts',(2.9779055997819,-1.03527059830275,-8.83783889164384));
#14516=CARTESIAN_POINT('Ctrl Pts',(2.98670832404251,-1.03999769069367,-8.8371758217598));
#14517=CARTESIAN_POINT('Ctrl Pts',(3.04657770056838,-1.07117275790117,-8.83273452174878));
#14518=CARTESIAN_POINT('Ctrl Pts',(3.09946859370275,-1.09396504642525,-8.8291419138987));
#14519=CARTESIAN_POINT('Ctrl Pts',(3.19913497165124,-1.12850961528438,-8.82260172546278));
#14520=CARTESIAN_POINT('Ctrl Pts',(3.24536697292716,-1.14143319377165,-8.81965237923606));
#14521=CARTESIAN_POINT('Ctrl Pts',(3.34442092574751,-1.16270299392756,-8.81331692873009));
#14522=CARTESIAN_POINT('Ctrl Pts',(3.39727873306971,-1.17034530686602,-8.80992542131133));
#14523=CARTESIAN_POINT('Ctrl Pts',(3.46126980497719,-1.17519762780947,-8.80570760389383));
#14524=CARTESIAN_POINT('Ctrl Pts',(3.47208192614711,-1.17586760747678,-8.80499129516506));
#14525=CARTESIAN_POINT('Ctrl Pts',(3.48911704761752,-1.1766874791496,-8.80385626827961));
#14526=CARTESIAN_POINT('Ctrl Pts',(3.49533480206862,-1.17693735396795,-8.80344064021155));
#14527=CARTESIAN_POINT('Ctrl Pts',(3.5069794176266,-1.17731291464548,-8.802659597622));
#14528=CARTESIAN_POINT('Ctrl Pts',(3.51240575520512,-1.17745037866853,-8.80229455713028));
#14529=CARTESIAN_POINT('Ctrl Pts',(3.5245564279757,-1.17767415073417,-8.80147465256933));
#14530=CARTESIAN_POINT('Ctrl Pts',(3.5312808972948,-1.17774038521574,-8.8010191807041));
#14531=CARTESIAN_POINT('Ctrl Pts',(3.54839348320659,-1.17776237774439,-8.79985554920618));
#14532=CARTESIAN_POINT('Ctrl Pts',(3.55878094268081,-1.17763828976162,-8.79914495935162));
#14533=CARTESIAN_POINT('Ctrl Pts',(3.64445378739264,-1.17548106781179,-8.79324761506457));
#14534=CARTESIAN_POINT('Ctrl Pts',(3.7193729583074,-1.1663686175127,-8.78784016432703));
#14535=CARTESIAN_POINT('Ctrl Pts',(3.8497285256343,-1.13765184422876,-8.77807623586314));
#14536=CARTESIAN_POINT('Ctrl Pts',(3.90555469519211,-1.12093701855502,-8.77377774225982));
#14537=CARTESIAN_POINT('Ctrl Pts',(3.97892912238956,-1.09289893176094,-8.76810670357589));
#14538=CARTESIAN_POINT('Ctrl Pts',(3.9977505134751,-1.08514206931875,-8.76665058505482));
#14539=CARTESIAN_POINT('Ctrl Pts',(4.02823573009161,-1.07164345030026,-8.76429956479538));
#14540=CARTESIAN_POINT('Ctrl Pts',(4.04002187807957,-1.06618977294646,-8.76339250896237));
#14541=CARTESIAN_POINT('Ctrl Pts',(4.05594175985787,-1.05850114302582,-8.7621722110569));
#14542=CARTESIAN_POINT('Ctrl Pts',(4.06015536865852,-1.05643500065844,-8.76184970093639));
#14543=CARTESIAN_POINT('Ctrl Pts',(4.06719449747374,-1.05293102069315,-8.76131185770972));
#14544=CARTESIAN_POINT('Ctrl Pts',(4.07002673003855,-1.05150687796724,-8.76109570838924));
#14545=CARTESIAN_POINT('Ctrl Pts',(4.07462752246215,-1.04917012245422,-8.76074504322008));
#14546=CARTESIAN_POINT('Ctrl Pts',(4.07639953927922,-1.04826445304739,-8.76061009249694));
#14547=CARTESIAN_POINT('Ctrl Pts',(4.07816926754756,-1.04735428871593,-8.76047541727166));
#14548=CARTESIAN_POINT('Ctrl Pts',(4.07816915742063,-1.04735434535377,-8.66209739867239));
#14549=CARTESIAN_POINT('Ctrl Pts',(3.9974608073836,-1.08886232360001,-8.66860021902885));
#14550=CARTESIAN_POINT('Ctrl Pts',(3.9121910246898,-1.12091888908839,-8.67535949568211));
#14551=CARTESIAN_POINT('Ctrl Pts',(3.80295645902651,-1.14811531261076,-8.68350208996762));
#14552=CARTESIAN_POINT('Ctrl Pts',(3.78170985860687,-1.15278435411068,-8.68506098222062));
#14553=CARTESIAN_POINT('Ctrl Pts',(3.74696882773482,-1.15941584067738,-8.68755796389704));
#14554=CARTESIAN_POINT('Ctrl Pts',(3.73354871872066,-1.16173707413847,-8.68851003417399));
#14555=CARTESIAN_POINT('Ctrl Pts',(3.71536907575789,-1.16455771054805,-8.68978032429001));
#14556=CARTESIAN_POINT('Ctrl Pts',(3.71064296518156,-1.1652615587842,-8.69010879091327));
#14557=CARTESIAN_POINT('Ctrl Pts',(3.70275712088072,-1.16638696610513,-8.69065377289713));
#14558=CARTESIAN_POINT('Ctrl Pts',(3.69959977072883,-1.16682448810688,-8.69087115044265));
#14559=CARTESIAN_POINT('Ctrl Pts',(3.69362286572639,-1.16762800578355,-8.6912810430475));
#14560=CARTESIAN_POINT('Ctrl Pts',(3.69080370318118,-1.16799661817063,-8.69147370580855));
#14561=CARTESIAN_POINT('Ctrl Pts',(3.68412993167606,-1.16884466158273,-8.69192825967762));
#14562=CARTESIAN_POINT('Ctrl Pts',(3.68027420150043,-1.1693152433769,-8.69218966554994));
#14563=CARTESIAN_POINT('Ctrl Pts',(3.66667920828045,-1.17090625721777,-8.6931073248795));
#14564=CARTESIAN_POINT('Ctrl Pts',(3.65692803206303,-1.17192419350708,-8.69375823543138));
#14565=CARTESIAN_POINT('Ctrl Pts',(3.57638729633102,-1.1793165244109,-8.69908283427172));
#14566=CARTESIAN_POINT('Ctrl Pts',(3.50515659306746,-1.17939339271543,-8.70346881539347));
#14567=CARTESIAN_POINT('Ctrl Pts',(3.37566820087746,-1.16778366451642,-8.71151053143475));
#14568=CARTESIAN_POINT('Ctrl Pts',(3.31747213223363,-1.15812792746867,-8.7151511905174));
#14569=CARTESIAN_POINT('Ctrl Pts',(3.23962288714567,-1.1391259629978,-8.72025881467248));
#14570=CARTESIAN_POINT('Ctrl Pts',(3.21914168993476,-1.13353603150022,-8.72162501662779));
#14571=CARTESIAN_POINT('Ctrl Pts',(3.18377904313101,-1.12284955277767,-8.72403147961915));
#14572=CARTESIAN_POINT('Ctrl Pts',(3.16882761329751,-1.11800263486215,-8.72506402673299));
#14573=CARTESIAN_POINT('Ctrl Pts',(3.14717836349303,-1.11050242466259,-8.72658341566333));
#14574=CARTESIAN_POINT('Ctrl Pts',(3.14040039252556,-1.10808444753885,-8.72706261987008));
#14575=CARTESIAN_POINT('Ctrl Pts',(3.1285011019195,-1.10371614810957,-8.7279103115993));
#14576=CARTESIAN_POINT('Ctrl Pts',(3.12337039133706,-1.10179189568675,-8.72827793399818));
#14577=CARTESIAN_POINT('Ctrl Pts',(3.11269578886876,-1.0977032312863,-8.72904730221079));
#14578=CARTESIAN_POINT('Ctrl Pts',(3.10715451345502,-1.09553246666253,-8.72944924960882));
#14579=CARTESIAN_POINT('Ctrl Pts',(3.0927297134724,-1.08975514371388,-8.73050241678896));
#14580=CARTESIAN_POINT('Ctrl Pts',(3.08387350838729,-1.08608200218113,-8.73115583450176));
#14581=CARTESIAN_POINT('Ctrl Pts',(3.04660893451506,-1.07009038831552,-8.73393489708089));
#14582=CARTESIAN_POINT('Ctrl Pts',(3.01864962864896,-1.05676324728888,-8.73609397126681));
#14583=CARTESIAN_POINT('Ctrl Pts',(2.91773099252175,-1.00368077754352,-8.74416946267091));
#14584=CARTESIAN_POINT('Ctrl Pts',(2.84851704391596,-0.957344434425838,
-8.7502922529012));
#14585=CARTESIAN_POINT('Ctrl Pts',(2.74472765957978,-0.870701745962381,
-8.76018915930182));
#14586=CARTESIAN_POINT('Ctrl Pts',(2.70695127873819,-0.834653874771428,
-8.76397278175873));
#14587=CARTESIAN_POINT('Ctrl Pts',(2.66698249561753,-0.791090020150359,
-8.76808479599442));
#14588=CARTESIAN_POINT('Ctrl Pts',(2.66232473464918,-0.78592213206882,-8.7685657755721));
#14589=CARTESIAN_POINT('Ctrl Pts',(2.65528618998126,-0.777972179902232,
-8.76929495459797));
#14590=CARTESIAN_POINT('Ctrl Pts',(2.65287222992097,-0.775219891899317,
-8.76954546645073));
#14591=CARTESIAN_POINT('Ctrl Pts',(2.64847626374007,-0.770160415417471,
-8.77000238434609));
#14592=CARTESIAN_POINT('Ctrl Pts',(2.64649035360601,-0.76785679672948,-8.77020906624987));
#14593=CARTESIAN_POINT('Ctrl Pts',(2.64202693822144,-0.762638579443017,
-8.77067421435091));
#14594=CARTESIAN_POINT('Ctrl Pts',(2.63955469344502,-0.759719587427232,
-8.77093230250886));
#14595=CARTESIAN_POINT('Ctrl Pts',(2.63320127463518,-0.752143538191937,
-8.77159688184241));
#14596=CARTESIAN_POINT('Ctrl Pts',(2.62934169925146,-0.747468397983037,
-8.77200188949428));
#14597=CARTESIAN_POINT('Ctrl Pts',(2.60366932200679,-0.715877493478427,
-8.77470620070683));
#14598=CARTESIAN_POINT('Ctrl Pts',(2.58301493252321,-0.688037555303019,
-8.77693295254152));
#14599=CARTESIAN_POINT('Ctrl Pts',(2.54783916841607,-0.635971961828979,
-8.78090331680849));
#14600=CARTESIAN_POINT('Ctrl Pts',(2.53290471655096,-0.612059660536366,
-8.78265818904448));
#14601=CARTESIAN_POINT('Ctrl Pts',(2.49494161028182,-0.546120513736313,
-8.78737575616374));
#14602=CARTESIAN_POINT('Ctrl Pts',(2.47359651584187,-0.5031885361905,-8.79032150375918));
#14603=CARTESIAN_POINT('Ctrl Pts',(2.4340991329798,-0.409873764049416,-8.79665774635196));
#14604=CARTESIAN_POINT('Ctrl Pts',(2.41664772513331,-0.35931684385472,-8.80005391721409));
#14605=CARTESIAN_POINT('Ctrl Pts',(2.39985779673868,-0.297295624501065,
-8.8042768975133));
#14606=CARTESIAN_POINT('Ctrl Pts',(2.39717105565113,-0.286798723063731,
-8.80499336421082));
#14607=CARTESIAN_POINT('Ctrl Pts',(2.39316992523516,-0.270217445195534,
-8.80612854492578));
#14608=CARTESIAN_POINT('Ctrl Pts',(2.3917582452502,-0.264156991407749,-8.80654416676548));
#14609=CARTESIAN_POINT('Ctrl Pts',(2.3892054044546,-0.252790491024977,-8.80732513892054));
#14610=CARTESIAN_POINT('Ctrl Pts',(2.38805276118713,-0.247487170412317,
-8.8076901148465));
#14611=CARTESIAN_POINT('Ctrl Pts',(2.38555451204194,-0.23559732256814,-8.80850979656875));
#14612=CARTESIAN_POINT('Ctrl Pts',(2.38422857218946,-0.229006903620162,
-8.80896510934774));
#14613=CARTESIAN_POINT('Ctrl Pts',(2.38099857394131,-0.212210176042844,
-8.81012818078284));
#14614=CARTESIAN_POINT('Ctrl Pts',(2.37917295526403,-0.201989555996275,
-8.8108383661953));
#14615=CARTESIAN_POINT('Ctrl Pts',(2.36696642770435,-0.128014622434676,
-8.81599763491008));
#14616=CARTESIAN_POINT('Ctrl Pts',(2.36171261891292,-0.0635365509780738,
-8.82060582498249));
#14617=CARTESIAN_POINT('Ctrl Pts',(2.36181433349692,0.0519195771972148,
-8.82901285139798));
#14618=CARTESIAN_POINT('Ctrl Pts',(2.36515651413367,0.102744742857314,-8.83276508705235));
#14619=CARTESIAN_POINT('Ctrl Pts',(2.3778751890873,0.199695647522794,-8.8399088433191));
#14620=CARTESIAN_POINT('Ctrl Pts',(2.38674892915628,0.245798462044947,-8.84329878187754));
#14621=CARTESIAN_POINT('Ctrl Pts',(2.3999257152051,0.29742676582827,-8.84700591707656));
#14622=CARTESIAN_POINT('Ctrl Pts',(2.40155132085988,0.303587057758833,-8.84744675703674));
#14623=CARTESIAN_POINT('Ctrl Pts',(2.4042571527352,0.313513689506547,-8.84815437436656));
#14624=CARTESIAN_POINT('Ctrl Pts',(2.40530629706599,0.317288261814352,-8.84842279897806));
#14625=CARTESIAN_POINT('Ctrl Pts',(2.40720491253418,0.323989259454611,-8.84889810020102));
#14626=CARTESIAN_POINT('Ctrl Pts',(2.40804692610096,0.326917695634533,-8.84910538888988));
#14627=CARTESIAN_POINT('Ctrl Pts',(2.40990513071156,0.333287154191222,-8.84955531254499));
#14628=CARTESIAN_POINT('Ctrl Pts',(2.4109256845474,0.336726818231201,-8.84979769587075));
#14629=CARTESIAN_POINT('Ctrl Pts',(2.41387130656833,0.346490868119096,-8.85048421364171));
#14630=CARTESIAN_POINT('Ctrl Pts',(2.41583396400575,0.352803906558349,-8.8509262619992));
#14631=CARTESIAN_POINT('Ctrl Pts',(2.42977748094404,0.396357244641593,-8.85396543418084));
#14632=CARTESIAN_POINT('Ctrl Pts',(2.44355552443413,0.433001232753845,-8.85646949173506));
#14633=CARTESIAN_POINT('Ctrl Pts',(2.4902530283988,0.540597345477947,-8.86385036691219));
#14634=CARTESIAN_POINT('Ctrl Pts',(2.52843315541402,0.609024420041593,-8.86859470968871));
#14635=CARTESIAN_POINT('Ctrl Pts',(2.59999073242161,0.711753501755807,-8.87645640607158));
#14636=CARTESIAN_POINT('Ctrl Pts',(2.62915337702536,0.748692232846074,-8.87945856176948));
#14637=CARTESIAN_POINT('Ctrl Pts',(2.667598761611,0.791811643273932,-8.88325503414764));
#14638=CARTESIAN_POINT('Ctrl Pts',(2.67486353588126,0.799738392945461,-8.8839659080122));
#14639=CARTESIAN_POINT('Ctrl Pts',(2.6865328737979,0.812126173364211,-8.88509829773899));
#14640=CARTESIAN_POINT('Ctrl Pts',(2.69086639221976,0.816653538620872,-8.88551681436602));
#14641=CARTESIAN_POINT('Ctrl Pts',(2.69901696684668,0.825033770216634,-8.88630039219691));
#14642=CARTESIAN_POINT('Ctrl Pts',(2.7028249186663,0.828895290548517,-8.88666505556511));
#14643=CARTESIAN_POINT('Ctrl Pts',(2.71137063056066,0.837442330187668,-8.88748036288836));
#14644=CARTESIAN_POINT('Ctrl Pts',(2.71612172788788,0.842114189286999,-8.88793158445108));
#14645=CARTESIAN_POINT('Ctrl Pts',(2.73021293812381,0.855737129817766,-8.8892640394302));
#14646=CARTESIAN_POINT('Ctrl Pts',(2.73966092889519,0.864574682176917,-8.89015005339014));
#14647=CARTESIAN_POINT('Ctrl Pts',(2.76150175211802,0.884339913236428,-8.89218245226908));
#14648=CARTESIAN_POINT('Ctrl Pts',(2.77398258521334,0.895165835069931,-8.89333273114648));
#14649=CARTESIAN_POINT('Ctrl Pts',(2.81684584474778,0.93079348183847,-8.89724718513228));
#14650=CARTESIAN_POINT('Ctrl Pts',(2.84823566606857,0.954337376119247,-8.90005584414333));
#14651=CARTESIAN_POINT('Ctrl Pts',(2.94065745780453,1.01670297898974,-8.90814548186253));
#14652=CARTESIAN_POINT('Ctrl Pts',(3.00416872283774,1.05153207825113,-8.91350572617452));
#14653=CARTESIAN_POINT('Ctrl Pts',(3.10049717885613,1.09335557254088,-8.92110739508938));
#14654=CARTESIAN_POINT('Ctrl Pts',(3.1310573092291,1.10513621200808,-8.92344538144226));
#14655=CARTESIAN_POINT('Ctrl Pts',(3.1682661599061,1.11772497543486,-8.92617474308405));
#14656=CARTESIAN_POINT('Ctrl Pts',(3.17447839397634,1.11976924116198,-8.92662656994381));
#14657=CARTESIAN_POINT('Ctrl Pts',(3.18414845399379,1.12286234828569,-8.92732357957514));
#14658=CARTESIAN_POINT('Ctrl Pts',(3.18759450376476,1.1239471643922,-8.92757073064642));
#14659=CARTESIAN_POINT('Ctrl Pts',(3.19395393603935,1.12591699716735,-8.92802448380522));
#14660=CARTESIAN_POINT('Ctrl Pts',(3.19686575915843,1.12680657397948,-8.92823133539416));
#14661=CARTESIAN_POINT('Ctrl Pts',(3.2035004005722,1.12880539427537,-8.92870060630465));
#14662=CARTESIAN_POINT('Ctrl Pts',(3.20722528125847,1.12990751977592,-8.92896261696778));
#14663=CARTESIAN_POINT('Ctrl Pts',(3.21870138820684,1.13324143527843,-8.92976559017846));
#14664=CARTESIAN_POINT('Ctrl Pts',(3.22647033874073,1.1354120996197,-8.93030320975343));
#14665=CARTESIAN_POINT('Ctrl Pts',(3.24468724806487,1.1403007501308,-8.93155125643204));
#14666=CARTESIAN_POINT('Ctrl Pts',(3.25515164026599,1.14295528635163,-8.93225856637352));
#14667=CARTESIAN_POINT('Ctrl Pts',(3.29236858716396,1.15185342809371,-8.9347450010297));
#14668=CARTESIAN_POINT('Ctrl Pts',(3.31930291656333,1.15730494356889,-8.93649151118519));
#14669=CARTESIAN_POINT('Ctrl Pts',(3.42661289111125,1.17514182710077,-8.94332756233797));
#14670=CARTESIAN_POINT('Ctrl Pts',(3.50798584085962,1.18013237872005,-8.94825762361707));
#14671=CARTESIAN_POINT('Ctrl Pts',(3.63203742391708,1.17489212978994,-8.95608164288481));
#14672=CARTESIAN_POINT('Ctrl Pts',(3.67471410817305,1.17074883756273,-8.95882626358399));
#14673=CARTESIAN_POINT('Ctrl Pts',(3.72743839243694,1.16270866958556,-8.96233314904268));
#14674=CARTESIAN_POINT('Ctrl Pts',(3.73778789280795,1.16098862352448,-8.9630270704972));
#14675=CARTESIAN_POINT('Ctrl Pts',(3.75422247413022,1.1580311048233,-8.96413845742952));
#14676=CARTESIAN_POINT('Ctrl Pts',(3.76032329199444,1.15688334948042,-8.96455311102073));
#14677=CARTESIAN_POINT('Ctrl Pts',(3.77169085769813,1.1546515603288,-8.96532975844936));
#14678=CARTESIAN_POINT('Ctrl Pts',(3.7769598294118,1.15357958056401,-8.96569136402008));
#14679=CARTESIAN_POINT('Ctrl Pts',(3.78879516213081,1.15108714536521,-8.96650735723418));
#14680=CARTESIAN_POINT('Ctrl Pts',(3.7953570356006,1.14964651880492,-8.96696237107496));
#14681=CARTESIAN_POINT('Ctrl Pts',(3.81478330215444,1.14520702781804,-8.96831735422135));
#14682=CARTESIAN_POINT('Ctrl Pts',(3.82760959976974,1.14204787798827,-8.96922235200541));
#14683=CARTESIAN_POINT('Ctrl Pts',(3.92377167321873,1.11663992015718,-8.97608829831713));
#14684=CARTESIAN_POINT('Ctrl Pts',(4.00447517380053,1.08551606524862,-8.98233993169424));
#14685=CARTESIAN_POINT('Ctrl Pts',(4.14211592463982,1.01424946341971,-8.99371241749511));
#14686=CARTESIAN_POINT('Ctrl Pts',(4.20030761664452,0.977335754283417,-8.99877607047694));
#14687=CARTESIAN_POINT('Ctrl Pts',(4.26278676169745,0.929557012329672,-9.00428974473512));
#14688=CARTESIAN_POINT('Ctrl Pts',(4.2705493939516,0.923464711869176,-9.00497608830097));
#14689=CARTESIAN_POINT('Ctrl Pts',(4.28128243508099,0.914820996256648,-9.00592586438695));
#14690=CARTESIAN_POINT('Ctrl Pts',(4.28431782290389,0.912351447423313,-9.00619455915131));
#14691=CARTESIAN_POINT('Ctrl Pts',(4.28954287146836,0.90805696651733,-9.00665715955587));
#14692=CARTESIAN_POINT('Ctrl Pts',(4.29173829579751,0.906239148296796,-9.00685155493939));
#14693=CARTESIAN_POINT('Ctrl Pts',(4.29636804003268,0.902377289734746,-9.00726150888845));
#14694=CARTESIAN_POINT('Ctrl Pts',(4.29880072645957,0.900331329573268,-9.00747692178079));
#14695=CARTESIAN_POINT('Ctrl Pts',(4.30483711502588,0.895212684173822,-9.00801153566787));
#14696=CARTESIAN_POINT('Ctrl Pts',(4.30843067125841,0.892128023976856,-9.00832988516646));
#14697=CARTESIAN_POINT('Ctrl Pts',(4.32204676994453,0.880296757079998,-9.00953688811507));
#14698=CARTESIAN_POINT('Ctrl Pts',(4.33193992625116,0.871401861724606,-9.010415467372));
#14699=CARTESIAN_POINT('Ctrl Pts',(4.35709153127294,0.848005480232825,-9.01265986497983));
#14700=CARTESIAN_POINT('Ctrl Pts',(4.37211620715281,0.83325874566758,-9.01401120966142));
#14701=CARTESIAN_POINT('Ctrl Pts',(4.41876033807699,0.784955335773308,-9.0182727352167));
#14702=CARTESIAN_POINT('Ctrl Pts',(4.44880950201938,0.749940972771195,-9.02112162475523));
#14703=CARTESIAN_POINT('Ctrl Pts',(4.52517695256765,0.649594585799723,-9.02892155309964));
#14704=CARTESIAN_POINT('Ctrl Pts',(4.56700625576475,0.58117352557196,-9.03387127172343));
#14705=CARTESIAN_POINT('Ctrl Pts',(4.60825665614847,0.495109903431162,-9.04009098670924));
#14706=CARTESIAN_POINT('Ctrl Pts',(4.61466093118684,0.481044474614414,-9.04110659686171));
#14707=CARTESIAN_POINT('Ctrl Pts',(4.62358955710461,0.460365297518273,-9.04260053289578));
#14708=CARTESIAN_POINT('Ctrl Pts',(4.62633415826455,0.453847979323356,-9.04307147184577));
#14709=CARTESIAN_POINT('Ctrl Pts',(4.63110084378756,0.442237801066509,-9.04391079849984));
#14710=CARTESIAN_POINT('Ctrl Pts',(4.63314640866122,0.437154759645407,-9.04427839092883));
#14711=CARTESIAN_POINT('Ctrl Pts',(4.63734020559166,0.426519882548052,-9.04504783533151));
#14712=CARTESIAN_POINT('Ctrl Pts',(4.63948195741612,0.420965675490522,-9.04544988981759));
#14713=CARTESIAN_POINT('Ctrl Pts',(4.64496555133035,0.406417463038636,-9.04650364977647));
#14714=CARTESIAN_POINT('Ctrl Pts',(4.64823969711617,0.397398589305234,-9.04715755775172));
#14715=CARTESIAN_POINT('Ctrl Pts',(4.66275860734872,0.355828555554678,-9.05017527196661));
#14716=CARTESIAN_POINT('Ctrl Pts',(4.67268141784162,0.322836946117174,-9.05258131289991));
#14717=CARTESIAN_POINT('Ctrl Pts',(4.6976792322256,0.224246296643933,-9.05980799065887));
#14718=CARTESIAN_POINT('Ctrl Pts',(4.70859442915503,0.157741295767165,-9.06473732090874));
#14719=CARTESIAN_POINT('Ctrl Pts',(4.71834851226276,0.0314267403889369,
-9.07403414748872));
#14720=CARTESIAN_POINT('Ctrl Pts',(4.71843333017632,-0.028090571689763,
-9.078384477558));
#14721=CARTESIAN_POINT('Ctrl Pts',(4.71328123415862,-0.0973535970792769,
-9.08325489659547));
#14722=CARTESIAN_POINT('Ctrl Pts',(4.71241081294352,-0.107332738819506,
-9.08395179033353));
#14723=CARTESIAN_POINT('Ctrl Pts',(4.71102095152054,-0.121218253733473,
-9.08491368179602));
#14724=CARTESIAN_POINT('Ctrl Pts',(4.71060909679236,-0.125134622392454,
-9.08518411340566));
#14725=CARTESIAN_POINT('Ctrl Pts',(4.70986459912649,-0.131888282537682,
-9.08564888418753));
#14726=CARTESIAN_POINT('Ctrl Pts',(4.70954126553003,-0.134726534286877,
-9.08584372366878));
#14727=CARTESIAN_POINT('Ctrl Pts',(4.70883718672259,-0.140713240091258,
-9.08625363989225));
#14728=CARTESIAN_POINT('Ctrl Pts',(4.70845404537703,-0.143861384066815,
-9.08646857613572));
#14729=CARTESIAN_POINT('Ctrl Pts',(4.70747146660269,-0.151671720433927,
-9.08700036231522));
#14730=CARTESIAN_POINT('Ctrl Pts',(4.70685681754308,-0.15633200747528,-9.0873163802876));
#14731=CARTESIAN_POINT('Ctrl Pts',(4.70443121416943,-0.173910519729584,
-9.08850394839288));
#14732=CARTESIAN_POINT('Ctrl Pts',(4.70243351044067,-0.186802600467899,
-9.08936583651887));
#14733=CARTESIAN_POINT('Ctrl Pts',(4.69674966681931,-0.219845127477472,
-9.09155765517416));
#14734=CARTESIAN_POINT('Ctrl Pts',(4.69275122180787,-0.239937987831161,
-9.09287394953953));
#14735=CARTESIAN_POINT('Ctrl Pts',(4.67546913130656,-0.31631659852697,-9.09784888405803));
#14736=CARTESIAN_POINT('Ctrl Pts',(4.65857075737889,-0.371702645805051,
-9.10139950373775));
#14737=CARTESIAN_POINT('Ctrl Pts',(4.61039727293505,-0.49599443776295,-9.10965336955307));
#14738=CARTESIAN_POINT('Ctrl Pts',(4.57642730481095,-0.563568730204873,
-9.11436669797401));
#14739=CARTESIAN_POINT('Ctrl Pts',(4.53069656898575,-0.636215442441299,
-9.12000056385331));
#14740=CARTESIAN_POINT('Ctrl Pts',(4.52504691559712,-0.644932382720282,
-9.12068627442287));
#14741=CARTESIAN_POINT('Ctrl Pts',(4.51555142579745,-0.659166957573447,
-9.12182279251113));
#14742=CARTESIAN_POINT('Ctrl Pts',(4.51177223848081,-0.664728524211055,
-9.12227114115186));
#14743=CARTESIAN_POINT('Ctrl Pts',(4.50485704497861,-0.674719996704366,
-9.12308459268932));
#14744=CARTESIAN_POINT('Ctrl Pts',(4.50173762532359,-0.679161195974529,
-9.12344906614468));
#14745=CARTESIAN_POINT('Ctrl Pts',(4.49497660692086,-0.688646954383387,
-9.12423386228174));
#14746=CARTESIAN_POINT('Ctrl Pts',(4.49132552186291,-0.693684516485572,
-9.12465453796427));
#14747=CARTESIAN_POINT('Ctrl Pts',(4.48121009473172,-0.707410999539437,
-9.12581169614539));
#14748=CARTESIAN_POINT('Ctrl Pts',(4.47466568515546,-0.716039875404399,
-9.12655123547111));
#14749=CARTESIAN_POINT('Ctrl Pts',(4.4352036206312,-0.766607182388941,-9.13095888137041));
#14750=CARTESIAN_POINT('Ctrl Pts',(4.39959269150756,-0.806355556431621,
-9.13473282140429));
#14751=CARTESIAN_POINT('Ctrl Pts',(4.3270483382367,-0.877037768770133,-9.14205316633322));
#14752=CARTESIAN_POINT('Ctrl Pts',(4.29066669011835,-0.908391113799367,
-9.14557724009955));
#14753=CARTESIAN_POINT('Ctrl Pts',(4.23000442925745,-0.954527152966829,
-9.15116891279376));
#14754=CARTESIAN_POINT('Ctrl Pts',(4.2069245558265,-0.970804887645627,-9.15323666776888));
#14755=CARTESIAN_POINT('Ctrl Pts',(4.15427424381766,-1.00517214255317,-9.15779524132576));
#14756=CARTESIAN_POINT('Ctrl Pts',(4.12444273561059,-1.02281951573375,-9.16027364188836));
#14757=CARTESIAN_POINT('Ctrl Pts',(4.08865973468563,-1.04190906216893,-9.16309254270584));
#14758=CARTESIAN_POINT('Ctrl Pts',(4.08342477633549,-1.04465140108734,-9.16350119446097));
#14759=CARTESIAN_POINT('Ctrl Pts',(4.07816926754757,-1.04735428871593,-9.16390755708093));
#14760=CARTESIAN_POINT('Origin',(3.53951905042299,8.32667268468867E-16,
0.924367114736157));
#14761=CARTESIAN_POINT('',(4.07816928770683,-1.0473542783481,-9.76220700099567));
#14762=CARTESIAN_POINT('',(4.07816926754759,-1.04735428871592,-9.66287031899079));
#14763=CARTESIAN_POINT('',(4.07816926754759,-1.04735428871592,0.924367114736157));
#14764=CARTESIAN_POINT('Ctrl Pts',(4.07816928770683,-1.0473542783481,-9.76220700099567));
#14765=CARTESIAN_POINT('Ctrl Pts',(4.11407533352626,-1.02888793844727,-9.75965837420743));
#14766=CARTESIAN_POINT('Ctrl Pts',(4.14901218989046,-1.00858528532369,-9.75706832671646));
#14767=CARTESIAN_POINT('Ctrl Pts',(4.19188554154775,-0.980627144611524,
-9.75370406310379));
#14768=CARTESIAN_POINT('Ctrl Pts',(4.20084762038751,-0.974605635827041,
-9.75299007620032));
#14769=CARTESIAN_POINT('Ctrl Pts',(4.21483607662237,-0.964925180569075,
-9.75185789672956));
#14770=CARTESIAN_POINT('Ctrl Pts',(4.21991858333983,-0.961348096726768,
-9.75144276766345));
#14771=CARTESIAN_POINT('Ctrl Pts',(4.2293872027655,-0.954571353162807,-9.75066216056236));
#14772=CARTESIAN_POINT('Ctrl Pts',(4.23377998234182,-0.951381255132004,
-9.75029705243418));
#14773=CARTESIAN_POINT('Ctrl Pts',(4.24357308273726,-0.944165425550996,
-9.749476335414));
#14774=CARTESIAN_POINT('Ctrl Pts',(4.24896120298996,-0.940123534502952,
-9.74902011338139));
#14775=CARTESIAN_POINT('Ctrl Pts',(4.26259857468276,-0.929709478957409,
-9.74785327941638));
#14776=CARTESIAN_POINT('Ctrl Pts',(4.2707982984519,-0.923273720499176,-9.74714021421116));
#14777=CARTESIAN_POINT('Ctrl Pts',(4.3357735615412,-0.870867670851135,-9.7413954704903));
#14778=CARTESIAN_POINT('Ctrl Pts',(4.3882350750605,-0.819822731635173,-9.73615707407001));
#14779=CARTESIAN_POINT('Ctrl Pts',(4.46969380638,-0.724311054365501,-9.72698171705269));
#14780=CARTESIAN_POINT('Ctrl Pts',(4.50105406666881,-0.682130520119811,
-9.72310696375967));
#14781=CARTESIAN_POINT('Ctrl Pts',(4.5498944918105,-0.606345249765476,-9.71655719987377));
#14782=CARTESIAN_POINT('Ctrl Pts',(4.56876601542285,-0.57372850389306,-9.71385734250554));
#14783=CARTESIAN_POINT('Ctrl Pts',(4.58905130246254,-0.534434373753748,
-9.71078523715096));
#14784=CARTESIAN_POINT('Ctrl Pts',(4.59201022335995,-0.528583374445563,
-9.71033234969264));
#14785=CARTESIAN_POINT('Ctrl Pts',(4.5965074243875,-0.519503060084191,-9.70963685792346));
#14786=CARTESIAN_POINT('Ctrl Pts',(4.59808005785059,-0.516291048289142,
-9.70939224931919));
#14787=CARTESIAN_POINT('Ctrl Pts',(4.60096609390146,-0.510327864828727,
-9.70894080114829));
#14788=CARTESIAN_POINT('Ctrl Pts',(4.60228344333917,-0.507578763568637,
-9.70873373228062));
#14789=CARTESIAN_POINT('Ctrl Pts',(4.60527631027862,-0.501270386380638,
-9.70826094985865));
#14790=CARTESIAN_POINT('Ctrl Pts',(4.60694468210666,-0.497707804982908,
-9.70799567038162));
#14791=CARTESIAN_POINT('Ctrl Pts',(4.61129108955581,-0.488304255355011,
-9.70729979844479));
#14792=CARTESIAN_POINT('Ctrl Pts',(4.61393927316881,-0.482449519773926,
-9.70687093067232));
#14793=CARTESIAN_POINT('Ctrl Pts',(4.63723488707272,-0.429803148344929,
-9.7030511037493));
#14794=CARTESIAN_POINT('Ctrl Pts',(4.65486465001841,-0.381728150681832,
-9.69981968358328));
#14795=CARTESIAN_POINT('Ctrl Pts',(4.68360244627311,-0.284125579344376,
-9.693479090371));
#14796=CARTESIAN_POINT('Ctrl Pts',(4.69474944676736,-0.234727487176759,
-9.69037486898479));
#14797=CARTESIAN_POINT('Ctrl Pts',(4.71144646138595,-0.129613564760626,
-9.68375035829787));
#14798=CARTESIAN_POINT('Ctrl Pts',(4.71627264706459,-0.0739148273208844,
-9.6802275890705));
#14799=CARTESIAN_POINT('Ctrl Pts',(4.7173512094203,-0.00369563409559671,
-9.67564270659136));
#14800=CARTESIAN_POINT('Ctrl Pts',(4.71730840046682,0.0106990694075942,
-9.67469553898085));
#14801=CARTESIAN_POINT('Ctrl Pts',(4.71685373717589,0.0320375338763051,
-9.67327902833316));
#14802=CARTESIAN_POINT('Ctrl Pts',(4.7166441774608,0.0389846128011234,-9.67281590696469));
#14803=CARTESIAN_POINT('Ctrl Pts',(4.71616067243691,0.0513735405179801,
-9.67198634059529));
#14804=CARTESIAN_POINT('Ctrl Pts',(4.71591042672405,0.0568161542440685,
-9.67162063756692));
#14805=CARTESIAN_POINT('Ctrl Pts',(4.71530123054156,0.0683245864914515,
-9.67084459173008));
#14806=CARTESIAN_POINT('Ctrl Pts',(4.71493308333927,0.0743897374645629,
-9.67043397489875));
#14807=CARTESIAN_POINT('Ctrl Pts',(4.71382396669183,0.0905884179969579,
-9.66933282267605));
#14808=CARTESIAN_POINT('Ctrl Pts',(4.71299878187619,0.10071547297047,-9.66863970712123));
#14809=CARTESIAN_POINT('Ctrl Pts',(4.70860263419762,0.147224292371707,-9.66543407965036));
#14810=CARTESIAN_POINT('Ctrl Pts',(4.70347036786912,0.183434599833315,-9.66287402859214));
#14811=CARTESIAN_POINT('Ctrl Pts',(4.67842658984711,0.315552157758278,-9.65329194281599));
#14812=CARTESIAN_POINT('Ctrl Pts',(4.64826222422651,0.40910656083041,-9.64599264173347));
#14813=CARTESIAN_POINT('Ctrl Pts',(4.59785786745818,0.517174611986315,-9.63737170011505));
#14814=CARTESIAN_POINT('Ctrl Pts',(4.58831107208256,0.536270488108361,-9.63584257391797));
#14815=CARTESIAN_POINT('Ctrl Pts',(4.57191711711579,0.566947821012102,-9.63338771971974));
#14816=CARTESIAN_POINT('Ctrl Pts',(4.56538158671188,0.57868963608482,-9.63244854927329));
#14817=CARTESIAN_POINT('Ctrl Pts',(4.55626341190939,0.594431296096817,-9.63119256127574));
#14818=CARTESIAN_POINT('Ctrl Pts',(4.55385568480442,0.598530581083619,-9.63086578073964));
#14819=CARTESIAN_POINT('Ctrl Pts',(4.54979479815457,0.605349571757633,-9.63032282484557));
#14820=CARTESIAN_POINT('Ctrl Pts',(4.54815533992218,0.608077319695706,-9.63010580021551));
#14821=CARTESIAN_POINT('Ctrl Pts',(4.54502796199032,0.613233235062464,-9.62969595713501));
#14822=CARTESIAN_POINT('Ctrl Pts',(4.54354226345232,0.615662699831442,-9.62950299484803));
#14823=CARTESIAN_POINT('Ctrl Pts',(4.54000031108172,0.621407700344293,-9.62904700348911));
#14824=CARTESIAN_POINT('Ctrl Pts',(4.53793634995609,0.624718480632793,-9.62878446686456));
#14825=CARTESIAN_POINT('Ctrl Pts',(4.53062607625356,0.636316052254224,-9.62786544952819));
#14826=CARTESIAN_POINT('Ctrl Pts',(4.52529256674838,0.644547783244873,-9.62721430529991));
#14827=CARTESIAN_POINT('Ctrl Pts',(4.48092931213473,0.711178930215897,-9.6219448359307));
#14828=CARTESIAN_POINT('Ctrl Pts',(4.43684397683373,0.766054480594075,-9.61760718887869));
#14829=CARTESIAN_POINT('Ctrl Pts',(4.34687781464075,0.859537693119933,-9.60958163811238));
#14830=CARTESIAN_POINT('Ctrl Pts',(4.3024466027896,0.899207490532058,-9.60590752441663));
#14831=CARTESIAN_POINT('Ctrl Pts',(4.23825928288069,0.948321017632823,-9.60075714607797));
#14832=CARTESIAN_POINT('Ctrl Pts',(4.22095889550473,0.960827935050228,-9.59938362501157));
#14833=CARTESIAN_POINT('Ctrl Pts',(4.19029105872178,0.981753525611999,-9.59696539429325));
#14834=CARTESIAN_POINT('Ctrl Pts',(4.17707614783968,0.990386339291828,-9.59592850385312));
#14835=CARTESIAN_POINT('Ctrl Pts',(4.15757846189519,1.00257149539461,-9.59440383454691));
#14836=CARTESIAN_POINT('Ctrl Pts',(4.15142984815065,1.00633603296716,-9.59392376814036));
#14837=CARTESIAN_POINT('Ctrl Pts',(4.14054525839276,1.01286357367133,-9.5930750204444));
#14838=CARTESIAN_POINT('Ctrl Pts',(4.13582378176725,1.01565042567846,-9.59270721042155));
#14839=CARTESIAN_POINT('Ctrl Pts',(4.12594020454067,1.02139153417161,-9.5919379131431));
#14840=CARTESIAN_POINT('Ctrl Pts',(4.12077485078062,1.02433985004403,-9.59153622732433));
#14841=CARTESIAN_POINT('Ctrl Pts',(4.10724357982106,1.03192801886719,-9.59048478140566));
#14842=CARTESIAN_POINT('Ctrl Pts',(4.0988432123873,1.03650520977218,-9.5898328376858));
#14843=CARTESIAN_POINT('Ctrl Pts',(4.06320925506919,1.05536211310066,-9.58707002921739));
#14844=CARTESIAN_POINT('Ctrl Pts',(4.03547981472979,1.06867358930714,-9.58492623046284));
#14845=CARTESIAN_POINT('Ctrl Pts',(3.93086723853399,1.11394389213195,-9.57685557577604));
#14846=CARTESIAN_POINT('Ctrl Pts',(3.85118892367654,1.13880766580559,-9.57072038403955));
#14847=CARTESIAN_POINT('Ctrl Pts',(3.71835802817732,1.16526321220012,-9.56080585355076));
#14848=CARTESIAN_POINT('Ctrl Pts',(3.66651823782439,1.17204703099362,-9.55701730492824));
#14849=CARTESIAN_POINT('Ctrl Pts',(3.60744874437532,1.17580995483347,-9.55290054212497));
#14850=CARTESIAN_POINT('Ctrl Pts',(3.60049960803846,1.17619083088256,-9.55241939351805));
#14851=CARTESIAN_POINT('Ctrl Pts',(3.58988923336225,1.17667808546796,-9.55168997219977));
#14852=CARTESIAN_POINT('Ctrl Pts',(3.58623034328498,1.17682901399722,-9.55143938571454));
#14853=CARTESIAN_POINT('Ctrl Pts',(3.57953062010502,1.1770740807305,-9.55098234808661));
#14854=CARTESIAN_POINT('Ctrl Pts',(3.57649011436457,1.1771735038285,-9.55077562082111));
#14855=CARTESIAN_POINT('Ctrl Pts',(3.56962491982827,1.17737136705581,-9.55031038342588));
#14856=CARTESIAN_POINT('Ctrl Pts',(3.56580011425955,1.17746295315486,-9.55005225137544));
#14857=CARTESIAN_POINT('Ctrl Pts',(3.55591274832304,1.17765150692738,-9.54938756077394));
#14858=CARTESIAN_POINT('Ctrl Pts',(3.54984967373851,1.17772030089445,-9.54898248618808));
#14859=CARTESIAN_POINT('Ctrl Pts',(3.50913359648603,1.17786782115899,-9.54627756032263));
#14860=CARTESIAN_POINT('Ctrl Pts',(3.47448858993076,1.17646394957894,-9.54405029270586));
#14861=CARTESIAN_POINT('Ctrl Pts',(3.41185380817387,1.17114980760335,-9.54007835748678));
#14862=CARTESIAN_POINT('Ctrl Pts',(3.38384863764922,1.16775730751478,-9.53832244782797));
#14863=CARTESIAN_POINT('Ctrl Pts',(3.30862457386425,1.15589024004626,-9.53360070984589));
#14864=CARTESIAN_POINT('Ctrl Pts',(3.26175926165969,1.14553215308036,-9.53065183906796));
#14865=CARTESIAN_POINT('Ctrl Pts',(3.16436062180328,1.11767513338016,-9.52431686788137));
#14866=CARTESIAN_POINT('Ctrl Pts',(3.11412724720195,1.09953730220981,-9.52092534674652));
#14867=CARTESIAN_POINT('Ctrl Pts',(3.05538442554571,1.07369738419034,-9.51670751801753));
#14868=CARTESIAN_POINT('Ctrl Pts',(3.04552967872351,1.06919918429276,-9.51599121203832));
#14869=CARTESIAN_POINT('Ctrl Pts',(3.03011391402821,1.06190404091029,-9.51485618984739));
#14870=CARTESIAN_POINT('Ctrl Pts',(3.02451046229175,1.0591977797992,-9.51444056370144));
#14871=CARTESIAN_POINT('Ctrl Pts',(3.01405981154416,1.05404796600537,-9.51365952494999));
#14872=CARTESIAN_POINT('Ctrl Pts',(3.00920753041028,1.05161505144025,-9.51329448637314));
#14873=CARTESIAN_POINT('Ctrl Pts',(2.99838184827737,1.04609311882411,-9.51247458648246));
#14874=CARTESIAN_POINT('Ctrl Pts',(2.99241777754237,1.04298632721945,-9.51201911737847));
#14875=CARTESIAN_POINT('Ctrl Pts',(2.97730927385138,1.03495079079668,-9.51085549409399));
#14876=CARTESIAN_POINT('Ctrl Pts',(2.96820300397594,1.02995190923377,-9.51014490971284));
#14877=CARTESIAN_POINT('Ctrl Pts',(2.89349361720467,0.987644594310454,-9.50423676839299));
#14878=CARTESIAN_POINT('Ctrl Pts',(2.83156172473463,0.944236860007519,-9.49881752582396));
#14879=CARTESIAN_POINT('Ctrl Pts',(2.73027024794587,0.85764453125423,-9.48906923374195));
#14880=CARTESIAN_POINT('Ctrl Pts',(2.68914945890945,0.816890185641653,-9.4847990361949));
#14881=CARTESIAN_POINT('Ctrl Pts',(2.63773113880377,0.75782165468623,-9.47914388297175));
#14882=CARTESIAN_POINT('Ctrl Pts',(2.6246797791115,0.742013682611282,-9.47767729434716));
#14883=CARTESIAN_POINT('Ctrl Pts',(2.60400360579447,0.715595019343629,-9.47531133584986));
#14884=CARTESIAN_POINT('Ctrl Pts',(2.59613123928143,0.705184268122686,-9.47439963031944));
#14885=CARTESIAN_POINT('Ctrl Pts',(2.58566004828756,0.690847430897071,-9.47317415656299));
#14886=CARTESIAN_POINT('Ctrl Pts',(2.58290964239466,0.687033922808045,-9.47285102099374));
#14887=CARTESIAN_POINT('Ctrl Pts',(2.57834212820566,0.680620340039304,-9.47231243080403));
#14888=CARTESIAN_POINT('Ctrl Pts',(2.57651257639882,0.678029243354913,-9.47209615513099));
#14889=CARTESIAN_POINT('Ctrl Pts',(2.57305509534424,0.673090371080681,-9.4716864546784));
#14890=CARTESIAN_POINT('Ctrl Pts',(2.57142521051235,0.670744020978176,-9.47149289423685));
#14891=CARTESIAN_POINT('Ctrl Pts',(2.56756896131582,0.665149302706287,-9.47103386247538));
#14892=CARTESIAN_POINT('Ctrl Pts',(2.56535030202431,0.661895627235493,-9.47076889951872));
#14893=CARTESIAN_POINT('Ctrl Pts',(2.55754708991352,0.65032794718151,-9.4698336869106));
#14894=CARTESIAN_POINT('Ctrl Pts',(2.55205212347535,0.64195362340983,-9.46916901956574));
#14895=CARTESIAN_POINT('Ctrl Pts',(2.51285936305731,0.580529620308051,-9.46437514958382));
#14896=CARTESIAN_POINT('Ctrl Pts',(2.48334453251741,0.524921157958253,-9.46046852681187));
#14897=CARTESIAN_POINT('Ctrl Pts',(2.43273894704692,0.407822611628489,-9.45257057238299));
#14898=CARTESIAN_POINT('Ctrl Pts',(2.41201074334849,0.346418625917711,-9.44859100733336));
#14899=CARTESIAN_POINT('Ctrl Pts',(2.39104525662936,0.261921813321265,-9.44305269929184));
#14900=CARTESIAN_POINT('Ctrl Pts',(2.38627967850891,0.240070718409826,-9.44161589092358));
#14901=CARTESIAN_POINT('Ctrl Pts',(2.37911045572934,0.202025860736381,-9.43909659431812));
#14902=CARTESIAN_POINT('Ctrl Pts',(2.37641701152134,0.18589287148543,-9.43802288093174));
#14903=CARTESIAN_POINT('Ctrl Pts',(2.37300696279521,0.162474812259917,-9.43645409060667));
#14904=CARTESIAN_POINT('Ctrl Pts',(2.37202086466274,0.15523046550557,-9.43596738519616));
#14905=CARTESIAN_POINT('Ctrl Pts',(2.37041159936238,0.142523858004274,-9.43511103668022));
#14906=CARTESIAN_POINT('Ctrl Pts',(2.36975910366827,0.137065485985869,-9.43474231651561));
#14907=CARTESIAN_POINT('Ctrl Pts',(2.36848519262718,0.125736301951045,-9.4339751428557));
#14908=CARTESIAN_POINT('Ctrl Pts',(2.36786966003469,0.119864997177633,-9.43357651757802));
#14909=CARTESIAN_POINT('Ctrl Pts',(2.36639188091101,0.1046681166765,-9.43254193067574));
#14910=CARTESIAN_POINT('Ctrl Pts',(2.3655966951893,0.0953365910568731,-9.43190391317055));
#14911=CARTESIAN_POINT('Ctrl Pts',(2.36279975629333,0.0571339892772362,
-9.42928011703436));
#14912=CARTESIAN_POINT('Ctrl Pts',(2.36175133567514,0.0282054716253936,
-9.42726541018417));
#14913=CARTESIAN_POINT('Ctrl Pts',(2.36180118691856,-0.0521957103151589,
-9.42158484718462));
#14914=CARTESIAN_POINT('Ctrl Pts',(2.36520643867323,-0.103598346739239,
-9.41785828306704));
#14915=CARTESIAN_POINT('Ctrl Pts',(2.3828125307164,-0.236554346500744,-9.40804432698333));
#14916=CARTESIAN_POINT('Ctrl Pts',(2.40226129397133,-0.31713509315628,-9.40191130330289));
#14917=CARTESIAN_POINT('Ctrl Pts',(2.43308947359687,-0.403725223710294,
-9.39548061616314));
#14918=CARTESIAN_POINT('Ctrl Pts',(2.43629151458784,-0.412394813427911,
-9.39483884302727));
#14919=CARTESIAN_POINT('Ctrl Pts',(2.44104668514614,-0.424817615849938,
-9.39392312791095));
#14920=CARTESIAN_POINT('Ctrl Pts',(2.44251759767079,-0.428601630777045,
-9.39364472334985));
#14921=CARTESIAN_POINT('Ctrl Pts',(2.44513540893358,-0.435234347389366,
-9.39315774517539));
#14922=CARTESIAN_POINT('Ctrl Pts',(2.44627392441374,-0.438086278310212,
-9.3929486893714));
#14923=CARTESIAN_POINT('Ctrl Pts',(2.44871754797896,-0.444138592774605,
-9.39250577536879));
#14924=CARTESIAN_POINT('Ctrl Pts',(2.45002559763501,-0.447337707365659,
-9.39227209305574));
#14925=CARTESIAN_POINT('Ctrl Pts',(2.45364327063395,-0.456075502084081,
-9.39163489397865));
#14926=CARTESIAN_POINT('Ctrl Pts',(2.45598121074319,-0.461602455028222,
-9.39123301517199));
#14927=CARTESIAN_POINT('Ctrl Pts',(2.46894745232236,-0.491613605800345,
-9.38905595250223));
#14928=CARTESIAN_POINT('Ctrl Pts',(2.48036439077368,-0.515751049216119,
-9.38732360033491));
#14929=CARTESIAN_POINT('Ctrl Pts',(2.52201573903935,-0.596580285953777,
-9.38151747898576));
#14930=CARTESIAN_POINT('Ctrl Pts',(2.55606262982425,-0.651180232579175,
-9.3775821969801));
#14931=CARTESIAN_POINT('Ctrl Pts',(2.63810293832692,-0.761518235316816,
-9.36906438739634));
#14932=CARTESIAN_POINT('Ctrl Pts',(2.6871935351425,-0.816088320537324,-9.36448176950083));
#14933=CARTESIAN_POINT('Ctrl Pts',(2.74868686456395,-0.872804687904558,
-9.35899177817387));
#14934=CARTESIAN_POINT('Ctrl Pts',(2.75643711410827,-0.879764877200301,
-9.35830417518023));
#14935=CARTESIAN_POINT('Ctrl Pts',(2.76934752990161,-0.891053439386297,
-9.35716512789644));
#14936=CARTESIAN_POINT('Ctrl Pts',(2.77445441751921,-0.895442073605985,
-9.3567161611152));
#14937=CARTESIAN_POINT('Ctrl Pts',(2.78374609656861,-0.903289420095142,
-9.3559019919276));
#14938=CARTESIAN_POINT('Ctrl Pts',(2.78791773289922,-0.906763470837173,
-9.35553742330541));
#14939=CARTESIAN_POINT('Ctrl Pts',(2.79691761080636,-0.914153603462526,
-9.35475287079718));
#14940=CARTESIAN_POINT('Ctrl Pts',(2.8017531210579,-0.918060531639803,-9.35433253696674));
#14941=CARTESIAN_POINT('Ctrl Pts',(2.81507644145531,-0.928652084249496,
-9.35317749129558));
#14942=CARTESIAN_POINT('Ctrl Pts',(2.82362548307331,-0.935258346133828,
-9.35243974198683));
#14943=CARTESIAN_POINT('Ctrl Pts',(2.87443320916738,-0.973415160993876,
-9.34807373592682));
#14944=CARTESIAN_POINT('Ctrl Pts',(2.91867576523064,-1.00221177496292,-9.34434203850923));
#14945=CARTESIAN_POINT('Ctrl Pts',(3.03551550876267,-1.06754849481583,-9.3346709683711));
#14946=CARTESIAN_POINT('Ctrl Pts',(3.11023604222774,-1.09972469168996,-9.32864000464155));
#14947=CARTESIAN_POINT('Ctrl Pts',(3.21701658302399,-1.13315179121082,-9.32055525224378));
#14948=CARTESIAN_POINT('Ctrl Pts',(3.24671692507621,-1.14118714702618,-9.31836278747098));
#14949=CARTESIAN_POINT('Ctrl Pts',(3.28297499967284,-1.14948755786919,-9.31577908645669));
#14950=CARTESIAN_POINT('Ctrl Pts',(3.28926139259676,-1.15087254074165,-9.31533446839429));
#14951=CARTESIAN_POINT('Ctrl Pts',(3.29907110002684,-1.15294957976711,-9.31464617951545));
#14952=CARTESIAN_POINT('Ctrl Pts',(3.30258664184232,-1.15367715803208,-9.31440061567144));
#14953=CARTESIAN_POINT('Ctrl Pts',(3.30909251847901,-1.15499262458313,-9.3139482758526));
#14954=CARTESIAN_POINT('Ctrl Pts',(3.31208180398964,-1.15558498119413,-9.31374126321002));
#14955=CARTESIAN_POINT('Ctrl Pts',(3.31891784443122,-1.15691205657279,-9.31326971409797));
#14956=CARTESIAN_POINT('Ctrl Pts',(3.32276599172356,-1.15763919740886,-9.31300560240899));
#14957=CARTESIAN_POINT('Ctrl Pts',(3.33471074446141,-1.15983461287209,-9.31218972052416));
#14958=CARTESIAN_POINT('Ctrl Pts',(3.3428193717281,-1.16123727857612,-9.31164145004327));
#14959=CARTESIAN_POINT('Ctrl Pts',(3.36187580797443,-1.1643284019545,-9.31036460092272));
#14960=CARTESIAN_POINT('Ctrl Pts',(3.37283421590279,-1.16594765516191,-9.3096393402229));
#14961=CARTESIAN_POINT('Ctrl Pts',(3.41212785866392,-1.17118848494921,-9.30706563918827));
#14962=CARTESIAN_POINT('Ctrl Pts',(3.44057150054868,-1.1739338109378,-9.30525232571142));
#14963=CARTESIAN_POINT('Ctrl Pts',(3.55657605992569,-1.18088341275141,-9.2979594968495));
#14964=CARTESIAN_POINT('Ctrl Pts',(3.64437371420832,-1.17634288920514,-9.29265554749893));
#14965=CARTESIAN_POINT('Ctrl Pts',(3.76619889220178,-1.1562846776639,-9.28482404214195));
#14966=CARTESIAN_POINT('Ctrl Pts',(3.80125434139498,-1.14885693530191,-9.28251694545781));
#14967=CARTESIAN_POINT('Ctrl Pts',(3.84571300046889,-1.13729628041287,-9.27949324840693));
#14968=CARTESIAN_POINT('Ctrl Pts',(3.85547795469347,-1.13462219474938,-9.27882302194834));
#14969=CARTESIAN_POINT('Ctrl Pts',(3.87103927309664,-1.13014434332153,-9.27774460520045));
#14970=CARTESIAN_POINT('Ctrl Pts',(3.87685841569274,-1.12842104069961,-9.27733899901627));
#14971=CARTESIAN_POINT('Ctrl Pts',(3.88787815316852,-1.12506475754984,-9.27656633976162));
#14972=CARTESIAN_POINT('Ctrl Pts',(3.89308125336504,-1.12344049245383,-9.27619957670212));
#14973=CARTESIAN_POINT('Ctrl Pts',(3.90490743935773,-1.11965838896917,-9.27536142901954));
#14974=CARTESIAN_POINT('Ctrl Pts',(3.91152298094019,-1.11747780954752,-9.27488931724002));
#14975=CARTESIAN_POINT('Ctrl Pts',(3.93182250177834,-1.1105865576994,-9.27343039892889));
#14976=CARTESIAN_POINT('Ctrl Pts',(3.94543886662927,-1.10568240041257,-9.27243734030591));
#14977=CARTESIAN_POINT('Ctrl Pts',(3.99966304081146,-1.08501607301893,-9.26842265176871));
#14978=CARTESIAN_POINT('Ctrl Pts',(4.03945944623859,-1.06726260004585,-9.26533780364408));
#14979=CARTESIAN_POINT('Ctrl Pts',(4.07816930022569,-1.0473542719097,-9.26219992867132));
#14980=CARTESIAN_POINT('',(2.36176909431237,-0.000321529814770908,-9.3256328853208));
#14981=CARTESIAN_POINT('Ctrl Pts',(4.07816926754757,-1.04735428871593,-9.16390755708093));
#14982=CARTESIAN_POINT('Ctrl Pts',(4.07803365602181,-1.04742403319359,-9.16391804273648));
#14983=CARTESIAN_POINT('Ctrl Pts',(4.07789803081295,-1.04749375140339,-9.16392852686769));
#14984=CARTESIAN_POINT('Ctrl Pts',(4.07436011394742,-1.04931155080043,-9.16420194831119));
#14985=CARTESIAN_POINT('Ctrl Pts',(4.07094927920735,-1.05104310418198,-9.16446392229401));
#14986=CARTESIAN_POINT('Ctrl Pts',(4.06481132593214,-1.05412159560051,-9.1649323644239));
#14987=CARTESIAN_POINT('Ctrl Pts',(4.06208737942917,-1.05547461133838,-9.16513919621324));
#14988=CARTESIAN_POINT('Ctrl Pts',(4.05607314747128,-1.05843295930138,-9.16559353665096));
#14989=CARTESIAN_POINT('Ctrl Pts',(4.05278060306722,-1.06003351079141,-9.16584075381723));
#14990=CARTESIAN_POINT('Ctrl Pts',(4.04320957028047,-1.06463107354835,-9.16655515320663));
#14991=CARTESIAN_POINT('Ctrl Pts',(4.0369117919088,-1.06758790225852,-9.16701997442936));
#14992=CARTESIAN_POINT('Ctrl Pts',(3.98317531120304,-1.09223861877764,-9.17094473204776));
#14993=CARTESIAN_POINT('Ctrl Pts',(3.93436332591809,-1.11081750915699,-9.17423838386207));
#14994=CARTESIAN_POINT('Ctrl Pts',(3.80502510020497,-1.15043733756748,-9.18266467335368));
#14995=CARTESIAN_POINT('Ctrl Pts',(3.7232275499597,-1.16629770348424,-9.18772111356704));
#14996=CARTESIAN_POINT('Ctrl Pts',(3.60962901150093,-1.17606808574868,-9.19499248766605));
#14997=CARTESIAN_POINT('Ctrl Pts',(3.57872557685839,-1.17750334965447,-9.19699306615452));
#14998=CARTESIAN_POINT('Ctrl Pts',(3.53821988052455,-1.17778827607322,-9.19966251798157));
#14999=CARTESIAN_POINT('Ctrl Pts',(3.5286361255151,-1.17773870791541,-9.20029753959641));
#15000=CARTESIAN_POINT('Ctrl Pts',(3.51310469816021,-1.17746879049728,-9.20133268104424));
#15001=CARTESIAN_POINT('Ctrl Pts',(3.50715608936,-1.177320307798,-9.20173057751616));
#15002=CARTESIAN_POINT('Ctrl Pts',(3.49573189239385,-1.1769485023783,-9.20249759843314));
#15003=CARTESIAN_POINT('Ctrl Pts',(3.49025622436059,-1.17673202756017,-9.20286650141776));
#15004=CARTESIAN_POINT('Ctrl Pts',(3.47759192682601,-1.17614280931011,-9.20372273743164));
#15005=CARTESIAN_POINT('Ctrl Pts',(3.47040486869317,-1.175742362268,-9.20421091392577));
#15006=CARTESIAN_POINT('Ctrl Pts',(3.44752831094209,-1.1742572539103,-9.20577223109689));
#15007=CARTESIAN_POINT('Ctrl Pts',(3.4318572286,-1.17292424530377,-9.20685296344739));
#15008=CARTESIAN_POINT('Ctrl Pts',(3.3950892312141,-1.16905366391506,-9.20941616319836));
#15009=CARTESIAN_POINT('Ctrl Pts',(3.37402556140187,-1.16625822617734,-9.21090605459889));
#15010=CARTESIAN_POINT('Ctrl Pts',(3.29479064869994,-1.1535529919175,-9.21659237683874));
#15011=CARTESIAN_POINT('Ctrl Pts',(3.23732170245688,-1.13984729359774,-9.220890020222));
#15012=CARTESIAN_POINT('Ctrl Pts',(3.11353789073206,-1.10030435807032,-9.23042219550642));
#15013=CARTESIAN_POINT('Ctrl Pts',(3.0480317418016,-1.07264703085901,-9.2356529447894));
#15014=CARTESIAN_POINT('Ctrl Pts',(2.97678672734416,-1.03466075743234,-9.24131155898583));
#15015=CARTESIAN_POINT('Ctrl Pts',(2.96822120013041,-1.02995598552017,-9.24199116531814));
#15016=CARTESIAN_POINT('Ctrl Pts',(2.95632288533187,-1.02322650554734,-9.24293319159622));
#15017=CARTESIAN_POINT('Ctrl Pts',(2.95294036803041,-1.02129119210658,-9.24320076553422));
#15018=CARTESIAN_POINT('Ctrl Pts',(2.94710402790389,-1.01791335820003,-9.24366196804589));
#15019=CARTESIAN_POINT('Ctrl Pts',(2.94464573943877,-1.01647868055689,-9.24385607956485));
#15020=CARTESIAN_POINT('Ctrl Pts',(2.939504156155,-1.01345296891955,-9.24426171851963));
#15021=CARTESIAN_POINT('Ctrl Pts',(2.93682193387862,-1.01186015819009,-9.24447312584525));
#15022=CARTESIAN_POINT('Ctrl Pts',(2.93019821731662,-1.00789104887233,-9.2449947703348));
#15023=CARTESIAN_POINT('Ctrl Pts',(2.92626421424049,-1.0055022385388,-9.24530421591827));
#15024=CARTESIAN_POINT('Ctrl Pts',(2.91776737238589,-1.00027435786373,-9.2459719885778));
#15025=CARTESIAN_POINT('Ctrl Pts',(2.91320973467658,-0.997426981656927,
-9.24632980900532));
#15026=CARTESIAN_POINT('Ctrl Pts',(2.90024918673126,-0.989206036683672,
-9.24734676910381));
#15027=CARTESIAN_POINT('Ctrl Pts',(2.8918946227635,-0.98375665533815,-9.24800162297749));
#15028=CARTESIAN_POINT('Ctrl Pts',(2.86334969278014,-0.964616553637265,
-9.25024033264891));
#15029=CARTESIAN_POINT('Ctrl Pts',(2.84351498868768,-0.950404438314745,
-9.25179821053643));
#15030=CARTESIAN_POINT('Ctrl Pts',(2.78171705429099,-0.903151395934863,
-9.25670816601492));
#15031=CARTESIAN_POINT('Ctrl Pts',(2.7415523339534,-0.867868617023603,-9.25998794106046));
#15032=CARTESIAN_POINT('Ctrl Pts',(2.65191715125259,-0.7776265738463,-9.26786662277023));
#15033=CARTESIAN_POINT('Ctrl Pts',(2.60495759770233,-0.720508835282365,
-9.27248135593848));
#15034=CARTESIAN_POINT('Ctrl Pts',(2.557844514296,-0.650782446425274,-9.2780044110663));
#15035=CARTESIAN_POINT('Ctrl Pts',(2.55215034689112,-0.642110364029272,
-9.27868926237893));
#15036=CARTESIAN_POINT('Ctrl Pts',(2.54295774571561,-0.627698803335919,
-9.27982465034495));
#15037=CARTESIAN_POINT('Ctrl Pts',(2.53939248552123,-0.622002470079831,
-9.28027273671909));
#15038=CARTESIAN_POINT('Ctrl Pts',(2.53303647530488,-0.611651322778518,
-9.28108590888114));
#15039=CARTESIAN_POINT('Ctrl Pts',(2.53022876134786,-0.607007104874284,
-9.28145036723139));
#15040=CARTESIAN_POINT('Ctrl Pts',(2.5242698643067,-0.596994888325641,-9.28223534996601));
#15041=CARTESIAN_POINT('Ctrl Pts',(2.52112895080394,-0.591621001171614,
-9.28265622890078));
#15042=CARTESIAN_POINT('Ctrl Pts',(2.5126336141708,-0.576817943587628,-9.28381452192691));
#15043=CARTESIAN_POINT('Ctrl Pts',(2.507366693477,-0.567339525902516,-9.28455500285155));
#15044=CARTESIAN_POINT('Ctrl Pts',(2.47684224705872,-0.510575104527115,
-9.28898395138158));
#15045=CARTESIAN_POINT('Ctrl Pts',(2.4547099138238,-0.461688823638722,-9.29277948430495));
#15046=CARTESIAN_POINT('Ctrl Pts',(2.4032065358682,-0.3235609397052,-9.3034363420057));
#15047=CARTESIAN_POINT('Ctrl Pts',(2.38105115370269,-0.23205400477592,-9.31044613798432));
#15048=CARTESIAN_POINT('Ctrl Pts',(2.36776221812918,-0.120154030170058,
-9.31847448961641));
#15049=CARTESIAN_POINT('Ctrl Pts',(2.36598754836386,-0.1013655624945,-9.31980316502493));
#15050=CARTESIAN_POINT('Ctrl Pts',(2.36427393903611,-0.0769748602457808,
-9.32149647978916));
#15051=CARTESIAN_POINT('Ctrl Pts',(2.36392241400495,-0.0714055493996037,
-9.32188100003162));
#15052=CARTESIAN_POINT('Ctrl Pts',(2.36342249161714,-0.0624760496777101,
-9.32249388965029));
#15053=CARTESIAN_POINT('Ctrl Pts',(2.36324888538704,-0.0591174422917492,
-9.32272359107107));
#15054=CARTESIAN_POINT('Ctrl Pts',(2.36295154953094,-0.0528440087180422,
-9.32315105203661));
#15055=CARTESIAN_POINT('Ctrl Pts',(2.3628242618068,-0.0499294305659315,
-9.32334899953403));
#15056=CARTESIAN_POINT('Ctrl Pts',(2.36258555840798,-0.0439544744893212,
-9.32375351656451));
#15057=CARTESIAN_POINT('Ctrl Pts',(2.36247524638575,-0.0408940626439322,
-9.32396002639935));
#15058=CARTESIAN_POINT('Ctrl Pts',(2.36219734518225,-0.0322474474697368,
-9.32454162996615));
#15059=CARTESIAN_POINT('Ctrl Pts',(2.36205757558635,-0.0266603409708362,
-9.32491525783357));
#15060=CARTESIAN_POINT('Ctrl Pts',(2.36183421626548,-0.0141785942426367,
-9.32574550289169));
#15061=CARTESIAN_POINT('Ctrl Pts',(2.36177138964286,-0.00728375808849353,
-9.3262010936582));
#15062=CARTESIAN_POINT('Ctrl Pts',(2.36176911453502,-0.000388607634483833,
-9.32665402875837));
#15063=CARTESIAN_POINT('Ctrl Pts',(2.36176909431237,-0.000321529814770908,
-9.3256328853208));
#15064=CARTESIAN_POINT('Ctrl Pts',(2.36175642361669,0.0460906863625701,
-9.32878688485889));
#15065=CARTESIAN_POINT('Ctrl Pts',(2.36449151834104,0.0926118372533591,
-9.33194088439699));
#15066=CARTESIAN_POINT('Ctrl Pts',(2.36998689602592,0.138887012824616,-9.33509488393508));
#15067=CARTESIAN_POINT('Ctrl Pts',(2.3754744886328,0.185096632237267,-9.33824441533034));
#15068=CARTESIAN_POINT('Ctrl Pts',(2.38371456675781,0.231060407841111,-9.34139394672561));
#15069=CARTESIAN_POINT('Ctrl Pts',(2.39466767807415,0.276424307417029,-9.34454347812087));
#15070=CARTESIAN_POINT('Ctrl Pts',(2.40561027401928,0.321744656057508,-9.34768998585547));
#15071=CARTESIAN_POINT('Ctrl Pts',(2.41926061835923,0.366465719637589,-9.35083649359008));
#15072=CARTESIAN_POINT('Ctrl Pts',(2.43552796540056,0.410242302415289,-9.35398300132468));
#15073=CARTESIAN_POINT('Ctrl Pts',(2.45178712202367,0.453996844197589,-9.35712792482959));
#15074=CARTESIAN_POINT('Ctrl Pts',(2.47066047495875,0.496807316693356,-9.36027284833449));
#15075=CARTESIAN_POINT('Ctrl Pts',(2.49200790654631,0.538345117888293,-9.3634177718394));
#15076=CARTESIAN_POINT('Ctrl Pts',(2.5133705567216,0.579912531389026,-9.36656493736082));
#15077=CARTESIAN_POINT('Ctrl Pts',(2.53721055893679,0.620204951373926,-9.36971210288225));
#15078=CARTESIAN_POINT('Ctrl Pts',(2.56334109987532,0.658917044372467,-9.37285926840368));
#15079=CARTESIAN_POINT('Ctrl Pts',(2.58947920398484,0.69764034212103,-9.37600734483434));
#15080=CARTESIAN_POINT('Ctrl Pts',(2.61790882911757,0.734781945756841,-9.37915542126499));
#15081=CARTESIAN_POINT('Ctrl Pts',(2.64840110485756,0.770067444832761,-9.38230349769565));
#15082=CARTESIAN_POINT('Ctrl Pts',(2.67895463818698,0.805423830864873,-9.38545789846809));
#15083=CARTESIAN_POINT('Ctrl Pts',(2.71157870879086,0.83891625046055,-9.38861229924053));
#15084=CARTESIAN_POINT('Ctrl Pts',(2.74600665764102,0.870306351235832,-9.39176670001297));
#15085=CARTESIAN_POINT('Ctrl Pts',(2.779527135029,0.900869053876759,-9.39483795529528));
#15086=CARTESIAN_POINT('Ctrl Pts',(2.81475708886051,0.929438704869481,-9.3979092105776));
#15087=CARTESIAN_POINT('Ctrl Pts',(2.85142333164823,0.955834370748326,-9.40098046585991));
#15088=CARTESIAN_POINT('Ctrl Pts',(2.89072087851314,0.984124286432069,-9.40427212568689));
#15089=CARTESIAN_POINT('Ctrl Pts',(2.93185630826946,1.01005172441407,-9.40756378551388));
#15090=CARTESIAN_POINT('Ctrl Pts',(2.97451190062849,1.03337407708007,-9.41085544534086));
#15091=CARTESIAN_POINT('Ctrl Pts',(3.01561844267913,1.0558494716899,-9.41402756757879));
#15092=CARTESIAN_POINT('Ctrl Pts',(3.0581360867317,1.07590545684509,-9.41719968981672));
#15093=CARTESIAN_POINT('Ctrl Pts',(3.10174938394377,1.09336763332864,-9.42037181205466));
#15094=CARTESIAN_POINT('Ctrl Pts',(3.14531933553677,1.11081245481043,-9.42354078163936));
#15095=CARTESIAN_POINT('Ctrl Pts',(3.18998226970298,1.12566836352484,-9.42670975122407));
#15096=CARTESIAN_POINT('Ctrl Pts',(3.23540026985237,1.13780790549382,-9.42987872080878));
#15097=CARTESIAN_POINT('Ctrl Pts',(3.28079312827094,1.14994072745983,-9.43304593616873));
#15098=CARTESIAN_POINT('Ctrl Pts',(3.32693968692441,1.15936001758168,-9.43621315152868));
#15099=CARTESIAN_POINT('Ctrl Pts',(3.3734868825787,1.16598815677559,-9.43938036688863));
#15100=CARTESIAN_POINT('Ctrl Pts',(3.42002880465217,1.17261554503214,-9.44254722341781));
#15101=CARTESIAN_POINT('Ctrl Pts',(3.46697072159953,1.17645233371627,-9.44571407994698));
#15102=CARTESIAN_POINT('Ctrl Pts',(3.51395210476496,1.17747245988589,-9.44888093647616));
#15103=CARTESIAN_POINT('Ctrl Pts',(3.56098104504664,1.1784936186828,-9.45205099867009));
#15104=CARTESIAN_POINT('Ctrl Pts',(3.60804897288831,1.17669241563071,-9.45522106086403));
#15105=CARTESIAN_POINT('Ctrl Pts',(3.6547950087258,1.17209492616314,-9.45839112305796));
#15106=CARTESIAN_POINT('Ctrl Pts',(3.70156953762244,1.16749463439294,-9.46156311749637));
#15107=CARTESIAN_POINT('Ctrl Pts',(3.74802123333352,1.16009475239235,-9.46473511193478));
#15108=CARTESIAN_POINT('Ctrl Pts',(3.79379763126187,1.14997281090753,-9.46790710637319));
#15109=CARTESIAN_POINT('Ctrl Pts',(3.83965631247037,1.13983267518759,-9.47108480248579));
#15110=CARTESIAN_POINT('Ctrl Pts',(3.8848367398193,1.12696087545485,-9.4742624985984));
#15111=CARTESIAN_POINT('Ctrl Pts',(3.92900174489472,1.11148472468453,-9.47744019471101));
#15112=CARTESIAN_POINT('Ctrl Pts',(3.94076958281003,1.10736107897211,-9.47828689704317));
#15113=CARTESIAN_POINT('Ctrl Pts',(3.95246544776122,1.10305279483476,-9.47913359937533));
#15114=CARTESIAN_POINT('Ctrl Pts',(3.96408323881276,1.09856283954853,-9.47998030170749));
#15115=CARTESIAN_POINT('Ctrl Pts',(4.00924883554026,1.0811075841663,-9.48327196153448));
#15116=CARTESIAN_POINT('Ctrl Pts',(4.05344000235874,1.0608222044012,-9.48656362136146));
#15117=CARTESIAN_POINT('Ctrl Pts',(4.09627994886804,1.03784024033695,-9.48985528118844));
#15118=CARTESIAN_POINT('Ctrl Pts',(4.13756422331136,1.01569283379271,-9.49302740904442));
#15119=CARTESIAN_POINT('Ctrl Pts',(4.17759319139836,0.991041627729338,-9.49619953690041));
#15120=CARTESIAN_POINT('Ctrl Pts',(4.21604842842676,0.964055529104958,-9.4993716647564));
#15121=CARTESIAN_POINT('Ctrl Pts',(4.25446544669328,0.937096250631923,-9.50254063999109));
#15122=CARTESIAN_POINT('Ctrl Pts',(4.29131137513436,0.907806991346767,-9.50570961522578));
#15123=CARTESIAN_POINT('Ctrl Pts',(4.32629483075051,0.876401126191668,-9.50887859046048));
#15124=CARTESIAN_POINT('Ctrl Pts',(4.36125892107534,0.845012645932292,-9.51204581149086));
#15125=CARTESIAN_POINT('Ctrl Pts',(4.39436216662497,0.811510252606919,-9.51521303252124));
#15126=CARTESIAN_POINT('Ctrl Pts',(4.42534664645601,0.776147236422549,-9.51838025355162));
#15127=CARTESIAN_POINT('Ctrl Pts',(4.45632761598408,0.740788226595598,-9.52154711576025));
#15128=CARTESIAN_POINT('Ctrl Pts',(4.48518993070384,0.703569432955103,-9.52471397796888));
#15129=CARTESIAN_POINT('Ctrl Pts',(4.5117147702804,0.664778568239782,-9.52788084017751));
#15130=CARTESIAN_POINT('Ctrl Pts',(4.53826645945181,0.625948437726135,-9.53105090802163));
#15131=CARTESIAN_POINT('Ctrl Pts',(4.56247563863267,0.585543522958146,-9.53422097586575));
#15132=CARTESIAN_POINT('Ctrl Pts',(4.58416696305745,0.543880318754466,-9.53739104370988));
#15133=CARTESIAN_POINT('Ctrl Pts',(4.6058715088721,0.502191719814401,-9.54056304378746));
#15134=CARTESIAN_POINT('Ctrl Pts',(4.62505491865147,0.459243814517834,-9.54373504386505));
#15135=CARTESIAN_POINT('Ctrl Pts',(4.64158954073585,0.41537416491831,-9.54690704394264));
#15136=CARTESIAN_POINT('Ctrl Pts',(4.65815388344539,0.371425660573533,-9.55008474562168));
#15137=CARTESIAN_POINT('Ctrl Pts',(4.67205977932429,0.326552639882582,-9.55326244730071));
#15138=CARTESIAN_POINT('Ctrl Pts',(4.68322962843374,0.281107054778652,-9.55644014897975));
#15139=CARTESIAN_POINT('Ctrl Pts',(4.68620570905126,0.268998589959227,-9.55728681183819));
#15140=CARTESIAN_POINT('Ctrl Pts',(4.68898784233463,0.256849522602019,-9.55813347469662));
#15141=CARTESIAN_POINT('Ctrl Pts',(4.69157518003766,0.244666582755543,-9.55898013755506));
#15142=CARTESIAN_POINT('Ctrl Pts',(4.70163424367916,0.197301692152735,-9.56227179738204));
#15143=CARTESIAN_POINT('Ctrl Pts',(4.70879057834815,0.149206535139714,-9.56556345720902));
#15144=CARTESIAN_POINT('Ctrl Pts',(4.71295014754609,0.100769652199884,-9.568855117036));
#15145=CARTESIAN_POINT('Ctrl Pts',(4.71695864328854,0.0540919724203997,
-9.57202722543814));
#15146=CARTESIAN_POINT('Ctrl Pts',(4.71818427734087,0.0070975774068678,
-9.57519933384028));
#15147=CARTESIAN_POINT('Ctrl Pts',(4.71659452666535,-0.0398545571900941,
-9.57837144224242));
#15148=CARTESIAN_POINT('Ctrl Pts',(4.71500635595994,-0.0867600285145284,
-9.58154039805181));
#15149=CARTESIAN_POINT('Ctrl Pts',(4.71060835732731,-0.13362276774729,-9.58470935386121));
#15150=CARTESIAN_POINT('Ctrl Pts',(4.7034200263374,-0.180082150046841,-9.5878783096706));
#15151=CARTESIAN_POINT('Ctrl Pts',(4.69623567436311,-0.22651581530468,-9.59104551134198));
#15152=CARTESIAN_POINT('Ctrl Pts',(4.68626413475648,-0.272546015795528,
-9.59421271301336));
#15153=CARTESIAN_POINT('Ctrl Pts',(4.67357661674705,-0.317818342395695,
-9.59737991468474));
#15154=CARTESIAN_POINT('Ctrl Pts',(4.66089053572761,-0.363085541446122,
-9.60054675763843));
#15155=CARTESIAN_POINT('Ctrl Pts',(4.64548923945076,-0.407594500986334,
-9.60371360059213));
#15156=CARTESIAN_POINT('Ctrl Pts',(4.62749413136536,-0.451004751359048,
-9.60688044354582));
#15157=CARTESIAN_POINT('Ctrl Pts',(4.60948080606262,-0.494458947784328,
-9.61005049243005));
#15158=CARTESIAN_POINT('Ctrl Pts',(4.58886864511359,-0.536811700499529,
-9.61322054131427));
#15159=CARTESIAN_POINT('Ctrl Pts',(4.56582691260045,-0.577743225432142,
-9.61639059019849));
#15160=CARTESIAN_POINT('Ctrl Pts',(4.5427711344045,-0.618699701232303,-9.61956257146784));
#15161=CARTESIAN_POINT('Ctrl Pts',(4.51728313985576,-0.658232756603897,
-9.62273455273718));
#15162=CARTESIAN_POINT('Ctrl Pts',(4.48957589663132,-0.696051040853093,
-9.62590653400653));
#15163=CARTESIAN_POINT('Ctrl Pts',(4.4618188463756,-0.733937307920058,-9.6290842172856));
#15164=CARTESIAN_POINT('Ctrl Pts',(4.43183494754508,-0.770102228310919,
-9.63226190056467));
#15165=CARTESIAN_POINT('Ctrl Pts',(4.3998765676401,-0.804288508601244,-9.63543958384374));
#15166=CARTESIAN_POINT('Ctrl Pts',(4.3913602233415,-0.813398549038413,-9.63628638036337));
#15167=CARTESIAN_POINT('Ctrl Pts',(4.38270385701534,-0.822368294345101,
-9.637133176883));
#15168=CARTESIAN_POINT('Ctrl Pts',(4.37391264430216,-0.831193354757727,
-9.63797997340262));
#15169=CARTESIAN_POINT('Ctrl Pts',(4.34092324961172,-0.864309764360973,
-9.64115761288422));
#15170=CARTESIAN_POINT('Ctrl Pts',(4.30588605809058,-0.895532622737997,
-9.6443352523658));
#15171=CARTESIAN_POINT('Ctrl Pts',(4.269046890181,-0.924599477351144,-9.6475128918474));
#15172=CARTESIAN_POINT('Ctrl Pts',(4.23226979794983,-0.953617352988332,
-9.65068517686151));
#15173=CARTESIAN_POINT('Ctrl Pts',(4.19369717942832,-0.980486080284995,
-9.65385746187562));
#15174=CARTESIAN_POINT('Ctrl Pts',(4.15361073600015,-1.00498082777981,-9.65702974688973));
#15175=CARTESIAN_POINT('Ctrl Pts',(4.1290093564398,-1.02001345549184,-9.65897660425675));
#15176=CARTESIAN_POINT('Ctrl Pts',(4.10383852032893,-1.0341526923382,-9.66092346162377));
#15177=CARTESIAN_POINT('Ctrl Pts',(4.07816926754759,-1.04735428871592,-9.66287031899079));
#15178=CARTESIAN_POINT('Origin',(3.53951905042299,8.32667268468867E-16,
0.924367114736157));
#15179=CARTESIAN_POINT('',(4.07816926754758,-1.04735428871592,-10.2615635160918));
#15180=CARTESIAN_POINT('',(4.07816926754651,-1.04735428871647,-10.1620324047392));
#15181=CARTESIAN_POINT('',(4.07816926754759,-1.04735428871592,0.924367114736157));
#15182=CARTESIAN_POINT('',(2.36176949287335,0.00102087787044271,-9.92436711477312));
#15183=CARTESIAN_POINT('Ctrl Pts',(2.36176949287335,0.00102087787044271,
-9.92436711477312));
#15184=CARTESIAN_POINT('Ctrl Pts',(2.36181953356955,0.0587510035938087,
-9.92826181891225));
#15185=CARTESIAN_POINT('Ctrl Pts',(2.36611819363635,0.11629608653358,-9.93215652305138));
#15186=CARTESIAN_POINT('Ctrl Pts',(2.3745609312197,0.173111648950421,-9.9360512271905));
#15187=CARTESIAN_POINT('Ctrl Pts',(2.38247315541436,0.226357111473627,-9.93970120114935));
#15188=CARTESIAN_POINT('Ctrl Pts',(2.39402444443252,0.278962151827222,-9.9433511751082));
#15189=CARTESIAN_POINT('Ctrl Pts',(2.4090909796731,0.330495747870812,-9.94700114906705));
#15190=CARTESIAN_POINT('Ctrl Pts',(2.42267844888313,0.376970344607428,-9.95029280889403));
#15191=CARTESIAN_POINT('Ctrl Pts',(2.43916788388295,0.422712270937087,-9.95358446872101));
#15192=CARTESIAN_POINT('Ctrl Pts',(2.45845795274245,0.46733496079551,-9.95687612854799));
#15193=CARTESIAN_POINT('Ctrl Pts',(2.47705158102658,0.510346611728898,-9.96004894766578));
#15194=CARTESIAN_POINT('Ctrl Pts',(2.49824681331542,0.552317904399127,-9.96322176678355));
#15195=CARTESIAN_POINT('Ctrl Pts',(2.52190210798983,0.592917212579454,-9.96639458590133));
#15196=CARTESIAN_POINT('Ctrl Pts',(2.5455338523531,0.633476101633617,-9.96956424628115));
#15197=CARTESIAN_POINT('Ctrl Pts',(2.57162053225186,0.672665230260555,-9.97273390666096));
#15198=CARTESIAN_POINT('Ctrl Pts',(2.59997401872786,0.710176172450892,-9.97590356704077));
#15199=CARTESIAN_POINT('Ctrl Pts',(2.62831174726544,0.747666267289082,-9.97907146582724));
#15200=CARTESIAN_POINT('Ctrl Pts',(2.65891345126779,0.783479579408872,-9.98223936461371));
#15201=CARTESIAN_POINT('Ctrl Pts',(2.69154840817892,0.817337661185501,-9.98540726340017));
#15202=CARTESIAN_POINT('Ctrl Pts',(2.72417957927749,0.851191815261177,-9.98857479469509));
#15203=CARTESIAN_POINT('Ctrl Pts',(2.75884314694137,0.883090789708585,-9.99174232599001));
#15204=CARTESIAN_POINT('Ctrl Pts',(2.79527079042507,0.912792194308251,-9.99490985728492));
#15205=CARTESIAN_POINT('Ctrl Pts',(2.83173509727546,0.942523492510248,-9.99808057660822));
#15206=CARTESIAN_POINT('Ctrl Pts',(2.86996658891186,0.970052456226129,-10.0012512959315));
#15207=CARTESIAN_POINT('Ctrl Pts',(2.90966459695419,0.995177587139862,-10.0044220152548));
#15208=CARTESIAN_POINT('Ctrl Pts',(2.94938667711143,1.02031795345377,-10.0075946572418));
#15209=CARTESIAN_POINT('Ctrl Pts',(2.99057655522839,1.04305131694122,-10.0107672992288));
#15210=CARTESIAN_POINT('Ctrl Pts',(3.03290854097937,1.06322192143563,-10.0139399412159));
#15211=CARTESIAN_POINT('Ctrl Pts',(3.07531633179523,1.08342864599281,-10.0171182645412));
#15212=CARTESIAN_POINT('Ctrl Pts',(3.11886979281923,1.10106325107664,-10.0202965878665));
#15213=CARTESIAN_POINT('Ctrl Pts',(3.1632246654204,1.11601863708252,-10.0234749111918));
#15214=CARTESIAN_POINT('Ctrl Pts',(3.1749754814627,1.11998072691596,-10.0243169357661));
#15215=CARTESIAN_POINT('Ctrl Pts',(3.18678247904297,1.12375504775244,-10.0251589603403));
#15216=CARTESIAN_POINT('Ctrl Pts',(3.19863913383181,1.12734020817355,-10.0260009849146));
#15217=CARTESIAN_POINT('Ctrl Pts',(3.24498941319832,1.14135539121225,-10.0292926447416));
#15218=CARTESIAN_POINT('Ctrl Pts',(3.29231139987383,1.15253933461149,-10.0325843045686));
#15219=CARTESIAN_POINT('Ctrl Pts',(3.3402259338014,1.16076583175387,-10.0358759643956));
#15220=CARTESIAN_POINT('Ctrl Pts',(3.38641503190162,1.16869608698927,-10.0390490892535));
#15221=CARTESIAN_POINT('Ctrl Pts',(3.43315411987754,1.17387817845893,-10.0422222141114));
#15222=CARTESIAN_POINT('Ctrl Pts',(3.48008801368417,1.17624955446204,-10.0453953389693));
#15223=CARTESIAN_POINT('Ctrl Pts',(3.52697541066531,1.1786185811724,-10.0485653202519));
#15224=CARTESIAN_POINT('Ctrl Pts',(3.57405667746869,1.17818237585373,-10.0517353015344));
#15225=CARTESIAN_POINT('Ctrl Pts',(3.62097062587361,1.17493008445465,-10.0549052828169));
#15226=CARTESIAN_POINT('Ctrl Pts',(3.66785871588435,1.17167958567879,-10.0580735168446));
#15227=CARTESIAN_POINT('Ctrl Pts',(3.7145791152668,1.16561611412995,-10.0612417508722));
#15228=CARTESIAN_POINT('Ctrl Pts',(3.7607724888495,1.15678086882713,-10.0644099848999));
#15229=CARTESIAN_POINT('Ctrl Pts',(3.80696070168783,1.14794661060187,-10.067577864971));
#15230=CARTESIAN_POINT('Ctrl Pts',(3.85262145907468,1.13634130014388,-10.0707457450422));
#15231=CARTESIAN_POINT('Ctrl Pts',(3.89740509739597,1.12205732468625,-10.0739136251133));
#15232=CARTESIAN_POINT('Ctrl Pts',(3.94223404549111,1.10775889743948,-10.077084710282));
#15233=CARTESIAN_POINT('Ctrl Pts',(3.9861835727123,1.09077656889708,-10.0802557954507));
#15234=CARTESIAN_POINT('Ctrl Pts',(4.02892060096838,1.07125215744183,-10.0834268806194));
#15235=CARTESIAN_POINT('Ctrl Pts',(4.07168368041955,1.05171584449803,-10.0865998987853));
#15236=CARTESIAN_POINT('Ctrl Pts',(4.11323229801876,1.02963462662897,-10.0897729169513));
#15237=CARTESIAN_POINT('Ctrl Pts',(4.15325802535948,1.00519626598188,-10.0929459351172));
#15238=CARTESIAN_POINT('Ctrl Pts',(4.19335555928565,0.98071406265287,-10.0961246457119));
#15239=CARTESIAN_POINT('Ctrl Pts',(4.23192429809895,0.953866601677069,-10.0993033563066));
#15240=CARTESIAN_POINT('Ctrl Pts',(4.26868642707439,0.924883776118556,-10.1024820669012));
#15241=CARTESIAN_POINT('Ctrl Pts',(4.27839631326216,0.917228617252182,-10.1033216515216));
#15242=CARTESIAN_POINT('Ctrl Pts',(4.28798035801678,0.909424693745959,-10.1041612361419));
#15243=CARTESIAN_POINT('Ctrl Pts',(4.29743387338196,0.901476668383086,-10.1050008207622));
#15244=CARTESIAN_POINT('Ctrl Pts',(4.33449714967136,0.870315788160264,-10.1082924805892));
#15245=CARTESIAN_POINT('Ctrl Pts',(4.36972230568576,0.8367923660712,-10.1115841404162));
#15246=CARTESIAN_POINT('Ctrl Pts',(4.40279526343513,0.801154942908937,-10.1148758002431));
#15247=CARTESIAN_POINT('Ctrl Pts',(4.43462101281622,0.766861436209441,-10.1180433288777));
#15248=CARTESIAN_POINT('Ctrl Pts',(4.46445357566618,0.73061098662132,-10.1212108575123));
#15249=CARTESIAN_POINT('Ctrl Pts',(4.4920468384816,0.692665774725574,-10.1243783861469));
#15250=CARTESIAN_POINT('Ctrl Pts',(4.51961266769324,0.654758288484654,-10.1275427655807));
#15251=CARTESIAN_POINT('Ctrl Pts',(4.54494327521734,0.615159824770047,-10.1307071450144));
#15252=CARTESIAN_POINT('Ctrl Pts',(4.56783251589978,0.574165898690546,-10.1338715244482));
#15253=CARTESIAN_POINT('Ctrl Pts',(4.59070915590108,0.533194540043413,-10.1370341618698));
#15254=CARTESIAN_POINT('Ctrl Pts',(4.61114681879182,0.490829728170074,-10.1401967992914));
#15255=CARTESIAN_POINT('Ctrl Pts',(4.62898394364436,0.447393908025294,-10.143359436713));
#15256=CARTESIAN_POINT('Ctrl Pts',(4.64681916300776,0.403962728005233,-10.146521736279));
#15257=CARTESIAN_POINT('Ctrl Pts',(4.66205418551195,0.359461284843025,-10.1496840358451));
#15258=CARTESIAN_POINT('Ctrl Pts',(4.6745755997863,0.314231908385285,-10.1528463354111));
#15259=CARTESIAN_POINT('Ctrl Pts',(4.68710996144185,0.26895576388955,-10.1560119048552));
#15260=CARTESIAN_POINT('Ctrl Pts',(4.69692496872652,0.222950724747961,-10.1591774742994));
#15261=CARTESIAN_POINT('Ctrl Pts',(4.70395767352118,0.176572238863296,-10.1623430437435));
#15262=CARTESIAN_POINT('Ctrl Pts',(4.71099474300782,0.130164969201755,-10.165510577828));
#15263=CARTESIAN_POINT('Ctrl Pts',(4.71524602425287,0.0833843488712431,
-10.1686781119124));
#15264=CARTESIAN_POINT('Ctrl Pts',(4.71670052190024,0.0365902406477502,
-10.1718456459969));
#15265=CARTESIAN_POINT('Ctrl Pts',(4.71815767980926,-0.0102894535315625,
-10.1750189734695));
#15266=CARTESIAN_POINT('Ctrl Pts',(4.71680787049338,-0.0571821265167829,
-10.1781923009422));
#15267=CARTESIAN_POINT('Ctrl Pts',(4.71269210976297,-0.103730590178981,
-10.1813656284148));
#15268=CARTESIAN_POINT('Ctrl Pts',(4.71155291169594,-0.116614701598565,
-10.1822439711464));
#15269=CARTESIAN_POINT('Ctrl Pts',(4.71020211070252,-0.1294724971845,-10.1831223138781));
#15270=CARTESIAN_POINT('Ctrl Pts',(4.70864126534676,-0.142296553267261,
-10.1840006566098));
#15271=CARTESIAN_POINT('Ctrl Pts',(4.70289827039364,-0.189481554068203,
-10.1872324424215));
#15272=CARTESIAN_POINT('Ctrl Pts',(4.69428146431621,-0.236422911045137,
-10.1904642282333));
#15273=CARTESIAN_POINT('Ctrl Pts',(4.68282581482345,-0.282744946862258,
-10.193696014045));
#15274=CARTESIAN_POINT('Ctrl Pts',(4.67156026021599,-0.328298315473704,
-10.1968741716488));
#15275=CARTESIAN_POINT('Ctrl Pts',(4.65754948265448,-0.373252197257797,
-10.2000523292526));
#15276=CARTESIAN_POINT('Ctrl Pts',(4.64087870123871,-0.417255296018016,
-10.2032304868564));
#15277=CARTESIAN_POINT('Ctrl Pts',(4.62422490200448,-0.461213569728162,
-10.2064054069366));
#15278=CARTESIAN_POINT('Ctrl Pts',(4.60491665903401,-0.504222460847839,
-10.2095803270167));
#15279=CARTESIAN_POINT('Ctrl Pts',(4.5830889618682,-0.545945878660368,-10.2127552470968));
#15280=CARTESIAN_POINT('Ctrl Pts',(4.56127398657655,-0.587644978741763,
-10.2159283167329));
#15281=CARTESIAN_POINT('Ctrl Pts',(4.53694272347648,-0.628059598796641,
-10.2191013863689));
#15282=CARTESIAN_POINT('Ctrl Pts',(4.51027712176019,-0.666876172489078,
-10.2222744560049));
#15283=CARTESIAN_POINT('Ctrl Pts',(4.48276258672367,-0.706928521137399,
-10.2255485443455));
#15284=CARTESIAN_POINT('Ctrl Pts',(4.45276281347156,-0.745278770559472,
-10.228822632686));
#15285=CARTESIAN_POINT('Ctrl Pts',(4.42052580014014,-0.78161510313761,-10.2320967210266));
#15286=CARTESIAN_POINT('Ctrl Pts',(4.3892593963524,-0.816857401636967,-10.2352722313334));
#15287=CARTESIAN_POINT('Ctrl Pts',(4.3558890494958,-0.850204999571246,-10.2384477416401));
#15288=CARTESIAN_POINT('Ctrl Pts',(4.32067953260879,-0.88140987263092,-10.2416232519469));
#15289=CARTESIAN_POINT('Ctrl Pts',(4.28383049107333,-0.914067794839122,
-10.2449466293044));
#15290=CARTESIAN_POINT('Ctrl Pts',(4.24496726564072,-0.944378053767438,
-10.2482700066618));
#15291=CARTESIAN_POINT('Ctrl Pts',(4.20443028105735,-0.972104993236993,
-10.2515933840193));
#15292=CARTESIAN_POINT('Ctrl Pts',(4.16389329647398,-0.999831932706549,
-10.2549167613768));
#15293=CARTESIAN_POINT('Ctrl Pts',(4.12168317836847,-1.02497525445393,-10.2582401387343));
#15294=CARTESIAN_POINT('Ctrl Pts',(4.07816926754758,-1.04735428871592,-10.2615635160918));
#15295=CARTESIAN_POINT('Ctrl Pts',(2.36176947427292,0.000999188840285452,
-9.92471602642876));
#15296=CARTESIAN_POINT('Ctrl Pts',(2.36171985495268,-0.0574873864968981,
-9.92108038399836));
#15297=CARTESIAN_POINT('Ctrl Pts',(2.36602676942147,-0.115891305276079,
-9.91739771552307));
#15298=CARTESIAN_POINT('Ctrl Pts',(2.37613384376762,-0.183659141572686,
-9.91292448630051));
#15299=CARTESIAN_POINT('Ctrl Pts',(2.37774134962737,-0.193567516473714,
-9.91226553567381));
#15300=CARTESIAN_POINT('Ctrl Pts',(2.38060667704903,-0.209904904468701,
-9.91117023956932));
#15301=CARTESIAN_POINT('Ctrl Pts',(2.3817918569559,-0.216346251945307,-9.91073612887373));
#15302=CARTESIAN_POINT('Ctrl Pts',(2.38401615399669,-0.227893092503701,
-9.90995369002595));
#15303=CARTESIAN_POINT('Ctrl Pts',(2.38503554800162,-0.233002245542662,
-9.90960598394544));
#15304=CARTESIAN_POINT('Ctrl Pts',(2.38718478374653,-0.243413617835199,
-9.90889428461842));
#15305=CARTESIAN_POINT('Ctrl Pts',(2.38831740243396,-0.248715129197281,
-9.90853021179256));
#15306=CARTESIAN_POINT('Ctrl Pts',(2.39083032104041,-0.260092454666618,
-9.90774520196162));
#15307=CARTESIAN_POINT('Ctrl Pts',(2.39222230963744,-0.266165489856491,
-9.90732390459827));
#15308=CARTESIAN_POINT('Ctrl Pts',(2.39611373268057,-0.282545244363976,
-9.90618131584407));
#15309=CARTESIAN_POINT('Ctrl Pts',(2.39870425299437,-0.292829508341833,
-9.90545715702933));
#15310=CARTESIAN_POINT('Ctrl Pts',(2.412913361162,-0.346186177086252,-9.90166368125109));
#15311=CARTESIAN_POINT('Ctrl Pts',(2.42683209708736,-0.388602766155844,
-9.89852178737399));
#15312=CARTESIAN_POINT('Ctrl Pts',(2.45979983240075,-0.472638530044206,
-9.89203959553921));
#15313=CARTESIAN_POINT('Ctrl Pts',(2.47893640772502,-0.51414463458435,-9.88870171058853));
#15314=CARTESIAN_POINT('Ctrl Pts',(2.51827352045945,-0.587868078467815,
-9.88257008750968));
#15315=CARTESIAN_POINT('Ctrl Pts',(2.53771801808256,-0.620424161851659,
-9.87978432708926));
#15316=CARTESIAN_POINT('Ctrl Pts',(2.57882726402113,-0.682267112639189,
-9.87439360672218));
#15317=CARTESIAN_POINT('Ctrl Pts',(2.60034945991651,-0.711602532803979,
-9.87178881143956));
#15318=CARTESIAN_POINT('Ctrl Pts',(2.62737382128112,-0.745070701398977,
-9.86879952549719));
#15319=CARTESIAN_POINT('Ctrl Pts',(2.63159465256203,-0.750208345752129,
-9.86834014864454));
#15320=CARTESIAN_POINT('Ctrl Pts',(2.63816368885226,-0.758067602860315,
-9.86763700759519));
#15321=CARTESIAN_POINT('Ctrl Pts',(2.64048113861525,-0.760814571587972,
-9.86739116662242));
#15322=CARTESIAN_POINT('Ctrl Pts',(2.6447856478766,-0.765869751563662,-9.86693867331643));
#15323=CARTESIAN_POINT('Ctrl Pts',(2.64676908223398,-0.768180859327639,
-9.86673178148662));
#15324=CARTESIAN_POINT('Ctrl Pts',(2.65131666329256,-0.773438321231054,
-9.86626104769743));
#15325=CARTESIAN_POINT('Ctrl Pts',(2.65388651937638,-0.776379635423801,
-9.86599762577208));
#15326=CARTESIAN_POINT('Ctrl Pts',(2.66065884799994,-0.78405348233827,-9.86531001466876));
#15327=CARTESIAN_POINT('Ctrl Pts',(2.66488498542338,-0.788765095088173,
-9.86488748374285));
#15328=CARTESIAN_POINT('Ctrl Pts',(2.699002108824,-0.826190013230937,-9.86152625311498));
#15329=CARTESIAN_POINT('Ctrl Pts',(2.73068340761933,-0.857230733093855,
-9.85870690131269));
#15330=CARTESIAN_POINT('Ctrl Pts',(2.80454029338702,-0.921844111327772,
-9.85256218201608));
#15331=CARTESIAN_POINT('Ctrl Pts',(2.84741896244193,-0.95445695610894,-9.84926337956484));
#15332=CARTESIAN_POINT('Ctrl Pts',(2.92853813529274,-1.00780476468787,-9.84323059024306));
#15333=CARTESIAN_POINT('Ctrl Pts',(2.96597879804629,-1.02957236508432,-9.84051764285344));
#15334=CARTESIAN_POINT('Ctrl Pts',(3.02021786676085,-1.05722818015854,-9.83661112625502));
#15335=CARTESIAN_POINT('Ctrl Pts',(3.03608219309112,-1.06487390175581,-9.83547144438125));
#15336=CARTESIAN_POINT('Ctrl Pts',(3.0643908576592,-1.07774310988006,-9.83343840158799));
#15337=CARTESIAN_POINT('Ctrl Pts',(3.07676491471131,-1.08311384263397,-9.83254995348445));
#15338=CARTESIAN_POINT('Ctrl Pts',(3.09530114928997,-1.09078353273428,-9.83121804560526));
#15339=CARTESIAN_POINT('Ctrl Pts',(3.1013950368387,-1.09324544579801,-9.83078001515608));
#15340=CARTESIAN_POINT('Ctrl Pts',(3.10754343191573,-1.09566971705732,-9.83033782098026));
#15341=CARTESIAN_POINT('Ctrl Pts',(3.10757775536683,-1.09568324870211,-9.83033535242107));
#15342=CARTESIAN_POINT('Ctrl Pts',(3.1076483549733,-1.09571107799099,-9.8303302748475));
#15343=CARTESIAN_POINT('Ctrl Pts',(3.10768463120147,-1.09572537544587,-9.830327665827));
#15344=CARTESIAN_POINT('Ctrl Pts',(3.10775925492901,-1.09575478241887,-9.83032229880059));
#15345=CARTESIAN_POINT('Ctrl Pts',(3.1077976025227,-1.09576989172988,-9.83031954078689));
#15346=CARTESIAN_POINT('Ctrl Pts',(3.10787649559497,-1.09580097155484,-9.83031386666474));
#15347=CARTESIAN_POINT('Ctrl Pts',(3.10791704115353,-1.0958169418263,-9.8303109505494));
#15348=CARTESIAN_POINT('Ctrl Pts',(3.10800046529989,-1.09584979596521,-9.83030495050062));
#15349=CARTESIAN_POINT('Ctrl Pts',(3.10804334399795,-1.09586667956857,-9.83030186655797));
#15350=CARTESIAN_POINT('Ctrl Pts',(3.10813157885383,-1.09590141630034,-9.83029552046282));
#15351=CARTESIAN_POINT('Ctrl Pts',(3.10817693513293,-1.09591926913118,-9.83029225830016));
#15352=CARTESIAN_POINT('Ctrl Pts',(3.10827027958136,-1.09595600404714,-9.83028554465343));
#15353=CARTESIAN_POINT('Ctrl Pts',(3.10831826787693,-1.09597488579395,-9.83028209315867));
#15354=CARTESIAN_POINT('Ctrl Pts',(3.10841704153571,-1.0960137423461,-9.83027498896254));
#15355=CARTESIAN_POINT('Ctrl Pts',(3.10846782704737,-1.09603371677359,-9.83027133624868));
#15356=CARTESIAN_POINT('Ctrl Pts',(3.10857237196038,-1.0960748268977,-9.83026381689092));
#15357=CARTESIAN_POINT('Ctrl Pts',(3.10862613152371,-1.0960959621672,-9.8302599502333));
#15358=CARTESIAN_POINT('Ctrl Pts',(3.1087368138989,-1.09613946691829,-9.830251989362));
#15359=CARTESIAN_POINT('Ctrl Pts',(3.10879373690068,-1.09616183592192,-9.83024789513233));
#15360=CARTESIAN_POINT('Ctrl Pts',(3.10891094908999,-1.09620788619768,-9.83023946451329));
#15361=CARTESIAN_POINT('Ctrl Pts',(3.108971238489,-1.09623156693029,-9.83023512810609));
#15362=CARTESIAN_POINT('Ctrl Pts',(3.1090954010752,-1.09628032422859,-9.83022619747242));
#15363=CARTESIAN_POINT('Ctrl Pts',(3.10915927449812,-1.09630540018487,-9.83022160322605));
#15364=CARTESIAN_POINT('Ctrl Pts',(3.10929083859044,-1.09635703743392,-9.83021214011275));
#15365=CARTESIAN_POINT('Ctrl Pts',(3.10935852952489,-1.09638359803866,-9.83020727122342));
#15366=CARTESIAN_POINT('Ctrl Pts',(3.10949797923664,-1.09643830048801,-9.83019724078879));
#15367=CARTESIAN_POINT('Ctrl Pts',(3.10956973831804,-1.0964664415575,-9.83019207921782));
#15368=CARTESIAN_POINT('Ctrl Pts',(3.11420107955089,-1.09828214559106,-9.82985894846596));
#15369=CARTESIAN_POINT('Ctrl Pts',(3.11877170467261,-1.10004123444432,-9.82953004497875));
#15370=CARTESIAN_POINT('Ctrl Pts',(3.12909485118052,-1.10394053754667,-9.82878680423127));
#15371=CARTESIAN_POINT('Ctrl Pts',(3.1348533622849,-1.10606437974786,-9.82837193837223));
#15372=CARTESIAN_POINT('Ctrl Pts',(3.15044324331368,-1.11167616606449,-9.82724792050189));
#15373=CARTESIAN_POINT('Ctrl Pts',(3.16030459128452,-1.11507859082579,-9.82653600192459));
#15374=CARTESIAN_POINT('Ctrl Pts',(3.20818679353909,-1.13089059927671,-9.82307386110841));
#15375=CARTESIAN_POINT('Ctrl Pts',(3.24677388441622,-1.14148772953117,-9.82026618572278));
#15376=CARTESIAN_POINT('Ctrl Pts',(3.36770775654436,-1.16816419057322,-9.81141165563014));
#15377=CARTESIAN_POINT('Ctrl Pts',(3.45128491175312,-1.17742896249921,-9.80519607767987));
#15378=CARTESIAN_POINT('Ctrl Pts',(3.56296907476481,-1.17784570040957,-9.79706445952686));
#15379=CARTESIAN_POINT('Ctrl Pts',(3.59081057252225,-1.17696209914155,-9.79505415112404));
#15380=CARTESIAN_POINT('Ctrl Pts',(3.62946521644012,-1.17436085550939,-9.79230689377025));
#15381=CARTESIAN_POINT('Ctrl Pts',(3.64032394472411,-1.173478642301,-9.79154000090286));
#15382=CARTESIAN_POINT('Ctrl Pts',(3.65925690341835,-1.17167568538445,-9.79021305861677));
#15383=CARTESIAN_POINT('Ctrl Pts',(3.66733661464515,-1.17082182443387,-9.78965003199249));
#15384=CARTESIAN_POINT('Ctrl Pts',(3.67927879441322,-1.16943467905838,-9.7888232889936));
#15385=CARTESIAN_POINT('Ctrl Pts',(3.68314828502214,-1.16896573888598,-9.78855625530948));
#15386=CARTESIAN_POINT('Ctrl Pts',(3.69003885347894,-1.16809594556067,-9.78808233029557));
#15387=CARTESIAN_POINT('Ctrl Pts',(3.69306077501046,-1.16770256858485,-9.78787503813181));
#15388=CARTESIAN_POINT('Ctrl Pts',(3.69965590172444,-1.1668180061097,-9.78742385308767));
#15389=CARTESIAN_POINT('Ctrl Pts',(3.70322839545239,-1.16632213463915,-9.78718022116522));
#15390=CARTESIAN_POINT('Ctrl Pts',(3.71324223751461,-1.16488526984143,-9.78649932710392));
#15391=CARTESIAN_POINT('Ctrl Pts',(3.71967826518759,-1.16390725563635,-9.78606405020752));
#15392=CARTESIAN_POINT('Ctrl Pts',(3.7578224088654,-1.15778691154034,-9.78349645671845));
#15393=CARTESIAN_POINT('Ctrl Pts',(3.78932058012659,-1.15140197073065,-9.78142599397901));
#15394=CARTESIAN_POINT('Ctrl Pts',(3.89799492378891,-1.12470200325839,-9.77433422040861));
#15395=CARTESIAN_POINT('Ctrl Pts',(3.97333713010549,-1.09784460183248,-9.76949720051125));
#15396=CARTESIAN_POINT('Ctrl Pts',(4.05640124512457,-1.05833670225327,-9.76374217171437));
#15397=CARTESIAN_POINT('Ctrl Pts',(4.06732943040864,-1.05292917485303,-9.76297641879315));
#15398=CARTESIAN_POINT('Ctrl Pts',(4.07816928770683,-1.0473542783481,-9.76220700099567));
#15399=CARTESIAN_POINT('',(2.36176926760077,-0.000715235775294672,-9.82563288520559));
#15400=CARTESIAN_POINT('Ctrl Pts',(4.07816926754759,-1.04735428871592,-9.66287031899079));
#15401=CARTESIAN_POINT('Ctrl Pts',(4.03640204496254,-1.06883500804511,-9.66603810987595));
#15402=CARTESIAN_POINT('Ctrl Pts',(3.9933141503434,-1.08783078014696,-9.66920590076111));
#15403=CARTESIAN_POINT('Ctrl Pts',(3.94923246509231,-1.10418747517802,-9.67237369164627));
#15404=CARTESIAN_POINT('Ctrl Pts',(3.90516395949031,-1.12053927984476,-9.67554053541764));
#15405=CARTESIAN_POINT('Ctrl Pts',(3.86010277492871,-1.13425337867765,-9.67870737918901));
#15406=CARTESIAN_POINT('Ctrl Pts',(3.81439467726135,-1.14522419301647,-9.68187422296037));
#15407=CARTESIAN_POINT('Ctrl Pts',(3.76864638056048,-1.15620465588926,-9.68504385188503));
#15408=CARTESIAN_POINT('Ctrl Pts',(3.72225057715234,-1.16443688268081,-9.68821348080969));
#15409=CARTESIAN_POINT('Ctrl Pts',(3.67556517756882,-1.16986602386283,-9.69138310973436));
#15410=CARTESIAN_POINT('Ctrl Pts',(3.62885909613471,-1.1752975701798,-9.69455414281947));
#15411=CARTESIAN_POINT('Ctrl Pts',(3.5818637204158,-1.17792352262935,-9.69772517590458));
#15412=CARTESIAN_POINT('Ctrl Pts',(3.53494037375074,-1.17774109982624,-9.7008962089897));
#15413=CARTESIAN_POINT('Ctrl Pts',(3.48792659891677,-1.17755832546765,-9.7040733531205));
#15414=CARTESIAN_POINT('Ctrl Pts',(3.44098568817978,-1.17455640149661,-9.70725049725131));
#15415=CARTESIAN_POINT('Ctrl Pts',(3.3944756066763,-1.16878460886773,-9.71042764138211));
#15416=CARTESIAN_POINT('Ctrl Pts',(3.36250330188285,-1.16481692041891,-9.71261169733814));
#15417=CARTESIAN_POINT('Ctrl Pts',(3.33073447233927,-1.15954140798911,-9.71479575329416));
#15418=CARTESIAN_POINT('Ctrl Pts',(3.29928186879577,-1.15298792667738,-9.71697980925019));
#15419=CARTESIAN_POINT('Ctrl Pts',(3.25187865494836,-1.14311096766395,-9.72027146907716));
#15420=CARTESIAN_POINT('Ctrl Pts',(3.20497661177928,-1.13028308409168,-9.72356312890415));
#15421=CARTESIAN_POINT('Ctrl Pts',(3.15896922680476,-1.11457475937872,-9.72685478873113));
#15422=CARTESIAN_POINT('Ctrl Pts',(3.11463212633289,-1.09943672074799,-9.73002694582176));
#15423=CARTESIAN_POINT('Ctrl Pts',(3.07112641688879,-1.08162400884126,-9.73319910291238));
#15424=CARTESIAN_POINT('Ctrl Pts',(3.02879375923831,-1.0612514967925,-9.73637126000301));
#15425=CARTESIAN_POINT('Ctrl Pts',(2.98650317201939,-1.04089923105998,-9.73954026458621));
#15426=CARTESIAN_POINT('Ctrl Pts',(2.9453838294259,-1.01799244096358,-9.7427092691694));
#15427=CARTESIAN_POINT('Ctrl Pts',(2.9057579425434,-0.99269427349977,-9.7458782737526));
#15428=CARTESIAN_POINT('Ctrl Pts',(2.86615398990713,-0.96741010941299,-9.74904552418637));
#15429=CARTESIAN_POINT('Ctrl Pts',(2.82804232459403,-0.939737489628927,
-9.75221277462014));
#15430=CARTESIAN_POINT('Ctrl Pts',(2.79171863284347,-0.909884387143714,
-9.75538002505391));
#15431=CARTESIAN_POINT('Ctrl Pts',(2.7553990562947,-0.880034666791066,-9.75854691666196));
#15432=CARTESIAN_POINT('Ctrl Pts',(2.72086748032072,-0.848005309651611,
-9.76171380827001));
#15433=CARTESIAN_POINT('Ctrl Pts',(2.6883866096355,-0.814044612253605,-9.76488069987807));
#15434=CARTESIAN_POINT('Ctrl Pts',(2.65587286301626,-0.780049541095812,
-9.76805079689649));
#15435=CARTESIAN_POINT('Ctrl Pts',(2.62541434795704,-0.744119633990367,
-9.7712208939149));
#15436=CARTESIAN_POINT('Ctrl Pts',(2.59723555364959,-0.706538657264058,
-9.77439099093332));
#15437=CARTESIAN_POINT('Ctrl Pts',(2.56903958472873,-0.668934775414841,
-9.77756302008518));
#15438=CARTESIAN_POINT('Ctrl Pts',(2.54312640863249,-0.629678286970802,
-9.78073504923704));
#15439=CARTESIAN_POINT('Ctrl Pts',(2.51967688301253,-0.58908150206193,-9.7839070783889));
#15440=CARTESIAN_POINT('Ctrl Pts',(2.49618521099785,-0.548411751578014,
-9.78708480870482));
#15441=CARTESIAN_POINT('Ctrl Pts',(2.47516626853492,-0.50639739884094,-9.79026253902073));
#15442=CARTESIAN_POINT('Ctrl Pts',(2.45675386851054,-0.46337309302342,-9.79344026933665));
#15443=CARTESIAN_POINT('Ctrl Pts',(2.45184931948999,-0.451912619827236,
-9.79428672792368));
#15444=CARTESIAN_POINT('Ctrl Pts',(2.44712944272375,-0.440380575424196,
-9.79513318651071));
#15445=CARTESIAN_POINT('Ctrl Pts',(2.4425961684122,-0.428783457494737,-9.79597964509774));
#15446=CARTESIAN_POINT('Ctrl Pts',(2.42336625378943,-0.379589084437358,
-9.79957027854317));
#15447=CARTESIAN_POINT('Ctrl Pts',(2.40742663073616,-0.329040465405448,
-9.80316091198859));
#15448=CARTESIAN_POINT('Ctrl Pts',(2.39494311029787,-0.277562569138398,
-9.80675154543401));
#15449=CARTESIAN_POINT('Ctrl Pts',(2.38255303096995,-0.226469993006811,
-9.81031530242437));
#15450=CARTESIAN_POINT('Ctrl Pts',(2.37356764353218,-0.174462259850974,
-9.81387905941473));
#15451=CARTESIAN_POINT('Ctrl Pts',(2.36810239749475,-0.121975767029384,
-9.81744281640509));
#15452=CARTESIAN_POINT('Ctrl Pts',(2.36391573519994,-0.0817683877132421,
-9.82017283933859));
#15453=CARTESIAN_POINT('Ctrl Pts',(2.36179390249004,-0.0412805101726955,
-9.82290286227209));
#15454=CARTESIAN_POINT('Ctrl Pts',(2.36176926760077,-0.000715235775294672,
-9.82563288520559));
#15455=CARTESIAN_POINT('Ctrl Pts',(4.07816926754606,-1.0473542887167,-10.1620324047393));
#15456=CARTESIAN_POINT('Ctrl Pts',(4.11166851029021,-1.03012575910453,-10.1593451640671));
#15457=CARTESIAN_POINT('Ctrl Pts',(4.14432478142673,-1.01129850207866,-10.1567044894124));
#15458=CARTESIAN_POINT('Ctrl Pts',(4.18465099112637,-0.985395825742646,
-10.1534149717822));
#15459=CARTESIAN_POINT('Ctrl Pts',(4.19320386985264,-0.979742988069625,
-10.152715498407));
#15460=CARTESIAN_POINT('Ctrl Pts',(4.20672468889827,-0.970550812183664,
-10.1516065546902));
#15461=CARTESIAN_POINT('Ctrl Pts',(4.21174066747047,-0.967083420925472,
-10.1511944434489));
#15462=CARTESIAN_POINT('Ctrl Pts',(4.22074020716762,-0.960758465173311,
-10.1504536576296));
#15463=CARTESIAN_POINT('Ctrl Pts',(4.22473325419787,-0.95791470861673,-10.1501244753992));
#15464=CARTESIAN_POINT('Ctrl Pts',(4.23410144147423,-0.951154348163961,
-10.1493509172429));
#15465=CARTESIAN_POINT('Ctrl Pts',(4.23946143132522,-0.947216954268419,
-10.1489073430298));
#15466=CARTESIAN_POINT('Ctrl Pts',(4.25509170414454,-0.935529991508297,
-10.1476106700208));
#15467=CARTESIAN_POINT('Ctrl Pts',(4.26526891203165,-0.927657128079991,
-10.1467623263627));
#15468=CARTESIAN_POINT('Ctrl Pts',(4.28812280417377,-0.909371496965137,
-10.1448462017761));
#15469=CARTESIAN_POINT('Ctrl Pts',(4.30071517653537,-0.89885738408202,-10.1437824169512));
#15470=CARTESIAN_POINT('Ctrl Pts',(4.34232059683862,-0.862616967717274,
-10.1402335078206));
#15471=CARTESIAN_POINT('Ctrl Pts',(4.37028296160212,-0.835721268162505,
-10.1377914920261));
#15472=CARTESIAN_POINT('Ctrl Pts',(4.44007817696513,-0.76161669609319,-10.1314454893765));
#15473=CARTESIAN_POINT('Ctrl Pts',(4.47953353278298,-0.712347593258341,
-10.1275960174921));
#15474=CARTESIAN_POINT('Ctrl Pts',(4.52146125685367,-0.650402488720235,
-10.1229045197741));
#15475=CARTESIAN_POINT('Ctrl Pts',(4.52791881486826,-0.640546475416325,
-10.1221619969));
#15476=CARTESIAN_POINT('Ctrl Pts',(4.55094777908877,-0.604220334616202,
-10.1194334243294));
#15477=CARTESIAN_POINT('Ctrl Pts',(4.5666110517894,-0.577193141720599,-10.1174189246061));
#15478=CARTESIAN_POINT('Ctrl Pts',(4.58419542312343,-0.543864030123283,
-10.1149139420247));
#15479=CARTESIAN_POINT('Ctrl Pts',(4.58716318576775,-0.538125048624946,
-10.1144818805222));
#15480=CARTESIAN_POINT('Ctrl Pts',(4.59170819704717,-0.529155914180496,
-10.113805056611));
#15481=CARTESIAN_POINT('Ctrl Pts',(4.59331818438885,-0.525942360125429,
-10.1135622444156));
#15482=CARTESIAN_POINT('Ctrl Pts',(4.59626448541928,-0.519993668047369,
-10.1131120993147));
#15483=CARTESIAN_POINT('Ctrl Pts',(4.59760493039593,-0.517260668413725,
-10.1129050227833));
#15484=CARTESIAN_POINT('Ctrl Pts',(4.60063984928993,-0.511011688587452,
-10.1124309444956));
#15485=CARTESIAN_POINT('Ctrl Pts',(4.60232744217774,-0.50749247972229,-10.1121635374083));
#15486=CARTESIAN_POINT('Ctrl Pts',(4.607494848954,-0.496577846909258,-10.1113330310723));
#15487=CARTESIAN_POINT('Ctrl Pts',(4.61091510449656,-0.489154730425527,
-10.1107665613824));
#15488=CARTESIAN_POINT('Ctrl Pts',(4.61874976709229,-0.471674412298479,
-10.1094297944437));
#15489=CARTESIAN_POINT('Ctrl Pts',(4.62310123497383,-0.46158999227168,-10.108656453785));
#15490=CARTESIAN_POINT('Ctrl Pts',(4.6381243482863,-0.425390762409366,-10.1058763677648));
#15491=CARTESIAN_POINT('Ctrl Pts',(4.64799747922974,-0.398956466529585,
-10.1038389034186));
#15492=CARTESIAN_POINT('Ctrl Pts',(4.68385429048858,-0.291308292914443,
-10.0955740863451));
#15493=CARTESIAN_POINT('Ctrl Pts',(4.70193773390399,-0.207723903788031,
-10.0892529308968));
#15494=CARTESIAN_POINT('Ctrl Pts',(4.71484627096173,-0.0847143797604495,
-10.0804227366325));
#15495=CARTESIAN_POINT('Ctrl Pts',(4.71698423271749,-0.046334865646207,
-10.077728572741));
#15496=CARTESIAN_POINT('Ctrl Pts',(4.71731162056922,0.00237606310295109,
-10.0743850355434));
#15497=CARTESIAN_POINT('Ctrl Pts',(4.71724588958997,0.0126683837430763,
-10.0736827767839));
#15498=CARTESIAN_POINT('Ctrl Pts',(4.71692632293037,0.0290585234999041,
-10.0725708597118));
#15499=CARTESIAN_POINT('Ctrl Pts',(4.71675999798506,0.035157317066796,-10.0721585254195));
#15500=CARTESIAN_POINT('Ctrl Pts',(4.71637489167241,0.0461447013263969,
-10.0714181288078));
#15501=CARTESIAN_POINT('Ctrl Pts',(4.71617302108258,0.0510337056252975,
-10.0710895529949));
#15502=CARTESIAN_POINT('Ctrl Pts',(4.71562621948057,0.0625368070761503,
-10.0703184501178));
#15503=CARTESIAN_POINT('Ctrl Pts',(4.71525595287784,0.0691495811071611,
-10.0698767148851));
#15504=CARTESIAN_POINT('Ctrl Pts',(4.71400925872773,0.0884905607197706,
-10.0685890079186));
#15505=CARTESIAN_POINT('Ctrl Pts',(4.71298175637836,0.101208335222971,-10.0677477037715));
#15506=CARTESIAN_POINT('Ctrl Pts',(4.71017765634749,0.130065538128462,-10.0658494040565));
#15507=CARTESIAN_POINT('Ctrl Pts',(4.70827355971496,0.146190120920674,-10.0647963057246));
#15508=CARTESIAN_POINT('Ctrl Pts',(4.70077428492776,0.200100227503268,-10.0612945272852));
#15509=CARTESIAN_POINT('Ctrl Pts',(4.69367465118615,0.237653143985456,-10.0588876915591));
#15510=CARTESIAN_POINT('Ctrl Pts',(4.67415255596877,0.319013340144446,-10.0536696874119));
#15511=CARTESIAN_POINT('Ctrl Pts',(4.66099126336457,0.362578016086178,-10.0508736958156));
#15512=CARTESIAN_POINT('Ctrl Pts',(4.63926941170991,0.421848134245943,-10.0469577753029));
#15513=CARTESIAN_POINT('Ctrl Pts',(4.63282295101693,0.438284452225309,-10.0458592209155));
#15514=CARTESIAN_POINT('Ctrl Pts',(4.61758362514522,0.474708786187078,-10.0433843037041));
#15515=CARTESIAN_POINT('Ctrl Pts',(4.60859965759033,0.494609162824384,-10.0420042452341));
#15516=CARTESIAN_POINT('Ctrl Pts',(4.58909230452171,0.534801884064379,-10.0391372178779));
#15517=CARTESIAN_POINT('Ctrl Pts',(4.57852104891252,0.555060134746424,-10.0376488897872));
#15518=CARTESIAN_POINT('Ctrl Pts',(4.56445605752608,0.580202357629179,-10.0357302556828));
#15519=CARTESIAN_POINT('Ctrl Pts',(4.56150439207674,0.585385857413958,-10.0353307671316));
#15520=CARTESIAN_POINT('Ctrl Pts',(4.55678584467183,0.593527762009445,-10.0346966880801));
#15521=CARTESIAN_POINT('Ctrl Pts',(4.55504508620572,0.596501303299116,-10.0344637135381));
#15522=CARTESIAN_POINT('Ctrl Pts',(4.55172798568358,0.602110926384337,-10.0340214661289));
#15523=CARTESIAN_POINT('Ctrl Pts',(4.55015435338888,0.604748526081976,-10.033812363926));
#15524=CARTESIAN_POINT('Ctrl Pts',(4.54643392897759,0.610929335547352,-10.0333196657103));
#15525=CARTESIAN_POINT('Ctrl Pts',(4.54427873953443,0.614467404762811,-10.0330355402782));
#15526=CARTESIAN_POINT('Ctrl Pts',(4.53714005011039,0.626048665975641,-10.0320988013784));
#15527=CARTESIAN_POINT('Ctrl Pts',(4.53207843790301,0.634042931796248,-10.031441511686));
#15528=CARTESIAN_POINT('Ctrl Pts',(4.50327938562384,0.678337876130907,-10.0277431665269));
#15529=CARTESIAN_POINT('Ctrl Pts',(4.4776491818813,0.713363398421631,-10.0246059439746));
#15530=CARTESIAN_POINT('Ctrl Pts',(4.43054094908304,0.770798977324831,-10.0191785866802));
#15531=CARTESIAN_POINT('Ctrl Pts',(4.40999900225179,0.793924249159746,-10.0169054365728));
#15532=CARTESIAN_POINT('Ctrl Pts',(4.3344886010232,0.872472576280763,-10.0089163017177));
#15533=CARTESIAN_POINT('Ctrl Pts',(4.27493989952936,0.923225416383328,-10.0032684650201));
#15534=CARTESIAN_POINT('Ctrl Pts',(4.19806104426981,0.976554032701125,-9.99678410147741));
#15535=CARTESIAN_POINT('Ctrl Pts',(4.1851508866706,0.985136999673151,-9.99571908618209));
#15536=CARTESIAN_POINT('Ctrl Pts',(4.16610062426853,0.997266638836645,-9.99418116447606));
#15537=CARTESIAN_POINT('Ctrl Pts',(4.1600924516165,1.00101642101442,-9.99370087620955));
#15538=CARTESIAN_POINT('Ctrl Pts',(4.14937351447643,1.00757265518793,-9.99285226109225));
#15539=CARTESIAN_POINT('Ctrl Pts',(4.14467633717077,1.01040080307155,-9.99248315717797));
#15540=CARTESIAN_POINT('Ctrl Pts',(4.13483901364542,1.01623059964736,-9.99171580851009));
#15541=CARTESIAN_POINT('Ctrl Pts',(4.12969550654026,1.01922629632226,-9.99131778472036));
#15542=CARTESIAN_POINT('Ctrl Pts',(4.1162118682032,1.02694318165454,-9.99028250046438));
#15543=CARTESIAN_POINT('Ctrl Pts',(4.10783632060286,1.03160185815931,-9.98964746137561));
#15544=CARTESIAN_POINT('Ctrl Pts',(4.06924341848271,1.05245544578049,-9.98675652842602));
#15545=CARTESIAN_POINT('Ctrl Pts',(4.03838308966577,1.06742933588016,-9.98454324538067));
#15546=CARTESIAN_POINT('Ctrl Pts',(3.94565303397733,1.10752166517873,-9.97812004127294));
#15547=CARTESIAN_POINT('Ctrl Pts',(3.88225426486694,1.12875250755144,-9.97402125003092));
#15548=CARTESIAN_POINT('Ctrl Pts',(3.75907413967879,1.15865981026454,-9.96616716643602));
#15549=CARTESIAN_POINT('Ctrl Pts',(3.69976260098377,1.16833948092059,-9.96242746122153));
#15550=CARTESIAN_POINT('Ctrl Pts',(3.62998104457627,1.17431359318376,-9.95781965141308));
#15551=CARTESIAN_POINT('Ctrl Pts',(3.61997130881696,1.1750417887249,-9.95715367202727));
#15552=CARTESIAN_POINT('Ctrl Pts',(3.60601834603003,1.17587773615314,-9.95621683256612));
#15553=CARTESIAN_POINT('Ctrl Pts',(3.60208170084995,1.17609375491992,-9.95595157385425));
#15554=CARTESIAN_POINT('Ctrl Pts',(3.59528856777066,1.17643231757813,-9.95549210065292));
#15555=CARTESIAN_POINT('Ctrl Pts',(3.59243254997252,1.17656423455301,-9.95529839567623));
#15556=CARTESIAN_POINT('Ctrl Pts',(3.58640729039202,1.17682055348271,-9.95488857072086));
#15557=CARTESIAN_POINT('Ctrl Pts',(3.58323799477549,1.17694255393065,-9.9546723159746));
#15558=CARTESIAN_POINT('Ctrl Pts',(3.57537144282337,1.17721355546381,-9.95413390646998));
#15559=CARTESIAN_POINT('Ctrl Pts',(3.57067375232767,1.17734724354175,-9.95381093208487));
#15560=CARTESIAN_POINT('Ctrl Pts',(3.55294431672716,1.17774561000984,-9.95258683915924));
#15561=CARTESIAN_POINT('Ctrl Pts',(3.53990984509297,1.17782204586383,-9.95167638161156));
#15562=CARTESIAN_POINT('Ctrl Pts',(3.50641952201881,1.17746255152787,-9.94931443980075));
#15563=CARTESIAN_POINT('Ctrl Pts',(3.4859719253822,1.1767099240049,-9.94785067109951));
#15564=CARTESIAN_POINT('Ctrl Pts',(3.4078203949716,1.17179225013658,-9.94219641426312));
#15565=CARTESIAN_POINT('Ctrl Pts',(3.35043286064573,1.16391055197607,-9.93792400994631));
#15566=CARTESIAN_POINT('Ctrl Pts',(3.22007496124566,1.13610831767881,-9.9281736756038));
#15567=CARTESIAN_POINT('Ctrl Pts',(3.14796290757953,1.11331680287793,-9.92275451057965));
#15568=CARTESIAN_POINT('Ctrl Pts',(3.06895501780716,1.07970945794833,-9.91684620350546));
#15569=CARTESIAN_POINT('Ctrl Pts',(3.0594476826702,1.07551593025369,-9.91613540986386));
#15570=CARTESIAN_POINT('Ctrl Pts',(3.0438803115349,1.06840185678349,-9.91497154925038));
#15571=CARTESIAN_POINT('Ctrl Pts',(3.03778775070248,1.06555431264159,-9.91451604999203));
#15572=CARTESIAN_POINT('Ctrl Pts',(3.02682293648184,1.06031467603284,-9.91369616307984));
#15573=CARTESIAN_POINT('Ctrl Pts',(3.02194223424367,1.05794081049147,-9.91333116714618));
#15574=CARTESIAN_POINT('Ctrl Pts',(3.01698178095538,1.05548561148612,-9.91296011997739));
#15575=CARTESIAN_POINT('Ctrl Pts',(3.01688552362932,1.05543795208819,-9.9129529197935));
#15576=CARTESIAN_POINT('Ctrl Pts',(3.01671703606709,1.05535450100128,-9.91294031662625));
#15577=CARTESIAN_POINT('Ctrl Pts',(3.01664480299475,1.05531871506887,-9.91293491344563));
#15578=CARTESIAN_POINT('Ctrl Pts',(3.01646257406813,1.05522841134728,-9.91292128230272));
#15579=CARTESIAN_POINT('Ctrl Pts',(3.01635258304072,1.05517388376421,-9.91291305467593));
#15580=CARTESIAN_POINT('Ctrl Pts',(3.01613910253037,1.0550680101256,-9.91289708566733));
#15581=CARTESIAN_POINT('Ctrl Pts',(3.01603561207763,1.05501666604117,-9.91288934421818));
#15582=CARTESIAN_POINT('Ctrl Pts',(3.01583473440515,1.05491696899766,-9.91287431778421));
#15583=CARTESIAN_POINT('Ctrl Pts',(3.01573734632957,1.05486861778104,-9.91286703274002));
#15584=CARTESIAN_POINT('Ctrl Pts',(3.01554829969533,1.05477472730295,-9.91285289117339));
#15585=CARTESIAN_POINT('Ctrl Pts',(3.01545664037686,1.05472918957985,-9.91284603459825));
#15586=CARTESIAN_POINT('Ctrl Pts',(3.00971714244538,1.05187678811162,-9.91241668943013));
#15587=CARTESIAN_POINT('Ctrl Pts',(3.00409184483775,1.04902457034529,-9.91199576439533));
#15588=CARTESIAN_POINT('Ctrl Pts',(2.98824145927402,1.04082716915612,-9.91080916586421));
#15589=CARTESIAN_POINT('Ctrl Pts',(2.97807143432156,1.03537663113004,-9.91004715541127));
#15590=CARTESIAN_POINT('Ctrl Pts',(2.95535603671599,1.02276936999385,-9.90834244044464));
#15591=CARTESIAN_POINT('Ctrl Pts',(2.94285879519073,1.01552950640833,-9.90740266706053));
#15592=CARTESIAN_POINT('Ctrl Pts',(2.90307992222631,0.991497047842256,-9.90440096582231));
#15593=CARTESIAN_POINT('Ctrl Pts',(2.87634825822561,0.973820256433688,-9.90236815363861));
#15594=CARTESIAN_POINT('Ctrl Pts',(2.80859602991565,0.924932492798933,-9.89712467840091));
#15595=CARTESIAN_POINT('Ctrl Pts',(2.76884532639873,0.892082264471316,-9.89395685010029));
#15596=CARTESIAN_POINT('Ctrl Pts',(2.68815696174492,0.815969955955608,-9.88708364091148));
#15597=CARTESIAN_POINT('Ctrl Pts',(2.64809324935974,0.771999095504211,-9.88337993285492));
#15598=CARTESIAN_POINT('Ctrl Pts',(2.60535368857308,0.7173078089846,-9.87881321617277));
#15599=CARTESIAN_POINT('Ctrl Pts',(2.59928650732665,0.709336425606377,-9.87814845109279));
#15600=CARTESIAN_POINT('Ctrl Pts',(2.59097720743559,0.698125304851623,-9.8772131594298));
#15601=CARTESIAN_POINT('Ctrl Pts',(2.58864834471278,0.694949975962603,-9.87694821776404));
#15602=CARTESIAN_POINT('Ctrl Pts',(2.5846577669473,0.689451340370706,-9.87648924413703));
#15603=CARTESIAN_POINT('Ctrl Pts',(2.58298848090638,0.687133531824313,-9.87629572061605));
#15604=CARTESIAN_POINT('Ctrl Pts',(2.57948395736393,0.682229973594607,-9.87588613299414));
#15605=CARTESIAN_POINT('Ctrl Pts',(2.57765071123529,0.67964285773079,-9.87566993348663));
#15606=CARTESIAN_POINT('Ctrl Pts',(2.57312642654383,0.673203122140363,-9.87513159090387));
#15607=CARTESIAN_POINT('Ctrl Pts',(2.57044798030795,0.669341770944382,-9.87480862778345));
#15608=CARTESIAN_POINT('Ctrl Pts',(2.56042509775549,0.654706133376354,-9.87358419142916));
#15609=CARTESIAN_POINT('Ctrl Pts',(2.55323697441191,0.643826623006103,-9.87267336829594));
#15610=CARTESIAN_POINT('Ctrl Pts',(2.53523147034626,0.615565274819328,-9.87031013372975));
#15611=CARTESIAN_POINT('Ctrl Pts',(2.52468426828429,0.598017070539264,-9.86884541681277));
#15612=CARTESIAN_POINT('Ctrl Pts',(2.46871959008831,0.499156599838894,-9.86064221196433));
#15613=CARTESIAN_POINT('Ctrl Pts',(2.43261202885941,0.412950812776566,-9.85370125799127));
#15614=CARTESIAN_POINT('Ctrl Pts',(2.39671037874418,0.287223833775087,-9.844334975543));
#15615=CARTESIAN_POINT('Ctrl Pts',(2.38812180487821,0.250587509652377,-9.84168526405144));
#15616=CARTESIAN_POINT('Ctrl Pts',(2.37916376817953,0.20201355784022,-9.83827640048387));
#15617=CARTESIAN_POINT('Ctrl Pts',(2.37720100497103,0.1903960011619,-9.83746871041783));
#15618=CARTESIAN_POINT('Ctrl Pts',(2.37434104438738,0.171770618151118,-9.83618557881491));
#15619=CARTESIAN_POINT('Ctrl Pts',(2.37333203921694,0.164781035508374,-9.83570668952124));
#15620=CARTESIAN_POINT('Ctrl Pts',(2.37165218572722,0.15235500247942,-9.83485986347754));
#15621=CARTESIAN_POINT('Ctrl Pts',(2.37095628930806,0.146922209039614,-9.83449115792062));
#15622=CARTESIAN_POINT('Ctrl Pts',(2.36968822413248,0.136442995899603,-9.83378284684814));
#15623=CARTESIAN_POINT('Ctrl Pts',(2.36911074985229,0.13139735382971,-9.83344308449042));
#15624=CARTESIAN_POINT('Ctrl Pts',(2.36793837113065,0.120532125987115,-9.83271412241372));
#15625=CARTESIAN_POINT('Ctrl Pts',(2.36735414986538,0.114711505266053,-9.83232525977258));
#15626=CARTESIAN_POINT('Ctrl Pts',(2.36604434526003,0.100604956054645,-9.83138667198957));
#15627=CARTESIAN_POINT('Ctrl Pts',(2.36536311530124,0.0923151481298986,
-9.83083830820046));
#15628=CARTESIAN_POINT('Ctrl Pts',(2.36275423588792,0.0558377771113773,
-9.82843851337979));
#15629=CARTESIAN_POINT('Ctrl Pts',(2.36175332805078,0.0275923818668629,
-9.82661507307611));
#15630=CARTESIAN_POINT('Ctrl Pts',(2.36176923710637,-0.000663123418161781,
-9.82481492042546));
#15631=CARTESIAN_POINT('Origin',(3.53951905042299,8.32667268468867E-16,
0.));
#15632=CARTESIAN_POINT('',(2.07451448579446,-0.00104776130442043,-0.160655045842906));
#15633=CARTESIAN_POINT('',(2.07598378213352,-0.00160958027810672,-0.0893449541570843));
#15634=CARTESIAN_POINT('',(2.07601905042299,1.01189432752408E-15,0.));
#15635=CARTESIAN_POINT('',(4.17447558192119,-1.32104331271118,-3.52050110134855E-5));
#15636=CARTESIAN_POINT('Ctrl Pts',(2.07451448579446,-0.00104776130442043,
-0.160655045842906));
#15637=CARTESIAN_POINT('Ctrl Pts',(2.07407030736436,-0.059925529006458,
-0.157443865218375));
#15638=CARTESIAN_POINT('Ctrl Pts',(2.10392157786283,-0.601150164264895,
-0.127899405977995));
#15639=CARTESIAN_POINT('Ctrl Pts',(2.74920669632528,-1.50947517628745,-0.0743594590340226));
#15640=CARTESIAN_POINT('Ctrl Pts',(3.77694222363607,-1.50905204600162,-0.0240306927145928));
#15641=CARTESIAN_POINT('Ctrl Pts',(4.17447558192119,-1.32104331271118,-3.52050110134856E-5));
#15642=CARTESIAN_POINT('',(2.90551195584778,-1.31904027763685,0.));
#15643=CARTESIAN_POINT('Origin',(3.53951905042299,8.32667268468867E-16,
0.));
#15644=CARTESIAN_POINT('Ctrl Pts',(2.90551195584777,-1.31904027763685,-4.5102810375397E-16));
#15645=CARTESIAN_POINT('Ctrl Pts',(2.46902340624,-1.10923861968598,-0.0263332786158544));
#15646=CARTESIAN_POINT('Ctrl Pts',(2.10648828248685,-0.609902210944796,
-0.0561149300015489));
#15647=CARTESIAN_POINT('Ctrl Pts',(2.0743190278226,-0.0648117932209503,
-0.0858965813872436));
#15648=CARTESIAN_POINT('Ctrl Pts',(2.07482541103651,-0.00161085424212562,
-0.0893449541570843));
#15649=CARTESIAN_POINT('Origin',(3.53951905042299,8.32667268468867E-16,
0.));
#15650=CARTESIAN_POINT('',(2.07827644886075,-0.000378700063536769,-0.660655045842906));
#15651=CARTESIAN_POINT('',(2.07601908529222,-0.000319471822349998,-0.589344954125452));
#15652=CARTESIAN_POINT('',(2.07601905042299,1.01189432752408E-15,0.));
#15653=CARTESIAN_POINT('Ctrl Pts',(2.07827644886075,-0.000378700063536769,
-0.660655045842906));
#15654=CARTESIAN_POINT('Ctrl Pts',(2.07776587840242,-0.219619213994846,
-0.648776870246833));
#15655=CARTESIAN_POINT('Ctrl Pts',(2.22661874708729,-0.924244535467465,
-0.610565416034906));
#15656=CARTESIAN_POINT('Ctrl Pts',(3.31520031757397,-1.7123247414839,-0.546020683207126));
#15657=CARTESIAN_POINT('Ctrl Pts',(4.85108637608084,-1.12351020784619,-0.467020847359564));
#15658=CARTESIAN_POINT('Ctrl Pts',(5.19709361453891,0.484647885353767,-0.388021011512002));
#15659=CARTESIAN_POINT('Ctrl Pts',(4.03936404899096,1.65296550581617,-0.309021175664439));
#15660=CARTESIAN_POINT('Ctrl Pts',(2.49361202232558,1.33546458710318,-0.233232520441406));
#15661=CARTESIAN_POINT('Ctrl Pts',(2.07771279146056,0.42290145659918,-0.183777143834229));
#15662=CARTESIAN_POINT('Ctrl Pts',(2.07451448579446,-0.00104776130442043,
-0.160655045842906));
#15663=CARTESIAN_POINT('Ctrl Pts',(2.07601993550036,-0.00160954051702442,
-0.0893449541570843));
#15664=CARTESIAN_POINT('Ctrl Pts',(2.07596079908734,0.0521611394986531,
-0.0922812167265794));
#15665=CARTESIAN_POINT('Ctrl Pts',(2.07886922409737,0.10606434640489,-0.0952174792960745));
#15666=CARTESIAN_POINT('Ctrl Pts',(2.08476241956241,0.159735390465519,-0.0981537418655696));
#15667=CARTESIAN_POINT('Ctrl Pts',(2.09064824768661,0.213339338011707,-0.101086333685085));
#15668=CARTESIAN_POINT('Ctrl Pts',(2.09951141065111,0.266711150229533,-0.1040189255046));
#15669=CARTESIAN_POINT('Ctrl Pts',(2.11131711806971,0.319486291446668,-0.106951517324116));
#15670=CARTESIAN_POINT('Ctrl Pts',(2.12311320475964,0.372218425049299,-0.109881719310547));
#15671=CARTESIAN_POINT('Ctrl Pts',(2.13784697264489,0.424354310406159,-0.112811921296979));
#15672=CARTESIAN_POINT('Ctrl Pts',(2.15543217948843,0.475537363102618,-0.115742123283411));
#15673=CARTESIAN_POINT('Ctrl Pts',(2.17301070165289,0.526700959543301,-0.11867121140976));
#15674=CARTESIAN_POINT('Ctrl Pts',(2.19343833596986,0.576911916944637,-0.121600299536108));
#15675=CARTESIAN_POINT('Ctrl Pts',(2.21657913201178,0.625829227724427,-0.124529387662457));
#15676=CARTESIAN_POINT('Ctrl Pts',(2.23973792130799,0.674784574430474,-0.127460753317521));
#15677=CARTESIAN_POINT('Ctrl Pts',(2.26561385320264,0.722443760890151,-0.130392118972585));
#15678=CARTESIAN_POINT('Ctrl Pts',(2.29402375449186,0.768487942529639,-0.133323484627649));
#15679=CARTESIAN_POINT('Ctrl Pts',(2.32244395550627,0.814548817026053,-0.136255913019974));
#15680=CARTESIAN_POINT('Ctrl Pts',(2.35339963776276,0.858993065166078,-0.1391883414123));
#15681=CARTESIAN_POINT('Ctrl Pts',(2.38666476771661,0.901531615000586,-0.142120769804625));
#15682=CARTESIAN_POINT('Ctrl Pts',(2.41999288509549,0.944150711453193,-0.145058750741424));
#15683=CARTESIAN_POINT('Ctrl Pts',(2.45563881424911,0.984856488107153,-0.147996731678223));
#15684=CARTESIAN_POINT('Ctrl Pts',(2.4933377924311,1.02339485313661,-0.150934712615022));
#15685=CARTESIAN_POINT('Ctrl Pts',(2.52355602097499,1.05428590584754,-0.153289698975056));
#15686=CARTESIAN_POINT('Ctrl Pts',(2.55509253490114,1.08378502701655,-0.15564468533509));
#15687=CARTESIAN_POINT('Ctrl Pts',(2.58779640634575,1.11178067025409,-0.157999671695124));
#15688=CARTESIAN_POINT('Ctrl Pts',(2.62966525203463,1.14762184791584,-0.161014622407449));
#15689=CARTESIAN_POINT('Ctrl Pts',(2.67364777126532,1.18116844514286,-0.164029573119773));
#15690=CARTESIAN_POINT('Ctrl Pts',(2.71946292469062,1.21216343809274,-0.167044523832097));
#15691=CARTESIAN_POINT('Ctrl Pts',(2.76519681446833,1.24310345433741,-0.17005412684014));
#15692=CARTESIAN_POINT('Ctrl Pts',(2.81275645448268,1.27150055651047,-0.173063729848182));
#15693=CARTESIAN_POINT('Ctrl Pts',(2.86182791208697,1.29713799228179,-0.176073332856224));
#15694=CARTESIAN_POINT('Ctrl Pts',(2.91085085370823,1.32275008082562,-0.179079960329085));
#15695=CARTESIAN_POINT('Ctrl Pts',(2.96138218748599,1.34560766618287,-0.182086587801947));
#15696=CARTESIAN_POINT('Ctrl Pts',(3.01308075284201,1.3655383439655,-0.185093215274809));
#15697=CARTESIAN_POINT('Ctrl Pts',(3.06474843345596,1.38545711515385,-0.188098046587305));
#15698=CARTESIAN_POINT('Ctrl Pts',(3.11758147341645,1.40245225608464,-0.191102877899802));
#15699=CARTESIAN_POINT('Ctrl Pts',(3.17121805515847,1.41639917639314,-0.194107709212299));
#15700=CARTESIAN_POINT('Ctrl Pts',(3.22484357973953,1.43034322154931,-0.197111921079961));
#15701=CARTESIAN_POINT('Ctrl Pts',(3.27927180820599,1.44124016178639,-0.200116132947624));
#15702=CARTESIAN_POINT('Ctrl Pts',(3.33412727462733,1.44901568950633,-0.203120344815286));
#15703=CARTESIAN_POINT('Ctrl Pts',(3.38903176753004,1.45679816652029,-0.206127241664897));
#15704=CARTESIAN_POINT('Ctrl Pts',(3.4443637392852,1.46145358319522,-0.209134138514508));
#15705=CARTESIAN_POINT('Ctrl Pts',(3.49974055646164,1.46295930272109,-0.212141035364119));
#15706=CARTESIAN_POINT('Ctrl Pts',(3.55514192643853,1.46446568984818,-0.215149265402275));
#15707=CARTESIAN_POINT('Ctrl Pts',(3.61058765464483,1.46281961068625,-0.218157495440431));
#15708=CARTESIAN_POINT('Ctrl Pts',(3.66569633293303,1.45805059698845,-0.221165725478586));
#15709=CARTESIAN_POINT('Ctrl Pts',(3.72090676766773,1.45327277745639,-0.224179510119183));
#15710=CARTESIAN_POINT('Ctrl Pts',(3.77577838710661,1.44536057860399,-0.22719329475978));
#15711=CARTESIAN_POINT('Ctrl Pts',(3.82993728420081,1.43439516852553,-0.230207079400376));
#15712=CARTESIAN_POINT('Ctrl Pts',(3.87062482059872,1.4261572695722,-0.23247122211448));
#15713=CARTESIAN_POINT('Ctrl Pts',(3.91091025465529,1.41619723790657,-0.234735364828584));
#15714=CARTESIAN_POINT('Ctrl Pts',(3.95064122796382,1.40456783571819,-0.236999507542687));
#15715=CARTESIAN_POINT('Ctrl Pts',(4.00355245674629,1.38908052421907,-0.2400147513982));
#15716=CARTESIAN_POINT('Ctrl Pts',(4.05569412745601,1.37056799884676,-0.243029995253713));
#15717=CARTESIAN_POINT('Ctrl Pts',(4.10669745483237,1.34912597913302,-0.246045239109226));
#15718=CARTESIAN_POINT('Ctrl Pts',(4.15761312718257,1.32772080997189,-0.24905530092481));
#15719=CARTESIAN_POINT('Ctrl Pts',(4.20739385781659,1.30339634107968,-0.252065362740393));
#15720=CARTESIAN_POINT('Ctrl Pts',(4.25568671822785,1.27629781853255,-0.255075424555976));
#15721=CARTESIAN_POINT('Ctrl Pts',(4.30393346467842,1.24922517186423,-0.258082612119112));
#15722=CARTESIAN_POINT('Ctrl Pts',(4.35069469917369,1.21938397594076,-0.261089799682248));
#15723=CARTESIAN_POINT('Ctrl Pts',(4.39563987438938,1.18696646320404,-0.264096987245384));
#15724=CARTESIAN_POINT('Ctrl Pts',(4.44055970480858,1.1545672308558,-0.267102479041255));
#15725=CARTESIAN_POINT('Ctrl Pts',(4.48366508027645,1.11959486885137,-0.270107970837126));
#15726=CARTESIAN_POINT('Ctrl Pts',(4.52465431683852,1.08228497026633,-0.273113462632997));
#15727=CARTESIAN_POINT('Ctrl Pts',(4.5656364640684,1.04498152465011,-0.27611843461119));
#15728=CARTESIAN_POINT('Ctrl Pts',(4.60450281077932,1.00534169956904,-0.279123406589384));
#15729=CARTESIAN_POINT('Ctrl Pts',(4.64098642029402,0.963639913613693,-0.282128378567578));
#15730=CARTESIAN_POINT('Ctrl Pts',(4.67750444356329,0.921898791774464,-0.285136185034178));
#15731=CARTESIAN_POINT('Ctrl Pts',(4.71163489275568,0.878092220415177,-0.288143991500778));
#15732=CARTESIAN_POINT('Ctrl Pts',(4.74315025731674,0.832528778956924,-0.291151797967377));
#15733=CARTESIAN_POINT('Ctrl Pts',(4.77468047668128,0.786943861117909,-0.294161022167029));
#15734=CARTESIAN_POINT('Ctrl Pts',(4.80359287980309,0.739600872161782,-0.297170246366681));
#15735=CARTESIAN_POINT('Ctrl Pts',(4.82970438381255,0.690835765943307,-0.300179470566333));
#15736=CARTESIAN_POINT('Ctrl Pts',(4.85586519016987,0.641978584054687,-0.303194376622466));
#15737=CARTESIAN_POINT('Ctrl Pts',(4.87921431079296,0.59169439909078,-0.306209282678599));
#15738=CARTESIAN_POINT('Ctrl Pts',(4.89961605177496,0.54034100058517,-0.309224188734732));
#15739=CARTESIAN_POINT('Ctrl Pts',(4.91489844618696,0.501873553564261,-0.311482573619904));
#15740=CARTESIAN_POINT('Ctrl Pts',(4.92852803145527,0.462806618524378,-0.313740958505077));
#15741=CARTESIAN_POINT('Ctrl Pts',(4.94046634319924,0.423295325822175,-0.315999343390249));
#15742=CARTESIAN_POINT('Ctrl Pts',(4.95635677614093,0.370704008005316,-0.319005355826847));
#15743=CARTESIAN_POINT('Ctrl Pts',(4.96931596167814,0.317103188847384,-0.322011368263446));
#15744=CARTESIAN_POINT('Ctrl Pts',(4.97922093326692,0.26285117183618,-0.325017380700044));
#15745=CARTESIAN_POINT('Ctrl Pts',(4.98910798703044,0.208697295253879,-0.328017955341587));
#15746=CARTESIAN_POINT('Ctrl Pts',(4.99595169590336,0.153895075152804,-0.331018529983131));
#15747=CARTESIAN_POINT('Ctrl Pts',(4.99967913163957,0.0988169379286829,
-0.334019104624674));
#15748=CARTESIAN_POINT('Ctrl Pts',(5.00340281149231,0.0437942991970763,
-0.337016655791248));
#15749=CARTESIAN_POINT('Ctrl Pts',(5.00401640212075,-0.011503180103168,
-0.340014206957822));
#15750=CARTESIAN_POINT('Ctrl Pts',(5.00149850268767,-0.0666958106319766,
-0.343011758124395));
#15751=CARTESIAN_POINT('Ctrl Pts',(4.99898213816164,-0.121854795830687,
-0.346007481989072));
#15752=CARTESIAN_POINT('Ctrl Pts',(4.99333809084124,-0.176908530788052,
-0.349003205853748));
#15753=CARTESIAN_POINT('Ctrl Pts',(4.98459704397959,-0.231477520589845,
-0.351998929718424));
#15754=CARTESIAN_POINT('Ctrl Pts',(4.97585784659602,-0.286034964389003,
-0.354994019731608));
#15755=CARTESIAN_POINT('Ctrl Pts',(4.96402303449634,-0.340107343854895,
-0.357989109744792));
#15756=CARTESIAN_POINT('Ctrl Pts',(4.9491748277167,-0.39332281848687,-0.360984199757975));
#15757=CARTESIAN_POINT('Ctrl Pts',(4.93431305450028,-0.446586914772849,
-0.363982026310321));
#15758=CARTESIAN_POINT('Ctrl Pts',(4.91643252835284,-0.498992030536336,
-0.366979852862666));
#15759=CARTESIAN_POINT('Ctrl Pts',(4.89566567284574,-0.550180505371983,
-0.369977679415011));
#15760=CARTESIAN_POINT('Ctrl Pts',(4.87488947926561,-0.601391997737453,
-0.372976853977085));
#15761=CARTESIAN_POINT('Ctrl Pts',(4.851224596326,-0.651385278977384,-0.375976028539159));
#15762=CARTESIAN_POINT('Ctrl Pts',(4.82485070969782,-0.699824817840734,
-0.378975203101233));
#15763=CARTESIAN_POINT('Ctrl Pts',(4.79842676241049,-0.74835630049978,-0.381980070440316));
#15764=CARTESIAN_POINT('Ctrl Pts',(4.76928381965483,-0.795327698123873,
-0.384984937779399));
#15765=CARTESIAN_POINT('Ctrl Pts',(4.73764580991827,-0.840431150173138,
-0.387989805118483));
#15766=CARTESIAN_POINT('Ctrl Pts',(4.71304542864684,-0.875501691155599,
-0.390326263158259));
#15767=CARTESIAN_POINT('Ctrl Pts',(4.68693746454828,-0.909443422819982,
-0.392662721198036));
#15768=CARTESIAN_POINT('Ctrl Pts',(4.65944323801357,-0.942126352486538,
-0.394999179237812));
#15769=CARTESIAN_POINT('Ctrl Pts',(4.62401033794178,-0.984246140052329,
-0.398010265370414));
#15770=CARTESIAN_POINT('Ctrl Pts',(4.58612386983908,-1.02445232578511,-0.401021351503017));
#15771=CARTESIAN_POINT('Ctrl Pts',(4.54601836869901,-1.06244593853518,-0.404032437635619));
#15772=CARTESIAN_POINT('Ctrl Pts',(4.50598404157429,-1.10037212517412,-0.407038180085072));
#15773=CARTESIAN_POINT('Ctrl Pts',(4.46373887671099,-1.13609317132882,-0.410043922534525));
#15774=CARTESIAN_POINT('Ctrl Pts',(4.41955646896318,-1.16934442828839,-0.413049664983978));
#15775=CARTESIAN_POINT('Ctrl Pts',(4.37541771414053,-1.20256283247454,-0.416052437711841));
#15776=CARTESIAN_POINT('Ctrl Pts',(4.32934592773248,-1.2333159657241,-0.419055210439705));
#15777=CARTESIAN_POINT('Ctrl Pts',(4.28164882806824,-1.26137846942629,-0.422057983167568));
#15778=CARTESIAN_POINT('Ctrl Pts',(4.23398004890087,-1.28942431081455,-0.425058972977471));
#15779=CARTESIAN_POINT('Ctrl Pts',(4.18468832324541,-1.31478242218084,-0.428059962787374));
#15780=CARTESIAN_POINT('Ctrl Pts',(4.13410956048888,-1.33727124224653,-0.431060952597277));
#15781=CARTESIAN_POINT('Ctrl Pts',(4.08354088934381,-1.35975557528206,-0.434061343641582));
#15782=CARTESIAN_POINT('Ctrl Pts',(4.03168617302838,-1.37937153969727,-0.437061734685886));
#15783=CARTESIAN_POINT('Ctrl Pts',(3.97890298125976,-1.39598496099436,-0.44006212573019));
#15784=CARTESIAN_POINT('Ctrl Pts',(3.92607143124894,-1.41261360296728,-0.443065265635106));
#15785=CARTESIAN_POINT('Ctrl Pts',(3.87231021076956,-1.42623404721551,-0.446068405540022));
#15786=CARTESIAN_POINT('Ctrl Pts',(3.81799237375506,-1.43676193511395,-0.449071545444937));
#15787=CARTESIAN_POINT('Ctrl Pts',(3.76364988103339,-1.44729460178371,-0.452076048521551));
#15788=CARTESIAN_POINT('Ctrl Pts',(3.70875079196186,-1.45473184269594,-0.455080551598165));
#15789=CARTESIAN_POINT('Ctrl Pts',(3.65367540862629,-1.45904097813658,-0.458085054674778));
#15790=CARTESIAN_POINT('Ctrl Pts',(3.59849643401324,-1.46335821862921,-0.461095208920627));
#15791=CARTESIAN_POINT('Ctrl Pts',(3.54314103162798,-1.46453558876919,-0.464105363166476));
#15792=CARTESIAN_POINT('Ctrl Pts',(3.48799047191199,-1.46259258017967,-0.467115517412325));
#15793=CARTESIAN_POINT('Ctrl Pts',(3.44595179011842,-1.46111151597584,-0.469410016636675));
#15794=CARTESIAN_POINT('Ctrl Pts',(3.4040321614047,-1.4578185062013,-0.471704515861025));
#15795=CARTESIAN_POINT('Ctrl Pts',(3.36239712990682,-1.45274226044149,-0.473999015085375));
#15796=CARTESIAN_POINT('Ctrl Pts',(3.30776586996789,-1.4460814824466,-0.477009734161245));
#15797=CARTESIAN_POINT('Ctrl Pts',(3.25339662216762,-1.43632083089672,-0.480020453237115));
#15798=CARTESIAN_POINT('Ctrl Pts',(3.19966786019915,-1.42349338547934,-0.483031172312986));
#15799=CARTESIAN_POINT('Ctrl Pts',(3.14603419204231,-1.41068864318471,-0.486036562757743));
#15800=CARTESIAN_POINT('Ctrl Pts',(3.09303926940122,-1.39482800039746,-0.489041953202501));
#15801=CARTESIAN_POINT('Ctrl Pts',(3.04105416113814,-1.37599600440926,-0.492047343647258));
#15802=CARTESIAN_POINT('Ctrl Pts',(2.98912025649314,-1.35718255731635,-0.495049773881494));
#15803=CARTESIAN_POINT('Ctrl Pts',(2.93819468975831,-1.33540373367036,-0.498052204115729));
#15804=CARTESIAN_POINT('Ctrl Pts',(2.88863426307353,-1.31079412708367,-0.501054634349964));
#15805=CARTESIAN_POINT('Ctrl Pts',(2.8391030990692,-1.28619905110339,-0.504055291815835));
#15806=CARTESIAN_POINT('Ctrl Pts',(2.79093594931848,-1.25877673941732,-0.507055949281707));
#15807=CARTESIAN_POINT('Ctrl Pts',(2.74446833136837,-1.22870932450711,-0.510056606747578));
#15808=CARTESIAN_POINT('Ctrl Pts',(2.6980098185465,-1.19864780117648,-0.513056676247631));
#15809=CARTESIAN_POINT('Ctrl Pts',(2.65325061907654,-1.16594249059498,-0.516056745747683));
#15810=CARTESIAN_POINT('Ctrl Pts',(2.61049839019024,-1.13081955362503,-0.519056815247735));
#15811=CARTESIAN_POINT('Ctrl Pts',(2.56770671146066,-1.09566420678089,-0.522059653077644));
#15812=CARTESIAN_POINT('Ctrl Pts',(2.52692611194843,-1.05808711242691,-0.525062490907552));
#15813=CARTESIAN_POINT('Ctrl Pts',(2.48843098092148,-1.01835461414557,-0.528065328737461));
#15814=CARTESIAN_POINT('Ctrl Pts',(2.44991824179449,-0.978603941778695,
-0.531069540098709));
#15815=CARTESIAN_POINT('Ctrl Pts',(2.41369340085686,-0.936696300222253,
-0.534073751459957));
#15816=CARTESIAN_POINT('Ctrl Pts',(2.37999151608081,-0.892932330640086,
-0.537077962821206));
#15817=CARTESIAN_POINT('Ctrl Pts',(2.34622600212414,-0.849085734654586,
-0.540087846135478));
#15818=CARTESIAN_POINT('Ctrl Pts',(2.31499325836578,-0.803376246283152,
-0.543097729449751));
#15819=CARTESIAN_POINT('Ctrl Pts',(2.28648517007055,-0.756133814009735,
-0.546107612764024));
#15820=CARTESIAN_POINT('Ctrl Pts',(2.26472839905209,-0.720079387256038,
-0.548404692153662));
#15821=CARTESIAN_POINT('Ctrl Pts',(2.24455769051474,-0.68313273160179,-0.550701771543299));
#15822=CARTESIAN_POINT('Ctrl Pts',(2.22603962976519,-0.645448728799149,
-0.552998850932937));
#15823=CARTESIAN_POINT('Ctrl Pts',(2.20008110709051,-0.592623486758152,
-0.556218885051406));
#15824=CARTESIAN_POINT('Ctrl Pts',(2.17727459283289,-0.538151764158661,
-0.559438919169876));
#15825=CARTESIAN_POINT('Ctrl Pts',(2.15781501561044,-0.482417050053909,
-0.562658953288345));
#15826=CARTESIAN_POINT('Ctrl Pts',(2.13840278776736,-0.426817950618098,
-0.565871152364185));
#15827=CARTESIAN_POINT('Ctrl Pts',(2.12232144068049,-0.369962354887564,
-0.569083351440025));
#15828=CARTESIAN_POINT('Ctrl Pts',(2.10971870822468,-0.312255074337636,
-0.572295550515864));
#15829=CARTESIAN_POINT('Ctrl Pts',(2.09716077482401,-0.254752926416818,
-0.575496331156537));
#15830=CARTESIAN_POINT('Ctrl Pts',(2.0880569275909,-0.196405520176387,-0.578697111797209));
#15831=CARTESIAN_POINT('Ctrl Pts',(2.08250507126076,-0.137631807827395,
-0.581897892437881));
#15832=CARTESIAN_POINT('Ctrl Pts',(2.0781993490831,-0.092050066932825,-0.584380246333738));
#15833=CARTESIAN_POINT('Ctrl Pts',(2.07602910338516,-0.0462123413419456,
-0.586862600229595));
#15834=CARTESIAN_POINT('Ctrl Pts',(2.07601908529222,-0.000319471822342703,
-0.589344954125452));
#15835=CARTESIAN_POINT('Origin',(3.53951905042299,8.32667268468867E-16,
0.));
#15836=CARTESIAN_POINT('',(2.07601962146617,0.00129284301226723,-1.1606550458429));
#15837=CARTESIAN_POINT('',(2.07601961090303,0.00128082971605478,-1.08934495412291));
#15838=CARTESIAN_POINT('',(2.07601905042299,1.01189432752408E-15,0.));
#15839=CARTESIAN_POINT('Ctrl Pts',(2.0758314534516,0.00129136347877342,
-1.16065495629856));
#15840=CARTESIAN_POINT('Ctrl Pts',(2.07926274667652,-0.376316335126734,
-1.14010981557906));
#15841=CARTESIAN_POINT('Ctrl Pts',(2.42031344695339,-1.24341589865127,-1.09323139624372));
#15842=CARTESIAN_POINT('Ctrl Pts',(3.87665396597672,-1.6937405805654,-1.0200196982925));
#15843=CARTESIAN_POINT('Ctrl Pts',(5.14228190560365,-0.643094266804824,
-0.941019862444937));
#15844=CARTESIAN_POINT('Ctrl Pts',(4.95387049003743,0.990974037173808,-0.862020026597378));
#15845=CARTESIAN_POINT('Ctrl Pts',(3.48234893238356,1.72601944824263,-0.783020190749813));
#15846=CARTESIAN_POINT('Ctrl Pts',(2.27614682897861,1.02013058486133,-0.715898530498322));
#15847=CARTESIAN_POINT('Ctrl Pts',(2.07889778574151,0.266425253906884,-0.675110148862687));
#15848=CARTESIAN_POINT('Ctrl Pts',(2.07827644886075,-0.000378700063536769,
-0.660655045842906));
#15849=CARTESIAN_POINT('Ctrl Pts',(2.0760190852921,-0.000319471237557788,
-0.589344954157083));
#15850=CARTESIAN_POINT('Ctrl Pts',(2.07600660206653,0.0568662720460612,
-0.592438141706959));
#15851=CARTESIAN_POINT('Ctrl Pts',(2.07935021510889,0.114012335576273,-0.595531329256835));
#15852=CARTESIAN_POINT('Ctrl Pts',(2.08601001953359,0.170715398025394,-0.598624516806711));
#15853=CARTESIAN_POINT('Ctrl Pts',(2.0926839307849,0.227538569147198,-0.601724256359864));
#15854=CARTESIAN_POINT('Ctrl Pts',(2.10268800075576,0.283916388418001,-0.604823995913016));
#15855=CARTESIAN_POINT('Ctrl Pts',(2.11593075498151,0.339453406349121,-0.607923735466169));
#15856=CARTESIAN_POINT('Ctrl Pts',(2.12918839109451,0.3950528354392,-0.611026958431741));
#15857=CARTESIAN_POINT('Ctrl Pts',(2.14569182168071,0.449809122313612,-0.614130181397313));
#15858=CARTESIAN_POINT('Ctrl Pts',(2.16529992555855,0.503342872063173,-0.617233404362885));
#15859=CARTESIAN_POINT('Ctrl Pts',(2.18495683587771,0.557009872423416,-0.620344351546491));
#15860=CARTESIAN_POINT('Ctrl Pts',(2.20773366690345,0.609447815871552,-0.623455298730097));
#15861=CARTESIAN_POINT('Ctrl Pts',(2.2334416826662,0.660298538112488,-0.626566245913703));
#15862=CARTESIAN_POINT('Ctrl Pts',(2.24840575064842,0.689897620032354,-0.628377059535968));
#15863=CARTESIAN_POINT('Ctrl Pts',(2.2643620934822,0.718959412202586,-0.630187873158234));
#15864=CARTESIAN_POINT('Ctrl Pts',(2.28126677168813,0.747417857064255,-0.631998686780499));
#15865=CARTESIAN_POINT('Ctrl Pts',(2.30936925475481,0.794727421617148,-0.635008998987377));
#15866=CARTESIAN_POINT('Ctrl Pts',(2.34020265453032,0.840549132069048,-0.638019311194254));
#15867=CARTESIAN_POINT('Ctrl Pts',(2.37358438157033,0.884549940912008,-0.641029623401131));
#15868=CARTESIAN_POINT('Ctrl Pts',(2.40690680684453,0.928472583467816,-0.644034587867034));
#15869=CARTESIAN_POINT('Ctrl Pts',(2.44276825883579,0.970580326613127,-0.647039552332936));
#15870=CARTESIAN_POINT('Ctrl Pts',(2.4809420158884,1.01056761869553,-0.650044516798839));
#15871=CARTESIAN_POINT('Ctrl Pts',(2.51907802320109,1.05051536764692,-0.653046509678085));
#15872=CARTESIAN_POINT('Ctrl Pts',(2.55952144303372,1.08834643934595,-0.656048502557331));
#15873=CARTESIAN_POINT('Ctrl Pts',(2.60200548448817,1.12378848707761,-0.659050495436577));
#15874=CARTESIAN_POINT('Ctrl Pts',(2.64446428811698,1.15920948030996,-0.662050704969176));
#15875=CARTESIAN_POINT('Ctrl Pts',(2.68896090595273,1.19224392497055,-0.665050914501775));
#15876=CARTESIAN_POINT('Ctrl Pts',(2.73519359964849,1.22265809580455,-0.668051124034374));
#15877=CARTESIAN_POINT('Ctrl Pts',(2.78141708196249,1.25306620693239,-0.671050735806533));
#15878=CARTESIAN_POINT('Ctrl Pts',(2.82937551230304,1.28085479098956,-0.674050347578691));
#15879=CARTESIAN_POINT('Ctrl Pts',(2.87873806733833,1.30583335169296,-0.67704995935085));
#15880=CARTESIAN_POINT('Ctrl Pts',(2.92814598812326,1.33083486848384,-0.680052327861118));
#15881=CARTESIAN_POINT('Ctrl Pts',(2.9789601395582,1.35302096349533,-0.683054696371386));
#15882=CARTESIAN_POINT('Ctrl Pts',(3.03082631367031,1.37224777266173,-0.686057064881654));
#15883=CARTESIAN_POINT('Ctrl Pts',(3.08271609195816,1.39148333190446,-0.68906079976288));
#15884=CARTESIAN_POINT('Ctrl Pts',(3.13565834171609,1.40775676518443,-0.692064534644105));
#15885=CARTESIAN_POINT('Ctrl Pts',(3.18928329956362,1.42097402116294,-0.695068269525331));
#15886=CARTESIAN_POINT('Ctrl Pts',(3.24300941273362,1.43421620948349,-0.698077670495309));
#15887=CARTESIAN_POINT('Ctrl Pts',(3.29742028630907,1.44439060667992,-0.701087071465287));
#15888=CARTESIAN_POINT('Ctrl Pts',(3.35213671825168,1.45145448140479,-0.704096472435265));
#15889=CARTESIAN_POINT('Ctrl Pts',(3.39396736421813,1.45685480507862,-0.706397155832865));
#15890=CARTESIAN_POINT('Ctrl Pts',(3.43597638473564,1.46043822272066,-0.708697839230464));
#15891=CARTESIAN_POINT('Ctrl Pts',(3.47799436027132,1.46220619698514,-0.710998522628063));
#15892=CARTESIAN_POINT('Ctrl Pts',(3.53297023865442,1.46451939596508,-0.714008712649165));
#15893=CARTESIAN_POINT('Ctrl Pts',(3.58819220241263,1.46373267579113,-0.717018902670267));
#15894=CARTESIAN_POINT('Ctrl Pts',(3.64328157668237,1.45981697076869,-0.720029092691368));
#15895=CARTESIAN_POINT('Ctrl Pts',(3.69827309153389,1.45590822150897,-0.723033935484477));
#15896=CARTESIAN_POINT('Ctrl Pts',(3.75313196180096,1.44888155494064,-0.726038778277585));
#15897=CARTESIAN_POINT('Ctrl Pts',(3.80747842507802,1.43875989085549,-0.729043621070694));
#15898=CARTESIAN_POINT('Ctrl Pts',(3.86177115079996,1.42864823502936,-0.732045492687842));
#15899=CARTESIAN_POINT('Ctrl Pts',(3.91555195660093,1.41544774026222,-0.73504736430499));
#15900=CARTESIAN_POINT('Ctrl Pts',(3.96844699483531,1.39923302866328,-0.738049235922138));
#15901=CARTESIAN_POINT('Ctrl Pts',(4.02131062043758,1.3830279464509,-0.741049324825975));
#15902=CARTESIAN_POINT('Ctrl Pts',(4.07328901720444,1.36381234986653,-0.744049413729812));
#15903=CARTESIAN_POINT('Ctrl Pts',(4.12402158794504,1.34171123332492,-0.747049502633649));
#15904=CARTESIAN_POINT('Ctrl Pts',(4.17474406482655,1.319614514068,-0.750048994633481));
#15905=CARTESIAN_POINT('Ctrl Pts',(4.22422072407499,1.29463362581086,-0.753048486633313));
#15906=CARTESIAN_POINT('Ctrl Pts',(4.27211128175114,1.26694154269155,-0.756047978633146));
#15907=CARTESIAN_POINT('Ctrl Pts',(4.32004589092698,1.23922398737375,-0.759050229676248));
#15908=CARTESIAN_POINT('Ctrl Pts',(4.36639102558828,1.20879051971965,-0.762052480719351));
#15909=CARTESIAN_POINT('Ctrl Pts',(4.41083268022885,1.17585917886223,-0.765054731762454));
#15910=CARTESIAN_POINT('Ctrl Pts',(4.45529457724241,1.14291283837235,-0.768058350276816));
#15911=CARTESIAN_POINT('Ctrl Pts',(4.49785085945377,1.10746669525194,-0.771061968791179));
#15912=CARTESIAN_POINT('Ctrl Pts',(4.53822074234987,1.06977903351225,-0.774065587305542));
#15913=CARTESIAN_POINT('Ctrl Pts',(4.57866682389853,1.03202023584555,-0.777074875186947));
#15914=CARTESIAN_POINT('Ctrl Pts',(4.61691789626551,0.992011850335824,-0.780084163068352));
#15915=CARTESIAN_POINT('Ctrl Pts',(4.65273100036834,0.95004810641297,-0.783093450949757));
#15916=CARTESIAN_POINT('Ctrl Pts',(4.68012243889575,0.917952387797172,-0.785395086791713));
#15917=CARTESIAN_POINT('Ctrl Pts',(4.70608847507237,0.884713570282592,-0.787696722633669));
#15918=CARTESIAN_POINT('Ctrl Pts',(4.73053765491137,0.850474534458592,-0.789998358475625));
#15919=CARTESIAN_POINT('Ctrl Pts',(4.7625119027294,0.805697268975813,-0.793008401155264));
#15920=CARTESIAN_POINT('Ctrl Pts',(4.79202470621447,0.759020214552427,-0.796018443834904));
#15921=CARTESIAN_POINT('Ctrl Pts',(4.8188448036111,0.710744586493403,-0.799028486514543));
#15922=CARTESIAN_POINT('Ctrl Pts',(4.84561721419754,0.662554793719687,-0.802033177262316));
#15923=CARTESIAN_POINT('Ctrl Pts',(4.86970616548129,0.612772525820783,-0.805037868010089));
#15924=CARTESIAN_POINT('Ctrl Pts',(4.89092333713011,0.561728318557669,-0.808042558757862));
#15925=CARTESIAN_POINT('Ctrl Pts',(4.91211950875181,0.51073463309616,-0.811044275566025));
#15926=CARTESIAN_POINT('Ctrl Pts',(4.93044932963856,0.458481967818713,-0.814045992374187));
#15927=CARTESIAN_POINT('Ctrl Pts',(4.94577101057565,0.405324159860732,-0.81704770918235));
#15928=CARTESIAN_POINT('Ctrl Pts',(4.96108357933088,0.35219796616328,-0.820047640795433));
#15929=CARTESIAN_POINT('Ctrl Pts',(4.97339140809001,0.298168203226823,-0.823047572408517));
#15930=CARTESIAN_POINT('Ctrl Pts',(4.98260213412084,0.243605138585195,-0.8260475040216));
#15931=CARTESIAN_POINT('Ctrl Pts',(4.99181102070509,0.189052970570174,-0.829046836527304));
#15932=CARTESIAN_POINT('Ctrl Pts',(4.99792394503188,0.133968232852556,-0.832046169033009));
#15933=CARTESIAN_POINT('Ctrl Pts',(5.00089982697954,0.0787304001702604,
-0.835045501538713));
#15934=CARTESIAN_POINT('Ctrl Pts',(5.00387844426227,0.0234417946470128,
-0.838047590934485));
#15935=CARTESIAN_POINT('Ctrl Pts',(5.00371422988948,-0.0319996584614357,
-0.841049680330258));
#15936=CARTESIAN_POINT('Ctrl Pts',(5.00041820516007,-0.0872118666724785,
-0.84405176972603));
#15937=CARTESIAN_POINT('Ctrl Pts',(4.99712068065652,-0.142449197826518,
-0.847055225147961));
#15938=CARTESIAN_POINT('Ctrl Pts',(4.9906885665012,-0.197456550651928,-0.850058680569893));
#15939=CARTESIAN_POINT('Ctrl Pts',(4.98118474231087,-0.251857663837041,
-0.853062135991825));
#15940=CARTESIAN_POINT('Ctrl Pts',(4.97166297965463,-0.306361459110359,
-0.856071260435152));
#15941=CARTESIAN_POINT('Ctrl Pts',(4.95905804543009,-0.360256213337277,
-0.859080384878479));
#15942=CARTESIAN_POINT('Ctrl Pts',(4.94348359275872,-0.413177702525217,
-0.862089509321806));
#15943=CARTESIAN_POINT('Ctrl Pts',(4.93156440168926,-0.453678730370079,
-0.864392404322266));
#15944=CARTESIAN_POINT('Ctrl Pts',(4.91790705213559,-0.493609960797262,
-0.866695299322727));
#15945=CARTESIAN_POINT('Ctrl Pts',(4.90258136217741,-0.532816463967382,
-0.868998194323188));
#15946=CARTESIAN_POINT('Ctrl Pts',(4.88254883971817,-0.584064085278177,
-0.872008355428095));
#15947=CARTESIAN_POINT('Ctrl Pts',(4.85958004900699,-0.634288036042029,
-0.875018516533003));
#15948=CARTESIAN_POINT('Ctrl Pts',(4.83380094152019,-0.683130028894825,
-0.87802867763791));
#15949=CARTESIAN_POINT('Ctrl Pts',(4.80806764621134,-0.731885224403334,
-0.881033489370802));
#15950=CARTESIAN_POINT('Ctrl Pts',(4.77953418972623,-0.779262872458853,
-0.884038301103693));
#15951=CARTESIAN_POINT('Ctrl Pts',(4.74837454173321,-0.824924633605481,
-0.887043112836585));
#15952=CARTESIAN_POINT('Ctrl Pts',(4.71724571796304,-0.870541224527396,
-0.890044952103724));
#15953=CARTESIAN_POINT('Ctrl Pts',(4.68349614525756,-0.914444856972351,
-0.893046791370863));
#15954=CARTESIAN_POINT('Ctrl Pts',(4.64734473137058,-0.956323434112651,
-0.896048630638002));
#15955=CARTESIAN_POINT('Ctrl Pts',(4.6112148016848,-0.99817712349115,-0.899048685960563));
#15956=CARTESIAN_POINT('Ctrl Pts',(4.57268620437191,-1.03800774393927,-0.902048741283124));
#15957=CARTESIAN_POINT('Ctrl Pts',(4.53201861258053,-1.07553561964125,-0.905048796605685));
#15958=CARTESIAN_POINT('Ctrl Pts',(4.49135912810842,-1.11305601394449,-0.908048253849891));
#15959=CARTESIAN_POINT('Ctrl Pts',(4.44856188390119,-1.14827421724515,-0.911047711094098));
#15960=CARTESIAN_POINT('Ctrl Pts',(4.40392228318567,-1.18094847524752,-0.914047168338305));
#15961=CARTESIAN_POINT('Ctrl Pts',(4.35924164396133,-1.21365277166428,-0.917049383072511));
#15962=CARTESIAN_POINT('Ctrl Pts',(4.31271569143074,-1.24380813772664,-0.920051597806717));
#15963=CARTESIAN_POINT('Ctrl Pts',(4.26467048770375,-1.27121502626804,-0.923053812540923));
#15964=CARTESIAN_POINT('Ctrl Pts',(4.21660341469196,-1.2986343899163,-0.926057393827541));
#15965=CARTESIAN_POINT('Ctrl Pts',(4.16701618560658,-1.32330254651983,-0.929060975114158));
#15966=CARTESIAN_POINT('Ctrl Pts',(4.11625831286334,-1.34506656830053,-0.932064556400776));
#15967=CARTESIAN_POINT('Ctrl Pts',(4.06540465061443,-1.36687166282078,-0.935073806001513));
#15968=CARTESIAN_POINT('Ctrl Pts',(4.0133764290597,-1.38576149341699,-0.93808305560225));
#15969=CARTESIAN_POINT('Ctrl Pts',(3.96054082058473,-1.40163223387944,-0.941092305202986));
#15970=CARTESIAN_POINT('Ctrl Pts',(3.92012452316368,-1.41377246629725,-0.943394213525574));
#15971=CARTESIAN_POINT('Ctrl Pts',(3.87923617383144,-1.4241471248127,-0.945696121848163));
#15972=CARTESIAN_POINT('Ctrl Pts',(3.838043453164,-1.43273006214294,-0.947998030170751));
#15973=CARTESIAN_POINT('Ctrl Pts',(3.78417701582501,-1.44395370186357,-0.951008163961618));
#15974=CARTESIAN_POINT('Ctrl Pts',(3.72956356181104,-1.45215886917292,-0.954018297752485));
#15975=CARTESIAN_POINT('Ctrl Pts',(3.6745719787831,-1.45725528187115,-0.957028431543353));
#15976=CARTESIAN_POINT('Ctrl Pts',(3.6196781255751,-1.46234263733792,-0.960033215791305));
#15977=CARTESIAN_POINT('Ctrl Pts',(3.56440799855432,-1.4643321538756,-0.963038000039257));
#15978=CARTESIAN_POINT('Ctrl Pts',(3.5091400161177,-1.46318466513105,-0.966042784287209));
#15979=CARTESIAN_POINT('Ctrl Pts',(3.45392670874686,-1.46203831156496,-0.969044595986333));
#15980=CARTESIAN_POINT('Ctrl Pts',(3.39871606716211,-1.45776111121616,-0.972046407685458));
#15981=CARTESIAN_POINT('Ctrl Pts',(3.34388908541655,-1.45036587342352,-0.975048219384582));
#15982=CARTESIAN_POINT('Ctrl Pts',(3.28909468735574,-1.44297503062199,-0.978048247106494));
#15983=CARTESIAN_POINT('Ctrl Pts',(3.23468401953469,-1.43246989369792,-0.981048274828406));
#15984=CARTESIAN_POINT('Ctrl Pts',(3.18103319700848,-1.41891512885784,-0.984048302550318));
#15985=CARTESIAN_POINT('Ctrl Pts',(3.12739306986512,-1.40536306618322,-0.987047732211594));
#15986=CARTESIAN_POINT('Ctrl Pts',(3.07451299892883,-1.38876271224259,-0.99004716187287));
#15987=CARTESIAN_POINT('Ctrl Pts',(3.02275686200019,-1.36922937837912,-0.993046591534146));
#15988=CARTESIAN_POINT('Ctrl Pts',(2.97095313936148,-1.34967808514663,-0.996048778935832));
#15989=CARTESIAN_POINT('Ctrl Pts',(2.9202759104247,-1.32718861132417,-0.999050966337517));
#15990=CARTESIAN_POINT('Ctrl Pts',(2.87107045544903,-1.30192500777784,-1.0020531537392));
#15991=CARTESIAN_POINT('Ctrl Pts',(2.82184260126877,-1.2766499037866,-1.00505670779038));
#15992=CARTESIAN_POINT('Ctrl Pts',(2.77408831276069,-1.24859842065337,-1.00806026184155));
#15993=CARTESIAN_POINT('Ctrl Pts',(2.72812663831067,-1.21797972214916,-1.01106381589272));
#15994=CARTESIAN_POINT('Ctrl Pts',(2.68207821720197,-1.18730323484983,-1.01407303875995));
#15995=CARTESIAN_POINT('Ctrl Pts',(2.63782959208944,-1.15405017102663,-1.01708226162718));
#15996=CARTESIAN_POINT('Ctrl Pts',(2.59566833675573,-1.11847131403081,-1.02009148449441));
#15997=CARTESIAN_POINT('Ctrl Pts',(2.56341397212314,-1.09125264092274,-1.02239361166905));
#15998=CARTESIAN_POINT('Ctrl Pts',(2.53238062274949,-1.06267364595761,-1.02469573884368));
#15999=CARTESIAN_POINT('Ctrl Pts',(2.50268184001776,-1.03286051774627,-1.02699786601831));
#16000=CARTESIAN_POINT('Ctrl Pts',(2.46440187434825,-0.994433167550155,
-1.02996517110983));
#16001=CARTESIAN_POINT('Ctrl Pts',(2.42816981499792,-0.953782886790655,
-1.03293247620135));
#16002=CARTESIAN_POINT('Ctrl Pts',(2.39425915283785,-0.911159709920974,
-1.03589978129287));
#16003=CARTESIAN_POINT('Ctrl Pts',(2.3603968099121,-0.868597266730304,-1.03886285827733));
#16004=CARTESIAN_POINT('Ctrl Pts',(2.32884965458755,-0.824067911680846,
-1.04182593526179));
#16005=CARTESIAN_POINT('Ctrl Pts',(2.29985429238519,-0.777858301799942,
-1.04478901224625));
#16006=CARTESIAN_POINT('Ctrl Pts',(2.27088801612938,-0.73169504589225,-1.04774911689679));
#16007=CARTESIAN_POINT('Ctrl Pts',(2.24446875270438,-0.683855331074661,
-1.05070922154733));
#16008=CARTESIAN_POINT('Ctrl Pts',(2.22079118378885,-0.634656650294132,
-1.05366932619786));
#16009=CARTESIAN_POINT('Ctrl Pts',(2.19701071433124,-0.585244156560942,
-1.05664229519161));
#16010=CARTESIAN_POINT('Ctrl Pts',(2.17599612692328,-0.534461322803746,
-1.05961526418537));
#16011=CARTESIAN_POINT('Ctrl Pts',(2.15789816163111,-0.482655124963916,
-1.06258823317912));
#16012=CARTESIAN_POINT('Ctrl Pts',(2.13988519957987,-0.431092252528085,
-1.06554723861424));
#16013=CARTESIAN_POINT('Ctrl Pts',(2.12476167223662,-0.378516136810143,
-1.06850624404935));
#16014=CARTESIAN_POINT('Ctrl Pts',(2.11262697227371,-0.325286408131106,
-1.07146524948447));
#16015=CARTESIAN_POINT('Ctrl Pts',(2.10040637676334,-0.27167989249402,-1.07444520025754));
#16016=CARTESIAN_POINT('Ctrl Pts',(2.09121722873746,-0.217411015904341,
-1.07742515103061));
#16017=CARTESIAN_POINT('Ctrl Pts',(2.08510855901616,-0.162856908007408,
-1.08040510180369));
#16018=CARTESIAN_POINT('Ctrl Pts',(2.07899988929486,-0.108302800110476,
-1.08338505257676));
#16019=CARTESIAN_POINT('Ctrl Pts',(2.07597169914304,-0.0534640227951241,
-1.08636500334984));
#16020=CARTESIAN_POINT('Ctrl Pts',(2.07601961090303,0.00128082971604727,
-1.08934495412291));
#16021=CARTESIAN_POINT('Origin',(3.53951905042299,8.32667268468867E-16,
0.));
#16022=CARTESIAN_POINT('',(2.07601930830571,-0.000868805298815955,-1.6606550458429));
#16023=CARTESIAN_POINT('',(2.07601934240537,-0.000924463273316875,-1.58934495415708));
#16024=CARTESIAN_POINT('',(2.07601905042299,1.01189432752408E-15,0.));
#16025=CARTESIAN_POINT('Ctrl Pts',(2.07601930830571,-0.000868805298815955,
-1.6606550458429));
#16026=CARTESIAN_POINT('Ctrl Pts',(2.07605060159967,-0.0535822587060049,
-1.6577761589196));
#16027=CARTESIAN_POINT('Ctrl Pts',(2.07892976381197,-0.106209644322961,
-1.6548972719963));
#16028=CARTESIAN_POINT('Ctrl Pts',(2.08462993641652,-0.158524180948704,
-1.652018385073));
#16029=CARTESIAN_POINT('Ctrl Pts',(2.09058996653434,-0.213223614723923,
-1.64900825644023));
#16030=CARTESIAN_POINT('Ctrl Pts',(2.09965160842919,-0.267701391860388,
-1.64599812780745));
#16031=CARTESIAN_POINT('Ctrl Pts',(2.11178681332887,-0.321578775982193,
-1.64298799917468));
#16032=CARTESIAN_POINT('Ctrl Pts',(2.1239004505508,-0.37536040481447,-1.63998322038848));
#16033=CARTESIAN_POINT('Ctrl Pts',(2.13907669513055,-0.428543247192843,
-1.63697844160228));
#16034=CARTESIAN_POINT('Ctrl Pts',(2.15723593766214,-0.480755287205635,
-1.63397366281607));
#16035=CARTESIAN_POINT('Ctrl Pts',(2.17537721463252,-0.532915672057198,
-1.63097185676054));
#16036=CARTESIAN_POINT('Ctrl Pts',(2.19649547077319,-0.584106660788554,
-1.62797005070501));
#16037=CARTESIAN_POINT('Ctrl Pts',(2.22046086605756,-0.633969838603209,
-1.62496824464948));
#16038=CARTESIAN_POINT('Ctrl Pts',(2.24441201730657,-0.683803379816431,
-1.62196822274276));
#16039=CARTESIAN_POINT('Ctrl Pts',(2.27120672528916,-0.732310199307741,
-1.61896820083604));
#16040=CARTESIAN_POINT('Ctrl Pts',(2.30066733449277,-0.77915253701489,-1.61596817892933));
#16041=CARTESIAN_POINT('Ctrl Pts',(2.33012206907523,-0.825985534080597,
-1.61296875524486));
#16042=CARTESIAN_POINT('Ctrl Pts',(2.36224136814464,-0.871154261717106,
-1.6099693315604));
#16043=CARTESIAN_POINT('Ctrl Pts',(2.39680318556378,-0.91434823902005,-1.60696990787594));
#16044=CARTESIAN_POINT('Ctrl Pts',(2.43139677757535,-0.957581926937968,
-1.60396772665521));
#16045=CARTESIAN_POINT('Ctrl Pts',(2.46843704357936,-0.998836824150021,
-1.60096554543448));
#16046=CARTESIAN_POINT('Ctrl Pts',(2.50766132347454,-1.03783518987206,-1.59796336421375));
#16047=CARTESIAN_POINT('Ctrl Pts',(2.54690345739522,-1.07685130678846,-1.59495981646646));
#16048=CARTESIAN_POINT('Ctrl Pts',(2.58833119117959,-1.11360849360256,-1.59195626871918));
#16049=CARTESIAN_POINT('Ctrl Pts',(2.63164705772915,-1.14786789086641,-1.58895272097189));
#16050=CARTESIAN_POINT('Ctrl Pts',(2.67504467569945,-1.18219194698678,-1.58594350453285));
#16051=CARTESIAN_POINT('Ctrl Pts',(2.72033711193837,-1.21400849197881,-1.58293428809381));
#16052=CARTESIAN_POINT('Ctrl Pts',(2.76719703399693,-1.24312145542726,-1.57992507165477));
#16053=CARTESIAN_POINT('Ctrl Pts',(2.80304679857745,-1.26539406792891,-1.57762289751166));
#16054=CARTESIAN_POINT('Ctrl Pts',(2.83981335928125,-1.28608518774595,-1.57532072336855));
#16055=CARTESIAN_POINT('Ctrl Pts',(2.8773416185596,-1.3051257788929,-1.57301854922543));
#16056=CARTESIAN_POINT('Ctrl Pts',(2.92641040360403,-1.33002164915373,-1.57000842058277));
#16057=CARTESIAN_POINT('Ctrl Pts',(2.97698825375561,-1.35219872375612,-1.5669982919401));
#16058=CARTESIAN_POINT('Ctrl Pts',(3.02874264136784,-1.37147355423017,-1.56398816329744));
#16059=CARTESIAN_POINT('Ctrl Pts',(3.0804050468403,-1.39071412789561,-1.56098338450212));
#16060=CARTESIAN_POINT('Ctrl Pts',(3.13323934918813,-1.40706251090189,-1.55797860570681));
#16061=CARTESIAN_POINT('Ctrl Pts',(3.18689047680632,-1.42038211023269,-1.55497382691149));
#16062=CARTESIAN_POINT('Ctrl Pts',(3.24048852551612,-1.43368853202512,-1.55197202084733));
#16063=CARTESIAN_POINT('Ctrl Pts',(3.29490128862576,-1.44397197940149,-1.54897021478317));
#16064=CARTESIAN_POINT('Ctrl Pts',(3.34975764001591,-1.45114536043786,-1.54596840871901));
#16065=CARTESIAN_POINT('Ctrl Pts',(3.40458138706076,-1.45831447791337,-1.54296838680416));
#16066=CARTESIAN_POINT('Ctrl Pts',(3.4598476772011,-1.46237712454654,-1.5399683648893));
#16067=CARTESIAN_POINT('Ctrl Pts',(3.51517655701911,-1.46329754083538,-1.53696834297445));
#16068=CARTESIAN_POINT('Ctrl Pts',(3.57049440391932,-1.46421777358758,-1.53396891928236));
#16069=CARTESIAN_POINT('Ctrl Pts',(3.62587428796392,-1.46199701157718,-1.53096949559027));
#16070=CARTESIAN_POINT('Ctrl Pts',(3.68093484790044,-1.45665157886978,-1.52797007189817));
#16071=CARTESIAN_POINT('Ctrl Pts',(3.73604602804309,-1.4513012318116,-1.52496789067064));
#16072=CARTESIAN_POINT('Ctrl Pts',(3.79083677078416,-1.44282052595196,-1.5219657094431));
#16073=CARTESIAN_POINT('Ctrl Pts',(3.84493094429205,-1.43127768971759,-1.51896352821556));
#16074=CARTESIAN_POINT('Ctrl Pts',(3.8990497402643,-1.41972959944095,-1.51595998046192));
#16075=CARTESIAN_POINT('Ctrl Pts',(3.9524708246704,-1.40511673990348,-1.51295643270828));
#16076=CARTESIAN_POINT('Ctrl Pts',(4.00483161143695,-1.38755773593845,-1.50995288495463));
#16077=CARTESIAN_POINT('Ctrl Pts',(4.05729122037734,-1.36996559230823,-1.50694366851004));
#16078=CARTESIAN_POINT('Ctrl Pts',(4.1086860425283,-1.34941639313085,-1.50393445206544));
#16079=CARTESIAN_POINT('Ctrl Pts',(4.15867301047219,-1.32607715603406,-1.50092523562084));
#16080=CARTESIAN_POINT('Ctrl Pts',(4.19691509245813,-1.30822168179233,-1.49862306153986));
#16081=CARTESIAN_POINT('Ctrl Pts',(4.23433356560751,-1.28873424481299,-1.49632088745887));
#16082=CARTESIAN_POINT('Ctrl Pts',(4.27078586574333,-1.26770702246664,-1.49401871337788));
#16083=CARTESIAN_POINT('Ctrl Pts',(4.31844782122865,-1.24021359868496,-1.49100858457507));
#16084=CARTESIAN_POINT('Ctrl Pts',(4.36465725919227,-1.20997075273416,-1.48799845577226));
#16085=CARTESIAN_POINT('Ctrl Pts',(4.40907884478412,-1.17715674998304,-1.48498832696945));
#16086=CARTESIAN_POINT('Ctrl Pts',(4.45342148071079,-1.14440106695409,-1.48198354801307));
#16087=CARTESIAN_POINT('Ctrl Pts',(4.49598214871869,-1.1090836069147,-1.47897876905669));
#16088=CARTESIAN_POINT('Ctrl Pts',(4.53645243873407,-1.07142711803957,-1.47597399010031));
#16089=CARTESIAN_POINT('Ctrl Pts',(4.57688269010578,-1.0338078840183,-1.47297218387464));
#16090=CARTESIAN_POINT('Ctrl Pts',(4.61522627552449,-0.993854563228126,
-1.46997037764897));
#16091=CARTESIAN_POINT('Ctrl Pts',(4.65120747129242,-0.95183039713219,-1.4669685714233));
#16092=CARTESIAN_POINT('Ctrl Pts',(4.68716728132948,-0.909831208458134,
-1.46396854934678));
#16093=CARTESIAN_POINT('Ctrl Pts',(4.72076714195681,-0.865764014414497,
-1.46096852727027));
#16094=CARTESIAN_POINT('Ctrl Pts',(4.75176949856182,-0.81992749739669,-1.45796850519376));
#16095=CARTESIAN_POINT('Ctrl Pts',(4.78276567310583,-0.774100120462913,
-1.45496908134014));
#16096=CARTESIAN_POINT('Ctrl Pts',(4.81116507655881,-0.726504558433568,
-1.45196965748652));
#16097=CARTESIAN_POINT('Ctrl Pts',(4.83677300646318,-0.677469131059185,
-1.4489702336329));
#16098=CARTESIAN_POINT('Ctrl Pts',(4.86240447913426,-0.628388622741825,
-1.44596805224533));
#16099=CARTESIAN_POINT('Ctrl Pts',(4.88523910601951,-0.577866073536125,
-1.44296587085776));
#16100=CARTESIAN_POINT('Ctrl Pts',(4.9051285132961,-0.526253783750209,-1.43996368947019));
#16101=CARTESIAN_POINT('Ctrl Pts',(4.92502697378405,-0.474618001209496,
-1.43696014155711));
#16102=CARTESIAN_POINT('Ctrl Pts',(4.94197738035999,-0.421891992946547,
-1.43395659364402));
#16103=CARTESIAN_POINT('Ctrl Pts',(4.95588096889684,-0.368444250731469,
-1.43095304573093));
#16104=CARTESIAN_POINT('Ctrl Pts',(4.96981079810235,-0.31489563495485,-1.42794382912983));
#16105=CARTESIAN_POINT('Ctrl Pts',(4.98068221806394,-0.260623083218473,
-1.42493461252873));
#16106=CARTESIAN_POINT('Ctrl Pts',(4.98844765983903,-0.206005181526372,
-1.42192539592764));
#16107=CARTESIAN_POINT('Ctrl Pts',(4.99438853788055,-0.164220270605003,
-1.41962322312853));
#16108=CARTESIAN_POINT('Ctrl Pts',(4.99851258859486,-0.122233456475762,
-1.41732105032942));
#16109=CARTESIAN_POINT('Ctrl Pts',(5.00081911649501,-0.0802145055330193,
-1.41501887753032));
#16110=CARTESIAN_POINT('Ctrl Pts',(5.00383493929472,-0.0252740427427241,
-1.41200874909616));
#16111=CARTESIAN_POINT('Ctrl Pts',(5.00375439789903,0.0299521711159732,
-1.408998620662));
#16112=CARTESIAN_POINT('Ctrl Pts',(5.00054356866753,0.0850858806637057,
-1.40598849222784));
#16113=CARTESIAN_POINT('Ctrl Pts',(4.99733844598335,0.140121602090493,-1.40298371363921));
#16114=CARTESIAN_POINT('Ctrl Pts',(4.99101410652874,0.195064622512907,-1.39997893505057));
#16115=CARTESIAN_POINT('Ctrl Pts',(4.9815885938022,0.24953493153882,-1.39697415646194));
#16116=CARTESIAN_POINT('Ctrl Pts',(4.97217240605668,0.303951351231319,-1.39397235060318));
#16117=CARTESIAN_POINT('Ctrl Pts',(4.95966121239473,0.357895468133609,-1.39097054474442));
#16118=CARTESIAN_POINT('Ctrl Pts',(4.94412483024175,0.410992522194417,-1.38796873888567));
#16119=CARTESIAN_POINT('Ctrl Pts',(4.9285976822637,0.46405801758988,-1.3849687171746));
#16120=CARTESIAN_POINT('Ctrl Pts',(4.9100490576525,0.516276942180214,-1.38196869546354));
#16121=CARTESIAN_POINT('Ctrl Pts',(4.88859931200724,0.567287138761122,-1.37896867375248));
#16122=CARTESIAN_POINT('Ctrl Pts',(4.86715384355899,0.618287163628853,-1.37596925026221));
#16123=CARTESIAN_POINT('Ctrl Pts',(4.84280860754731,0.668078452602508,-1.37296982677194));
#16124=CARTESIAN_POINT('Ctrl Pts',(4.81573219590353,0.716318544575429,-1.36997040328167));
#16125=CARTESIAN_POINT('Ctrl Pts',(4.78863089137961,0.764602986399556,-1.36696822225136));
#16126=CARTESIAN_POINT('Ctrl Pts',(4.75879365376755,0.811332920532059,-1.36396604122104));
#16127=CARTESIAN_POINT('Ctrl Pts',(4.7264344731455,0.856191584461946,-1.36096386019073));
#16128=CARTESIAN_POINT('Ctrl Pts',(4.69406056331908,0.90107066709267,-1.35796031263206));
#16129=CARTESIAN_POINT('Ctrl Pts',(4.65916275550649,0.944076370791778,-1.35495676507338));
#16130=CARTESIAN_POINT('Ctrl Pts',(4.62199570711233,0.984924635554761,-1.35195321751471));
#16131=CARTESIAN_POINT('Ctrl Pts',(4.58475851208888,1.02584999463136,-1.348944001259));
#16132=CARTESIAN_POINT('Ctrl Pts',(4.54524389884154,1.06460940998231,-1.34593478500329));
#16133=CARTESIAN_POINT('Ctrl Pts',(4.50374295181336,1.1009561835003,-1.34292556874758));
#16134=CARTESIAN_POINT('Ctrl Pts',(4.47199299994219,1.12876297810392,-1.34062339305931));
#16135=CARTESIAN_POINT('Ctrl Pts',(4.43908123842446,1.15515844654347,-1.33832121737103));
#16136=CARTESIAN_POINT('Ctrl Pts',(4.40514947174087,1.18004924629823,-1.33601904168276));
#16137=CARTESIAN_POINT('Ctrl Pts',(4.36078318702258,1.21259433359309,-1.33300891306169));
#16138=CARTESIAN_POINT('Ctrl Pts',(4.3144857366899,1.24270226555692,-1.32999878444062));
#16139=CARTESIAN_POINT('Ctrl Pts',(4.26655538408495,1.27013795295447,-1.32698865581956));
#16140=CARTESIAN_POINT('Ctrl Pts',(4.21871021728604,1.29752487936826,-1.32398387704924));
#16141=CARTESIAN_POINT('Ctrl Pts',(4.16923836214326,1.32224872606814,-1.32097909827893));
#16142=CARTESIAN_POINT('Ctrl Pts',(4.11846794650935,1.3441169687644,-1.31797431950861));
#16143=CARTESIAN_POINT('Ctrl Pts',(4.06774775983131,1.36596357643987,-1.3149725134715));
#16144=CARTESIAN_POINT('Ctrl Pts',(4.01573204026505,1.38495996870533,-1.31197070743439));
#16145=CARTESIAN_POINT('Ctrl Pts',(3.96277280743289,1.4009598520932,-1.30896890139728));
#16146=CARTESIAN_POINT('Ctrl Pts',(3.90984505141247,1.41695022580182,-1.30596887951145));
#16147=CARTESIAN_POINT('Ctrl Pts',(3.85597539817924,1.42994746826775,-1.30296885762563));
#16148=CARTESIAN_POINT('Ctrl Pts',(3.80153292599353,1.43985449924932,-1.29996883573981));
#16149=CARTESIAN_POINT('Ctrl Pts',(3.74710131000526,1.44975955470186,-1.29696941207865));
#16150=CARTESIAN_POINT('Ctrl Pts',(3.69209762120056,1.45657552793798,-1.2939699884175));
#16151=CARTESIAN_POINT('Ctrl Pts',(3.63690079797329,1.46025649981229,-1.29097056475635));
#16152=CARTESIAN_POINT('Ctrl Pts',(3.58165322931397,1.46394085580362,-1.28796838356241));
#16153=CARTESIAN_POINT('Ctrl Pts',(3.52621269957035,1.46448441700204,-1.28496620236847));
#16154=CARTESIAN_POINT('Ctrl Pts',(3.47096142924254,1.46189332804349,-1.28196402117453));
#16155=CARTESIAN_POINT('Ctrl Pts',(3.41568500979353,1.4593010596802,-1.27896047345602));
#16156=CARTESIAN_POINT('Ctrl Pts',(3.36059854768577,1.45357135162118,-1.27595692573751));
#16157=CARTESIAN_POINT('Ctrl Pts',(3.30607909466244,1.44476227700425,-1.272953378019));
#16158=CARTESIAN_POINT('Ctrl Pts',(3.25145674538153,1.43593657674711,-1.26994416161156));
#16159=CARTESIAN_POINT('Ctrl Pts',(3.19740405994049,1.42402001396884,-1.26693494520412));
#16160=CARTESIAN_POINT('Ctrl Pts',(3.14428670208302,1.40912158482711,-1.26392572879668));
#16161=CARTESIAN_POINT('Ctrl Pts',(3.10364973860981,1.39772367376262,-1.26162355447618));
#16162=CARTESIAN_POINT('Ctrl Pts',(3.06355998990276,1.38458157482829,-1.25932138015568));
#16163=CARTESIAN_POINT('Ctrl Pts',(3.02417311397034,1.36976305096237,-1.25701920583518));
#16164=CARTESIAN_POINT('Ctrl Pts',(2.97267414679388,1.35038759515105,-1.25400907626895));
#16165=CARTESIAN_POINT('Ctrl Pts',(2.92216118266346,1.32806308233131,-1.25099894670271));
#16166=CARTESIAN_POINT('Ctrl Pts',(2.87299408520618,1.30291086446569,-1.24798881713648));
#16167=CARTESIAN_POINT('Ctrl Pts',(2.82391437144947,1.27780334913466,-1.24498403741342));
#16168=CARTESIAN_POINT('Ctrl Pts',(2.77617624382463,1.24987834071752,-1.24197925769036));
#16169=CARTESIAN_POINT('Ctrl Pts',(2.73012023449984,1.21930546081866,-1.2389744779673));
#16170=CARTESIAN_POINT('Ctrl Pts',(2.68410978992882,1.18876282769465,-1.23597267097353));
#16171=CARTESIAN_POINT('Ctrl Pts',(2.63977860483815,1.15557780308831,-1.23297086397977));
#16172=CARTESIAN_POINT('Ctrl Pts',(2.59744154618989,1.1199652789341,-1.22996905698601));
#16173=CARTESIAN_POINT('Ctrl Pts',(2.55512965092677,1.08437392138167,-1.22696903414135));
#16174=CARTESIAN_POINT('Ctrl Pts',(2.5148099362524,1.04635826329255,-1.2239690112967));
#16175=CARTESIAN_POINT('Ctrl Pts',(2.47676537248869,1.00617437357405,-1.22096898845204));
#16176=CARTESIAN_POINT('Ctrl Pts',(2.43872839506025,0.965998496786419,-1.2179695638316));
#16177=CARTESIAN_POINT('Ctrl Pts',(2.40296603043599,0.923655630305217,-1.21497013921115));
#16178=CARTESIAN_POINT('Ctrl Pts',(2.36972378767427,0.879438055380055,-1.21197071459071));
#16179=CARTESIAN_POINT('Ctrl Pts',(2.3364509836035,0.835179828956672,-1.20896853244445));
#16180=CARTESIAN_POINT('Ctrl Pts',(2.30570324825082,0.78904387376498,-1.20596635029818));
#16181=CARTESIAN_POINT('Ctrl Pts',(2.27768427918276,0.741353667347177,-1.20296416815191));
#16182=CARTESIAN_POINT('Ctrl Pts',(2.2496525565439,0.69364175347745,-1.19996061948347));
#16183=CARTESIAN_POINT('Ctrl Pts',(2.22435231784351,0.644374648722026,-1.19695707081503));
#16184=CARTESIAN_POINT('Ctrl Pts',(2.20194094494239,0.593899875180095,-1.19395352214659));
#16185=CARTESIAN_POINT('Ctrl Pts',(2.17948727449227,0.543329839325739,-1.19094430480504));
#16186=CARTESIAN_POINT('Ctrl Pts',(2.15993354854111,0.491548076777288,-1.18793508746349));
#16187=CARTESIAN_POINT('Ctrl Pts',(2.14338827719297,0.438920396017478,-1.18492587012193));
#16188=CARTESIAN_POINT('Ctrl Pts',(2.13073050987142,0.398658201236042,-1.1826237034105));
#16189=CARTESIAN_POINT('Ctrl Pts',(2.1198325312392,0.357901299628314,-1.18032153669906));
#16190=CARTESIAN_POINT('Ctrl Pts',(2.11072263870117,0.316817082637371,-1.17801936998763));
#16191=CARTESIAN_POINT('Ctrl Pts',(2.09449554620332,0.243635386307748,-1.17391861116792));
#16192=CARTESIAN_POINT('Ctrl Pts',(2.08388602429248,0.169166356842432,-1.16981785234821));
#16193=CARTESIAN_POINT('Ctrl Pts',(2.07904990501698,0.0941388618851819,
-1.1657170935285));
#16194=CARTESIAN_POINT('Ctrl Pts',(2.07705997522901,0.0632671156302568,
-1.16402974429997));
#16195=CARTESIAN_POINT('Ctrl Pts',(2.07604701387719,0.0323010764233835,
-1.16234239507143));
#16196=CARTESIAN_POINT('Ctrl Pts',(2.07601962146617,0.00129284301226723,
-1.1606550458429));
#16197=CARTESIAN_POINT('Ctrl Pts',(2.07601961090358,0.00128083034372539,
-1.08934495415708));
#16198=CARTESIAN_POINT('Ctrl Pts',(2.076086813979,0.0780682547590463,-1.09352475799718));
#16199=CARTESIAN_POINT('Ctrl Pts',(2.08220099158433,0.154597466853534,-1.09770456183728));
#16200=CARTESIAN_POINT('Ctrl Pts',(2.0942199806277,0.230093130816347,-1.10188436567738));
#16201=CARTESIAN_POINT('Ctrl Pts',(2.09816260126035,0.254858172313705,-1.10325547774021));
#16202=CARTESIAN_POINT('Ctrl Pts',(2.10274024984205,0.279512224846894,-1.10462658980304));
#16203=CARTESIAN_POINT('Ctrl Pts',(2.10794686135528,0.30402848137613,-1.10599770186587));
#16204=CARTESIAN_POINT('Ctrl Pts',(2.11937743601969,0.357851375601575,-1.10900783595551));
#16205=CARTESIAN_POINT('Ctrl Pts',(2.13387162028759,0.411141823683592,-1.11201797004515));
#16206=CARTESIAN_POINT('Ctrl Pts',(2.15136341936914,0.463525828809443,-1.11502810413479));
#16207=CARTESIAN_POINT('Ctrl Pts',(2.16882413118407,0.515816734561915,-1.11803288846935));
#16208=CARTESIAN_POINT('Ctrl Pts',(2.18927171942787,0.567203897473393,-1.12103767280391));
#16209=CARTESIAN_POINT('Ctrl Pts',(2.21258956591817,0.617325192383872,-1.12404245713847));
#16210=CARTESIAN_POINT('Ctrl Pts',(2.23588434370741,0.667396901533078,-1.12704426879407));
#16211=CARTESIAN_POINT('Ctrl Pts',(2.26204353297963,0.71620474703446,-1.13004608044967));
#16212=CARTESIAN_POINT('Ctrl Pts',(2.29090190738579,0.76340518737667,-1.13304789210528));
#16213=CARTESIAN_POINT('Ctrl Pts',(2.3197431300039,0.810577574442678,-1.13604791965355));
#16214=CARTESIAN_POINT('Ctrl Pts',(2.35128008311007,0.856144000245483,-1.13904794720183));
#16215=CARTESIAN_POINT('Ctrl Pts',(2.38530204441923,0.89978628187571,-1.1420479747501));
#16216=CARTESIAN_POINT('Ctrl Pts',(2.41931722191452,0.943419861446911,-1.14504740410745));
#16217=CARTESIAN_POINT('Ctrl Pts',(2.45581609906172,0.985129642514446,-1.1480468334648));
#16218=CARTESIAN_POINT('Ctrl Pts',(2.49454653130814,1.02462904716525,-1.15104626282215));
#16219=CARTESIAN_POINT('Ctrl Pts',(2.53331257055859,1.06416476577846,-1.15404844971891));
#16220=CARTESIAN_POINT('Ctrl Pts',(2.57431389318075,1.10148567016794,-1.15705063661567));
#16221=CARTESIAN_POINT('Ctrl Pts',(2.61726123903304,1.13634184087809,-1.16005282351243));
#16222=CARTESIAN_POINT('Ctrl Pts',(2.66022813368107,1.17121387743859,-1.16305637694622));
#16223=CARTESIAN_POINT('Ctrl Pts',(2.70514238829615,1.20361863435593,-1.16605993038001));
#16224=CARTESIAN_POINT('Ctrl Pts',(2.75168402223468,1.23334837672067,-1.1690634838138));
#16225=CARTESIAN_POINT('Ctrl Pts',(2.79831349468582,1.2631342283392,-1.17207270588541));
#16226=CARTESIAN_POINT('Ctrl Pts',(2.8465760203861,1.29023472087032,-1.17508192795701));
#16227=CARTESIAN_POINT('Ctrl Pts',(2.89612620774829,1.31448769488154,-1.17809115002862));
#16228=CARTESIAN_POINT('Ctrl Pts',(2.93403332522867,1.33304181917519,-1.18039327925689));
#16229=CARTESIAN_POINT('Ctrl Pts',(2.9726935207184,1.34993033683131,-1.18269540848516));
#16230=CARTESIAN_POINT('Ctrl Pts',(3.0119455503449,1.36510016189852,-1.18499753771344));
#16231=CARTESIAN_POINT('Ctrl Pts',(3.0632691966508,1.38493533331972,-1.18800766654975));
#16232=CARTESIAN_POINT('Ctrl Pts',(3.11582084811984,1.40191373474239,-1.19101779538605));
#16233=CARTESIAN_POINT('Ctrl Pts',(3.16925121455922,1.41588628770984,-1.19402792422236));
#16234=CARTESIAN_POINT('Ctrl Pts',(3.22258662075321,1.42983400766291,-1.19703270324373));
#16235=CARTESIAN_POINT('Ctrl Pts',(3.27679713588248,1.440786348274,-1.20003748226509));
#16236=CARTESIAN_POINT('Ctrl Pts',(3.3315157520175,1.44864311610984,-1.20304226128645));
#16237=CARTESIAN_POINT('Ctrl Pts',(3.38618023350355,1.45649211102673,-1.20604406759635));
#16238=CARTESIAN_POINT('Ctrl Pts',(3.44135130002867,1.46125152521475,-1.20904587390625));
#16239=CARTESIAN_POINT('Ctrl Pts',(3.49665094853118,1.46287202989195,-1.21204768021614));
#16240=CARTESIAN_POINT('Ctrl Pts',(3.55191772956816,1.4644915714187,-1.21504770239598));
#16241=CARTESIAN_POINT('Ctrl Pts',(3.60731241427164,1.46297588577288,-1.21804772457581));
#16242=CARTESIAN_POINT('Ctrl Pts',(3.66245337918994,1.4583276040762,-1.22104774675565));
#16243=CARTESIAN_POINT('Ctrl Pts',(3.71758334900887,1.45368024924612,-1.22404717073155));
#16244=CARTESIAN_POINT('Ctrl Pts',(3.77245917356105,1.44590158320879,-1.22704659470745));
#16245=CARTESIAN_POINT('Ctrl Pts',(3.82670306639338,1.43504619820099,-1.23004601868335));
#16246=CARTESIAN_POINT('Ctrl Pts',(3.88099682911028,1.42418083314255,-1.23304820022181));
#16247=CARTESIAN_POINT('Ctrl Pts',(3.93465698043322,1.41023320174446,-1.23605038176026));
#16248=CARTESIAN_POINT('Ctrl Pts',(3.98731615649071,1.39330901159699,-1.23905256329871));
#16249=CARTESIAN_POINT('Ctrl Pts',(4.03999930210369,1.37637711784788,-1.24205611137881));
#16250=CARTESIAN_POINT('Ctrl Pts',(4.09168007052456,1.35646615468641,-1.2450596594589));
#16251=CARTESIAN_POINT('Ctrl Pts',(4.14200964300066,1.33373060842713,-1.248063207539));
#16252=CARTESIAN_POINT('Ctrl Pts',(4.19243420442704,1.31095215249136,-1.25107242433164));
#16253=CARTESIAN_POINT('Ctrl Pts',(4.2415020062414,1.28533870905188,-1.25408164112429));
#16254=CARTESIAN_POINT('Ctrl Pts',(4.2888885159357,1.25709094903957,-1.25709085791694));
#16255=CARTESIAN_POINT('Ctrl Pts',(4.32514110180467,1.23548027646505,-1.25939302979829));
#16256=CARTESIAN_POINT('Ctrl Pts',(4.36041014090153,1.2123287418024,-1.26169520167965));
#16257=CARTESIAN_POINT('Ctrl Pts',(4.39456306180988,1.18774239151064,-1.263997373561));
#16258=CARTESIAN_POINT('Ctrl Pts',(4.43921855961942,1.15559533988526,-1.26700750062103));
#16259=CARTESIAN_POINT('Ctrl Pts',(4.48215241690794,1.12085887548091,-1.27001762768105));
#16260=CARTESIAN_POINT('Ctrl Pts',(4.52304892570035,1.08374408161562,-1.27302775474107));
#16261=CARTESIAN_POINT('Ctrl Pts',(4.56387274924154,1.04669525177016,-1.27603253191065));
#16262=CARTESIAN_POINT('Ctrl Pts',(4.60266602221789,1.00727683301475,-1.27903730908023));
#16263=CARTESIAN_POINT('Ctrl Pts',(4.63914429820567,0.965741458382562,-1.28204208624981));
#16264=CARTESIAN_POINT('Ctrl Pts',(4.675586484654,0.924247176496708,-1.28504389066311));
#16265=CARTESIAN_POINT('Ctrl Pts',(4.70971786435798,0.880640482490543,-1.2880456950764));
#16266=CARTESIAN_POINT('Ctrl Pts',(4.74129058364919,0.835211010420215,-1.29104749948969));
#16267=CARTESIAN_POINT('Ctrl Pts',(4.77284453717947,0.789808540097948,-1.29404751973155));
#16268=CARTESIAN_POINT('Ctrl Pts',(4.80184254379426,0.74258587188108,-1.2970475399734));
#16269=CARTESIAN_POINT('Ctrl Pts',(4.82807828942966,0.693864062746124,-1.30004756021526));
#16270=CARTESIAN_POINT('Ctrl Pts',(4.85430880332614,0.645151969355036,-1.3030469822152));
#16271=CARTESIAN_POINT('Ctrl Pts',(4.87777789992078,0.594941793470117,-1.30604640421515));
#16272=CARTESIAN_POINT('Ctrl Pts',(4.8983248804711,0.543579769884119,-1.30904582621509));
#16273=CARTESIAN_POINT('Ctrl Pts',(4.91889075089191,0.492170526611925,-1.31204800573422));
#16274=CARTESIAN_POINT('Ctrl Pts',(4.93652894151735,0.439607811381876,-1.31505018525336));
#16275=CARTESIAN_POINT('Ctrl Pts',(4.95112725892788,0.386257059070259,-1.31805236477249));
#16276=CARTESIAN_POINT('Ctrl Pts',(4.96573222111481,0.33288202287649,-1.32105591080607));
#16277=CARTESIAN_POINT('Ctrl Pts',(4.97729444138771,0.27871875194974,-1.32405945683964));
#16278=CARTESIAN_POINT('Ctrl Pts',(4.98575271279183,0.224143801679205,-1.32706300287322));
#16279=CARTESIAN_POINT('Ctrl Pts',(4.99422694777541,0.169465850273618,-1.33007221760002));
#16280=CARTESIAN_POINT('Ctrl Pts',(4.99958547999956,0.114375194319197,-1.33308143232681));
#16281=CARTESIAN_POINT('Ctrl Pts',(5.00181905327494,0.0592532839526826,
-1.33609064705361));
#16282=CARTESIAN_POINT('Ctrl Pts',(5.00352783939816,0.0170824912781934,
-1.33839283450526));
#16283=CARTESIAN_POINT('Ctrl Pts',(5.00340868074502,-0.0251064766897208,
-1.34069502195691));
#16284=CARTESIAN_POINT('Ctrl Pts',(5.00147795791863,-0.0671446408445567,
-1.34299720940856));
#16285=CARTESIAN_POINT('Ctrl Pts',(4.99895352151999,-0.122109895449789,
-1.34600733894141));
#16286=CARTESIAN_POINT('Ctrl Pts',(4.99331967897896,-0.177048072556392,
-1.34901746847425));
#16287=CARTESIAN_POINT('Ctrl Pts',(4.98458071728794,-0.231579422569218,
-1.35202759800709));
#16288=CARTESIAN_POINT('Ctrl Pts',(4.97585728714247,-0.286013855330727,
-1.35503237770942));
#16289=CARTESIAN_POINT('Ctrl Pts',(4.9640397725431,-0.340042378639619,-1.35803715741174));
#16290=CARTESIAN_POINT('Ctrl Pts',(4.94918434067214,-0.393288722781086,
-1.36104193711407));
#16291=CARTESIAN_POINT('Ctrl Pts',(4.93434360573965,-0.446482388666503,
-1.36404374409485));
#16292=CARTESIAN_POINT('Ctrl Pts',(4.9164710485214,-0.498894902124361,-1.36704555107562));
#16293=CARTESIAN_POINT('Ctrl Pts',(4.89567381967488,-0.55016042372689,-1.3700473580564));
#16294=CARTESIAN_POINT('Ctrl Pts',(4.8748889517819,-0.601395475369454,-1.3730473808958));
#16295=CARTESIAN_POINT('Ctrl Pts',(4.85118305581007,-0.651484397970665,
-1.3760474037352));
#16296=CARTESIAN_POINT('Ctrl Pts',(4.82471229701215,-0.70007897334631,-1.37904742657459));
#16297=CARTESIAN_POINT('Ctrl Pts',(4.79824681658887,-0.748663858770234,
-1.3820468511975));
#16298=CARTESIAN_POINT('Ctrl Pts',(4.76901782073415,-0.795754525229392,
-1.3850462758204));
#16299=CARTESIAN_POINT('Ctrl Pts',(4.73722748580544,-0.841027201589646,
-1.38804570044331));
#16300=CARTESIAN_POINT('Ctrl Pts',(4.70540792425556,-0.886341499636643,
-1.39104788260391));
#16301=CARTESIAN_POINT('Ctrl Pts',(4.67102262322822,-0.929834035254669,
-1.39405006476452));
#16302=CARTESIAN_POINT('Ctrl Pts',(4.63431634276002,-0.971211171008397,
-1.39705224692513));
#16303=CARTESIAN_POINT('Ctrl Pts',(4.59759335438184,-1.01260714074505,-1.40005579561454));
#16304=CARTESIAN_POINT('Ctrl Pts',(4.55854765355551,-1.05188541597891,-1.40305934430394));
#16305=CARTESIAN_POINT('Ctrl Pts',(4.51746117282878,-1.08878898562782,-1.40606289299335));
#16306=CARTESIAN_POINT('Ctrl Pts',(4.47629714840745,-1.12576220444317,-1.40907211036642));
#16307=CARTESIAN_POINT('Ctrl Pts',(4.43308506318119,-1.16035143364744,-1.41208132773949));
#16308=CARTESIAN_POINT('Ctrl Pts',(4.38813933485548,-1.19234049786532,-1.41509054511257));
#16309=CARTESIAN_POINT('Ctrl Pts',(4.35375412870948,-1.21681335899193,-1.41739271182709));
#16310=CARTESIAN_POINT('Ctrl Pts',(4.31835493766681,-1.23976522522809,-1.41969487854161));
#16311=CARTESIAN_POINT('Ctrl Pts',(4.28209223229497,-1.26111748840642,-1.42199704525612));
#16312=CARTESIAN_POINT('Ctrl Pts',(4.23467802637467,-1.28903599566673,-1.42500717385921));
#16313=CARTESIAN_POINT('Ctrl Pts',(4.18558753179959,-1.31433549866122,-1.4280173024623));
#16314=CARTESIAN_POINT('Ctrl Pts',(4.13514114118776,-1.33681209412281,-1.43102743106538));
#16315=CARTESIAN_POINT('Ctrl Pts',(4.08478440798254,-1.35924874236054,-1.43403220982439));
#16316=CARTESIAN_POINT('Ctrl Pts',(4.03307703951899,-1.37887222633654,-1.4370369885834));
#16317=CARTESIAN_POINT('Ctrl Pts',(3.98036486107862,-1.39552399521734,-1.44004176734241));
#16318=CARTESIAN_POINT('Ctrl Pts',(3.9277048325768,-1.41215928994076,-1.4430435733723));
#16319=CARTESIAN_POINT('Ctrl Pts',(3.87404246445814,-1.42582853530268,-1.44604537940219));
#16320=CARTESIAN_POINT('Ctrl Pts',(3.81974270355202,-1.43642157956048,-1.44904718543208));
#16321=CARTESIAN_POINT('Ctrl Pts',(3.76547521613932,-1.44700832775844,-1.45204720731476));
#16322=CARTESIAN_POINT('Ctrl Pts',(3.71057160413364,-1.45452239787162,-1.45504722919743));
#16323=CARTESIAN_POINT('Ctrl Pts',(3.65540883750058,-1.45890431737352,-1.45804725108011));
#16324=CARTESIAN_POINT('Ctrl Pts',(3.60025707062169,-1.46328536309697,-1.46104667474219));
#16325=CARTESIAN_POINT('Ctrl Pts',(3.54484677790598,-1.46453545677763,-1.46404609840427));
#16326=CARTESIAN_POINT('Ctrl Pts',(3.48955959455852,-1.46264701919832,-1.46704552206635));
#16327=CARTESIAN_POINT('Ctrl Pts',(3.43422158259052,-1.46075684547202,-1.47004770326748));
#16328=CARTESIAN_POINT('Ctrl Pts',(3.37900743505493,-1.4557223938416,-1.47304988446862));
#16329=CARTESIAN_POINT('Ctrl Pts',(3.32429681693925,-1.44758821500255,-1.47605206566975));
#16330=CARTESIAN_POINT('Ctrl Pts',(3.26956129573133,-1.4394503336609,-1.47905561339895));
#16331=CARTESIAN_POINT('Ctrl Pts',(3.21533027885597,-1.42821001989111,-1.48205916112815));
#16332=CARTESIAN_POINT('Ctrl Pts',(3.16197306666285,-1.41396296986399,-1.48506270885735));
#16333=CARTESIAN_POINT('Ctrl Pts',(3.10851515164676,-1.39968903091037,-1.48807192528106));
#16334=CARTESIAN_POINT('Ctrl Pts',(3.05593483868087,-1.38239718497146,-1.49108114170476));
#16335=CARTESIAN_POINT('Ctrl Pts',(3.00458497687674,-1.36223264788333,-1.49409035812846));
#16336=CARTESIAN_POINT('Ctrl Pts',(2.96530022071548,-1.34680594769796,-1.49639253245354));
#16337=CARTESIAN_POINT('Ctrl Pts',(2.92673530585453,-1.32969893096072,-1.49869470677861));
#16338=CARTESIAN_POINT('Ctrl Pts',(2.88903828678348,-1.31099467052119,-1.50099688110369));
#16339=CARTESIAN_POINT('Ctrl Pts',(2.83974885266478,-1.28653856138068,-1.50400700955739));
#16340=CARTESIAN_POINT('Ctrl Pts',(2.79173698722558,-1.25924750199659,-1.50701713801109));
#16341=CARTESIAN_POINT('Ctrl Pts',(2.74534852619855,-1.22927841779358,-1.51002726646479));
#16342=CARTESIAN_POINT('Ctrl Pts',(2.69904251063669,-1.19936259716157,-1.51303204506564));
#16343=CARTESIAN_POINT('Ctrl Pts',(2.65435461369543,-1.16677848145454,-1.51603682366649));
#16344=CARTESIAN_POINT('Ctrl Pts',(2.611606583539,-1.13172907703269,-1.51904160226734));
#16345=CARTESIAN_POINT('Ctrl Pts',(2.56890084552963,-1.09671434823357,-1.52204340813382));
#16346=CARTESIAN_POINT('Ctrl Pts',(2.52813157888946,-1.05923949545577,-1.5250452140003));
#16347=CARTESIAN_POINT('Ctrl Pts',(2.48959044418768,-1.01954998494865,-1.52804701986678));
#16348=CARTESIAN_POINT('Ctrl Pts',(2.4510722167798,-0.979884064283605,-1.53104704158109));
#16349=CARTESIAN_POINT('Ctrl Pts',(2.41477986361633,-0.938006473007482,
-1.5340470632954));
#16350=CARTESIAN_POINT('Ctrl Pts',(2.38096916945945,-0.894200437999985,
-1.5370470850097));
#16351=CARTESIAN_POINT('Ctrl Pts',(2.34716521739095,-0.850403138221584,
-1.54004650849874));
#16352=CARTESIAN_POINT('Ctrl Pts',(2.31584226405684,-0.804678576239946,
-1.54304593198778));
#16353=CARTESIAN_POINT('Ctrl Pts',(2.28721518124924,-0.75734224050455,-1.54604535547683));
#16354=CARTESIAN_POINT('Ctrl Pts',(2.25856178000732,-0.709962385900982,
-1.54904753649903));
#16355=CARTESIAN_POINT('Ctrl Pts',(2.23260947481426,-0.660968249992565,
-1.55204971752123));
#16356=CARTESIAN_POINT('Ctrl Pts',(2.2095284007412,-0.610702154703102,-1.55505189854343));
#16357=CARTESIAN_POINT('Ctrl Pts',(2.18643682068818,-0.560413179430315,
-1.55805544609014));
#16358=CARTESIAN_POINT('Ctrl Pts',(2.16621927013087,-0.508851583173669,
-1.56105899363686));
#16359=CARTESIAN_POINT('Ctrl Pts',(2.14899738523307,-0.456378952886151,
-1.56406254118358));
#16360=CARTESIAN_POINT('Ctrl Pts',(2.13174299692356,-0.403807289332768,
-1.56707175742122));
#16361=CARTESIAN_POINT('Ctrl Pts',(2.11749570491818,-0.350321668506178,
-1.57008097365886));
#16362=CARTESIAN_POINT('Ctrl Pts',(2.10632668243752,-0.296296956360021,
-1.57309018989649));
#16363=CARTESIAN_POINT('Ctrl Pts',(2.09778191531256,-0.254965802708777,
-1.57539236558141));
#16364=CARTESIAN_POINT('Ctrl Pts',(2.0910377791532,-0.213319416672938,-1.57769454126633));
#16365=CARTESIAN_POINT('Ctrl Pts',(2.08610559463042,-0.171527188868424,
-1.57999671695125));
#16366=CARTESIAN_POINT('Ctrl Pts',(2.07942970231923,-0.114959878586476,
-1.58311279601986));
#16367=CARTESIAN_POINT('Ctrl Pts',(2.07605539298674,-0.057995432812559,
-1.58622887508847));
#16368=CARTESIAN_POINT('Ctrl Pts',(2.07601934240537,-0.000924463273316875,
-1.58934495415708));
#16369=CARTESIAN_POINT('Origin',(3.53951905042299,8.32667268468867E-16,
0.));
#16370=CARTESIAN_POINT('',(2.07822263712103,-0.00047059340223754,-2.16065504584291));
#16371=CARTESIAN_POINT('',(2.07826209366837,-0.000404147104298556,-2.08934495415708));
#16372=CARTESIAN_POINT('',(2.07601905042299,1.01189432752408E-15,0.));
#16373=CARTESIAN_POINT('Ctrl Pts',(2.07822263712103,-0.00047059340223754,
-2.16065504584291));
#16374=CARTESIAN_POINT('Ctrl Pts',(2.07760197824254,-0.213557672618783,
-2.14910916394806));
#16375=CARTESIAN_POINT('Ctrl Pts',(2.22069645106389,-0.91184954544291,-2.11123000343738));
#16376=CARTESIAN_POINT('Ctrl Pts',(3.29376990923637,-1.70939328955503,-2.04701756431081));
#16377=CARTESIAN_POINT('Ctrl Pts',(4.8369055691126,-1.139827302423,-1.96801772846324));
#16378=CARTESIAN_POINT('Ctrl Pts',(5.20304199322948,0.46379896208315,-1.88901789261569));
#16379=CARTESIAN_POINT('Ctrl Pts',(4.06001734279725,1.64666316760928,-1.81001805676813));
#16380=CARTESIAN_POINT('Ctrl Pts',(2.50365865871826,1.34699592201261,-1.73389733257609));
#16381=CARTESIAN_POINT('Ctrl Pts',(2.0773938370103,0.429087924422116,-1.6841098869999));
#16382=CARTESIAN_POINT('Ctrl Pts',(2.07435250273762,-0.000857435948038469,
-1.66065572003956));
#16383=CARTESIAN_POINT('Ctrl Pts',(2.07445498749166,-0.000913275611314609,
-1.58934561824827));
#16384=CARTESIAN_POINT('Ctrl Pts',(2.07761216204631,0.424762299842239,-1.61256259643179));
#16385=CARTESIAN_POINT('Ctrl Pts',(2.49649649616959,1.33865665927285,-1.66211285323115));
#16386=CARTESIAN_POINT('Ctrl Pts',(4.04527237248975,1.65125152232427,-1.73799638864638));
#16387=CARTESIAN_POINT('Ctrl Pts',(5.19882826886049,0.478655327125651,-1.81699622449393));
#16388=CARTESIAN_POINT('Ctrl Pts',(4.84704581275503,-1.12818073352081,-1.89599606034151));
#16389=CARTESIAN_POINT('Ctrl Pts',(3.30906481316853,-1.71152237792777,-1.97499589618906));
#16390=CARTESIAN_POINT('Ctrl Pts',(2.22491280319792,-0.920695290287707,
-2.03944552746092));
#16391=CARTESIAN_POINT('Ctrl Pts',(2.07771897242739,-0.217883449584588,
-2.07756188011693));
#16392=CARTESIAN_POINT('Ctrl Pts',(2.07826209366837,-0.000404147104298556,
-2.08934495415708));
#16393=CARTESIAN_POINT('Origin',(3.53951905042299,8.32667268468867E-16,
0.));
#16394=CARTESIAN_POINT('',(2.07601386707336,0.00130271582805805,-2.66065504584291));
#16395=CARTESIAN_POINT('',(2.07601962469904,0.00129649745615735,-2.58934495415708));
#16396=CARTESIAN_POINT('',(2.07601905042299,1.01189432752408E-15,0.));
#16397=CARTESIAN_POINT('Ctrl Pts',(2.07601386707336,0.00130271582805805,
-2.66065504584291));
#16398=CARTESIAN_POINT('Ctrl Pts',(2.07937356612051,-0.37031688775017,-2.64044216897652));
#16399=CARTESIAN_POINT('Ctrl Pts',(2.411408495879,-1.2314244916919,-2.59389601349429));
#16400=CARTESIAN_POINT('Ctrl Pts',(3.85541032199574,-1.69783119393702,-2.52101657939618));
#16401=CARTESIAN_POINT('Ctrl Pts',(5.13410011968933,-0.663120857830193,
-2.44201674354863));
#16402=CARTESIAN_POINT('Ctrl Pts',(4.96617345192722,0.973177926803775,-2.36301690770107));
#16403=CARTESIAN_POINT('Ctrl Pts',(3.50397471012939,1.72660205561732,-2.28401707185351));
#16404=CARTESIAN_POINT('Ctrl Pts',(2.28301066241746,1.03245433367608,-2.21656311790078));
#16405=CARTESIAN_POINT('Ctrl Pts',(2.07901754643573,0.27244083988585,-2.17544244256392));
#16406=CARTESIAN_POINT('Ctrl Pts',(2.07822263712103,-0.00047059340223754,
-2.16065504584291));
#16407=CARTESIAN_POINT('Ctrl Pts',(2.07826209366837,-0.000404147104298556,
-2.08934495415708));
#16408=CARTESIAN_POINT('Ctrl Pts',(2.07893276119865,0.268147873470814,-2.10389515873278));
#16409=CARTESIAN_POINT('Ctrl Pts',(2.27810024031952,1.02365674713459,-2.14477864192436));
#16410=CARTESIAN_POINT('Ctrl Pts',(3.48853717707201,1.72621518156014,-2.21199540373174));
#16411=CARTESIAN_POINT('Ctrl Pts',(4.95741442700981,0.985895889670252,-2.29099523957932));
#16412=CARTESIAN_POINT('Ctrl Pts',(5.13996585904884,-0.648835893708398,
-2.36999507542687));
#16413=CARTESIAN_POINT('Ctrl Pts',(3.8705793808516,-1.69493866021592,-2.44899491127443));
#16414=CARTESIAN_POINT('Ctrl Pts',(2.41775219469909,-1.2399868630121,-2.52211151597577));
#16415=CARTESIAN_POINT('Ctrl Pts',(2.07929642712637,-0.374598926333502,
-2.56889484206127));
#16416=CARTESIAN_POINT('Ctrl Pts',(2.07588373256422,0.00129542995082815,
-2.5893448895309));
#16417=CARTESIAN_POINT('Origin',(3.53951905042299,8.32667268468867E-16,
0.));
#16418=CARTESIAN_POINT('',(2.07601926119859,-0.000785455376519445,-3.16065504584291));
#16419=CARTESIAN_POINT('',(2.07601929469955,-0.000845575214941048,-3.08934495419128));
#16420=CARTESIAN_POINT('',(2.07601905042299,1.01189432752408E-15,0.));
#16421=CARTESIAN_POINT('Ctrl Pts',(2.07421776459465,-0.000786422233640862,
-3.16065504584291));
#16422=CARTESIAN_POINT('Ctrl Pts',(2.07391318880368,-0.0474574829802449,
-3.15810845262083));
#16423=CARTESIAN_POINT('Ctrl Pts',(2.09703130803367,-0.57642940013294,-3.12922858078293));
#16424=CARTESIAN_POINT('Ctrl Pts',(2.73890147350281,-1.53017304710381,-3.07401543032911));
#16425=CARTESIAN_POINT('Ctrl Pts',(4.38362585771088,-1.50661931371105,-2.99501559448158));
#16426=CARTESIAN_POINT('Ctrl Pts',(5.26256991907278,-0.116248710108447,
-2.91601575863399));
#16427=CARTESIAN_POINT('Ctrl Pts',(4.57834870433128,1.37958363599936,-2.83701592278644));
#16428=CARTESIAN_POINT('Ctrl Pts',(2.95169307147619,1.62384687610397,-2.75801608693887));
#16429=CARTESIAN_POINT('Ctrl Pts',(2.13806849098069,0.709370374933544,-2.6992291279577));
#16430=CARTESIAN_POINT('Ctrl Pts',(2.07499655973696,0.113828077107039,-2.66677544759238));
#16431=CARTESIAN_POINT('Ctrl Pts',(2.07601386707336,0.00130271582805805,
-2.66065504584291));
#16432=CARTESIAN_POINT('Ctrl Pts',(2.07601962469904,0.00129649745615735,
-2.58934495415708));
#16433=CARTESIAN_POINT('Ctrl Pts',(2.07608591186512,0.076122120167986,-2.59341615963068));
#16434=CARTESIAN_POINT('Ctrl Pts',(2.08189439960235,0.150699246533157,-2.59748736510427));
#16435=CARTESIAN_POINT('Ctrl Pts',(2.09330987021167,0.224301709918793,-2.60155857057787));
#16436=CARTESIAN_POINT('Ctrl Pts',(2.09839064543428,0.257060549662797,-2.60337057470843));
#16437=CARTESIAN_POINT('Ctrl Pts',(2.1045815205659,0.289626688434001,-2.605182578839));
#16438=CARTESIAN_POINT('Ctrl Pts',(2.11186768165337,0.321937601485487,-2.60699458296956));
#16439=CARTESIAN_POINT('Ctrl Pts',(2.12397156262673,0.375612978823534,-2.61000471163077));
#16440=CARTESIAN_POINT('Ctrl Pts',(2.13913213185262,0.42871758077564,-2.61301484029198));
#16441=CARTESIAN_POINT('Ctrl Pts',(2.15727871612348,0.480878267585018,-2.61602496895319));
#16442=CARTESIAN_POINT('Ctrl Pts',(2.17539304880093,0.532946250156664,-2.6190297477676));
#16443=CARTESIAN_POINT('Ctrl Pts',(2.19648269264047,0.5840731520418,-2.62203452658202));
#16444=CARTESIAN_POINT('Ctrl Pts',(2.22042650369009,0.633898338185006,-2.62503930539644));
#16445=CARTESIAN_POINT('Ctrl Pts',(2.24434662630552,0.683674230561216,-2.62804111148003));
#16446=CARTESIAN_POINT('Ctrl Pts',(2.27111509484355,0.732150484663586,-2.63104291756362));
#16447=CARTESIAN_POINT('Ctrl Pts',(2.30056239373894,0.778985656388025,-2.63404472364721));
#16448=CARTESIAN_POINT('Ctrl Pts',(2.32999219038134,0.825792991229121,-2.63704474558178));
#16449=CARTESIAN_POINT('Ctrl Pts',(2.36209738102242,0.870960730786668,-2.64004476751635));
#16450=CARTESIAN_POINT('Ctrl Pts',(2.39666327533235,0.914173357379207,-2.64304478945092));
#16451=CARTESIAN_POINT('Ctrl Pts',(2.431222276994,0.957377367112778,-2.64604421316299));
#16452=CARTESIAN_POINT('Ctrl Pts',(2.46824067815461,0.998626625951487,-2.64904363687505));
#16453=CARTESIAN_POINT('Ctrl Pts',(2.50746276531876,1.03763773754469,-2.65204306058711));
#16454=CARTESIAN_POINT('Ctrl Pts',(2.54672091151118,1.07668471420467,-2.65504524183484));
#16455=CARTESIAN_POINT('Ctrl Pts',(2.58818641608737,1.11348905947106,-2.65804742308257));
#16456=CARTESIAN_POINT('Ctrl Pts',(2.63156691203819,1.14780449746569,-2.6610496043303));
#16457=CARTESIAN_POINT('Ctrl Pts',(2.67496715382778,1.18213555508594,-2.6640531521043));
#16458=CARTESIAN_POINT('Ctrl Pts',(2.72028369171559,1.21397514294683,-2.66705669987829));
#16459=CARTESIAN_POINT('Ctrl Pts',(2.7671939690093,1.24311955121755,-2.67006024765228));
#16460=CARTESIAN_POINT('Ctrl Pts',(2.81419278155671,1.27231896465408,-2.67306946411722));
#16461=CARTESIAN_POINT('Ctrl Pts',(2.86279087746172,1.29881278362652,-2.67607868058216));
#16462=CARTESIAN_POINT('Ctrl Pts',(2.91264086197523,1.32244318851452,-2.67908789704709));
#16463=CARTESIAN_POINT('Ctrl Pts',(2.95077814314568,1.34052141670617,-2.68139007097044));
#16464=CARTESIAN_POINT('Ctrl Pts',(2.98964760867792,1.35692467056039,-2.68369224489378));
#16465=CARTESIAN_POINT('Ctrl Pts',(3.02908735246642,1.37160188528639,-2.68599441881713));
#16466=CARTESIAN_POINT('Ctrl Pts',(3.08065543859831,1.39079257468908,-2.68900454747836));
#16467=CARTESIAN_POINT('Ctrl Pts',(3.13341564744505,1.40711133598551,-2.6920146761396));
#16468=CARTESIAN_POINT('Ctrl Pts',(3.18701684885484,1.42041347779075,-2.69502480480084));
#16469=CARTESIAN_POINT('Ctrl Pts',(3.24052278582655,1.43369197794187,-2.69802958361528));
#16470=CARTESIAN_POINT('Ctrl Pts',(3.29486624073509,1.44396437212753,-2.70103436242972));
#16471=CARTESIAN_POINT('Ctrl Pts',(3.34967897943601,1.45113507208931,-2.70403914124417));
#16472=CARTESIAN_POINT('Ctrl Pts',(3.40443749001298,1.45829867783148,-2.70704094732778));
#16473=CARTESIAN_POINT('Ctrl Pts',(3.45966384358912,1.46236659995511,-2.7100427534114));
#16474=CARTESIAN_POINT('Ctrl Pts',(3.51497944889858,1.46329424859015,-2.71304455949502));
#16475=CARTESIAN_POINT('Ctrl Pts',(3.57026217690675,1.46422134586933,-2.71604458142962));
#16476=CARTESIAN_POINT('Ctrl Pts',(3.62563352451692,1.46201186024534,-2.71904460336421));
#16477=CARTESIAN_POINT('Ctrl Pts',(3.68071193122592,1.45667320302481,-2.72204462529881));
#16478=CARTESIAN_POINT('Ctrl Pts',(3.73577935496769,1.45133561036481,-2.7250440490109));
#16479=CARTESIAN_POINT('Ctrl Pts',(3.79055342845848,1.44287013621935,-2.72804347272299));
#16480=CARTESIAN_POINT('Ctrl Pts',(3.84465707877754,1.43133610086936,-2.73104289643508));
#16481=CARTESIAN_POINT('Ctrl Pts',(3.89881046956672,1.41979146164445,-2.73404507768283));
#16482=CARTESIAN_POINT('Ctrl Pts',(3.95229168816361,1.40517273537683,-2.73704725893059));
#16483=CARTESIAN_POINT('Ctrl Pts',(4.00473472370613,1.38759022313207,-2.74004944017835));
#16484=CARTESIAN_POINT('Ctrl Pts',(4.05720163015428,1.36999970771804,-2.74305298795237));
#16485=CARTESIAN_POINT('Ctrl Pts',(4.1086289202916,1.34944291345259,-2.74605653572639));
#16486=CARTESIAN_POINT('Ctrl Pts',(4.15866973794188,1.32607868399462,-2.7490600835004));
#16487=CARTESIAN_POINT('Ctrl Pts',(4.20880499921394,1.30267035848558,-2.75206929996537));
#16488=CARTESIAN_POINT('Ctrl Pts',(4.25754809445522,1.27644426392905,-2.75507851643033));
#16489=CARTESIAN_POINT('Ctrl Pts',(4.30457703035911,1.24760512075579,-2.7580877328953));
#16490=CARTESIAN_POINT('Ctrl Pts',(4.34055609372366,1.22554199430677,-2.76038990681843));
#16491=CARTESIAN_POINT('Ctrl Pts',(4.37553238366331,1.20195044434714,-2.76269208074156));
#16492=CARTESIAN_POINT('Ctrl Pts',(4.40937466718105,1.17693816999639,-2.76499425466469));
#16493=CARTESIAN_POINT('Ctrl Pts',(4.45362398585987,1.1442342273665,-2.76800438332594));
#16494=CARTESIAN_POINT('Ctrl Pts',(4.49611935862923,1.10896263963622,-2.77101451198718));
#16495=CARTESIAN_POINT('Ctrl Pts',(4.53654774642365,1.07133842895288,-2.77402464064843));
#16496=CARTESIAN_POINT('Ctrl Pts',(4.57690428158148,1.03378108709327,-2.77702941946288));
#16497=CARTESIAN_POINT('Ctrl Pts',(4.615200738603,0.993879776922777,-2.78003419827733));
#16498=CARTESIAN_POINT('Ctrl Pts',(4.65115585805821,0.951890675398488,-2.78303897709178));
#16499=CARTESIAN_POINT('Ctrl Pts',(4.68707540587953,0.909943115133671,-2.78604078317541));
#16500=CARTESIAN_POINT('Ctrl Pts',(4.72065786293454,0.865912254389309,-2.78904258925904));
#16501=CARTESIAN_POINT('Ctrl Pts',(4.75165902322557,0.820090809809592,-2.79204439534267));
#16502=CARTESIAN_POINT('Ctrl Pts',(4.78264175771287,0.774296599595849,-2.79504441727727));
#16503=CARTESIAN_POINT('Ctrl Pts',(4.81104594100673,0.726714351495139,-2.79804443921188));
#16504=CARTESIAN_POINT('Ctrl Pts',(4.83666929711483,0.677667682206619,-2.80104446114649));
#16505=CARTESIAN_POINT('Ctrl Pts',(4.86228754377085,0.628630793120422,-2.80404388485859));
#16506=CARTESIAN_POINT('Ctrl Pts',(4.88512582007675,0.57813053059954,-2.80704330857069));
#16507=CARTESIAN_POINT('Ctrl Pts',(4.90502777720061,0.526515115731879,-2.81004273228279));
#16508=CARTESIAN_POINT('Ctrl Pts',(4.92494803129146,0.474852247966205,-2.81304491353055));
#16509=CARTESIAN_POINT('Ctrl Pts',(4.94192638250413,0.422072673409251,-2.81604709477832));
#16510=CARTESIAN_POINT('Ctrl Pts',(4.95585522405133,0.368543204077658,-2.81904927602609));
#16511=CARTESIAN_POINT('Ctrl Pts',(4.96979040569801,0.314989369319897,-2.82205282380012));
#16512=CARTESIAN_POINT('Ctrl Pts',(4.98067320670421,0.260685478081652,-2.82505637157414));
#16513=CARTESIAN_POINT('Ctrl Pts',(4.98844714205617,0.206008823297058,-2.82805991934817));
#16514=CARTESIAN_POINT('Ctrl Pts',(4.9962357494028,0.151228975528263,-2.83106913581315));
#16515=CARTESIAN_POINT('Ctrl Pts',(5.00090372528359,0.0960754863314583,
-2.83407835227812));
#16516=CARTESIAN_POINT('Ctrl Pts',(5.0024465926902,0.0409298922064158,-2.8370875687431));
#16517=CARTESIAN_POINT('Ctrl Pts',(5.00362694948791,-0.00125874734258944,
-2.83938974266614));
#16518=CARTESIAN_POINT('Ctrl Pts',(5.00297929899839,-0.0434426617668592,
-2.84169191658919));
#16519=CARTESIAN_POINT('Ctrl Pts',(5.0005221369383,-0.0854530935234426,
-2.84399409051224));
#16520=CARTESIAN_POINT('Ctrl Pts',(4.99730935884699,-0.14038239466579,-2.84700421917348));
#16521=CARTESIAN_POINT('Ctrl Pts',(4.99098775972164,-0.19524567010842,-2.85001434783471));
#16522=CARTESIAN_POINT('Ctrl Pts',(4.98156638308101,-0.249663253951969,
-2.85302447649594));
#16523=CARTESIAN_POINT('Ctrl Pts',(4.97216175088133,-0.303984122415817,
-2.85602925531038));
#16524=CARTESIAN_POINT('Ctrl Pts',(4.95966836353162,-0.357860355081316,
-2.85903403412482));
#16525=CARTESIAN_POINT('Ctrl Pts',(4.94414709707948,-0.410916415522626,
-2.86203881293926));
#16526=CARTESIAN_POINT('Ctrl Pts',(4.92864118634904,-0.463919985782113,
-2.86504061902288));
#16527=CARTESIAN_POINT('Ctrl Pts',(4.91011347817907,-0.516104486830642,
-2.86804242510649));
#16528=CARTESIAN_POINT('Ctrl Pts',(4.88867569743848,-0.56710545034758,-2.87104423119011));
#16529=CARTESIAN_POINT('Ctrl Pts',(4.86725065842551,-0.618076101007325,
-2.87404425312471));
#16530=CARTESIAN_POINT('Ctrl Pts',(4.84291917931119,-0.667864122528489,
-2.8770442750593));
#16531=CARTESIAN_POINT('Ctrl Pts',(4.81584177498237,-0.716123280429649,
-2.88004429699389));
#16532=CARTESIAN_POINT('Ctrl Pts',(4.78876977005164,-0.764372815163025,
-2.88304372070598));
#16533=CARTESIAN_POINT('Ctrl Pts',(4.75895318559949,-0.811093631411098,
-2.88604314441807));
#16534=CARTESIAN_POINT('Ctrl Pts',(4.72659823777069,-0.855964516183891,
-2.88904256813016));
#16535=CARTESIAN_POINT('Ctrl Pts',(4.69421354425364,-0.900876653236148,
-2.89204474937791));
#16536=CARTESIAN_POINT('Ctrl Pts',(4.65928613456119,-0.943935031659692,
-2.89504693062567));
#16537=CARTESIAN_POINT('Ctrl Pts',(4.6220644277031,-0.984849103228237,-2.89804911187342));
#16538=CARTESIAN_POINT('Ctrl Pts',(4.58482577835032,-1.02578179797393,-2.90105265964744));
#16539=CARTESIAN_POINT('Ctrl Pts',(4.54529112770943,-1.06456786970122,-2.90405620742145));
#16540=CARTESIAN_POINT('Ctrl Pts',(4.50374560557704,-1.1009538593128,-2.90705975519547));
#16541=CARTESIAN_POINT('Ctrl Pts',(4.46212167326346,-1.13740852135626,-2.91006897166043));
#16542=CARTESIAN_POINT('Ctrl Pts',(4.41847970541559,-1.17145372677122,-2.91307818812539));
#16543=CARTESIAN_POINT('Ctrl Pts',(4.37313680290049,-1.20287725589703,-2.91608740459035));
#16544=CARTESIAN_POINT('Ctrl Pts',(4.33844762417712,-1.22691754351648,-2.91838957851351));
#16545=CARTESIAN_POINT('Ctrl Pts',(4.30276358686709,-1.24942424404609,-2.92069175243666));
#16546=CARTESIAN_POINT('Ctrl Pts',(4.26623613594139,-1.27032063968733,-2.92299392635982));
#16547=CARTESIAN_POINT('Ctrl Pts',(4.21847591858875,-1.29764300608357,-2.92600405502105));
#16548=CARTESIAN_POINT('Ctrl Pts',(4.16907235192759,-1.32232557501314,-2.92901418368229));
#16549=CARTESIAN_POINT('Ctrl Pts',(4.11834835770971,-1.34416847270942,-2.93202431234353));
#16550=CARTESIAN_POINT('Ctrl Pts',(4.06771451432204,-1.36597254942182,-2.93502909115798));
#16551=CARTESIAN_POINT('Ctrl Pts',(4.01576538169322,-1.38494676331384,-2.93803386997242));
#16552=CARTESIAN_POINT('Ctrl Pts',(3.96284874412012,-1.40093690808483,-2.94103864878686));
#16553=CARTESIAN_POINT('Ctrl Pts',(3.90998445879302,-1.41691123325672,-2.94404045487048));
#16554=CARTESIAN_POINT('Ctrl Pts',(3.85615506771511,-1.42990718554602,-2.9470422609541));
#16555=CARTESIAN_POINT('Ctrl Pts',(3.80172686894361,-1.43981919347766,-2.95004406703772));
#16556=CARTESIAN_POINT('Ctrl Pts',(3.74733102003577,-1.44972531012294,-2.95304408897232));
#16557=CARTESIAN_POINT('Ctrl Pts',(3.6923375873977,-1.45655102104369,-2.95604411090692));
#16558=CARTESIAN_POINT('Ctrl Pts',(3.63712425642985,-1.46024158061615,-2.95904413284152));
#16559=CARTESIAN_POINT('Ctrl Pts',(3.58192193533393,-1.46393140426872,-2.96204355655361));
#16560=CARTESIAN_POINT('Ctrl Pts',(3.52650032963541,-1.46448728292818,-2.9650429802657));
#16561=CARTESIAN_POINT('Ctrl Pts',(3.47124113955017,-1.4619064186489,-2.96804240397779));
#16562=CARTESIAN_POINT('Ctrl Pts',(3.41593114664336,-1.45932318163872,-2.97104458522555));
#16563=CARTESIAN_POINT('Ctrl Pts',(3.36078439634166,-1.45359746496208,-2.97404676647331));
#16564=CARTESIAN_POINT('Ctrl Pts',(3.30617996577585,-1.44477857181508,-2.97704894772107));
#16565=CARTESIAN_POINT('Ctrl Pts',(3.25155068048537,-1.43595566450369,-2.98005249549509));
#16566=CARTESIAN_POINT('Ctrl Pts',(3.19746472365413,-1.42403688793092,-2.98305604326911));
#16567=CARTESIAN_POINT('Ctrl Pts',(3.14429016789902,-1.40912255691932,-2.98605959104313));
#16568=CARTESIAN_POINT('Ctrl Pts',(3.09101525411885,-1.39418007761793,-2.98906880750809));
#16569=CARTESIAN_POINT('Ctrl Pts',(3.0386556784167,-1.37623092160208,-2.99207802397306));
#16570=CARTESIAN_POINT('Ctrl Pts',(2.98756244313878,-1.35542471339256,-2.99508724043803));
#16571=CARTESIAN_POINT('Ctrl Pts',(2.94847402418526,-1.33950711140662,-2.99738941436114));
#16572=CARTESIAN_POINT('Ctrl Pts',(2.91012643886648,-1.32191834261422,-2.99969158828426));
#16573=CARTESIAN_POINT('Ctrl Pts',(2.87266668934103,-1.30274332795045,-3.00199376220737));
#16574=CARTESIAN_POINT('Ctrl Pts',(2.82368747688569,-1.27767169429168,-3.00500389086861));
#16575=CARTESIAN_POINT('Ctrl Pts',(2.77602124624238,-1.24978133638672,-3.00801401952985));
#16576=CARTESIAN_POINT('Ctrl Pts',(2.73001184024735,-1.21923349965199,-3.01102414819109));
#16577=CARTESIAN_POINT('Ctrl Pts',(2.68408420593083,-1.1887399550306,-3.01402892700553));
#16578=CARTESIAN_POINT('Ctrl Pts',(2.63980798900827,-1.15559859433535,-3.01703370581998));
#16579=CARTESIAN_POINT('Ctrl Pts',(2.59750236938113,-1.12001643855743,-3.02003848463442));
#16580=CARTESIAN_POINT('Ctrl Pts',(2.55523860415568,-1.08446948542763,-3.02304029071804));
#16581=CARTESIAN_POINT('Ctrl Pts',(2.51494197638256,-1.04648685900659,-3.02604209680166));
#16582=CARTESIAN_POINT('Ctrl Pts',(2.47690104883388,-1.00631765993585,-3.02904390288528));
#16583=CARTESIAN_POINT('Ctrl Pts',(2.4388827312346,-0.966172335770815,-3.03204392481988));
#16584=CARTESIAN_POINT('Ctrl Pts',(2.40311781892806,-0.923843397553574,
-3.03504394675448));
#16585=CARTESIAN_POINT('Ctrl Pts',(2.3698585286677,-0.879617254177708,-3.03804396868908));
#16586=CARTESIAN_POINT('Ctrl Pts',(2.33660587051082,-0.835399929762124,
-3.04104339240118));
#16587=CARTESIAN_POINT('Ctrl Pts',(2.30585815938332,-0.789286573348689,
-3.04404281611327));
#16588=CARTESIAN_POINT('Ctrl Pts',(2.2778262981395,-0.741595340354364,-3.04704223982537));
#16589=CARTESIAN_POINT('Ctrl Pts',(2.24976866565941,-0.693860262178921,
-3.05004442107313));
#16590=CARTESIAN_POINT('Ctrl Pts',(2.22443213959196,-0.644544865525007,
-3.05304660232089));
#16591=CARTESIAN_POINT('Ctrl Pts',(2.20198255343965,-0.593993576764533,
-3.05604878356865));
#16592=CARTESIAN_POINT('Ctrl Pts',(2.17952274873406,-0.543419278179571,
-3.05905233134267));
#16593=CARTESIAN_POINT('Ctrl Pts',(2.15995269039105,-0.491608460990556,
-3.06205587911669));
#16594=CARTESIAN_POINT('Ctrl Pts',(2.14338947547991,-0.438924207545298,
-3.06505942689071));
#16595=CARTESIAN_POINT('Ctrl Pts',(2.12679500028811,-0.386140521438059,
-3.06806864335568));
#16596=CARTESIAN_POINT('Ctrl Pts',(2.11321883489573,-0.332480619251878,
-3.07107785982064));
#16597=CARTESIAN_POINT('Ctrl Pts',(2.10272745104385,-0.278320229148988,
-3.07408707628561));
#16598=CARTESIAN_POINT('Ctrl Pts',(2.09470111242638,-0.236885311052606,
-3.07638925020872));
#16599=CARTESIAN_POINT('Ctrl Pts',(2.08847920957511,-0.195157742080637,
-3.07869142413183));
#16600=CARTESIAN_POINT('Ctrl Pts',(2.08407094032382,-0.153307040962717,
-3.08099359805493));
#16601=CARTESIAN_POINT('Ctrl Pts',(2.07874046754152,-0.102701233896012,
-3.08377738342232));
#16602=CARTESIAN_POINT('Ctrl Pts',(2.07604874230331,-0.0518126899422588,
-3.0865611687897));
#16603=CARTESIAN_POINT('Ctrl Pts',(2.07601929469992,-0.000845575841055191,
-3.08934495415708));
#16604=CARTESIAN_POINT('Origin',(3.53951905042299,8.32667268468867E-16,
0.));
#16605=CARTESIAN_POINT('',(2.07614743105272,-0.000562648890241308,-3.66065501978387));
#16606=CARTESIAN_POINT('',(2.07617134745593,-0.000497992070551351,-3.58934493090286));
#16607=CARTESIAN_POINT('',(2.07601905042299,1.01189432752408E-15,0.));
#16608=CARTESIAN_POINT('Ctrl Pts',(2.07601915861015,-0.000562728902602422,
-3.66065501812075));
#16609=CARTESIAN_POINT('Ctrl Pts',(2.07604233637565,-0.060841589897486,
-3.65739327834551));
#16610=CARTESIAN_POINT('Ctrl Pts',(2.07979389092341,-0.121006025409188,
-3.65413153857028));
#16611=CARTESIAN_POINT('Ctrl Pts',(2.08720649254477,-0.180611417770944,
-3.65086979879504));
#16612=CARTESIAN_POINT('Ctrl Pts',(2.09464146722324,-0.240396713885171,
-3.64759821428594));
#16613=CARTESIAN_POINT('Ctrl Pts',(2.10575947781169,-0.299619235945275,
-3.64432662977683));
#16614=CARTESIAN_POINT('Ctrl Pts',(2.12044242524502,-0.357846030959535,
-3.64105504526772));
#16615=CARTESIAN_POINT('Ctrl Pts',(2.13518799272812,-0.416321152464037,
-3.63776950805697));
#16616=CARTESIAN_POINT('Ctrl Pts',(2.15352880326591,-0.47379169729044,-3.63448397084622));
#16617=CARTESIAN_POINT('Ctrl Pts',(2.17529705639333,-0.529840165527046,
-3.63119843363546));
#16618=CARTESIAN_POINT('Ctrl Pts',(2.18453772564011,-0.553632858203489,
-3.62980371617767));
#16619=CARTESIAN_POINT('Ctrl Pts',(2.19439545034132,-0.577169577394221,
-3.62840899871987));
#16620=CARTESIAN_POINT('Ctrl Pts',(2.20485490604248,-0.600419746265086,
-3.62701428126207));
#16621=CARTESIAN_POINT('Ctrl Pts',(2.22742887413253,-0.650599084958731,
-3.62400415260083));
#16622=CARTESIAN_POINT('Ctrl Pts',(2.25288409438884,-0.699609016294227,
-3.62099402393959));
#16623=CARTESIAN_POINT('Ctrl Pts',(2.28107683673418,-0.747098015528093,
-3.61798389527836));
#16624=CARTESIAN_POINT('Ctrl Pts',(2.30921947263254,-0.794502613429382,
-3.61497911646391));
#16625=CARTESIAN_POINT('Ctrl Pts',(2.34008970788798,-0.840391193152254,
-3.61197433764947));
#16626=CARTESIAN_POINT('Ctrl Pts',(2.37349685323573,-0.884434557028728,
-3.60896955883502));
#16627=CARTESIAN_POINT('Ctrl Pts',(2.40687094774785,-0.928434347293463,
-3.6059677527514));
#16628=CARTESIAN_POINT('Ctrl Pts',(2.44277666286921,-0.97059211930943,-3.60296594666778));
#16629=CARTESIAN_POINT('Ctrl Pts',(2.48097974161949,-1.01060713520032,-3.59996414058416));
#16630=CARTESIAN_POINT('Ctrl Pts',(2.51916011404443,-1.0505983678256,-3.59696411864956));
#16631=CARTESIAN_POINT('Ctrl Pts',(2.55963477971373,-1.08844898739587,-3.59396409671496));
#16632=CARTESIAN_POINT('Ctrl Pts',(2.60213039085658,-1.12389267766824,-3.59096407478036));
#16633=CARTESIAN_POINT('Ctrl Pts',(2.6446175281177,-1.15932930025452,-3.58796465106826));
#16634=CARTESIAN_POINT('Ctrl Pts',(2.6891244051954,-1.1923596086406,-3.58496522735617));
#16635=CARTESIAN_POINT('Ctrl Pts',(2.73534388809484,-1.22275694980421,-3.58196580364408));
#16636=CARTESIAN_POINT('Ctrl Pts',(2.78160586311438,-1.25318223692027,-3.57896362239632));
#16637=CARTESIAN_POINT('Ctrl Pts',(2.82958314739795,-1.28096942988885,-3.57596144114856));
#16638=CARTESIAN_POINT('Ctrl Pts',(2.87894010028208,-1.30593556526757,-3.5729592599008));
#16639=CARTESIAN_POINT('Ctrl Pts',(2.92831951935554,-1.33091306467692,-3.56995571212678));
#16640=CARTESIAN_POINT('Ctrl Pts',(2.97907937402391,-1.35306673514907,-3.56695216435275));
#16641=CARTESIAN_POINT('Ctrl Pts',(3.03086293765722,-1.3722613486308,-3.56394861657873));
#16642=CARTESIAN_POINT('Ctrl Pts',(3.08274423405206,-1.39149218871514,-3.56093940011377));
#16643=CARTESIAN_POINT('Ctrl Pts',(3.13565259298671,-1.40775265993323,-3.5579301836488));
#16644=CARTESIAN_POINT('Ctrl Pts',(3.18921610930756,-1.42095745870377,-3.55492096718383));
#16645=CARTESIAN_POINT('Ctrl Pts',(3.23019439449889,-1.43105967093853,-3.55261879326072));
#16646=CARTESIAN_POINT('Ctrl Pts',(3.2715558042486,-1.43937446924751,-3.55031661933761));
#16647=CARTESIAN_POINT('Ctrl Pts',(3.31313149786576,-1.44588413299515,-3.5480144454145));
#16648=CARTESIAN_POINT('Ctrl Pts',(3.36749237204281,-1.45439562086543,-3.54500431675327));
#16649=CARTESIAN_POINT('Ctrl Pts',(3.42244814095818,-1.45985502291367,-3.54199418809203));
#16650=CARTESIAN_POINT('Ctrl Pts',(3.47762585962868,-1.46219064520783,-3.53898405943079));
#16651=CARTESIAN_POINT('Ctrl Pts',(3.53270551194573,-1.46452211644308,-3.53597928061635));
#16652=CARTESIAN_POINT('Ctrl Pts',(3.58800580781906,-1.46374080342766,-3.5329745018019));
#16653=CARTESIAN_POINT('Ctrl Pts',(3.64314684347637,-1.45982654123936,-3.52996972298746));
#16654=CARTESIAN_POINT('Ctrl Pts',(3.69823332621429,-1.45591615156501,-3.52696791690384));
#16655=CARTESIAN_POINT('Ctrl Pts',(3.75316033665749,-1.448878989957,-3.52396611082022));
#16656=CARTESIAN_POINT('Ctrl Pts',(3.80754800164634,-1.43874693094585,-3.5209643047366));
#16657=CARTESIAN_POINT('Ctrl Pts',(3.86190334086315,-1.4286208940103,-3.517964282802));
#16658=CARTESIAN_POINT('Ctrl Pts',(3.9157194518584,-1.4154037021664,-3.5149642608674));
#16659=CARTESIAN_POINT('Ctrl Pts',(3.96862393146242,-1.39917877737912,-3.5119642389328));
#16660=CARTESIAN_POINT('Ctrl Pts',(4.0215178615934,-1.38295708793992,-3.50896481522071));
#16661=CARTESIAN_POINT('Ctrl Pts',(4.0735000167278,-1.36372901141447,-3.50596539150862));
#16662=CARTESIAN_POINT('Ctrl Pts',(4.12421275205047,-1.34162793846772,-3.50296596779653));
#16663=CARTESIAN_POINT('Ctrl Pts',(4.17497211038806,-1.31950654678551,-3.49996378654877));
#16664=CARTESIAN_POINT('Ctrl Pts',(4.22445923212649,-1.29450709314462,-3.49696160530101));
#16665=CARTESIAN_POINT('Ctrl Pts',(4.27233748771777,-1.2668107151271,-3.49395942405325));
#16666=CARTESIAN_POINT('Ctrl Pts',(4.32023753642817,-1.23910173033312,-3.49095587627923));
#16667=CARTESIAN_POINT('Ctrl Pts',(4.36652681699616,-1.20869366453081,-3.48795232850521));
#16668=CARTESIAN_POINT('Ctrl Pts',(4.4108971582575,-1.1758113977959,-3.4849487807312));
#16669=CARTESIAN_POINT('Ctrl Pts',(4.45535124107075,-1.14286707131638,-3.48193956426623));
#16670=CARTESIAN_POINT('Ctrl Pts',(4.49787874295706,-1.1074395544305,-3.47893034780126));
#16671=CARTESIAN_POINT('Ctrl Pts',(4.53820501235536,-1.06979371817151,-3.4759211313363));
#16672=CARTESIAN_POINT('Ctrl Pts',(4.56905626114596,-1.04099311058529,-3.47361895741318));
#16673=CARTESIAN_POINT('Ctrl Pts',(4.59861984042386,-1.01089498991805,-3.47131678349006));
#16674=CARTESIAN_POINT('Ctrl Pts',(4.62678865478913,-0.979631082306754,
-3.46901460956694));
#16675=CARTESIAN_POINT('Ctrl Pts',(4.66361982320017,-0.938753030732151,
-3.4660044809057));
#16676=CARTESIAN_POINT('Ctrl Pts',(4.69821983574435,-0.895709091091989,
-3.46299435224446));
#16677=CARTESIAN_POINT('Ctrl Pts',(4.73032487114932,-0.850772441563712,
-3.45998422358323));
#16678=CARTESIAN_POINT('Ctrl Pts',(4.76237284686017,-0.805915657123414,
-3.45697944476878));
#16679=CARTESIAN_POINT('Ctrl Pts',(4.79193434075991,-0.759173264671589,
-3.45397466595434));
#16680=CARTESIAN_POINT('Ctrl Pts',(4.81878488625366,-0.710852425807533,
-3.4509698871399));
#16681=CARTESIAN_POINT('Ctrl Pts',(4.84560886758107,-0.66257939240805,-3.44796808105628));
#16682=CARTESIAN_POINT('Ctrl Pts',(4.86972695822759,-0.61273146543722,-3.44496627497266));
#16683=CARTESIAN_POINT('Ctrl Pts',(4.89095829276723,-0.561644215008064,
-3.44196446888904));
#16684=CARTESIAN_POINT('Ctrl Pts',(4.9121770082823,-0.510587328721452,-3.43896444695444));
#16685=CARTESIAN_POINT('Ctrl Pts',(4.93051216618611,-0.458293065675363,
-3.43596442501984));
#16686=CARTESIAN_POINT('Ctrl Pts',(4.94583015498946,-0.405118904981052,
-3.43296440308524));
#16687=CARTESIAN_POINT('Ctrl Pts',(4.96114508929324,-0.351955347535801,
-3.42996497937315));
#16688=CARTESIAN_POINT('Ctrl Pts',(4.97344390322272,-0.297912748086719,
-3.42696555566106));
#16689=CARTESIAN_POINT('Ctrl Pts',(4.98264289932671,-0.24336352792746,-3.42396613194897));
#16690=CARTESIAN_POINT('Ctrl Pts',(4.99185035257525,-0.188764157661157,
-3.42096395070121));
#16691=CARTESIAN_POINT('Ctrl Pts',(4.99795220639281,-0.133657758030206,
-3.41796176945345));
#16692=CARTESIAN_POINT('Ctrl Pts',(5.00091623531578,-0.0784252382045063,
-3.4149595882057));
#16693=CARTESIAN_POINT('Ctrl Pts',(5.00388161339891,-0.0231675777618596,
-3.41195604043168));
#16694=CARTESIAN_POINT('Ctrl Pts',(5.00370632110761,0.03221578827842,-3.40895249265766));
#16695=CARTESIAN_POINT('Ctrl Pts',(5.00041031804309,0.0873438846819063,
-3.40594894488364));
#16696=CARTESIAN_POINT('Ctrl Pts',(4.99710809432749,0.142576026089676,-3.40293972841868));
#16697=CARTESIAN_POINT('Ctrl Pts',(4.99067345556114,0.19755140961117,-3.39993051195371));
#16698=CARTESIAN_POINT('Ctrl Pts',(4.98117816982806,0.251895282679516,-3.39692129548874));
#16699=CARTESIAN_POINT('Ctrl Pts',(4.97391388709474,0.293470572764479,-3.39461912156562));
#16700=CARTESIAN_POINT('Ctrl Pts',(4.96485932466931,0.334676361031509,-3.3923169476425));
#16701=CARTESIAN_POINT('Ctrl Pts',(4.95406629023054,0.375350977556793,-3.39001477371938));
#16702=CARTESIAN_POINT('Ctrl Pts',(4.93995422772319,0.428533679244945,-3.38700464505814));
#16703=CARTESIAN_POINT('Ctrl Pts',(4.92280908086353,0.481031160584219,-3.3839945163969));
#16704=CARTESIAN_POINT('Ctrl Pts',(4.90271549281963,0.532473200675057,-3.38098438773566));
#16705=CARTESIAN_POINT('Ctrl Pts',(4.88265761674345,0.58382381376586,-3.37797960892122));
#16706=CARTESIAN_POINT('Ctrl Pts',(4.85966188930974,0.634122220236664,-3.37497483010677));
#16707=CARTESIAN_POINT('Ctrl Pts',(4.83386291895825,0.683012591381131,-3.37197005129233));
#16708=CARTESIAN_POINT('Ctrl Pts',(4.80808947241373,0.73185459360319,-3.36896824520871));
#16709=CARTESIAN_POINT('Ctrl Pts',(4.77951852207243,0.779290855221503,-3.36596643912509));
#16710=CARTESIAN_POINT('Ctrl Pts',(4.74833229277643,0.82498654238173,-3.36296463304147));
#16711=CARTESIAN_POINT('Ctrl Pts',(4.71716459928151,0.870655069920977,-3.35996461110687));
#16712=CARTESIAN_POINT('Ctrl Pts',(4.68338500489004,0.914584638159706,-3.35696458917227));
#16713=CARTESIAN_POINT('Ctrl Pts',(4.64721990318528,0.956468018696754,-3.35396456723767));
#16714=CARTESIAN_POINT('Ctrl Pts',(4.61106201302042,0.998343047434538,-3.35096514352558));
#16715=CARTESIAN_POINT('Ctrl Pts',(4.57251990518736,1.03817229928629,-3.34796571981349));
#16716=CARTESIAN_POINT('Ctrl Pts',(4.53185976058371,1.07568218585125,-3.34496629610139));
#16717=CARTESIAN_POINT('Ctrl Pts',(4.4911622348663,1.11322655732398,-3.34196411485363));
#16718=CARTESIAN_POINT('Ctrl Pts',(4.44834317107264,1.14844694454692,-3.33896193360588));
#16719=CARTESIAN_POINT('Ctrl Pts',(4.40370398301709,1.18110823055185,-3.33595975235812));
#16720=CARTESIAN_POINT('Ctrl Pts',(4.35904447619406,1.21378438324915,-3.3329562045841));
#16721=CARTESIAN_POINT('Ctrl Pts',(4.31256363758637,1.24389882502826,-3.32995265681008));
#16722=CARTESIAN_POINT('Ctrl Pts',(4.26459145005377,1.27126010921985,-3.32694910903606));
#16723=CARTESIAN_POINT('Ctrl Pts',(4.21652872309059,1.29867303323064,-3.32393989257109));
#16724=CARTESIAN_POINT('Ctrl Pts',(4.16696949848021,1.32332218383281,-3.32093067610612));
#16725=CARTESIAN_POINT('Ctrl Pts',(4.11626685538243,1.3450629053968,-3.31792145964115));
#16726=CARTESIAN_POINT('Ctrl Pts',(4.07747725545448,1.36169544839827,-3.31561928571804));
#16727=CARTESIAN_POINT('Ctrl Pts',(4.03801892144761,1.37662668963314,-3.31331711179493));
#16728=CARTESIAN_POINT('Ctrl Pts',(3.99805556378633,1.38981168361494,-3.31101493787181));
#16729=CARTESIAN_POINT('Ctrl Pts',(3.94580284426425,1.40705127089563,-3.30800480921057));
#16730=CARTESIAN_POINT('Ctrl Pts',(3.89246674984226,1.42137616669333,-3.30499468054934));
#16731=CARTESIAN_POINT('Ctrl Pts',(3.83840359918223,1.43265497469313,-3.3019845518881));
#16732=CARTESIAN_POINT('Ctrl Pts',(3.78443653397428,1.4439137370731,-3.29897977307365));
#16733=CARTESIAN_POINT('Ctrl Pts',(3.72974548967968,1.45213704830831,-3.29597499425921));
#16734=CARTESIAN_POINT('Ctrl Pts',(3.67470203193942,1.45724322318147,-3.29297021544476));
#16735=CARTESIAN_POINT('Ctrl Pts',(3.61971303058135,1.46234434634056,-3.28996840936114));
#16736=CARTESIAN_POINT('Ctrl Pts',(3.5643728297189,1.46433439363332,-3.28696660327752));
#16737=CARTESIAN_POINT('Ctrl Pts',(3.5090614286548,1.4631830313656,-3.28396479719391));
#16738=CARTESIAN_POINT('Ctrl Pts',(3.45378290239316,1.46203235341986,-3.28096477525931));
#16739=CARTESIAN_POINT('Ctrl Pts',(3.39853366894963,1.457743977644,-3.27796475332471));
#16740=CARTESIAN_POINT('Ctrl Pts',(3.3436947409438,1.4503396463646,-3.27496473139011));
#16741=CARTESIAN_POINT('Ctrl Pts',(3.28886674815168,1.44293679155362,-3.27196530767802));
#16742=CARTESIAN_POINT('Ctrl Pts',(3.23444942138508,1.43241928581962,-3.26896588396592));
#16743=CARTESIAN_POINT('Ctrl Pts',(3.18081733849026,1.41886057519988,-3.26596646025383));
#16744=CARTESIAN_POINT('Ctrl Pts',(3.12713594866328,1.40528939930957,-3.26296427900607));
#16745=CARTESIAN_POINT('Ctrl Pts',(3.07424175811424,1.38867156231255,-3.25996209775831));
#16746=CARTESIAN_POINT('Ctrl Pts',(3.02249637495661,1.36913103940185,-3.25695991651055));
#16747=CARTESIAN_POINT('Ctrl Pts',(2.97072743844921,1.34958162207888,-3.25395636873653));
#16748=CARTESIAN_POINT('Ctrl Pts',(2.92010883524168,1.32710708157945,-3.25095282096251));
#16749=CARTESIAN_POINT('Ctrl Pts',(2.87098120841114,1.30187918172084,-3.24794927318849));
#16750=CARTESIAN_POINT('Ctrl Pts',(2.82176086145281,1.27660366844695,-3.24494005672353));
#16751=CARTESIAN_POINT('Ctrl Pts',(2.7740375686657,1.2485646831774,-3.24193084025856));
#16752=CARTESIAN_POINT('Ctrl Pts',(2.72812540409954,1.21797889994283,-3.23892162379359));
#16753=CARTESIAN_POINT('Ctrl Pts',(2.69300071657754,1.19457952226413,-3.23661944987048));
#16754=CARTESIAN_POINT('Ctrl Pts',(2.65893552139658,1.16969047719012,-3.23431727594736));
#16755=CARTESIAN_POINT('Ctrl Pts',(2.62605691234446,1.14342431856989,-3.23201510202425));
#16756=CARTESIAN_POINT('Ctrl Pts',(2.5835930740428,1.1095006841884,-3.22904176635002));
#16757=CARTESIAN_POINT('Ctrl Pts',(2.54292174979811,1.07312835563625,-3.2260684306758));
#16758=CARTESIAN_POINT('Ctrl Pts',(2.50434371988584,1.0345261161746,-3.22309509500158));
#16759=CARTESIAN_POINT('Ctrl Pts',(2.46583075694527,0.995988984517273,-3.22012677425292));
#16760=CARTESIAN_POINT('Ctrl Pts',(2.42940446987904,0.955229777174039,-3.21715845350425));
#16761=CARTESIAN_POINT('Ctrl Pts',(2.39533283488617,0.912507618694519,-3.21419013275559));
#16762=CARTESIAN_POINT('Ctrl Pts',(2.36129435586734,0.869827034233313,-3.21122470055529));
#16763=CARTESIAN_POINT('Ctrl Pts',(2.32960632975867,0.825187701629692,-3.20825926835499));
#16764=CARTESIAN_POINT('Ctrl Pts',(2.30049855645537,0.778884115596297,-3.2052938361547));
#16765=CARTESIAN_POINT('Ctrl Pts',(2.27140692485811,0.732606207201201,-3.20233004843385));
#16766=CARTESIAN_POINT('Ctrl Pts',(2.24489299935041,0.684666332099463,-3.199366260713));
#16767=CARTESIAN_POINT('Ctrl Pts',(2.22114359965401,0.635388401538536,-3.19640247299214));
#16768=CARTESIAN_POINT('Ctrl Pts',(2.19727268357613,0.58585833509691,-3.19342352072971));
#16769=CARTESIAN_POINT('Ctrl Pts',(2.17619494012542,0.534976960907847,-3.19044456846727));
#16770=CARTESIAN_POINT('Ctrl Pts',(2.1580524439776,0.483096538257368,-3.18746561620484));
#16771=CARTESIAN_POINT('Ctrl Pts',(2.13998954434235,0.431443730411376,-3.18449973348968));
#16772=CARTESIAN_POINT('Ctrl Pts',(2.12483631177765,0.378801157227782,-3.18153385077452));
#16773=CARTESIAN_POINT('Ctrl Pts',(2.11268295892437,0.325531900121845,-3.17856796805937));
#16774=CARTESIAN_POINT('Ctrl Pts',(2.10044927308004,0.27191053616886,-3.17558248102329));
#16775=CARTESIAN_POINT('Ctrl Pts',(2.0912553792392,0.217654718773236,-3.17259699398722));
#16776=CARTESIAN_POINT('Ctrl Pts',(2.08514055124846,0.16314236463543,-3.16961150695114));
#16777=CARTESIAN_POINT('Ctrl Pts',(2.07902572325772,0.108630010497624,-3.16662601991506));
#16778=CARTESIAN_POINT('Ctrl Pts',(2.07598993226836,0.0538616760797857,
-3.16364053287899));
#16779=CARTESIAN_POINT('Ctrl Pts',(2.07601926119859,-0.000785455376519445,
-3.16065504584291));
#16780=CARTESIAN_POINT('Ctrl Pts',(2.07601929469955,-0.000845575214942023,
-3.08934495419128));
#16781=CARTESIAN_POINT('Ctrl Pts',(2.07598788830133,0.0535118081616528,
-3.09231391351179));
#16782=CARTESIAN_POINT('Ctrl Pts',(2.07898914341997,0.107988214496755,-3.09528287283231));
#16783=CARTESIAN_POINT('Ctrl Pts',(2.08503651530545,0.162212222221544,-3.09825183215282));
#16784=CARTESIAN_POINT('Ctrl Pts',(2.09107644060574,0.216369459835164,-3.10121713556976));
#16785=CARTESIAN_POINT('Ctrl Pts',(2.10015500184333,0.270274378399644,-3.10418243898669));
#16786=CARTESIAN_POINT('Ctrl Pts',(2.11223365853967,0.323556270402055,-3.10714774240363));
#16787=CARTESIAN_POINT('Ctrl Pts',(2.12430251114413,0.376794914170989,-3.11011063892153));
#16788=CARTESIAN_POINT('Ctrl Pts',(2.13936651916553,0.429411004753964,-3.11307353543942));
#16789=CARTESIAN_POINT('Ctrl Pts',(2.15733575241434,0.481042181836397,-3.11603643195732));
#16790=CARTESIAN_POINT('Ctrl Pts',(2.1752979395256,0.532653113181575,-3.11899816665735));
#16791=CARTESIAN_POINT('Ctrl Pts',(2.19616291584931,0.583279384128728,-3.12195990135737));
#16792=CARTESIAN_POINT('Ctrl Pts',(2.21979111334346,0.632574439960861,-3.1249216360574));
#16793=CARTESIAN_POINT('Ctrl Pts',(2.24343713421129,0.681906680356117,-3.12788560487216));
#16794=CARTESIAN_POINT('Ctrl Pts',(2.26985031141326,0.729905205751302,-3.13084957368693));
#16795=CARTESIAN_POINT('Ctrl Pts',(2.29884387362766,0.776245679977589,-3.13381354250169));
#16796=CARTESIAN_POINT('Ctrl Pts',(2.32784691981308,0.822601312455631,-3.13677848084874));
#16797=CARTESIAN_POINT('Ctrl Pts',(2.3594317215764,0.867297366745525,-3.13974341919578));
#16798=CARTESIAN_POINT('Ctrl Pts',(2.39336858699972,0.910039210800623,-3.14270835754282));
#16799=CARTESIAN_POINT('Ctrl Pts',(2.42737043916069,0.952862902515246,-3.14567897354064));
#16800=CARTESIAN_POINT('Ctrl Pts',(2.46373299244548,0.993724499544306,-3.14864958953847));
#16801=CARTESIAN_POINT('Ctrl Pts',(2.50218756820692,1.03236410534434,-3.15162020553629));
#16802=CARTESIAN_POINT('Ctrl Pts',(2.53831800319773,1.06866838741702,-3.15441128165836));
#16803=CARTESIAN_POINT('Ctrl Pts',(2.57629459257143,1.10301125847451,-3.15720235778043));
#16804=CARTESIAN_POINT('Ctrl Pts',(2.61586914384278,1.13521059723488,-3.1599934339025));
#16805=CARTESIAN_POINT('Ctrl Pts',(2.65854963187952,1.16993704260453,-3.16300356256374));
#16806=CARTESIAN_POINT('Ctrl Pts',(2.70328093322167,1.20232611928244,-3.16601369122498));
#16807=CARTESIAN_POINT('Ctrl Pts',(2.7497769339639,1.23212809378357,-3.16902381988622));
#16808=CARTESIAN_POINT('Ctrl Pts',(2.79619029821165,1.2618771017787,-3.17202859870067));
#16809=CARTESIAN_POINT('Ctrl Pts',(2.84436169668854,1.28904784969789,-3.17503337751511));
#16810=CARTESIAN_POINT('Ctrl Pts',(2.89397305648445,1.31343161973127,-3.17803815632955));
#16811=CARTESIAN_POINT('Ctrl Pts',(2.94353533405915,1.33779126606395,-3.18103996241318));
#16812=CARTESIAN_POINT('Ctrl Pts',(2.99453427924996,1.35936916469082,-3.1840417684968));
#16813=CARTESIAN_POINT('Ctrl Pts',(3.04662564177115,1.37800157391331,-3.18704357458042));
#16814=CARTESIAN_POINT('Ctrl Pts',(3.09868604334722,1.39662290880464,-3.19004359651502));
#16815=CARTESIAN_POINT('Ctrl Pts',(3.15183707905261,1.4123020467382,-3.19304361844962));
#16816=CARTESIAN_POINT('Ctrl Pts',(3.20571499639883,1.42492354304259,-3.19604364038422));
#16817=CARTESIAN_POINT('Ctrl Pts',(3.25958217016266,1.43754252254432,-3.19904306409631));
#16818=CARTESIAN_POINT('Ctrl Pts',(3.31417542380638,1.44710495089077,-3.2020424878084));
#16819=CARTESIAN_POINT('Ctrl Pts',(3.36911859454331,1.45354598641942,-3.2050419115205));
#16820=CARTESIAN_POINT('Ctrl Pts',(3.42411227756775,1.45999294354731,-3.20804409276826));
#16821=CARTESIAN_POINT('Ctrl Pts',(3.47945599474517,1.4633127130099,-3.21104627401601));
#16822=CARTESIAN_POINT('Ctrl Pts',(3.53476769754728,1.46349228718359,-3.21404845526377));
#16823=CARTESIAN_POINT('Ctrl Pts',(3.59010457700865,1.46367194309545,-3.21705200303779));
#16824=CARTESIAN_POINT('Ctrl Pts',(3.64540888476693,1.46070858272001,-3.22005555081181));
#16825=CARTESIAN_POINT('Ctrl Pts',(3.70030113358416,1.45464132064724,-3.22305909858583));
#16826=CARTESIAN_POINT('Ctrl Pts',(3.75529698228306,1.4485626076384,-3.22606831505079));
#16827=CARTESIAN_POINT('Ctrl Pts',(3.80987869642373,1.43936837842353,-3.22907753151576));
#16828=CARTESIAN_POINT('Ctrl Pts',(3.86367561185656,1.42714917709382,-3.23208674798073));
#16829=CARTESIAN_POINT('Ctrl Pts',(3.90483245693408,1.41780098729424,-3.23438892190384));
#16830=CARTESIAN_POINT('Ctrl Pts',(3.94553013665897,1.40668339077255,-3.23669109582695));
#16831=CARTESIAN_POINT('Ctrl Pts',(3.98560979439686,1.39385626882432,-3.23899326975006));
#16832=CARTESIAN_POINT('Ctrl Pts',(4.03801457810078,1.37708460486359,-3.2420033984113));
#16833=CARTESIAN_POINT('Ctrl Pts',(4.08958230895929,1.3573182004886,-3.24501352707254));
#16834=CARTESIAN_POINT('Ctrl Pts',(4.1399474969429,1.33466023039937,-3.24802365573378));
#16835=CARTESIAN_POINT('Ctrl Pts',(4.19022317179605,1.31204252990732,-3.25102843454823));
#16836=CARTESIAN_POINT('Ctrl Pts',(4.23930006744847,1.28654367725026,-3.25403321336267));
#16837=CARTESIAN_POINT('Ctrl Pts',(4.28682958332776,1.25831602445872,-3.25703799217712));
#16838=CARTESIAN_POINT('Ctrl Pts',(4.3343120766255,1.23011629825302,-3.26003979826074));
#16839=CARTESIAN_POINT('Ctrl Pts',(4.38024977090027,1.19919338822748,-3.26304160434436));
#16840=CARTESIAN_POINT('Ctrl Pts',(4.42431743106801,1.16574614543989,-3.26604341042798));
#16841=CARTESIAN_POINT('Ctrl Pts',(4.46835889924644,1.13231878230604,-3.26904343236258));
#16842=CARTESIAN_POINT('Ctrl Pts',(4.51053211649643,1.09637037886893,-3.27204345429718));
#16843=CARTESIAN_POINT('Ctrl Pts',(4.55054164186696,1.05814250911204,-3.27504347623178));
#16844=CARTESIAN_POINT('Ctrl Pts',(4.59054318909628,1.01992226222347,-3.27804289994387));
#16845=CARTESIAN_POINT('Ctrl Pts',(4.62838151966835,0.979423816342135,-3.28104232365596));
#16846=CARTESIAN_POINT('Ctrl Pts',(4.66379679307575,0.936926788695683,-3.28404174736805));
#16847=CARTESIAN_POINT('Ctrl Pts',(4.69924462569751,0.894390691187572,-3.28704392861581));
#16848=CARTESIAN_POINT('Ctrl Pts',(4.73226461177485,0.84985274759171,-3.29004610986357));
#16849=CARTESIAN_POINT('Ctrl Pts',(4.76263710725688,0.803625826518099,-3.29304829111132));
#16850=CARTESIAN_POINT('Ctrl Pts',(4.79302342762465,0.757377863976139,-3.29605183888535));
#16851=CARTESIAN_POINT('Ctrl Pts',(4.82075959021328,0.709439849350995,-3.29905538665937));
#16852=CARTESIAN_POINT('Ctrl Pts',(4.84567100420749,0.660150985476005,-3.30205893443339));
#16853=CARTESIAN_POINT('Ctrl Pts',(4.87062943430318,0.610769097165448,-3.30506815089835));
#16854=CARTESIAN_POINT('Ctrl Pts',(4.89275225423175,0.560031751868331,-3.30807736736332));
#16855=CARTESIAN_POINT('Ctrl Pts',(4.9119127676701,0.5082988637216,-3.31108658382829));
#16856=CARTESIAN_POINT('Ctrl Pts',(4.92657134571018,0.468721084108464,-3.3133887577514));
#16857=CARTESIAN_POINT('Ctrl Pts',(4.93949711185437,0.428561070948688,-3.31569093167451));
#16858=CARTESIAN_POINT('Ctrl Pts',(4.95065341965792,0.38798458985369,-3.31799310559762));
#16859=CARTESIAN_POINT('Ctrl Pts',(4.96524046781094,0.33493020178591,-3.32100323425886));
#16860=CARTESIAN_POINT('Ctrl Pts',(4.97686197788097,0.280940553597557,-3.3240133629201));
#16861=CARTESIAN_POINT('Ctrl Pts',(4.98540465913867,0.226378127275795,-3.32702349158134));
#16862=CARTESIAN_POINT('Ctrl Pts',(4.99393215764469,0.171912673759671,-3.33002827039579));
#16863=CARTESIAN_POINT('Ctrl Pts',(4.99939160542292,0.116876979854145,-3.33303304921023));
#16864=CARTESIAN_POINT('Ctrl Pts',(5.00172012741486,0.061646252471897,-3.33603782802467));
#16865=CARTESIAN_POINT('Ctrl Pts',(5.00404634572006,0.0064701667441437,
-3.33903963410829));
#16866=CARTESIAN_POINT('Ctrl Pts',(5.00324775216541,-0.0489000451757802,
-3.34204144019191));
#16867=CARTESIAN_POINT('Ctrl Pts',(4.99931318269029,-0.104083338714585,
-3.34504324627553));
#16868=CARTESIAN_POINT('Ctrl Pts',(4.99538095176005,-0.159233833592706,
-3.34804326821013));
#16869=CARTESIAN_POINT('Ctrl Pts',(4.98831647675397,-0.214197104563205,
-3.35104329014472));
#16870=CARTESIAN_POINT('Ctrl Pts',(4.97816065460882,-0.268593716802175,
-3.35404331207932));
#16871=CARTESIAN_POINT('Ctrl Pts',(4.96800685759601,-0.322979482027846,
-3.35704273579141));
#16872=CARTESIAN_POINT('Ctrl Pts',(4.95476303452417,-0.376798294070876,
-3.3600421595035));
#16873=CARTESIAN_POINT('Ctrl Pts',(4.93852139651355,-0.429679747757702,
-3.36304158321559));
#16874=CARTESIAN_POINT('Ctrl Pts',(4.92226482666919,-0.482609818281916,
-3.36604376446335));
#16875=CARTESIAN_POINT('Ctrl Pts',(4.9030050910297,-0.53460030282857,-3.36904594571111));
#16876=CARTESIAN_POINT('Ctrl Pts',(4.88088421282898,-0.585296293413464,
-3.37204812695887));
#16877=CARTESIAN_POINT('Ctrl Pts',(4.85875326569557,-0.636015359687887,
-3.37505167473289));
#16878=CARTESIAN_POINT('Ctrl Pts',(4.8337588186512,-0.685438285322511,-3.3780552225069));
#16879=CARTESIAN_POINT('Ctrl Pts',(4.80608956746164,-0.733233506714226,
-3.38105877028092));
#16880=CARTESIAN_POINT('Ctrl Pts',(4.77836809521701,-0.781118933542707,
-3.38406798674589));
#16881=CARTESIAN_POINT('Ctrl Pts',(4.747962025003,-0.82737007691808,-3.38707720321085));
#16882=CARTESIAN_POINT('Ctrl Pts',(4.71510356822208,-0.871684169588439,
-3.39008641967582));
#16883=CARTESIAN_POINT('Ctrl Pts',(4.68996550213884,-0.905586266616097,
-3.39238859359894));
#16884=CARTESIAN_POINT('Ctrl Pts',(4.66339299817311,-0.938355217170147,
-3.39469076752206));
#16885=CARTESIAN_POINT('Ctrl Pts',(4.63550486601212,-0.969869755187481,
-3.39699294144519));
#16886=CARTESIAN_POINT('Ctrl Pts',(4.59904069400365,-1.0110755099651,-3.40000307010642));
#16887=CARTESIAN_POINT('Ctrl Pts',(4.56017285810662,-1.05030856924529,-3.40301319876766));
#16888=CARTESIAN_POINT('Ctrl Pts',(4.51914304513095,-1.08727599025842,-3.40602332742889));
#16889=CARTESIAN_POINT('Ctrl Pts',(4.47818615369389,-1.12417770974811,-3.40902810624334));
#16890=CARTESIAN_POINT('Ctrl Pts',(4.43507529971017,-1.15882143129324,-3.41203288505778));
#16891=CARTESIAN_POINT('Ctrl Pts',(4.39009037438196,-1.190949483756,-3.41503766387222));
#16892=CARTESIAN_POINT('Ctrl Pts',(4.3451499541845,-1.22304575083365,-3.41803946995584));
#16893=CARTESIAN_POINT('Ctrl Pts',(4.29833956314318,-1.25263097367015,-3.42104127603946));
#16894=CARTESIAN_POINT('Ctrl Pts',(4.24997223634424,-1.27948760080524,-3.42404308212308));
#16895=CARTESIAN_POINT('Ctrl Pts',(4.20163365707812,-1.30632826547515,-3.42704310405768));
#16896=CARTESIAN_POINT('Ctrl Pts',(4.15174043700631,-1.33044329302549,-3.43004312599228));
#16897=CARTESIAN_POINT('Ctrl Pts',(4.10063270893127,-1.35165961404322,-3.43304314792688));
#16898=CARTESIAN_POINT('Ctrl Pts',(4.04953517204602,-1.37287170439833,-3.43604257163897));
#16899=CARTESIAN_POINT('Ctrl Pts',(3.9972240956012,-1.39118603377396,-3.43904199535107));
#16900=CARTESIAN_POINT('Ctrl Pts',(3.94406008769248,-1.40647744353222,-3.44204141906316));
#16901=CARTESIAN_POINT('Ctrl Pts',(3.89084720317884,-1.42178291152692,-3.44504360031092));
#16902=CARTESIAN_POINT('Ctrl Pts',(3.83678032920723,-1.4340597612545,-3.44804578155868));
#16903=CARTESIAN_POINT('Ctrl Pts',(3.78223431170352,-1.44323302066628,-3.45104796280644));
#16904=CARTESIAN_POINT('Ctrl Pts',(3.72766346606344,-1.45241045554212,-3.45405151058046));
#16905=CARTESIAN_POINT('Ctrl Pts',(3.67261356798181,-1.45848142601991,-3.45705505835448));
#16906=CARTESIAN_POINT('Ctrl Pts',(3.61746541352522,-1.46142280483067,-3.4600586061285));
#16907=CARTESIAN_POINT('Ctrl Pts',(3.56221317620818,-1.46436973499892,-3.46306782259346));
#16908=CARTESIAN_POINT('Ctrl Pts',(3.5068628414747,-1.46417527605418,-3.46607703905843));
#16909=CARTESIAN_POINT('Ctrl Pts',(3.45179486444536,-1.46086848045762,-3.46908625552339));
#16910=CARTESIAN_POINT('Ctrl Pts',(3.40966560515415,-1.45833864630307,-3.47138842944651));
#16911=CARTESIAN_POINT('Ctrl Pts',(3.36770161530294,-1.45398828503212,-3.47369060336963));
#16912=CARTESIAN_POINT('Ctrl Pts',(3.32606937562991,-1.44785064365449,-3.47599277729275));
#16913=CARTESIAN_POINT('Ctrl Pts',(3.27163456659456,-1.43982558089202,-3.47900290595399));
#16914=CARTESIAN_POINT('Ctrl Pts',(3.21753859061648,-1.42870951185746,-3.48201303461522));
#16915=CARTESIAN_POINT('Ctrl Pts',(3.16415885187338,-1.41454479297928,-3.48502316327646));
#16916=CARTESIAN_POINT('Ctrl Pts',(3.11087398396675,-1.40040524879772,-3.48802794209091));
#16917=CARTESIAN_POINT('Ctrl Pts',(3.05830333342818,-1.38322794180099,-3.49103272090535));
#16918=CARTESIAN_POINT('Ctrl Pts',(3.00681563822438,-1.36310649790541,-3.4940374997198));
#16919=CARTESIAN_POINT('Ctrl Pts',(2.95537888156484,-1.34300496084498,-3.49703930580342));
#16920=CARTESIAN_POINT('Ctrl Pts',(2.90502344730855,-1.31996524816041,-3.50004111188704));
#16921=CARTESIAN_POINT('Ctrl Pts',(2.85610258180067,-1.2941306658973,-3.50304291797066));
#16922=CARTESIAN_POINT('Ctrl Pts',(2.80721079282602,-1.26831143863827,-3.50604293990526));
#16923=CARTESIAN_POINT('Ctrl Pts',(2.75975234866062,-1.2397008804422,-3.50904296183986));
#16924=CARTESIAN_POINT('Ctrl Pts',(2.71405804682371,-1.20848929723721,-3.51204298377445));
#16925=CARTESIAN_POINT('Ctrl Pts',(2.66837285670687,-1.17728393781061,-3.51504240748654));
#16926=CARTESIAN_POINT('Ctrl Pts',(2.62445154614612,-1.14347888111928,-3.51804183119863));
#16927=CARTESIAN_POINT('Ctrl Pts',(2.58259597371697,-1.10730775995993,-3.52104125491072));
#16928=CARTESIAN_POINT('Ctrl Pts',(2.54070192115126,-1.07110338469365,-3.52404343615847));
#16929=CARTESIAN_POINT('Ctrl Pts',(2.50087780140589,-1.03252894514098,-3.52704561740623));
#16930=CARTESIAN_POINT('Ctrl Pts',(2.46339121993172,-0.991857420419962,
-3.53004779865399));
#16931=CARTESIAN_POINT('Ctrl Pts',(2.42588757539782,-0.95116738292376,-3.53305134642801));
#16932=CARTESIAN_POINT('Ctrl Pts',(2.39072392602788,-0.908378766162718,
-3.53605489420202));
#16933=CARTESIAN_POINT('Ctrl Pts',(2.35812770700803,-0.863797860442005,
-3.53905844197604));
#16934=CARTESIAN_POINT('Ctrl Pts',(2.32546996811047,-0.819132815764377,
-3.54206765844101));
#16935=CARTESIAN_POINT('Ctrl Pts',(2.2953896270958,-0.772669169180946,-3.54507687490597));
#16936=CARTESIAN_POINT('Ctrl Pts',(2.26807023093027,-0.724741436245074,
-3.54808609137094));
#16937=CARTESIAN_POINT('Ctrl Pts',(2.24716977322639,-0.688074756315559,
-3.55038826529406));
#16938=CARTESIAN_POINT('Ctrl Pts',(2.22788435855148,-0.650551765120204,
-3.55269043921719));
#16939=CARTESIAN_POINT('Ctrl Pts',(2.21027710606191,-0.612330060793335,
-3.55499261314031));
#16940=CARTESIAN_POINT('Ctrl Pts',(2.18529599781639,-0.558101240386331,
-3.5582589294499));
#16941=CARTESIAN_POINT('Ctrl Pts',(2.16360293385677,-0.50226721692865,-3.56152524575948));
#16942=CARTESIAN_POINT('Ctrl Pts',(2.14538703089759,-0.445228213542251,
-3.56479156206906));
#16943=CARTESIAN_POINT('Ctrl Pts',(2.1272219106246,-0.388348224716697,-3.56804877247176));
#16944=CARTESIAN_POINT('Ctrl Pts',(2.11251478421498,-0.330270296838304,
-3.57130598287446));
#16945=CARTESIAN_POINT('Ctrl Pts',(2.10140693884337,-0.271414451582842,
-3.57456319327716));
#16946=CARTESIAN_POINT('Ctrl Pts',(2.09034632600109,-0.21280887182384,-3.57780655344332));
#16947=CARTESIAN_POINT('Ctrl Pts',(2.08285459652992,-0.153432331059518,
-3.58104991360948));
#16948=CARTESIAN_POINT('Ctrl Pts',(2.07902279640965,-0.093717351717778,
-3.58429327377564));
#16949=CARTESIAN_POINT('Ctrl Pts',(2.07703340549742,-0.0627145766519451,
-3.58597715890459));
#16950=CARTESIAN_POINT('Ctrl Pts',(2.07602972725318,-0.0316208373297955,
-3.58766104403353));
#16951=CARTESIAN_POINT('Ctrl Pts',(2.07601913517861,-0.000498075992148151,
-3.58934492916248));
#16952=CARTESIAN_POINT('Origin',(3.53951905042299,8.32667268468867E-16,
0.));
#16953=CARTESIAN_POINT('',(2.076195135922,0.00130430976331031,-4.16065504584291));
#16954=CARTESIAN_POINT('',(2.07606592154595,0.00130399798662343,-4.08934495415709));
#16955=CARTESIAN_POINT('',(2.07601905042299,1.01189432752408E-15,0.));
#16956=CARTESIAN_POINT('Ctrl Pts',(2.076195135922,0.00130430976331031,-4.16065504584291));
#16957=CARTESIAN_POINT('Ctrl Pts',(2.07946608474589,-0.364321824825649,
-4.14077446267775));
#16958=CARTESIAN_POINT('Ctrl Pts',(2.40262791122405,-1.21940508752796,-4.09456060089675));
#16959=CARTESIAN_POINT('Ctrl Pts',(3.83411705959719,-1.70165509770555,-4.02201346049987));
#16960=CARTESIAN_POINT('Ctrl Pts',(5.12566818702416,-0.683043904164373,
-3.94301362465232));
#16961=CARTESIAN_POINT('Ctrl Pts',(4.97825236450885,0.955230081967798,-3.86401378880474));
#16962=CARTESIAN_POINT('Ctrl Pts',(3.52560638363233,1.72691183801013,-3.78501395295721));
#16963=CARTESIAN_POINT('Ctrl Pts',(2.2899855395789,1.0447694976777,-3.71722770530323));
#16964=CARTESIAN_POINT('Ctrl Pts',(2.07912945035243,0.278451525816697,-3.67577473626515));
#16965=CARTESIAN_POINT('Ctrl Pts',(2.07815730775203,-0.000561395191652214,
-3.66065504584291));
#16966=CARTESIAN_POINT('Ctrl Pts',(2.07820514495938,-0.000496870744879993,
-3.58934495415708));
#16967=CARTESIAN_POINT('Ctrl Pts',(2.07905042986027,0.274161491287648,-3.60422745243401));
#16968=CARTESIAN_POINT('Ctrl Pts',(2.28499543959671,1.0359800857574,-3.64544322932679));
#16969=CARTESIAN_POINT('Ctrl Pts',(3.51016521557272,1.7267183779139,-3.71299228483544));
#16970=CARTESIAN_POINT('Ctrl Pts',(4.96965334285999,0.968056769947792,-3.79199212068301));
#16971=CARTESIAN_POINT('Ctrl Pts',(5.13171241173874,-0.668833540148877,
-3.87099195653056));
#16972=CARTESIAN_POINT('Ctrl Pts',(3.84932116255957,-1.6989528114582,-3.94999179237812));
#16973=CARTESIAN_POINT('Ctrl Pts',(2.40888291571603,-1.22798739644682,-4.0227761249203));
#16974=CARTESIAN_POINT('Ctrl Pts',(2.07940194346651,-0.368600809769743,
-4.06922717884662));
#16975=CARTESIAN_POINT('Ctrl Pts',(2.07606592154595,0.00130399798662343,
-4.08934495415709));
#16976=CARTESIAN_POINT('Origin',(3.53951905042299,8.32667268468867E-16,
0.));
#16977=CARTESIAN_POINT('',(2.07409469887417,-0.000697191783334949,-4.66065504584291));
#16978=CARTESIAN_POINT('',(2.07601924802061,-0.000760505223226088,-4.58934495415708));
#16979=CARTESIAN_POINT('',(2.07601905042299,1.01189432752408E-15,0.));
#16980=CARTESIAN_POINT('Ctrl Pts',(2.07409469887417,-0.000697191783334949,
-4.66065504584291));
#16981=CARTESIAN_POINT('Ctrl Pts',(2.07385459663328,-0.0412693483006937,
-4.65844074632206));
#16982=CARTESIAN_POINT('Ctrl Pts',(2.09371445821182,-0.564102276336072,
-4.62989316818539));
#16983=CARTESIAN_POINT('Ctrl Pts',(2.71979604533931,-1.52002376741039,-4.57501231143279));
#16984=CARTESIAN_POINT('Ctrl Pts',(4.36468643187272,-1.51707509739907,-4.49601247558526));
#16985=CARTESIAN_POINT('Ctrl Pts',(5.26097849137829,-0.13782398812516,-4.41701263973768));
#16986=CARTESIAN_POINT('Ctrl Pts',(4.59554903047943,1.36646212526309,-4.33801280389013));
#16987=CARTESIAN_POINT('Ctrl Pts',(2.97208088054184,1.63108307020786,-4.25901296804256));
#16988=CARTESIAN_POINT('Ctrl Pts',(2.1424012204092,0.721759407375466,-4.19989371536015));
#16989=CARTESIAN_POINT('Ctrl Pts',(2.07513347508338,0.119976587921299,-4.1671077412936));
#16990=CARTESIAN_POINT('Ctrl Pts',(2.076195135922,0.00130430976331031,-4.16065504584291));
#16991=CARTESIAN_POINT('Ctrl Pts',(2.07606592154595,0.00130399798662343,
-4.08934495415709));
#16992=CARTESIAN_POINT('Ctrl Pts',(2.0750352382346,0.11558823268988,-4.09556045746248));
#16993=CARTESIAN_POINT('Ctrl Pts',(2.13929924925922,0.712915691466917,-4.12810923938368));
#16994=CARTESIAN_POINT('Ctrl Pts',(2.95751872983224,1.62594392002861,-4.18699129992084));
#16995=CARTESIAN_POINT('Ctrl Pts',(4.5832881519124,1.37585030690918,-4.26599113576836));
#16996=CARTESIAN_POINT('Ctrl Pts',(5.26214205025278,-0.122425506752148,
-4.34499097161594));
#16997=CARTESIAN_POINT('Ctrl Pts',(4.37821883844248,-1.50963593949734,-4.4239908074635));
#16998=CARTESIAN_POINT('Ctrl Pts',(2.73342059411813,-1.52729279543541,-4.50299064331106));
#16999=CARTESIAN_POINT('Ctrl Pts',(2.09607364483251,-0.572900753676928,
-4.55810869220892));
#17000=CARTESIAN_POINT('Ctrl Pts',(2.07389563130326,-0.0456866571895436,
-4.58689346249093));
#17001=CARTESIAN_POINT('Ctrl Pts',(2.07418131521338,-0.00076146030193382,
-4.58934495415708));
#17002=CARTESIAN_POINT('Origin',(3.53951905042299,8.32667268468867E-16,
0.));
#17003=CARTESIAN_POINT('',(2.07610901343792,-0.000650317076287153,-5.16065502546599));
#17004=CARTESIAN_POINT('',(2.07601916841636,-0.000587678975572513,-5.08934495412951));
#17005=CARTESIAN_POINT('',(2.07601905042299,1.01189432752408E-15,0.));
#17006=CARTESIAN_POINT('Ctrl Pts',(2.07808044699004,-0.000657693853875153,
-5.16065457821226));
#17007=CARTESIAN_POINT('Ctrl Pts',(2.0772701732856,-0.201427577003968,-5.14977343959675));
#17008=CARTESIAN_POINT('Ctrl Pts',(2.20916534632738,-0.887056648995822,
-5.11255902236538));
#17009=CARTESIAN_POINT('Ctrl Pts',(3.25102377061198,-1.70270036473932,-5.0490113265182));
#17010=CARTESIAN_POINT('Ctrl Pts',(4.80794374219368,-1.17197135624689,-4.97001149067062));
#17011=CARTESIAN_POINT('Ctrl Pts',(5.21413887471018,0.421979268046491,-4.89101165482307));
#17012=CARTESIAN_POINT('Ctrl Pts',(4.10110575481217,1.63310698731284,-4.81201181897551));
#17013=CARTESIAN_POINT('Ctrl Pts',(2.52407434145005,1.37024742679016,-4.73522628264877));
#17014=CARTESIAN_POINT('Ctrl Pts',(2.0767099823415,0.441229921360335,-4.68477402493792));
#17015=CARTESIAN_POINT('Ctrl Pts',(2.07409469887417,-0.000697191783334949,
-4.66065504584291));
#17016=CARTESIAN_POINT('Ctrl Pts',(2.07601924802061,-0.000760505223226088,
-4.58934495415708));
#17017=CARTESIAN_POINT('Ctrl Pts',(2.07599085580295,0.0538768643349187,
-4.59233017752579));
#17018=CARTESIAN_POINT('Ctrl Pts',(2.07902648452409,0.108635686348704,-4.59531540089451));
#17019=CARTESIAN_POINT('Ctrl Pts',(2.08514018297494,0.163139081524142,-4.59830062426322));
#17020=CARTESIAN_POINT('Ctrl Pts',(2.09121901100316,0.217331608173781,-4.60126882094975));
#17021=CARTESIAN_POINT('Ctrl Pts',(2.10034087561815,0.271271068644694,-4.60423701763627));
#17022=CARTESIAN_POINT('Ctrl Pts',(2.11246753287747,0.324586223168858,-4.6072052143228));
#17023=CARTESIAN_POINT('Ctrl Pts',(2.12458396202739,0.377856409552088,-4.61017090751312));
#17024=CARTESIAN_POINT('Ctrl Pts',(2.13970004715109,0.430502805880079,-4.61313660070344));
#17025=CARTESIAN_POINT('Ctrl Pts',(2.15772614502274,0.482162437966234,-4.61610229389376));
#17026=CARTESIAN_POINT('Ctrl Pts',(2.17574457529192,0.533800096049706,-4.6190667255933));
#17027=CARTESIAN_POINT('Ctrl Pts',(2.19667038709155,0.584451310505765,-4.62203115729283));
#17028=CARTESIAN_POINT('Ctrl Pts',(2.22036427111649,0.633768820811523,-4.62499558899236));
#17029=CARTESIAN_POINT('Ctrl Pts',(2.24433892995291,0.683670748372119,-4.62799514949351));
#17030=CARTESIAN_POINT('Ctrl Pts',(2.27114750041236,0.732206621938655,-4.63099470999467));
#17031=CARTESIAN_POINT('Ctrl Pts',(2.3005968689088,0.77904048556677,-4.63399427049582));
#17032=CARTESIAN_POINT('Ctrl Pts',(2.32973135258981,0.825373582174859,-4.63696175845678));
#17033=CARTESIAN_POINT('Ctrl Pts',(2.36145006211764,0.870040477621746,-4.63992924641774));
#17034=CARTESIAN_POINT('Ctrl Pts',(2.39552297687357,0.912745985312182,-4.6428967343787));
#17035=CARTESIAN_POINT('Ctrl Pts',(2.43014828052323,0.956143833188909,-4.64591233114995));
#17036=CARTESIAN_POINT('Ctrl Pts',(2.46720443639282,0.997515679329537,-4.6489279279212));
#17037=CARTESIAN_POINT('Ctrl Pts',(2.506410426729,1.0365899968884,-4.65194352469245));
#17038=CARTESIAN_POINT('Ctrl Pts',(2.54561641706517,1.07566431444727,-4.65495912146369));
#17039=CARTESIAN_POINT('Ctrl Pts',(2.58697176139739,1.11244077224011,-4.65797471823494));
#17040=CARTESIAN_POINT('Ctrl Pts',(2.63016222976418,1.14669194761336,-4.66099031500619));
#17041=CARTESIAN_POINT('Ctrl Pts',(2.67327438188038,1.1808810161437,-4.66400044366743));
#17042=CARTESIAN_POINT('Ctrl Pts',(2.71840790652042,1.21270720915157,-4.66701057232867));
#17043=CARTESIAN_POINT('Ctrl Pts',(2.76527358385478,1.24192439685295,-4.67002070098991));
#17044=CARTESIAN_POINT('Ctrl Pts',(2.81205596767518,1.27108965737926,-4.67302547980435));
#17045=CARTESIAN_POINT('Ctrl Pts',(2.8605639503056,1.29765483749972,-4.6760302586188));
#17046=CARTESIAN_POINT('Ctrl Pts',(2.91047686921657,1.32141522023286,-4.67903503743324));
#17047=CARTESIAN_POINT('Ctrl Pts',(2.96034040756352,1.34515209600376,-4.68203684351686));
#17048=CARTESIAN_POINT('Ctrl Pts',(3.01160565426423,1.36608944541669,-4.68503864960048));
#17049=CARTESIAN_POINT('Ctrl Pts',(3.06392633487658,1.38406785199252,-4.6880404556841));
#17050=CARTESIAN_POINT('Ctrl Pts',(3.11621591824668,1.40203557294925,-4.6910404776187));
#17051=CARTESIAN_POINT('Ctrl Pts',(3.16955919371126,1.41704766559505,-4.6940404995533));
#17052=CARTESIAN_POINT('Ctrl Pts',(3.22359099116527,1.42899325098954,-4.6970405214879));
#17053=CARTESIAN_POINT('Ctrl Pts',(3.27761201435219,1.44093645436208,-4.70003994519999));
#17054=CARTESIAN_POINT('Ctrl Pts',(3.33232077149073,1.4498142509152,-4.70303936891208));
#17055=CARTESIAN_POINT('Ctrl Pts',(3.38734031704768,1.45556651620882,-4.70603879262417));
#17056=CARTESIAN_POINT('Ctrl Pts',(3.44241044510778,1.46132406987723,-4.70904097387193));
#17057=CARTESIAN_POINT('Ctrl Pts',(3.4977914060457,1.46395029642692,-4.71204315511969));
#17058=CARTESIAN_POINT('Ctrl Pts',(3.55310101836569,1.46343697511946,-4.71504533636744));
#17059=CARTESIAN_POINT('Ctrl Pts',(3.60843580639342,1.46292342015954,-4.71804888414146));
#17060=CARTESIAN_POINT('Ctrl Pts',(3.66369865318093,1.45926750354695,-4.72105243191548));
#17061=CARTESIAN_POINT('Ctrl Pts',(3.71851059124897,1.45251309058223,-4.7240559796895));
#17062=CARTESIAN_POINT('Ctrl Pts',(3.77342597762567,1.44574592979976,-4.72706519615447));
#17063=CARTESIAN_POINT('Ctrl Pts',(3.82788823433538,1.4358686850687,-4.73007441261943));
#17064=CARTESIAN_POINT('Ctrl Pts',(3.88152786054452,1.42297653662991,-4.7330836290844));
#17065=CARTESIAN_POINT('Ctrl Pts',(3.92256437291978,1.41311351471232,-4.73538580300752));
#17066=CARTESIAN_POINT('Ctrl Pts',(3.96311959087821,1.40148697680282,-4.73768797693064));
#17067=CARTESIAN_POINT('Ctrl Pts',(4.00303542037397,1.38815878947168,-4.73999015085375));
#17068=CARTESIAN_POINT('Ctrl Pts',(4.05522599607103,1.37073197463159,-4.74300027951499));
#17069=CARTESIAN_POINT('Ctrl Pts',(4.10654206993801,1.35032113999199,-4.74601040817623));
#17070=CARTESIAN_POINT('Ctrl Pts',(4.15661947307721,1.32703403059604,-4.74902053683747));
#17071=CARTESIAN_POINT('Ctrl Pts',(4.20660787456074,1.3037883089551,-4.75202531565191));
#17072=CARTESIAN_POINT('Ctrl Pts',(4.25536149914432,1.27767667814298,-4.75503009446636));
#17073=CARTESIAN_POINT('Ctrl Pts',(4.30253368209914,1.24885584510307,-4.7580348732808));
#17074=CARTESIAN_POINT('Ctrl Pts',(4.3496591959941,1.22006352550261,-4.76103667936442));
#17075=CARTESIAN_POINT('Ctrl Pts',(4.39520591916271,1.18856758721965,-4.76403848544803));
#17076=CARTESIAN_POINT('Ctrl Pts',(4.43885113301751,1.15457093988035,-4.76704029153165));
#17077=CARTESIAN_POINT('Ctrl Pts',(4.48247040596762,1.12059449873803,-4.77004031346625));
#17078=CARTESIAN_POINT('Ctrl Pts',(4.52418999388672,1.0841206184022,-4.77304033540085));
#17079=CARTESIAN_POINT('Ctrl Pts',(4.56371750516629,1.04539455484589,-4.77604035733545));
#17080=CARTESIAN_POINT('Ctrl Pts',(4.60323713442113,1.00667621350079,-4.77903978104754));
#17081=CARTESIAN_POINT('Ctrl Pts',(4.64056517809698,0.965706950209743,-4.78203920475962));
#17082=CARTESIAN_POINT('Ctrl Pts',(4.67544531879757,0.922769615243488,-4.78503862847171));
#17083=CARTESIAN_POINT('Ctrl Pts',(4.71035752673553,0.879792805616716,-4.78804080971947));
#17084=CARTESIAN_POINT('Ctrl Pts',(4.74281700180259,0.834844720244073,-4.79104299096723));
#17085=CARTESIAN_POINT('Ctrl Pts',(4.77260803644009,0.788240954634642,-4.79404517221498));
#17086=CARTESIAN_POINT('Ctrl Pts',(4.80241263129523,0.741615976025646,-4.797048719989));
#17087=CARTESIAN_POINT('Ctrl Pts',(4.82954610528484,0.69333427607016,-4.80005226776302));
#17088=CARTESIAN_POINT('Ctrl Pts',(4.85383813043568,0.643737218059205,-4.80305581553704));
#17089=CARTESIAN_POINT('Ctrl Pts',(4.87817600269582,0.594046553948078,-4.806065032002));
#17090=CARTESIAN_POINT('Ctrl Pts',(4.89966150767629,0.543036060467595,-4.80907424846697));
#17091=CARTESIAN_POINT('Ctrl Pts',(4.91817246758545,0.491067210620182,-4.81208346493193));
#17092=CARTESIAN_POINT('Ctrl Pts',(4.93233411055499,0.451308910635268,-4.81438563885506));
#17093=CARTESIAN_POINT('Ctrl Pts',(4.94475578403992,0.410990129462399,-4.81668781277819));
#17094=CARTESIAN_POINT('Ctrl Pts',(4.9554029209918,0.37027707877086,-4.81898998670131));
#17095=CARTESIAN_POINT('Ctrl Pts',(4.96932422023727,0.317044123805193,-4.82200011536255));
#17096=CARTESIAN_POINT('Ctrl Pts',(4.9802684982249,0.26291313095329,-4.82501024402378));
#17097=CARTESIAN_POINT('Ctrl Pts',(4.98812701387199,0.208247972936449,-4.82802037268502));
#17098=CARTESIAN_POINT('Ctrl Pts',(4.99597156272249,0.15367997030835,-4.83102515149947));
#17099=CARTESIAN_POINT('Ctrl Pts',(5.00074115826121,0.0985802050447489,
-4.83402993031391));
#17100=CARTESIAN_POINT('Ctrl Pts',(5.00237763052374,0.0433246422444861,
-4.83703470912836));
#17101=CARTESIAN_POINT('Ctrl Pts',(5.00401248376809,-0.0118762543307643,
-4.84003651521198));
#17102=CARTESIAN_POINT('Ctrl Pts',(5.00252033854837,-0.0672321178175497,
-4.8430383212956));
#17103=CARTESIAN_POINT('Ctrl Pts',(4.99789480496805,-0.122361793690387,
-4.84604012737922));
#17104=CARTESIAN_POINT('Ctrl Pts',(4.99327202061302,-0.177458702770685,
-4.84904014931382));
#17105=CARTESIAN_POINT('Ctrl Pts',(4.98551958327649,-0.232329165482758,
-4.85204017124842));
#17106=CARTESIAN_POINT('Ctrl Pts',(4.97468313980935,-0.286594289084472,
-4.85504019318302));
#17107=CARTESIAN_POINT('Ctrl Pts',(4.96384885719453,-0.340848591892532,
-4.85803961689511));
#17108=CARTESIAN_POINT('Ctrl Pts',(4.94993189311401,-0.394497277711197,
-4.8610390406072));
#17109=CARTESIAN_POINT('Ctrl Pts',(4.93302909146274,-0.447171125545251,
-4.86403846431929));
#17110=CARTESIAN_POINT('Ctrl Pts',(4.91611075013354,-0.499893399353124,
-4.86704064556705));
#17111=CARTESIAN_POINT('Ctrl Pts',(4.89620124870217,-0.551638540700445,
-4.87004282681481));
#17112=CARTESIAN_POINT('Ctrl Pts',(4.87344704513782,-0.602053448554247,
-4.87304500806257));
#17113=CARTESIAN_POINT('Ctrl Pts',(4.85068248436513,-0.652491304154955,
-4.87604855583659));
#17114=CARTESIAN_POINT('Ctrl Pts',(4.82507088492237,-0.701597250183144,
-4.87905210361061));
#17115=CARTESIAN_POINT('Ctrl Pts',(4.79680508121693,-0.749042112815041,
-4.88205565138463));
#17116=CARTESIAN_POINT('Ctrl Pts',(4.76848593056393,-0.796576519640517,
-4.88506486784959));
#17117=CARTESIAN_POINT('Ctrl Pts',(4.7375028650093,-0.84244314168997,-4.88807408431456));
#17118=CARTESIAN_POINT('Ctrl Pts',(4.70409187045511,-0.88634214434519,-4.89108330077953));
#17119=CARTESIAN_POINT('Ctrl Pts',(4.67853109033062,-0.919926680499441,
-4.89338547470264));
#17120=CARTESIAN_POINT('Ctrl Pts',(4.6515501796311,-0.952360190103516,-4.89568764862576));
#17121=CARTESIAN_POINT('Ctrl Pts',(4.62326945780324,-0.983522904920442,
-4.89798982254888));
#17122=CARTESIAN_POINT('Ctrl Pts',(4.58629196862232,-1.02426864532286,-4.90099995121011));
#17123=CARTESIAN_POINT('Ctrl Pts',(4.54693571581419,-1.06301173467712,-4.90401007987136));
#17124=CARTESIAN_POINT('Ctrl Pts',(4.5054460368751,-1.09946228077344,-4.90702020853259));
#17125=CARTESIAN_POINT('Ctrl Pts',(4.46403009678604,-1.13584804397867,-4.91002498734704));
#17126=CARTESIAN_POINT('Ctrl Pts',(4.42048864875999,-1.16994900404581,-4.91302976616148));
#17127=CARTESIAN_POINT('Ctrl Pts',(4.37510478984533,-1.20151101621001,-4.91603454497593));
#17128=CARTESIAN_POINT('Ctrl Pts',(4.32976583074014,-1.23304180299219,-4.91903635105955));
#17129=CARTESIAN_POINT('Ctrl Pts',(4.28258850299054,-1.26203831771611,-4.92203815714317));
#17130=CARTESIAN_POINT('Ctrl Pts',(4.23388854235524,-1.288286947335,-4.92503996322679));
#17131=CARTESIAN_POINT('Ctrl Pts',(4.18521752695648,-1.31451997585724,-4.92803998516139));
#17132=CARTESIAN_POINT('Ctrl Pts',(4.13502613638216,-1.33800810637266,-4.93104000709599));
#17133=CARTESIAN_POINT('Ctrl Pts',(4.08365664476106,-1.35858254384045,-4.93404002903059));
#17134=CARTESIAN_POINT('Ctrl Pts',(4.03229739652721,-1.37915287864099,-4.93703945274267));
#17135=CARTESIAN_POINT('Ctrl Pts',(3.97976100376948,-1.39681047800443,-4.94003887645476));
#17136=CARTESIAN_POINT('Ctrl Pts',(3.9264096141322,-1.41143471039675,-4.94303830016684));
#17137=CARTESIAN_POINT('Ctrl Pts',(3.87300917561944,-1.42607238765262,-4.9460404814146));
#17138=CARTESIAN_POINT('Ctrl Pts',(3.81879275370222,-1.43767098648142,-4.94904266266236));
#17139=CARTESIAN_POINT('Ctrl Pts',(3.76413610405804,-1.44616023635568,-4.95204484391012));
#17140=CARTESIAN_POINT('Ctrl Pts',(3.70945457592029,-1.45465335034802,-4.95504839168414));
#17141=CARTESIAN_POINT('Ctrl Pts',(3.65433294714216,-1.46003424267016,-4.95805193945816));
#17142=CARTESIAN_POINT('Ctrl Pts',(3.59915227362332,-1.46228455804291,-4.96105548723217));
#17143=CARTESIAN_POINT('Ctrl Pts',(3.54386745586965,-1.46453912050721,-4.96406470369714));
#17144=CARTESIAN_POINT('Ctrl Pts',(3.48852390010615,-1.46365131149307,-4.96707392016211));
#17145=CARTESIAN_POINT('Ctrl Pts',(3.43350166766549,-1.45965494708621,-4.97008313662708));
#17146=CARTESIAN_POINT('Ctrl Pts',(3.39140740485943,-1.45659756453103,-4.9723853105502));
#17147=CARTESIAN_POINT('Ctrl Pts',(3.34950120399534,-1.45172186801083,-4.97468748447332));
#17148=CARTESIAN_POINT('Ctrl Pts',(3.30794911626834,-1.44506318740587,-4.97698965839643));
#17149=CARTESIAN_POINT('Ctrl Pts',(3.25361910716469,-1.43635685764783,-4.97999978705767));
#17150=CARTESIAN_POINT('Ctrl Pts',(3.19966662510328,-1.42456400866142,-4.98300991571891));
#17151=CARTESIAN_POINT('Ctrl Pts',(3.14646851405652,-1.40973172123707,-4.98602004438014));
#17152=CARTESIAN_POINT('Ctrl Pts',(3.0933649510427,-1.39492579496676,-4.98902482319459));
#17153=CARTESIAN_POINT('Ctrl Pts',(3.04101360295494,-1.37709129113015,-4.99202960200903));
#17154=CARTESIAN_POINT('Ctrl Pts',(2.9897820059895,-1.35632644742242,-4.99503438082347));
#17155=CARTESIAN_POINT('Ctrl Pts',(2.93860109420154,-1.33558214708735,-4.99803618690709));
#17156=CARTESIAN_POINT('Ctrl Pts',(2.88853822605648,-1.31191344723265,-5.00103799299071));
#17157=CARTESIAN_POINT('Ctrl Pts',(2.83994482500906,-1.28546806772339,-5.00403979907433));
#17158=CARTESIAN_POINT('Ctrl Pts',(2.7913803058636,-1.25903840625077,-5.00703982100892));
#17159=CARTESIAN_POINT('Ctrl Pts',(2.7442839856446,-1.22983558815535,-5.01003984294352));
#17160=CARTESIAN_POINT('Ctrl Pts',(2.69898425198183,-1.19805404828392,-5.01303986487811));
#17161=CARTESIAN_POINT('Ctrl Pts',(2.65369355135973,-1.1662788458436,-5.0160392885902));
#17162=CARTESIAN_POINT('Ctrl Pts',(2.61019915790964,-1.13192624597554,-5.0190387123023));
#17163=CARTESIAN_POINT('Ctrl Pts',(2.56879997983906,-1.0952336444817,-5.02203813601439));
#17164=CARTESIAN_POINT('Ctrl Pts',(2.5273627412205,-1.05850730945534,-5.02504031726215));
#17165=CARTESIAN_POINT('Ctrl Pts',(2.48802496244617,-1.01943702584492,-5.0280424985099));
#17166=CARTESIAN_POINT('Ctrl Pts',(2.45105080840114,-0.978299103602709,
-5.03104467975766));
#17167=CARTESIAN_POINT('Ctrl Pts',(2.41405982454195,-0.937142456291482,
-5.03404822753168));
#17168=CARTESIAN_POINT('Ctrl Pts',(2.37943494082837,-0.893916707146323,
-5.0370517753057));
#17169=CARTESIAN_POINT('Ctrl Pts',(2.34739973774838,-0.848930971486027,
-5.04005532307972));
#17170=CARTESIAN_POINT('Ctrl Pts',(2.31530407361389,-0.803860332820476,
-5.04306453954468));
#17171=CARTESIAN_POINT('Ctrl Pts',(2.28580813594504,-0.757023520050787,
-5.04607375600965));
#17172=CARTESIAN_POINT('Ctrl Pts',(2.25909126688016,-0.708757321748141,
-5.04908297247461));
#17173=CARTESIAN_POINT('Ctrl Pts',(2.23865176710177,-0.671831701941607,
-5.05138514639774));
#17174=CARTESIAN_POINT('Ctrl Pts',(2.21983791051209,-0.634070069460272,
-5.05368732032087));
#17175=CARTESIAN_POINT('Ctrl Pts',(2.20271083710676,-0.595630800756864,
-5.055989494244));
#17176=CARTESIAN_POINT('Ctrl Pts',(2.17822463627681,-0.540675022209486,
-5.05928086175864));
#17177=CARTESIAN_POINT('Ctrl Pts',(2.15709871382792,-0.484134691290982,
-5.06257222927328));
#17178=CARTESIAN_POINT('Ctrl Pts',(2.13951937131544,-0.42641898233868,-5.06586359678792));
#17179=CARTESIAN_POINT('Ctrl Pts',(2.12199297534358,-0.368877105094038,
-5.06914505116027));
#17180=CARTESIAN_POINT('Ctrl Pts',(2.10799201218925,-0.310167235961898,
-5.07242650553261));
#17181=CARTESIAN_POINT('Ctrl Pts',(2.09765464740422,-0.250717556839019,
-5.07570795990495));
#17182=CARTESIAN_POINT('Ctrl Pts',(2.08736539805606,-0.191544587239539,
-5.07897414069317));
#17183=CARTESIAN_POINT('Ctrl Pts',(2.08070586389208,-0.131639017030512,
-5.08224032148139));
#17184=CARTESIAN_POINT('Ctrl Pts',(2.0777637777177,-0.071440693713586,-5.0855065022696));
#17185=CARTESIAN_POINT('Ctrl Pts',(2.07661125362505,-0.047858781476013,
-5.08678598622291));
#17186=CARTESIAN_POINT('Ctrl Pts',(2.07602866300798,-0.0242321078209353,
-5.08806547017621));
#17187=CARTESIAN_POINT('Ctrl Pts',(2.07601916841636,-0.000587678975561644,
-5.08934495412951));
#17188=CARTESIAN_POINT('Origin',(3.53951905042299,8.32667268468867E-16,
0.));
#17189=CARTESIAN_POINT('',(2.07601962619751,0.00129818785261296,-5.66065504584291));
#17190=CARTESIAN_POINT('',(2.07601963090622,0.00130348536077232,-5.58934495415709));
#17191=CARTESIAN_POINT('',(2.07601905042299,1.01189432752408E-15,0.));
#17192=CARTESIAN_POINT('Ctrl Pts',(2.07601962619751,0.00129818785261296,
-5.66065504584291));
#17193=CARTESIAN_POINT('Ctrl Pts',(2.07597114765928,-0.0533536197810684,
-5.65768502711364));
#17194=CARTESIAN_POINT('Ctrl Pts',(2.07898825837672,-0.108079334828836,
-5.65471500838437));
#17195=CARTESIAN_POINT('Ctrl Pts',(2.08506915307526,-0.162504603335374,
-5.65174498965511));
#17196=CARTESIAN_POINT('Ctrl Pts',(2.09114622993757,-0.216895701415943,
-5.64877683562597));
#17197=CARTESIAN_POINT('Ctrl Pts',(2.10028322128251,-0.270986190441087,
-5.64580868159683));
#17198=CARTESIAN_POINT('Ctrl Pts',(2.11242635184785,-0.324405116595802,
-5.64284052756769));
#17199=CARTESIAN_POINT('Ctrl Pts',(2.12456691007413,-0.377812726756688,
-5.63987300229721));
#17200=CARTESIAN_POINT('Ctrl Pts',(2.1397122236165,-0.430548529546075,-5.63690547702674));
#17201=CARTESIAN_POINT('Ctrl Pts',(2.15775758481954,-0.482252529462938,
-5.63393795175626));
#17202=CARTESIAN_POINT('Ctrl Pts',(2.1758191975795,-0.534003093728829,-5.63096775394821));
#17203=CARTESIAN_POINT('Ctrl Pts',(2.19678589465581,-0.584719488164479,
-5.62799755614017));
#17204=CARTESIAN_POINT('Ctrl Pts',(2.22050385984984,-0.634059285112427,
-5.62502735833212));
#17205=CARTESIAN_POINT('Ctrl Pts',(2.24423325748627,-0.683422864639618,
-5.62205572884074));
#17206=CARTESIAN_POINT('Ctrl Pts',(2.27071630107471,-0.731408052320245,
-5.61908409934937));
#17207=CARTESIAN_POINT('Ctrl Pts',(2.29975359853863,-0.77769780397914,-5.61611246985799));
#17208=CARTESIAN_POINT('Ctrl Pts',(2.32884376638286,-0.824071838852668,
-5.61313542969844));
#17209=CARTESIAN_POINT('Ctrl Pts',(2.36049715663055,-0.868743835850679,
-5.61015838953888));
#17210=CARTESIAN_POINT('Ctrl Pts',(2.39447240308624,-0.911427685240511,
-5.60718134937933));
#17211=CARTESIAN_POINT('Ctrl Pts',(2.41414427305429,-0.936141888153728,
-5.60545762540326));
#17212=CARTESIAN_POINT('Ctrl Pts',(2.43459380573541,-0.960190211352025,
-5.6037339014272));
#17213=CARTESIAN_POINT('Ctrl Pts',(2.45576864304273,-0.983522904920427,
-5.60201017745113));
#17214=CARTESIAN_POINT('Ctrl Pts',(2.49274613222366,-1.02426864532286,-5.59900004878989));
#17215=CARTESIAN_POINT('Ctrl Pts',(2.53210238503181,-1.06301173467714,-5.59598992012865));
#17216=CARTESIAN_POINT('Ctrl Pts',(2.57359206397092,-1.09946228077348,-5.59297979146741));
#17217=CARTESIAN_POINT('Ctrl Pts',(2.61500800405997,-1.1358480439787,-5.58997501265296));
#17218=CARTESIAN_POINT('Ctrl Pts',(2.65854945208602,-1.16994900404583,-5.58697023383852));
#17219=CARTESIAN_POINT('Ctrl Pts',(2.70393331100067,-1.20151101621002,-5.58396545502407));
#17220=CARTESIAN_POINT('Ctrl Pts',(2.74927227010583,-1.23304180299218,-5.58096364894045));
#17221=CARTESIAN_POINT('Ctrl Pts',(2.79644959785539,-1.26203831771608,-5.57796184285684));
#17222=CARTESIAN_POINT('Ctrl Pts',(2.84514955849066,-1.28828694733496,-5.57496003677322));
#17223=CARTESIAN_POINT('Ctrl Pts',(2.8938205738894,-1.31451997585719,-5.57196001483862));
#17224=CARTESIAN_POINT('Ctrl Pts',(2.9440119644637,-1.3380081063726,-5.56895999290402));
#17225=CARTESIAN_POINT('Ctrl Pts',(2.99538145608477,-1.35858254384039,-5.56595997096942));
#17226=CARTESIAN_POINT('Ctrl Pts',(3.04674070431875,-1.37915287864099,-5.56296054725732));
#17227=CARTESIAN_POINT('Ctrl Pts',(3.09927709707663,-1.39681047800447,-5.55996112354523));
#17228=CARTESIAN_POINT('Ctrl Pts',(3.15262848671406,-1.41143471039683,-5.55696169983314));
#17229=CARTESIAN_POINT('Ctrl Pts',(3.20602892522683,-1.42607238765269,-5.55395951858537));
#17230=CARTESIAN_POINT('Ctrl Pts',(3.26024534714408,-1.43767098648148,-5.55095733733761));
#17231=CARTESIAN_POINT('Ctrl Pts',(3.31490199678827,-1.44616023635573,-5.54795515608985));
#17232=CARTESIAN_POINT('Ctrl Pts',(3.36958352492605,-1.45465335034806,-5.54495160831583));
#17233=CARTESIAN_POINT('Ctrl Pts',(3.4247051537042,-1.46003424267019,-5.54194806054181));
#17234=CARTESIAN_POINT('Ctrl Pts',(3.47988582722307,-1.46228455804292,-5.5389445127678));
#17235=CARTESIAN_POINT('Ctrl Pts',(3.53517064497669,-1.46453912050721,-5.53593529630283));
#17236=CARTESIAN_POINT('Ctrl Pts',(3.59051420074016,-1.46365131149306,-5.53292607983786));
#17237=CARTESIAN_POINT('Ctrl Pts',(3.64553643318078,-1.45965494708619,-5.5299168633729));
#17238=CARTESIAN_POINT('Ctrl Pts',(3.68763069598673,-1.45659756453101,-5.52761468944978));
#17239=CARTESIAN_POINT('Ctrl Pts',(3.72953689685072,-1.45172186801082,-5.52531251552667));
#17240=CARTESIAN_POINT('Ctrl Pts',(3.77108898457761,-1.44506318740587,-5.52301034160356));
#17241=CARTESIAN_POINT('Ctrl Pts',(3.82541899368129,-1.43635685764783,-5.52000021294232));
#17242=CARTESIAN_POINT('Ctrl Pts',(3.87937147574273,-1.42456400866141,-5.51699008428108));
#17243=CARTESIAN_POINT('Ctrl Pts',(3.93256958678952,-1.40973172123705,-5.51397995561984));
#17244=CARTESIAN_POINT('Ctrl Pts',(3.98567314980338,-1.39492579496673,-5.5109751768054));
#17245=CARTESIAN_POINT('Ctrl Pts',(4.03802449789117,-1.37709129113011,-5.50797039799095));
#17246=CARTESIAN_POINT('Ctrl Pts',(4.08925609485665,-1.35632644742235,-5.50496561917651));
#17247=CARTESIAN_POINT('Ctrl Pts',(4.14043700664466,-1.33558214708726,-5.50196381309289));
#17248=CARTESIAN_POINT('Ctrl Pts',(4.19049987478974,-1.31191344723253,-5.49896200700927));
#17249=CARTESIAN_POINT('Ctrl Pts',(4.23909327583719,-1.28546806772324,-5.49596020092565));
#17250=CARTESIAN_POINT('Ctrl Pts',(4.2876577949827,-1.25903840625058,-5.49296017899105));
#17251=CARTESIAN_POINT('Ctrl Pts',(4.33475411520175,-1.22983558815512,-5.48996015705645));
#17252=CARTESIAN_POINT('Ctrl Pts',(4.38005384886455,-1.19805404828363,-5.48696013512185));
#17253=CARTESIAN_POINT('Ctrl Pts',(4.42534454948663,-1.16627884584332,-5.48396071140976));
#17254=CARTESIAN_POINT('Ctrl Pts',(4.46883894293668,-1.13192624597526,-5.48096128769767));
#17255=CARTESIAN_POINT('Ctrl Pts',(4.51023812100723,-1.09523364448143,-5.47796186398559));
#17256=CARTESIAN_POINT('Ctrl Pts',(4.55167535962579,-1.05850730945505,-5.47495968273783));
#17257=CARTESIAN_POINT('Ctrl Pts',(4.59101313840011,-1.01943702584461,-5.47195750149007));
#17258=CARTESIAN_POINT('Ctrl Pts',(4.62798729244513,-0.978299103602381,
-5.46895532024231));
#17259=CARTESIAN_POINT('Ctrl Pts',(4.66497827630434,-0.937142456291102,
-5.46595177246829));
#17260=CARTESIAN_POINT('Ctrl Pts',(4.69960316001795,-0.89391670714589,-5.46294822469427));
#17261=CARTESIAN_POINT('Ctrl Pts',(4.73163836309795,-0.848930971485537,
-5.45994467692025));
#17262=CARTESIAN_POINT('Ctrl Pts',(4.76373402723243,-0.803860332819957,
-5.45693546045528));
#17263=CARTESIAN_POINT('Ctrl Pts',(4.79322996490127,-0.757023520050236,
-5.45392624399032));
#17264=CARTESIAN_POINT('Ctrl Pts',(4.81994683396614,-0.708757321747561,
-5.45091702752535));
#17265=CARTESIAN_POINT('Ctrl Pts',(4.84038633374441,-0.671831701941208,
-5.44861485360224));
#17266=CARTESIAN_POINT('Ctrl Pts',(4.85920019033398,-0.634070069460065,
-5.44631267967912));
#17267=CARTESIAN_POINT('Ctrl Pts',(4.87632726373923,-0.595630800756855,
-5.44401050575601));
#17268=CARTESIAN_POINT('Ctrl Pts',(4.89872118194956,-0.545370851550297,
-5.44100037709477));
#17269=CARTESIAN_POINT('Ctrl Pts',(4.91832377794496,-0.493740629412078,
-5.43799024843354));
#17270=CARTESIAN_POINT('Ctrl Pts',(4.93496857708735,-0.441081476070143,
-5.4349801197723));
#17271=CARTESIAN_POINT('Ctrl Pts',(4.95158379373167,-0.388515912881416,
-5.43197534095786));
#17272=CARTESIAN_POINT('Ctrl Pts',(4.9652514878736,-0.33492554704438,-5.42897056214341));
#17273=CARTESIAN_POINT('Ctrl Pts',(4.97585311589188,-0.280671876705873,
-5.42596578332897));
#17274=CARTESIAN_POINT('Ctrl Pts',(4.98644425535566,-0.226471881385757,
-5.42296397724535));
#17275=CARTESIAN_POINT('Ctrl Pts',(4.99397523686006,-0.171610397288949,
-5.41996217116173));
#17276=CARTESIAN_POINT('Ctrl Pts',(4.99837776337159,-0.116462464571016,
-5.41696036507811));
#17277=CARTESIAN_POINT('Ctrl Pts',(5.00277767320397,-0.0613473094967593,
-5.41396034314351));
#17278=CARTESIAN_POINT('Ctrl Pts',(5.00405277160113,-0.00594656864460139,
-5.41096032120891));
#17279=CARTESIAN_POINT('Ctrl Pts',(5.00218647326826,0.0493584860706374,
-5.40796029927431));
#17280=CARTESIAN_POINT('Ctrl Pts',(5.00032054708656,0.104652512623676,-5.40496087556222));
#17281=CARTESIAN_POINT('Ctrl Pts',(4.9953144860066,0.159850363412901,-5.40196145185013));
#17282=CARTESIAN_POINT('Ctrl Pts',(4.98720379313038,0.214571982635766,-5.39896202813804));
#17283=CARTESIAN_POINT('Ctrl Pts',(4.97908564364681,0.269343910461643,-5.39595984689028));
#17284=CARTESIAN_POINT('Ctrl Pts',(4.96785723752433,0.323638208470234,-5.39295766564252));
#17285=CARTESIAN_POINT('Ctrl Pts',(4.95360565312807,0.377082656787611,-5.38995548439476));
#17286=CARTESIAN_POINT('Ctrl Pts',(4.93934758172696,0.430551431831492,-5.38695193662074));
#17287=CARTESIAN_POINT('Ctrl Pts',(4.92206375402316,0.483169083444289,-5.38394838884672));
#17288=CARTESIAN_POINT('Ctrl Pts',(4.90189089891441,0.534579457553378,-5.3809448410727));
#17289=CARTESIAN_POINT('Ctrl Pts',(4.8816799709366,0.586086860091577,-5.37793562460774));
#17290=CARTESIAN_POINT('Ctrl Pts',(4.85856934427834,0.636381952345708,-5.37492640814277));
#17291=CARTESIAN_POINT('Ctrl Pts',(4.8327430965916,0.685130510495105,-5.3719171916778));
#17292=CARTESIAN_POINT('Ctrl Pts',(4.81298495866809,0.722425155352967,-5.36961501775468));
#17293=CARTESIAN_POINT('Ctrl Pts',(4.79163839257322,0.758815074333101,-5.36731284383156));
#17294=CARTESIAN_POINT('Ctrl Pts',(4.76880263619492,0.794162524771662,-5.36501066990844));
#17295=CARTESIAN_POINT('Ctrl Pts',(4.73894452509179,0.840379872904255,-5.3620005412472));
#17296=CARTESIAN_POINT('Ctrl Pts',(4.70641360602975,0.885008125309868,-5.35899041258596));
#17297=CARTESIAN_POINT('Ctrl Pts',(4.67140480080371,0.927721347218594,-5.35598028392473));
#17298=CARTESIAN_POINT('Ctrl Pts',(4.63645821608895,0.970358655696731,-5.35297550511028));
#17299=CARTESIAN_POINT('Ctrl Pts',(4.5990428168513,1.01108728289669,-5.34997072629584));
#17300=CARTESIAN_POINT('Ctrl Pts',(4.55939659574844,1.04961042417696,-5.3469659474814));
#17301=CARTESIAN_POINT('Ctrl Pts',(4.519789598013,1.08809545319123,-5.34396414139778));
#17302=CARTESIAN_POINT('Ctrl Pts',(4.47795652732849,1.12437895242752,-5.34096233531416));
#17303=CARTESIAN_POINT('Ctrl Pts',(4.4341741726876,1.15819880081345,-5.33796052923054));
#17304=CARTESIAN_POINT('Ctrl Pts',(4.39041784046222,1.19199854808434,-5.33496050729594));
#17305=CARTESIAN_POINT('Ctrl Pts',(4.34471493776048,1.22333722462832,-5.33196048536134));
#17306=CARTESIAN_POINT('Ctrl Pts',(4.29737572793224,1.2519926143371,-5.32896046342674));
#17307=CARTESIAN_POINT('Ctrl Pts',(4.25004595782853,1.28064228998799,-5.32596103971465));
#17308=CARTESIAN_POINT('Ctrl Pts',(4.20108098013394,1.30660946809153,-5.32296161600255));
#17309=CARTESIAN_POINT('Ctrl Pts',(4.15081850056707,1.32971622245258,-5.31996219229046));
#17310=CARTESIAN_POINT('Ctrl Pts',(4.10050981193029,1.35284422012746,-5.3169600110427));
#17311=CARTESIAN_POINT('Ctrl Pts',(4.04890171910207,1.37310631910392,-5.31395782979494));
#17312=CARTESIAN_POINT('Ctrl Pts',(3.99635354552124,1.3903720703784,-5.31095564854718));
#17313=CARTESIAN_POINT('Ctrl Pts',(3.94378145317827,1.40764568063959,-5.30795210077316));
#17314=CARTESIAN_POINT('Ctrl Pts',(3.89026893824923,1.42192008806373,-5.30494855299914));
#17315=CARTESIAN_POINT('Ctrl Pts',(3.83618899748807,1.43311520559528,-5.30194500522513));
#17316=CARTESIAN_POINT('Ctrl Pts',(3.78200698994002,1.44433145202711,-5.29893578876016));
#17317=CARTESIAN_POINT('Ctrl Pts',(3.7272559409058,1.4524567211945,-5.29592657229519));
#17318=CARTESIAN_POINT('Ctrl Pts',(3.6723163511366,1.45746256450146,-5.29291735583023));
#17319=CARTESIAN_POINT('Ctrl Pts',(3.63028531336119,1.46129223978693,-5.29061518190711));
#17320=CARTESIAN_POINT('Ctrl Pts',(3.58814409693993,1.46329722506164,-5.28831300798399));
#17321=CARTESIAN_POINT('Ctrl Pts',(3.54606228825325,1.46348537267671,-5.28601083406088));
#17322=CARTESIAN_POINT('Ctrl Pts',(3.4910396606522,1.46373137864654,-5.28300070539964));
#17323=CARTESIAN_POINT('Ctrl Pts',(3.43588753171339,1.46087056035062,-5.2799905767384));
#17324=CARTESIAN_POINT('Ctrl Pts',(3.38098538508204,1.45488808055931,-5.27698044807717));
#17325=CARTESIAN_POINT('Ctrl Pts',(3.32618081503499,1.44891623332028,-5.27397566926272));
#17326=CARTESIAN_POINT('Ctrl Pts',(3.27162586636294,1.43983379151762,-5.27097089044828));
#17327=CARTESIAN_POINT('Ctrl Pts',(3.21769915919492,1.42767790751624,-5.26796611163383));
#17328=CARTESIAN_POINT('Ctrl Pts',(3.16382580356946,1.41553404974818,-5.26496430555021));
#17329=CARTESIAN_POINT('Ctrl Pts',(3.110579970862,1.40032288874678,-5.26196249946659));
#17330=CARTESIAN_POINT('Ctrl Pts',(3.05833243094417,1.38213302081766,-5.25896069338298));
#17331=CARTESIAN_POINT('Ctrl Pts',(3.00611594479678,1.3639539641915,-5.25596067144838));
#17332=CARTESIAN_POINT('Ctrl Pts',(2.95489707315103,1.34279988301949,-5.25296064951378));
#17333=CARTESIAN_POINT('Ctrl Pts',(2.90503145465448,1.31880921319799,-5.24996062757917));
#17334=CARTESIAN_POINT('Ctrl Pts',(2.85517577966366,1.29482332726106,-5.24696120386708));
#17335=CARTESIAN_POINT('Ctrl Pts',(2.80667329755418,1.2680022048291,-5.24396178015499));
#17336=CARTESIAN_POINT('Ctrl Pts',(2.75985754738192,1.23853146535554,-5.24096235644289));
#17337=CARTESIAN_POINT('Ctrl Pts',(2.71299875690819,1.20903363180559,-5.23796017519514));
#17338=CARTESIAN_POINT('Ctrl Pts',(2.66783024437489,1.17688159647613,-5.23495799394737));
#17339=CARTESIAN_POINT('Ctrl Pts',(2.62465759724969,1.14230502559415,-5.23195581269962));
#17340=CARTESIAN_POINT('Ctrl Pts',(2.58146529889392,1.10771271622468,-5.2289522649256));
#17341=CARTESIAN_POINT('Ctrl Pts',(2.54027107042225,1.07069402497338,-5.22594871715158));
#17342=CARTESIAN_POINT('Ctrl Pts',(2.50134579086117,1.0315175874074,-5.22294516937757));
#17343=CARTESIAN_POINT('Ctrl Pts',(2.46234704638573,0.992267210908591,-5.2199359529126));
#17344=CARTESIAN_POINT('Ctrl Pts',(2.42562615652234,0.950851349007231,-5.21692673644763));
#17345=CARTESIAN_POINT('Ctrl Pts',(2.39141485185252,0.90757313712166,-5.21391751998266));
#17346=CARTESIAN_POINT('Ctrl Pts',(2.36524180169027,0.874463531348206,-5.21161534605955));
#17347=CARTESIAN_POINT('Ctrl Pts',(2.34053677734022,0.840264644534776,-5.20931317213643));
#17348=CARTESIAN_POINT('Ctrl Pts',(2.31738586357953,0.805122800332869,-5.20701099821332));
#17349=CARTESIAN_POINT('Ctrl Pts',(2.28656148700224,0.758333051535187,-5.20394575954991));
#17350=CARTESIAN_POINT('Ctrl Pts',(2.25836766374379,0.709679539907307,-5.2008805208865));
#17351=CARTESIAN_POINT('Ctrl Pts',(2.23302982051775,0.659483238711648,-5.19781528222309));
#17352=CARTESIAN_POINT('Ctrl Pts',(2.20743202463528,0.608771950438284,-5.19471859585807));
#17353=CARTESIAN_POINT('Ctrl Pts',(2.18474950720201,0.55648641724976,-5.19162190949306));
#17354=CARTESIAN_POINT('Ctrl Pts',(2.16517011740709,0.502988330200676,-5.18852522312805));
#17355=CARTESIAN_POINT('Ctrl Pts',(2.14585640794371,0.450216179437288,-5.18547055690098));
#17356=CARTESIAN_POINT('Ctrl Pts',(2.12956232042806,0.396264660733128,-5.18241589067391));
#17357=CARTESIAN_POINT('Ctrl Pts',(2.11642128931065,0.341504044364121,-5.17936122444685));
#17358=CARTESIAN_POINT('Ctrl Pts',(2.10300910519356,0.285613493421454,-5.17624352801286));
#17359=CARTESIAN_POINT('Ctrl Pts',(2.09288180219176,0.228880562508218,-5.17312583157887));
#17360=CARTESIAN_POINT('Ctrl Pts',(2.08612790286529,0.171716109322651,-5.17000813514488));
#17361=CARTESIAN_POINT('Ctrl Pts',(2.07937400353882,0.114551656137083,-5.16689043871089));
#17362=CARTESIAN_POINT('Ctrl Pts',(2.07599361023914,0.0569562315344585,
-5.1637727422769));
#17363=CARTESIAN_POINT('Ctrl Pts',(2.0760191947603,-0.000649980989682889,
-5.16065504584291));
#17364=CARTESIAN_POINT('Ctrl Pts',(2.07601916841615,-0.000587678466146558,
-5.08934495415708));
#17365=CARTESIAN_POINT('Ctrl Pts',(2.07599647908465,0.0559157258477616,
-5.09240255388168));
#17366=CARTESIAN_POINT('Ctrl Pts',(2.0792503896227,0.112403252583727,-5.09546015360627));
#17367=CARTESIAN_POINT('Ctrl Pts',(2.08574917914879,0.168479706123322,-5.09851775333087));
#17368=CARTESIAN_POINT('Ctrl Pts',(2.09225826286632,0.224644985704336,-5.10158019634463));
#17369=CARTESIAN_POINT('Ctrl Pts',(2.10202243211027,0.280397394683112,-5.1046426393584));
#17370=CARTESIAN_POINT('Ctrl Pts',(2.11495823197472,0.335348661160296,-5.10770508237216));
#17371=CARTESIAN_POINT('Ctrl Pts',(2.12790393526328,0.390341997374393,-5.1107698699392));
#17372=CARTESIAN_POINT('Ctrl Pts',(2.1440259636609,0.444532490215689,-5.11383465750624));
#17373=CARTESIAN_POINT('Ctrl Pts',(2.16319090346734,0.49754706500755,-5.11689944507328));
#17374=CARTESIAN_POINT('Ctrl Pts',(2.18240188203802,0.550688993474133,-5.11997159499228));
#17375=CARTESIAN_POINT('Ctrl Pts',(2.20467018624253,0.602648896761848,-5.12304374491128));
#17376=CARTESIAN_POINT('Ctrl Pts',(2.22981434073402,0.653074133172129,-5.12611589483029));
#17377=CARTESIAN_POINT('Ctrl Pts',(2.25402268917208,0.701622661360063,-5.12907370658405));
#17378=CARTESIAN_POINT('Ctrl Pts',(2.28089629616199,0.748748447528253,-5.1320315183378));
#17379=CARTESIAN_POINT('Ctrl Pts',(2.31023546465109,0.794162524771709,-5.13498933009156));
#17380=CARTESIAN_POINT('Ctrl Pts',(2.34009357575423,0.840379872904314,-5.1379994587528));
#17381=CARTESIAN_POINT('Ctrl Pts',(2.37262449481628,0.885008125309938,-5.14100958741403));
#17382=CARTESIAN_POINT('Ctrl Pts',(2.40763330004234,0.927721347218673,-5.14401971607527));
#17383=CARTESIAN_POINT('Ctrl Pts',(2.4425798847571,0.970358655696808,-5.14702449488971));
#17384=CARTESIAN_POINT('Ctrl Pts',(2.47999528399475,1.01108728289676,-5.15002927370416));
#17385=CARTESIAN_POINT('Ctrl Pts',(2.51964150509762,1.04961042417703,-5.1530340525186));
#17386=CARTESIAN_POINT('Ctrl Pts',(2.55924850283305,1.08809545319129,-5.15603585860222));
#17387=CARTESIAN_POINT('Ctrl Pts',(2.60108157351756,1.12437895242757,-5.15903766468584));
#17388=CARTESIAN_POINT('Ctrl Pts',(2.64486392815845,1.1581988008135,-5.16203947076946));
#17389=CARTESIAN_POINT('Ctrl Pts',(2.68862026038384,1.1919985480844,-5.16503949270406));
#17390=CARTESIAN_POINT('Ctrl Pts',(2.73432316308559,1.22333722462838,-5.16803951463866));
#17391=CARTESIAN_POINT('Ctrl Pts',(2.78166237291385,1.25199261433716,-5.17103953657326));
#17392=CARTESIAN_POINT('Ctrl Pts',(2.82899214301756,1.28064228998806,-5.17403896028535));
#17393=CARTESIAN_POINT('Ctrl Pts',(2.87795712071217,1.3066094680916,-5.17703838399745));
#17394=CARTESIAN_POINT('Ctrl Pts',(2.92821960027905,1.32971622245264,-5.18003780770955));
#17395=CARTESIAN_POINT('Ctrl Pts',(2.97852828891583,1.35284422012751,-5.1830399889573));
#17396=CARTESIAN_POINT('Ctrl Pts',(3.03013638174404,1.37310631910397,-5.18604217020506));
#17397=CARTESIAN_POINT('Ctrl Pts',(3.08268455532486,1.39037207037844,-5.18904435145282));
#17398=CARTESIAN_POINT('Ctrl Pts',(3.13525664766784,1.40764568063963,-5.19204789922684));
#17399=CARTESIAN_POINT('Ctrl Pts',(3.18876916259689,1.42192008806376,-5.19505144700086));
#17400=CARTESIAN_POINT('Ctrl Pts',(3.24284910335806,1.43311520559531,-5.19805499477488));
#17401=CARTESIAN_POINT('Ctrl Pts',(3.29703111090612,1.44433145202714,-5.20106421123985));
#17402=CARTESIAN_POINT('Ctrl Pts',(3.35178215994035,1.45245672119452,-5.20407342770481));
#17403=CARTESIAN_POINT('Ctrl Pts',(3.40672174970956,1.45746256450148,-5.20708264416978));
#17404=CARTESIAN_POINT('Ctrl Pts',(3.44875278748493,1.46129223978694,-5.2093848180929));
#17405=CARTESIAN_POINT('Ctrl Pts',(3.49089400390613,1.46329722506164,-5.21168699201601));
#17406=CARTESIAN_POINT('Ctrl Pts',(3.53297581259277,1.46348537267671,-5.21398916593912));
#17407=CARTESIAN_POINT('Ctrl Pts',(3.58799844019384,1.46373137864654,-5.21699929460036));
#17408=CARTESIAN_POINT('Ctrl Pts',(3.64315056913268,1.46087056035061,-5.2200094232616));
#17409=CARTESIAN_POINT('Ctrl Pts',(3.69805271576405,1.4548880805593,-5.22301955192284));
#17410=CARTESIAN_POINT('Ctrl Pts',(3.75285728581109,1.44891623332026,-5.22602433073728));
#17411=CARTESIAN_POINT('Ctrl Pts',(3.8074122344831,1.43983379151761,-5.22902910955173));
#17412=CARTESIAN_POINT('Ctrl Pts',(3.86133894165111,1.42767790751623,-5.23203388836617));
#17413=CARTESIAN_POINT('Ctrl Pts',(3.91521229727657,1.41553404974817,-5.23503569444979));
#17414=CARTESIAN_POINT('Ctrl Pts',(3.96845812998403,1.40032288874676,-5.23803750053341));
#17415=CARTESIAN_POINT('Ctrl Pts',(4.02070566990185,1.38213302081764,-5.24103930661702));
#17416=CARTESIAN_POINT('Ctrl Pts',(4.07292215604919,1.3639539641915,-5.24403932855162));
#17417=CARTESIAN_POINT('Ctrl Pts',(4.12414102769489,1.34279988301951,-5.24703935048622));
#17418=CARTESIAN_POINT('Ctrl Pts',(4.17400664619139,1.31880921319804,-5.25003937242082));
#17419=CARTESIAN_POINT('Ctrl Pts',(4.22386232118207,1.29482332726118,-5.2530387961329));
#17420=CARTESIAN_POINT('Ctrl Pts',(4.27236480329143,1.2680022048293,-5.25603821984499));
#17421=CARTESIAN_POINT('Ctrl Pts',(4.31918055346358,1.23853146535584,-5.25903764355707));
#17422=CARTESIAN_POINT('Ctrl Pts',(4.36603934393731,1.20903363180591,-5.26203982480483));
#17423=CARTESIAN_POINT('Ctrl Pts',(4.41120785647062,1.17688159647647,-5.26504200605259));
#17424=CARTESIAN_POINT('Ctrl Pts',(4.45438050359583,1.14230502559452,-5.26804418730035));
#17425=CARTESIAN_POINT('Ctrl Pts',(4.49757280195163,1.10771271622504,-5.27104773507437));
#17426=CARTESIAN_POINT('Ctrl Pts',(4.53876703042334,1.07069402497375,-5.27405128284839));
#17427=CARTESIAN_POINT('Ctrl Pts',(4.57769230998446,1.03151758740776,-5.27705483062241));
#17428=CARTESIAN_POINT('Ctrl Pts',(4.61669105445989,0.992267210908983,-5.28006404708737));
#17429=CARTESIAN_POINT('Ctrl Pts',(4.65341194432327,0.950851349007655,-5.28307326355234));
#17430=CARTESIAN_POINT('Ctrl Pts',(4.6876232489931,0.907573137122119,-5.2860824800173));
#17431=CARTESIAN_POINT('Ctrl Pts',(4.71379629915549,0.874463531348512,-5.28838465394043));
#17432=CARTESIAN_POINT('Ctrl Pts',(4.73850132350566,0.840264644534916,-5.29068682786356));
#17433=CARTESIAN_POINT('Ctrl Pts',(4.76165223726647,0.805122800332836,-5.29298900178668));
#17434=CARTESIAN_POINT('Ctrl Pts',(4.79192242161058,0.759174285592591,-5.29599913044792));
#17435=CARTESIAN_POINT('Ctrl Pts',(4.81966131604092,0.711419753414092,-5.29900925910916));
#17436=CARTESIAN_POINT('Ctrl Pts',(4.84464914560435,0.662168924559209,-5.3020193877704));
#17437=CARTESIAN_POINT('Ctrl Pts',(4.86959256475384,0.613005628304572,-5.30502416658484));
#17438=CARTESIAN_POINT('Ctrl Pts',(4.89179438510166,0.562351780010985,-5.30802894539928));
#17439=CARTESIAN_POINT('Ctrl Pts',(4.91107884620114,0.510544784132602,-5.31103372421373));
#17440=CARTESIAN_POINT('Ctrl Pts',(4.93034422852127,0.458789042693621,-5.31403553029735));
#17441=CARTESIAN_POINT('Ctrl Pts',(4.94669778577434,0.405882906141302,-5.31703733638096));
#17442=CARTESIAN_POINT('Ctrl Pts',(4.96001113254836,0.352185312895246,-5.32003914246458));
#17443=CARTESIAN_POINT('Ctrl Pts',(4.97331656642131,0.29851963527119,-5.32303916439918));
#17444=CARTESIAN_POINT('Ctrl Pts',(4.983585244523,0.24406394490794,-5.32603918633378));
#17445=CARTESIAN_POINT('Ctrl Pts',(4.99073879108145,0.189191739574429,-5.32903920826838));
#17446=CARTESIAN_POINT('Ctrl Pts',(4.99789091117947,0.134330476090335,-5.33203863198048));
#17447=CARTESIAN_POINT('Ctrl Pts',(5.00192906513011,0.0790533859719109,
-5.33503805569257));
#17448=CARTESIAN_POINT('Ctrl Pts',(5.0028264697904,0.0237412388956652,-5.33803747940466));
#17449=CARTESIAN_POINT('Ctrl Pts',(5.00372469948429,-0.0316217596883739,
-5.34103966065242));
#17450=CARTESIAN_POINT('Ctrl Pts',(5.0014764025242,-0.0870193504399114,
-5.34404184190018));
#17451=CARTESIAN_POINT('Ctrl Pts',(4.99610695876351,-0.142070106905666,
-5.34704402314794));
#17452=CARTESIAN_POINT('Ctrl Pts',(4.99073507095122,-0.197145921253763,
-5.35004757092196));
#17453=CARTESIAN_POINT('Ctrl Pts',(4.98223928547081,-0.251874063835189,
-5.35305111869598));
#17454=CARTESIAN_POINT('Ctrl Pts',(4.97069658460281,-0.305880884755777,
-5.35605466647));
#17455=CARTESIAN_POINT('Ctrl Pts',(4.95913209882948,-0.359989634461847,
-5.35906388293496));
#17456=CARTESIAN_POINT('Ctrl Pts',(4.94450934993391,-0.413373832349662,
-5.36207309939993));
#17457=CARTESIAN_POINT('Ctrl Pts',(4.92695560530715,-0.465673765818067,
-5.36508231586489));
#17458=CARTESIAN_POINT('Ctrl Pts',(4.91352627125848,-0.505685358341731,
-5.36738448978801));
#17459=CARTESIAN_POINT('Ctrl Pts',(4.89838251148219,-0.54506261862293,-5.36968666371113));
#17460=CARTESIAN_POINT('Ctrl Pts',(4.88159983959011,-0.583653497675247,
-5.37198883763425));
#17461=CARTESIAN_POINT('Ctrl Pts',(4.85965623178218,-0.634111679801032,
-5.37499896629549));
#17462=CARTESIAN_POINT('Ctrl Pts',(4.83481694889245,-0.683436639338129,
-5.37800909495673));
#17463=CARTESIAN_POINT('Ctrl Pts',(4.80722130622284,-0.731275078640029,
-5.38101922361797));
#17464=CARTESIAN_POINT('Ctrl Pts',(4.77967470878589,-0.779028495555822,
-5.38402400243241));
#17465=CARTESIAN_POINT('Ctrl Pts',(4.74938173507842,-0.825300181473497,
-5.38702878124686));
#17466=CARTESIAN_POINT('Ctrl Pts',(4.71652893559323,-0.869758575819491,
-5.3900335600613));
#17467=CARTESIAN_POINT('Ctrl Pts',(4.68370863851028,-0.91417298594985,-5.39303536614492));
#17468=CARTESIAN_POINT('Ctrl Pts',(4.64833384477347,-0.956777235594704,
-5.39603717222854));
#17469=CARTESIAN_POINT('Ctrl Pts',(4.61063502568417,-0.997267675972856,
-5.39903897831216));
#17470=CARTESIAN_POINT('Ctrl Pts',(4.57295861320917,-1.0377340505128,-5.40203900024676));
#17471=CARTESIAN_POINT('Ctrl Pts',(4.53296127237125,-1.07608872022572,-5.40503902218136));
#17472=CARTESIAN_POINT('Ctrl Pts',(4.49091299338967,-1.11206196557849,-5.40803904411596));
#17473=CARTESIAN_POINT('Ctrl Pts',(4.44887309908909,-1.1480280376487,-5.41103846782805));
#17474=CARTESIAN_POINT('Ctrl Pts',(4.40478347991244,-1.18161328530514,-5.41403789154014));
#17475=CARTESIAN_POINT('Ctrl Pts',(4.35894840650725,-1.21258722588824,-5.41703731525223));
#17476=CARTESIAN_POINT('Ctrl Pts',(4.3130711943908,-1.24358964252345,-5.42003949649999));
#17477=CARTESIAN_POINT('Ctrl Pts',(4.26544576059141,-1.2719756594282,-5.42304167774775));
#17478=CARTESIAN_POINT('Ctrl Pts',(4.21640542748126,-1.29755812299601,-5.42604385899551));
#17479=CARTESIAN_POINT('Ctrl Pts',(4.16734277230008,-1.32315223113336,-5.42904740676953));
#17480=CARTESIAN_POINT('Ctrl Pts',(4.1168644161577,-1.34594002441191,-5.43205095454355));
#17481=CARTESIAN_POINT('Ctrl Pts',(4.0653253637124,-1.36578181672806,-5.43505450231757));
#17482=CARTESIAN_POINT('Ctrl Pts',(4.01368903997931,-1.38566105708796,-5.43806371878253));
#17483=CARTESIAN_POINT('Ctrl Pts',(3.96098852492938,-1.40258302750694,-5.4410729352475));
#17484=CARTESIAN_POINT('Ctrl Pts',(3.90759462594989,-1.41645777229699,-5.44408215171247));
#17485=CARTESIAN_POINT('Ctrl Pts',(3.86674610497601,-1.42707252069326,-5.44638432563558));
#17486=CARTESIAN_POINT('Ctrl Pts',(3.82549209883954,-1.43590479475528,-5.4486864995587));
#17487=CARTESIAN_POINT('Ctrl Pts',(3.78400121299976,-1.44293476019596,-5.45098867348181));
#17488=CARTESIAN_POINT('Ctrl Pts',(3.72975122632739,-1.45212655072405,-5.45399880214305));
#17489=CARTESIAN_POINT('Ctrl Pts',(3.67486815857402,-1.45827394706616,-5.45700893080429));
#17490=CARTESIAN_POINT('Ctrl Pts',(3.61972402736092,-1.46130058908986,-5.46001905946553));
#17491=CARTESIAN_POINT('Ctrl Pts',(3.56467790280697,-1.46432185191788,-5.46302383827997));
#17492=CARTESIAN_POINT('Ctrl Pts',(3.50937215862868,-1.46423333870561,-5.46602861709442));
#17493=CARTESIAN_POINT('Ctrl Pts',(3.45418641618661,-1.46101012711558,-5.46903339590886));
#17494=CARTESIAN_POINT('Ctrl Pts',(3.39905527089387,-1.45779010435941,-5.47203520199248));
#17495=CARTESIAN_POINT('Ctrl Pts',(3.34404441678076,-1.45144155732333,-5.4750370080761));
#17496=CARTESIAN_POINT('Ctrl Pts',(3.28953409648797,-1.44199159942286,-5.47803881415972));
#17497=CARTESIAN_POINT('Ctrl Pts',(3.2350561748684,-1.43254725818537,-5.48103883609432));
#17498=CARTESIAN_POINT('Ctrl Pts',(3.18107871672722,-1.42000524975318,-5.48403885802892));
#17499=CARTESIAN_POINT('Ctrl Pts',(3.12797514102828,-1.40444432450707,-5.48703887996352));
#17500=CARTESIAN_POINT('Ctrl Pts',(3.07488215450339,-1.38888650220353,-5.49003830367561));
#17501=CARTESIAN_POINT('Ctrl Pts',(3.02266321087416,-1.37031110703868,-5.4930377273877));
#17502=CARTESIAN_POINT('Ctrl Pts',(2.97167759785829,-1.34884703904824,-5.49603715109979));
#17503=CARTESIAN_POINT('Ctrl Pts',(2.92064511095596,-1.32736323795612,-5.49903933234755));
#17504=CARTESIAN_POINT('Ctrl Pts',(2.87084870777818,-1.30298566361301,-5.5020415135953));
#17505=CARTESIAN_POINT('Ctrl Pts',(2.8226272605429,-1.27589122248039,-5.50504369484306));
#17506=CARTESIAN_POINT('Ctrl Pts',(2.77438386397531,-1.24878444855966,-5.50804724261708));
#17507=CARTESIAN_POINT('Ctrl Pts',(2.72771729818045,-1.21895862756092,-5.5110507903911));
#17508=CARTESIAN_POINT('Ctrl Pts',(2.68293852718109,-1.18663476150104,-5.51405433816511));
#17509=CARTESIAN_POINT('Ctrl Pts',(2.6380752437874,-1.15424988958383,-5.51706355463008));
#17510=CARTESIAN_POINT('Ctrl Pts',(2.59510728360013,-1.11935788811164,-5.52007277109505));
#17511=CARTESIAN_POINT('Ctrl Pts',(2.55431259462973,-1.08222016681602,-5.52308198756001));
#17512=CARTESIAN_POINT('Ctrl Pts',(2.52310298566911,-1.05380828800096,-5.52538416148313));
#17513=CARTESIAN_POINT('Ctrl Pts',(2.493164691434,-1.0240828674705,-5.52768633540625));
#17514=CARTESIAN_POINT('Ctrl Pts',(2.46460644903469,-0.993174279457856,
-5.52998850932937));
#17515=CARTESIAN_POINT('Ctrl Pts',(2.42770723493981,-0.95323825711789,-5.53296307643631));
#17516=CARTESIAN_POINT('Ctrl Pts',(2.39295012736766,-0.911149160200317,
-5.53593764354324));
#17517=CARTESIAN_POINT('Ctrl Pts',(2.36059970343556,-0.867168624489341,
-5.53891221065018));
#17518=CARTESIAN_POINT('Ctrl Pts',(2.32829617987034,-0.823251850021937,
-5.54188246534721));
#17519=CARTESIAN_POINT('Ctrl Pts',(2.2983927516882,-0.77744949631226,-5.54485272004424));
#17520=CARTESIAN_POINT('Ctrl Pts',(2.27111569915588,-0.730058345952124,
-5.54782297474127));
#17521=CARTESIAN_POINT('Ctrl Pts',(2.24386679721609,-0.682716104430726,
-5.55079016406202));
#17522=CARTESIAN_POINT('Ctrl Pts',(2.21923917147809,-0.633788780753086,
-5.55375735338278));
#17523=CARTESIAN_POINT('Ctrl Pts',(2.19741602064055,-0.583602353875314,
-5.55672454270353));
#17524=CARTESIAN_POINT('Ctrl Pts',(2.17559980709139,-0.533431880592808,
-5.55969078879441));
#17525=CARTESIAN_POINT('Ctrl Pts',(2.15658653224062,-0.482003586647679,
-5.56265703488528));
#17526=CARTESIAN_POINT('Ctrl Pts',(2.14051259108434,-0.429666355127702,
-5.56562328097615));
#17527=CARTESIAN_POINT('Ctrl Pts',(2.1244421866726,-0.377340639353387,-5.56858887440477));
#17528=CARTESIAN_POINT('Ctrl Pts',(2.11130998532965,-0.324106902664438,
-5.57155446783338));
#17529=CARTESIAN_POINT('Ctrl Pts',(2.10120260055936,-0.270329502740076,
-5.574520061262));
#17530=CARTESIAN_POINT('Ctrl Pts',(2.09108705510497,-0.2165086830407,-5.57748804910537));
#17531=CARTESIAN_POINT('Ctrl Pts',(2.08400129502276,-0.162143858228026,
-5.58045603694873));
#17532=CARTESIAN_POINT('Ctrl Pts',(2.07998051047228,-0.107608087049964,
-5.5834240247921));
#17533=CARTESIAN_POINT('Ctrl Pts',(2.07730678194287,-0.0713430632861772,
-5.58539766791376));
#17534=CARTESIAN_POINT('Ctrl Pts',(2.07598729440754,-0.0350025971489008,
-5.58737131103543));
#17535=CARTESIAN_POINT('Ctrl Pts',(2.07601963090622,0.00130348536077232,
-5.58934495415709));
#17536=CARTESIAN_POINT('Origin',(3.53951905042299,8.32667268468867E-16,
0.));
#17537=CARTESIAN_POINT('',(2.07398455785054,-0.000602649354525531,-6.16065504584291));
#17538=CARTESIAN_POINT('',(2.07406181082671,-0.00067065111815213,-6.08934495415709));
#17539=CARTESIAN_POINT('',(2.07601905042299,1.01189432752408E-15,0.));
#17540=CARTESIAN_POINT('Ctrl Pts',(2.07398455785054,-0.000602649354525531,
-6.16065504584291));
#17541=CARTESIAN_POINT('Ctrl Pts',(2.07380392810973,-0.0350793873735884,
-6.15877304002329));
#17542=CARTESIAN_POINT('Ctrl Pts',(2.09047948666901,-0.551781602873419,
-6.1305577555879));
#17543=CARTESIAN_POINT('Ctrl Pts',(2.700819254767,-1.50963595324291,-6.07600919253644));
#17544=CARTESIAN_POINT('Ctrl Pts',(4.34561751406752,-1.52729280934158,-5.99700935668896));
#17545=CARTESIAN_POINT('Ctrl Pts',(5.25911691828729,-0.159377637682488,
-5.91800952084136));
#17546=CARTESIAN_POINT('Ctrl Pts',(4.61258363582657,1.35312617819235,-5.83900968499382));
#17547=CARTESIAN_POINT('Ctrl Pts',(2.9925577366135,1.6380633015096,-5.76000984914625));
#17548=CARTESIAN_POINT('Ctrl Pts',(2.1468259724859,0.734152894754073,-5.70055836087874));
#17549=CARTESIAN_POINT('Ctrl Pts',(2.07527553244525,0.126122538347039,-5.66744015122709));
#17550=CARTESIAN_POINT('Ctrl Pts',(2.07637422736057,0.00130108074448911,
-5.66065522019129));
#17551=CARTESIAN_POINT('Ctrl Pts',(2.0762466562035,0.00130536003002751,
-5.58934506707585));
#17552=CARTESIAN_POINT('Ctrl Pts',(2.07517374542601,0.121736799127538,-5.59589282644287));
#17553=CARTESIAN_POINT('Ctrl Pts',(2.14365852969769,0.725306357571781,-5.62877386442578));
#17554=CARTESIAN_POINT('Ctrl Pts',(2.97793235114716,1.6331069724431,-5.68798818102447));
#17555=CARTESIAN_POINT('Ctrl Pts',(4.60044132363883,1.36266721338727,-5.76698801687208));
#17556=CARTESIAN_POINT('Ctrl Pts',(5.26047328032698,-0.143994940263915,
-5.84598785271962));
#17557=CARTESIAN_POINT('Ctrl Pts',(4.35924204804306,-1.52002375357057,-5.92498768856719));
#17558=CARTESIAN_POINT('Ctrl Pts',(2.71435167648648,-1.51707508358577,-6.00398752441476));
#17559=CARTESIAN_POINT('Ctrl Pts',(2.09278029747244,-0.560575463951796,
-6.05877327961139));
#17560=CARTESIAN_POINT('Ctrl Pts',(2.0738392940555,-0.0394979728212691,
-6.08722575619216));
#17561=CARTESIAN_POINT('Ctrl Pts',(2.07406181082671,-0.00067065111815213,
-6.08934495415709));
#17562=CARTESIAN_POINT('Origin',(3.53951905042299,8.32667268468867E-16,
0.));
#17563=CARTESIAN_POINT('',(2.0779924908381,-0.000733103778174787,-6.66065504584291));
#17564=CARTESIAN_POINT('',(2.07609699915992,-0.000674750808749472,-6.58934493582576));
#17565=CARTESIAN_POINT('',(2.07601905042299,1.01189432752408E-15,0.));
#17566=CARTESIAN_POINT('Ctrl Pts',(2.0779924908381,-0.000733103778174787,
-6.66065504584291));
#17567=CARTESIAN_POINT('Ctrl Pts',(2.07710078135123,-0.195345291847198,
-6.65010604505175));
#17568=CARTESIAN_POINT('Ctrl Pts',(2.2035492442434,-0.874652820981799,-6.61322376564476));
#17569=CARTESIAN_POINT('Ctrl Pts',(3.22971693546565,-1.69895282692743,-6.55000820762186));
#17570=CARTESIAN_POINT('Ctrl Pts',(4.79316310733731,-1.18776876416246,-6.47100837177433));
#17571=CARTESIAN_POINT('Ctrl Pts',(5.21929354813173,0.400968446893448,-6.39200853592674));
#17572=CARTESIAN_POINT('Ctrl Pts',(4.12151937631297,1.62594393483315,-6.31300870007919));
#17573=CARTESIAN_POINT('Ctrl Pts',(2.53448049511705,1.38180827662175,-6.23589087005124));
#17574=CARTESIAN_POINT('Ctrl Pts',(2.07633132374345,0.447323769173315,-6.18510631863914));
#17575=CARTESIAN_POINT('Ctrl Pts',(2.07398455785054,-0.000602649354525531,
-6.16065504584291));
#17576=CARTESIAN_POINT('Ctrl Pts',(2.07406181082671,-0.00067065111815213,
-6.08934495415709));
#17577=CARTESIAN_POINT('Ctrl Pts',(2.07660430054847,0.442972611446132,-6.11355903480801));
#17578=CARTESIAN_POINT('Ctrl Pts',(2.52703917513374,1.37356066127882,-6.16410639407482));
#17579=CARTESIAN_POINT('Ctrl Pts',(4.10695721513758,1.63108305535657,-6.24098703195743));
#17580=CARTESIAN_POINT('Ctrl Pts',(5.21564099217811,0.415972644068219,-6.31998686780501));
#17581=CARTESIAN_POINT('Ctrl Pts',(4.80373378404372,-1.1765114158147,-6.39898670365256));
#17582=CARTESIAN_POINT('Ctrl Pts',(3.24492104393115,-1.70165508221173,-6.47798653950012));
#17583=CARTESIAN_POINT('Ctrl Pts',(2.20754846303831,-0.883507584733025,
-6.54143912965251));
#17584=CARTESIAN_POINT('Ctrl Pts',(2.07722212510776,-0.199689226725607,
-6.57855844118906));
#17585=CARTESIAN_POINT('Ctrl Pts',(2.0780563998582,-0.000682366665369591,
-6.58934447410974));
#17586=CARTESIAN_POINT('Origin',(3.53951905042299,8.32667268468867E-16,
0.));
#17587=CARTESIAN_POINT('',(2.0760196139518,0.00128430857734538,-7.16065506268004));
#17588=CARTESIAN_POINT('',(2.07601962331082,0.00129492948150966,-7.08934495420698));
#17589=CARTESIAN_POINT('',(2.07601905042299,1.01189432752408E-15,0.));
#17590=CARTESIAN_POINT('Ctrl Pts',(2.07655027563832,0.00128353304686551,
-7.16065504584291));
#17591=CARTESIAN_POINT('Ctrl Pts',(2.07959752967489,-0.352338916278862,
-7.14143905008021));
#17592=CARTESIAN_POINT('Ctrl Pts',(2.38543525504794,-1.19528620059351,-7.09588977570168));
#17593=CARTESIAN_POINT('Ctrl Pts',(3.79139519143046,-1.70850123445903,-7.02400722270725));
#17594=CARTESIAN_POINT('Ctrl Pts',(5.10805894974804,-0.72256532077177,-6.94500738685969));
#17595=CARTESIAN_POINT('Ctrl Pts',(5.00173099643442,0.918887524944285,-6.86600755101213));
#17596=CARTESIAN_POINT('Ctrl Pts',(3.56887288554054,1.72671839363593,-6.78700771516457));
#17597=CARTESIAN_POINT('Ctrl Pts',(2.30427301763542,1.06936233072511,-6.71855688010815));
#17598=CARTESIAN_POINT('Ctrl Pts',(2.0793267395085,0.29046157004619,-6.67643932366761));
#17599=CARTESIAN_POINT('Ctrl Pts',(2.0779924908381,-0.000733103778174787,
-6.66065504584291));
#17600=CARTESIAN_POINT('Ctrl Pts',(2.0760192058315,-0.000674448439338396,
-6.58934495415709));
#17601=CARTESIAN_POINT('Ctrl Pts',(2.07599326113436,0.0556234952179208,
-6.59239202230984));
#17602=CARTESIAN_POINT('Ctrl Pts',(2.07922016311911,0.111913354676178,-6.59543909046259));
#17603=CARTESIAN_POINT('Ctrl Pts',(2.08567083734158,0.167802334071928,-6.59848615861535));
#17604=CARTESIAN_POINT('Ctrl Pts',(2.09228650335208,0.225120810962692,-6.601611162997));
#17605=CARTESIAN_POINT('Ctrl Pts',(2.10229309861054,0.282017059273543,-6.60473616737866));
#17606=CARTESIAN_POINT('Ctrl Pts',(2.11560311694291,0.338076417961319,-6.60786117176032));
#17607=CARTESIAN_POINT('Ctrl Pts',(2.1286086080415,0.392853163732831,-6.61091467744707));
#17608=CARTESIAN_POINT('Ctrl Pts',(2.14476771993851,0.44683044349619,-6.61396818313383));
#17609=CARTESIAN_POINT('Ctrl Pts',(2.16394835432136,0.499637378532147,-6.61702168882059));
#17610=CARTESIAN_POINT('Ctrl Pts',(2.18380266863138,0.55429904743349,-6.6201824425497));
#17611=CARTESIAN_POINT('Ctrl Pts',(2.2068945099148,0.607706069216808,-6.62334319627881));
#17612=CARTESIAN_POINT('Ctrl Pts',(2.23302458651292,0.659472869625687,-6.62650395000792));
#17613=CARTESIAN_POINT('Ctrl Pts',(2.25915466311103,0.71123967003456,-6.62966470373703));
#17614=CARTESIAN_POINT('Ctrl Pts',(2.28832261198184,0.761365777376941,-6.63282545746614));
#17615=CARTESIAN_POINT('Ctrl Pts',(2.32028027386689,0.809499262348018,-6.63598621119525));
#17616=CARTESIAN_POINT('Ctrl Pts',(2.35071499995783,0.855338956007899,-6.63899633985649));
#17617=CARTESIAN_POINT('Ctrl Pts',(2.38380241792489,0.899556196763958,-6.64200646851773));
#17618=CARTESIAN_POINT('Ctrl Pts',(2.41934353833162,0.941827517176493,-6.64501659717896));
#17619=CARTESIAN_POINT('Ctrl Pts',(2.45482149215298,0.984023709541885,-6.64802137599341));
#17620=CARTESIAN_POINT('Ctrl Pts',(2.4927441570204,1.02428044392336,-6.65102615480785));
#17621=CARTESIAN_POINT('Ctrl Pts',(2.53286984092293,1.06230392026618,-6.6540309336223));
#17622=CARTESIAN_POINT('Ctrl Pts',(2.572955827109,1.10028977867865,-6.65703273970592));
#17623=CARTESIAN_POINT('Ctrl Pts',(2.61524013334466,1.13604639437272,-6.66003454578954));
#17624=CARTESIAN_POINT('Ctrl Pts',(2.65944270880389,1.16931513413722,-6.66303635187316));
#17625=CARTESIAN_POINT('Ctrl Pts',(2.7036190120858,1.2025641003428,-6.66603637380776));
#17626=CARTESIAN_POINT('Ctrl Pts',(2.74971090364499,1.23332780453115,-6.66903639574236));
#17627=CARTESIAN_POINT('Ctrl Pts',(2.79740536080833,1.26138793465235,-6.67203641767696));
#17628=CARTESIAN_POINT('Ctrl Pts',(2.84509030740863,1.28944246941399,-6.67503584138905));
#17629=CARTESIAN_POINT('Ctrl Pts',(2.89437673005101,1.31479423310812,-6.67803526510114));
#17630=CARTESIAN_POINT('Ctrl Pts',(2.94492472065994,1.3372695438892,-6.68103468881323));
#17631=CARTESIAN_POINT('Ctrl Pts',(2.99551918282488,1.35976551746323,-6.68403687006099));
#17632=CARTESIAN_POINT('Ctrl Pts',(3.04737704654229,1.37937953976781,-6.68703905130875));
#17633=CARTESIAN_POINT('Ctrl Pts',(3.10013738245228,1.39598567322565,-6.69004123255651));
#17634=CARTESIAN_POINT('Ctrl Pts',(3.15292173369599,1.41259936542682,-6.69304478033053));
#17635=CARTESIAN_POINT('Ctrl Pts',(3.20660886317306,1.42620230958812,-6.69604832810455));
#17636=CARTESIAN_POINT('Ctrl Pts',(3.26082480015785,1.43671909741228,-6.69905187587857));
#17637=CARTESIAN_POINT('Ctrl Pts',(3.31514306059952,1.44725573390355,-6.70206109234354));
#17638=CARTESIAN_POINT('Ctrl Pts',(3.36999159767024,1.45469450736379,-6.7050703088085));
#17639=CARTESIAN_POINT('Ctrl Pts',(3.42498958410318,1.45901173790498,-6.70807952527347));
#17640=CARTESIAN_POINT('Ctrl Pts',(3.4670652977196,1.46231459620304,-6.71038169919659));
#17641=CARTESIAN_POINT('Ctrl Pts',(3.50922832371918,1.46379152747159,-6.7126838731197));
#17642=CARTESIAN_POINT('Ctrl Pts',(3.55130918739314,1.46345250782874,-6.71498604704281));
#17643=CARTESIAN_POINT('Ctrl Pts',(3.60633057937528,1.46300923430651,-6.71799617570406));
#17644=CARTESIAN_POINT('Ctrl Pts',(3.66144254381316,1.45945775804877,-6.72100630436529));
#17645=CARTESIAN_POINT('Ctrl Pts',(3.71626544097366,1.45278799672468,-6.72401643302654));
#17646=CARTESIAN_POINT('Ctrl Pts',(3.77099090239841,1.44613008944581,-6.72702121184098));
#17647=CARTESIAN_POINT('Ctrl Pts',(3.82542779608369,1.43636495864267,-6.73002599065542));
#17648=CARTESIAN_POINT('Ctrl Pts',(3.87919799701067,1.4235344966825,-6.73303076946987));
#17649=CARTESIAN_POINT('Ctrl Pts',(3.93291500123211,1.41071672833877,-6.73603257555349));
#17650=CARTESIAN_POINT('Ctrl Pts',(3.98596610812677,1.39483975832007,-6.73903438163711));
#17651=CARTESIAN_POINT('Ctrl Pts',(4.03798168674773,1.3759968205589,-6.74203618772072));
#17652=CARTESIAN_POINT('Ctrl Pts',(4.08996634946638,1.35716508225832,-6.74503620965532));
#17653=CARTESIAN_POINT('Ctrl Pts',(4.14091620827475,1.33537104981138,-6.74803623158992));
#17654=CARTESIAN_POINT('Ctrl Pts',(4.19047738659582,1.31075760328411,-6.75103625352452));
#17655=CARTESIAN_POINT('Ctrl Pts',(4.24002868211836,1.28614906482685,-6.75403567723661));
#17656=CARTESIAN_POINT('Ctrl Pts',(4.28819137435497,1.25872246358266,-6.7570351009487));
#17657=CARTESIAN_POINT('Ctrl Pts',(4.33463427564759,1.22866758263415,-6.76003452466079));
#17658=CARTESIAN_POINT('Ctrl Pts',(4.38111987446117,1.19858507057574,-6.76303670590855));
#17659=CARTESIAN_POINT('Ctrl Pts',(4.42588207917347,1.16586973885509,-6.76603888715631));
#17660=CARTESIAN_POINT('Ctrl Pts',(4.46861820328876,1.13075506372694,-6.76904106840407));
#17661=CARTESIAN_POINT('Ctrl Pts',(4.51137377993907,1.09562440517816,-6.77204461617809));
#17662=CARTESIAN_POINT('Ctrl Pts',(4.55210104856066,1.05809258465259,-6.77504816395211));
#17663=CARTESIAN_POINT('Ctrl Pts',(4.5905325165387,1.01843160989997,-6.77805171172613));
#17664=CARTESIAN_POINT('Ctrl Pts',(4.62903651744478,0.978695781732188,-6.78106092819109));
#17665=CARTESIAN_POINT('Ctrl Pts',(4.66523571575824,0.936823172417134,-6.78407014465606));
#17666=CARTESIAN_POINT('Ctrl Pts',(4.69890219641194,0.893119796442098,-6.78707936112102));
#17667=CARTESIAN_POINT('Ctrl Pts',(4.72465843387322,0.859684922715576,-6.78938153504414));
#17668=CARTESIAN_POINT('Ctrl Pts',(4.74893311544962,0.825179243157287,-6.79168370896726));
#17669=CARTESIAN_POINT('Ctrl Pts',(4.77164199609297,0.789750148308652,-6.79398588289037));
#17670=CARTESIAN_POINT('Ctrl Pts',(4.80133421517459,0.74342604882393,-6.79699601155161));
#17671=CARTESIAN_POINT('Ctrl Pts',(4.82847271924862,0.695327782696866,-6.80000614021285));
#17672=CARTESIAN_POINT('Ctrl Pts',(4.85284163043178,0.645767799475205,-6.80301626887409));
#17673=CARTESIAN_POINT('Ctrl Pts',(4.87716723119335,0.596295898308248,-6.80602104768853));
#17674=CARTESIAN_POINT('Ctrl Pts',(4.89873277634878,0.545367905653401,-6.80902582650297));
#17675=CARTESIAN_POINT('Ctrl Pts',(4.91736674585716,0.493323401215406,-6.81203060531742));
#17676=CARTESIAN_POINT('Ctrl Pts',(4.93598228013988,0.441330386192138,-6.81503241140104));
#17677=CARTESIAN_POINT('Ctrl Pts',(4.95167180700242,0.388223542315351,-6.81803421748465));
#17678=CARTESIAN_POINT('Ctrl Pts',(4.96431144747405,0.334363388105644,-6.82103602356827));
#17679=CARTESIAN_POINT('Ctrl Pts',(4.97694357546769,0.280535246137471,-6.82403604550287));
#17680=CARTESIAN_POINT('Ctrl Pts',(4.98652928959537,0.225955194401018,-6.82703606743747));
#17681=CARTESIAN_POINT('Ctrl Pts',(4.99299489898523,0.170997683160591,-6.83003608937207));
#17682=CARTESIAN_POINT('Ctrl Pts',(4.99945921909348,0.116051130780102,-6.83303551308416));
#17683=CARTESIAN_POINT('Ctrl Pts',(5.00280460839102,0.0607277925788181,
-6.83603493679625));
#17684=CARTESIAN_POINT('Ctrl Pts',(5.0030090556809,0.00540874386492178,
-6.83903436050834));
#17685=CARTESIAN_POINT('Ctrl Pts',(5.00321369093046,-0.0499611627018728,
-6.8420365417561));
#17686=CARTESIAN_POINT('Ctrl Pts',(5.0002716130844,-0.105326242655259,-6.84503872300386));
#17687=CARTESIAN_POINT('Ctrl Pts',(4.99421297807659,-0.160305417399837,
-6.84804090425162));
#17688=CARTESIAN_POINT('Ctrl Pts',(4.98815158531262,-0.215309617444318,
-6.85104445202564));
#17689=CARTESIAN_POINT('Ctrl Pts',(4.97897089522622,-0.269927040405111,
-6.85404799979966));
#17690=CARTESIAN_POINT('Ctrl Pts',(4.96675256471366,-0.323785030051597,
-6.85705154757368));
#17691=CARTESIAN_POINT('Ctrl Pts',(4.95451117415852,-0.377744667589602,
-6.86006076403864));
#17692=CARTESIAN_POINT('Ctrl Pts',(4.93922083679664,-0.430941499757968,
-6.86306998050361));
#17693=CARTESIAN_POINT('Ctrl Pts',(4.92101331609888,-0.483017436439539,
-6.86607919696858));
#17694=CARTESIAN_POINT('Ctrl Pts',(4.90708381656203,-0.522857662241221,
-6.8683813708917));
#17695=CARTESIAN_POINT('Ctrl Pts',(4.89144797200305,-0.562042129219201,
-6.87068354481482));
#17696=CARTESIAN_POINT('Ctrl Pts',(4.87418319480349,-0.600419746265117,
-6.87298571873794));
#17697=CARTESIAN_POINT('Ctrl Pts',(4.85160922671344,-0.650599084958741,
-6.87599584739917));
#17698=CARTESIAN_POINT('Ctrl Pts',(4.82615400645715,-0.699609016294218,
-6.87900597606041));
#17699=CARTESIAN_POINT('Ctrl Pts',(4.79796126411181,-0.747098015528067,
-6.88201610472165));
#17700=CARTESIAN_POINT('Ctrl Pts',(4.76981862821346,-0.794502613429359,
-6.8850208835361));
#17701=CARTESIAN_POINT('Ctrl Pts',(4.73894839295802,-0.840391193152233,
-6.88802566235054));
#17702=CARTESIAN_POINT('Ctrl Pts',(4.70554124761026,-0.884434557028712,
-6.89103044116499));
#17703=CARTESIAN_POINT('Ctrl Pts',(4.67216715309817,-0.92843434729342,-6.89403224724861));
#17704=CARTESIAN_POINT('Ctrl Pts',(4.63626143797683,-0.970592119309363,
-6.89703405333222));
#17705=CARTESIAN_POINT('Ctrl Pts',(4.59805835922658,-1.01060713520023,-6.90003585941584));
#17706=CARTESIAN_POINT('Ctrl Pts',(4.55987798680168,-1.05059836782546,-6.90303588135044));
#17707=CARTESIAN_POINT('Ctrl Pts',(4.51940332113245,-1.08844898739569,-6.90603590328504));
#17708=CARTESIAN_POINT('Ctrl Pts',(4.47690770998966,-1.12389267766802,-6.90903592521963));
#17709=CARTESIAN_POINT('Ctrl Pts',(4.43442057272858,-1.15932930025429,-6.91203534893173));
#17710=CARTESIAN_POINT('Ctrl Pts',(4.38991369565091,-1.19235960864036,-6.91503477264382));
#17711=CARTESIAN_POINT('Ctrl Pts',(4.34369421275151,-1.22275694980397,-6.91803419635591));
#17712=CARTESIAN_POINT('Ctrl Pts',(4.297432237732,-1.25318223692003,-6.92103637760367));
#17713=CARTESIAN_POINT('Ctrl Pts',(4.24945495344846,-1.28096942988862,-6.92403855885143));
#17714=CARTESIAN_POINT('Ctrl Pts',(4.20009800056435,-1.30593556526734,-6.92704074009919));
#17715=CARTESIAN_POINT('Ctrl Pts',(4.15071858149094,-1.33091306467668,-6.9300442878732));
#17716=CARTESIAN_POINT('Ctrl Pts',(4.09995872682262,-1.35306673514884,-6.93304783564722));
#17717=CARTESIAN_POINT('Ctrl Pts',(4.04817516318935,-1.37226134863058,-6.93605138342124));
#17718=CARTESIAN_POINT('Ctrl Pts',(3.99629386679455,-1.39149218871494,-6.93906059988621));
#17719=CARTESIAN_POINT('Ctrl Pts',(3.94338550785993,-1.40775265993304,-6.94206981635118));
#17720=CARTESIAN_POINT('Ctrl Pts',(3.88982199153912,-1.4209574587036,-6.94507903281614));
#17721=CARTESIAN_POINT('Ctrl Pts',(3.84884370634756,-1.43105967093844,-6.94738120673926));
#17722=CARTESIAN_POINT('Ctrl Pts',(3.8074822965976,-1.43937446924747,-6.94968338066238));
#17723=CARTESIAN_POINT('Ctrl Pts',(3.76590660298021,-1.44588413299516,-6.95198555458551));
#17724=CARTESIAN_POINT('Ctrl Pts',(3.71154572880312,-1.45439562086544,-6.95499568324674));
#17725=CARTESIAN_POINT('Ctrl Pts',(3.65658995988772,-1.45985502291367,-6.95800581190798));
#17726=CARTESIAN_POINT('Ctrl Pts',(3.60141224121718,-1.46219064520784,-6.96101594056922));
#17727=CARTESIAN_POINT('Ctrl Pts',(3.54633258890015,-1.46452211644307,-6.96402071938366));
#17728=CARTESIAN_POINT('Ctrl Pts',(3.49103229302684,-1.46374080342766,-6.96702549819811));
#17729=CARTESIAN_POINT('Ctrl Pts',(3.43589125736956,-1.45982654123936,-6.97003027701255));
#17730=CARTESIAN_POINT('Ctrl Pts',(3.38080477463164,-1.45591615156501,-6.97303208309617));
#17731=CARTESIAN_POINT('Ctrl Pts',(3.32587776418845,-1.44887898995699,-6.97603388917979));
#17732=CARTESIAN_POINT('Ctrl Pts',(3.2714900991996,-1.43874693094585,-6.97903569526341));
#17733=CARTESIAN_POINT('Ctrl Pts',(3.2171347599828,-1.42862089401029,-6.98203571719801));
#17734=CARTESIAN_POINT('Ctrl Pts',(3.16331864898754,-1.41540370216639,-6.9850357391326));
#17735=CARTESIAN_POINT('Ctrl Pts',(3.11041416938353,-1.39917877737911,-6.9880357610672));
#17736=CARTESIAN_POINT('Ctrl Pts',(3.05752023925256,-1.38295708793992,-6.99103518477929));
#17737=CARTESIAN_POINT('Ctrl Pts',(3.00553808411818,-1.36372901141447,-6.99403460849138));
#17738=CARTESIAN_POINT('Ctrl Pts',(2.95482534879553,-1.34162793846773,-6.99703403220347));
#17739=CARTESIAN_POINT('Ctrl Pts',(2.90406599045795,-1.31950654678553,-7.00003621345123));
#17740=CARTESIAN_POINT('Ctrl Pts',(2.85457886871953,-1.29450709314464,-7.00303839469899));
#17741=CARTESIAN_POINT('Ctrl Pts',(2.80670061312826,-1.26681071512713,-7.00604057594674));
#17742=CARTESIAN_POINT('Ctrl Pts',(2.7588005644179,-1.23910173033318,-7.00904412372076));
#17743=CARTESIAN_POINT('Ctrl Pts',(2.71251128384996,-1.20869366453091,-7.01204767149478));
#17744=CARTESIAN_POINT('Ctrl Pts',(2.66814094258865,-1.17581139779603,-7.01505121926879));
#17745=CARTESIAN_POINT('Ctrl Pts',(2.6236868597754,-1.14286707131651,-7.01806043573376));
#17746=CARTESIAN_POINT('Ctrl Pts',(2.58115935788908,-1.10743955443064,-7.02106965219873));
#17747=CARTESIAN_POINT('Ctrl Pts',(2.54083308849079,-1.06979371817166,-7.02407886866369));
#17748=CARTESIAN_POINT('Ctrl Pts',(2.50998183970012,-1.04099311058539,-7.02638104258681));
#17749=CARTESIAN_POINT('Ctrl Pts',(2.48041826042216,-1.01089498991809,-7.02868321650994));
#17750=CARTESIAN_POINT('Ctrl Pts',(2.45224944605684,-0.979631082306741,
-7.03098539043306));
#17751=CARTESIAN_POINT('Ctrl Pts',(2.41581120538601,-0.939189132032269,
-7.03396340599272));
#17752=CARTESIAN_POINT('Ctrl Pts',(2.3815476665173,-0.896617035648219,-7.03694142155237));
#17753=CARTESIAN_POINT('Ctrl Pts',(2.34972042974617,-0.852180434083961,
-7.03991943711203));
#17754=CARTESIAN_POINT('Ctrl Pts',(2.31793967594817,-0.807808731190343,
-7.04289310334603));
#17755=CARTESIAN_POINT('Ctrl Pts',(2.28858849220199,-0.761578348565858,
-7.04586676958003));
#17756=CARTESIAN_POINT('Ctrl Pts',(2.26188971872353,-0.71378956337369,-7.04884043581404));
#17757=CARTESIAN_POINT('Ctrl Pts',(2.23521883903141,-0.666050705949342,
-7.05181099528321));
#17758=CARTESIAN_POINT('Ctrl Pts',(2.21119514271729,-0.616757140291217,
-7.05478155475238));
#17759=CARTESIAN_POINT('Ctrl Pts',(2.18999801491327,-0.566237781075023,
-7.05775211422155));
#17760=CARTESIAN_POINT('Ctrl Pts',(2.1688087009087,-0.515737044577197,-7.06072157866708));
#17761=CARTESIAN_POINT('Ctrl Pts',(2.15044411167435,-0.46401190207085,-7.06369104311261));
#17762=CARTESIAN_POINT('Ctrl Pts',(2.13503653174213,-0.41141354464803,-7.06666050755815));
#17763=CARTESIAN_POINT('Ctrl Pts',(2.11963252895492,-0.358827398873818,
-7.06962928258945));
#17764=CARTESIAN_POINT('Ctrl Pts',(2.10718431885292,-0.305368960812494,
-7.07259805762075));
#17765=CARTESIAN_POINT('Ctrl Pts',(2.09777422802999,-0.251404290144346,
-7.07556683265205));
#17766=CARTESIAN_POINT('Ctrl Pts',(2.08835749173144,-0.197401509227279,
-7.07853770425419));
#17767=CARTESIAN_POINT('Ctrl Pts',(2.08198324268079,-0.142892316244514,
-7.08150857585634));
#17768=CARTESIAN_POINT('Ctrl Pts',(2.07868228623638,-0.0882507699727326,
-7.08447944745849));
#17769=CARTESIAN_POINT('Ctrl Pts',(2.07688025327064,-0.0584212737832516,
-7.08610128302469));
#17770=CARTESIAN_POINT('Ctrl Pts',(2.07599321388797,-0.0285524121464094,
-7.08772311859089));
#17771=CARTESIAN_POINT('Ctrl Pts',(2.07601962331001,0.00129492856329364,
-7.08934495415709));
#17772=CARTESIAN_POINT('Origin',(3.53951905042299,8.32667268468867E-16,
0.));
#17773=CARTESIAN_POINT('',(2.07589476394848,-0.00050215083052111,-7.6606550766331));
#17774=CARTESIAN_POINT('',(2.07592822643732,-0.000573461297524445,-7.5893449794238));
#17775=CARTESIAN_POINT('',(2.07601905042299,1.01189432752408E-15,0.));
#17776=CARTESIAN_POINT('Ctrl Pts',(2.07601913675002,-0.000502672062860379,
-7.66065504584291));
#17777=CARTESIAN_POINT('Ctrl Pts',(2.07602887184672,-0.0288458290411398,
-7.65910533372452));
#17778=CARTESIAN_POINT('Ctrl Pts',(2.07686192127292,-0.0571737031003173,
-7.65755562160613));
#17779=CARTESIAN_POINT('Ctrl Pts',(2.07851596390768,-0.0854530935234271,
-7.65600590948774));
#17780=CARTESIAN_POINT('Ctrl Pts',(2.08172874199899,-0.140382394665887,
-7.65299578082649));
#17781=CARTESIAN_POINT('Ctrl Pts',(2.08805034112436,-0.195245670108624,
-7.64998565216525));
#17782=CARTESIAN_POINT('Ctrl Pts',(2.09747171776502,-0.249663253952273,
-7.64697552350401));
#17783=CARTESIAN_POINT('Ctrl Pts',(2.10687634996474,-0.303984122416255,
-7.64397074468956));
#17784=CARTESIAN_POINT('Ctrl Pts',(2.1193697373145,-0.357860355081879,-7.64096596587511));
#17785=CARTESIAN_POINT('Ctrl Pts',(2.1348910037667,-0.410916415523307,-7.63796118706066));
#17786=CARTESIAN_POINT('Ctrl Pts',(2.15039691449719,-0.463919985782878,
-7.63495938097704));
#17787=CARTESIAN_POINT('Ctrl Pts',(2.16892462266722,-0.516104486831484,
-7.63195757489342));
#17788=CARTESIAN_POINT('Ctrl Pts',(2.19036240340789,-0.56710545034849,-7.6289557688098));
#17789=CARTESIAN_POINT('Ctrl Pts',(2.21178744242093,-0.618076101008329,
-7.6259557468752));
#17790=CARTESIAN_POINT('Ctrl Pts',(2.23611892153535,-0.667864122529575,
-7.6229557249406));
#17791=CARTESIAN_POINT('Ctrl Pts',(2.26319632586426,-0.716123280430809,
-7.619955703006));
#17792=CARTESIAN_POINT('Ctrl Pts',(2.29026833079506,-0.764372815164213,
-7.61695627929391));
#17793=CARTESIAN_POINT('Ctrl Pts',(2.32008491524729,-0.811093631412306,
-7.61395685558183));
#17794=CARTESIAN_POINT('Ctrl Pts',(2.35243986307617,-0.855964516185112,
-7.61095743186974));
#17795=CARTESIAN_POINT('Ctrl Pts',(2.38482455659332,-0.900876653237421,
-7.60795525062198));
#17796=CARTESIAN_POINT('Ctrl Pts',(2.4197519662859,-0.943935031661007,-7.60495306937423));
#17797=CARTESIAN_POINT('Ctrl Pts',(2.4569736731441,-0.984849103229583,-7.60195088812647));
#17798=CARTESIAN_POINT('Ctrl Pts',(2.49421232249701,-1.02578179797531,-7.59894734035245));
#17799=CARTESIAN_POINT('Ctrl Pts',(2.53374697313804,-1.06456786970263,-7.59594379257843));
#17800=CARTESIAN_POINT('Ctrl Pts',(2.57529249527056,-1.10095385931422,-7.59294024480442));
#17801=CARTESIAN_POINT('Ctrl Pts',(2.61691642758427,-1.13740852135769,-7.58993102833945));
#17802=CARTESIAN_POINT('Ctrl Pts',(2.66055839543228,-1.17145372677265,-7.58692181187449));
#17803=CARTESIAN_POINT('Ctrl Pts',(2.70590129794752,-1.20287725589844,-7.58391259540953));
#17804=CARTESIAN_POINT('Ctrl Pts',(2.74059047667024,-1.22691754351735,-7.58161042148642));
#17805=CARTESIAN_POINT('Ctrl Pts',(2.77627451397957,-1.24942424404648,-7.57930824756331));
#17806=CARTESIAN_POINT('Ctrl Pts',(2.81280196490454,-1.27032063968731,-7.57700607364021));
#17807=CARTESIAN_POINT('Ctrl Pts',(2.86056218225717,-1.29764300608354,-7.57399594497897));
#17808=CARTESIAN_POINT('Ctrl Pts',(2.90996574891832,-1.32232557501311,-7.57098581631774));
#17809=CARTESIAN_POINT('Ctrl Pts',(2.96068974313619,-1.34416847270939,-7.5679756876565));
#17810=CARTESIAN_POINT('Ctrl Pts',(3.01132358652386,-1.36597254942179,-7.56497090884205));
#17811=CARTESIAN_POINT('Ctrl Pts',(3.06327271915266,-1.38494676331381,-7.56196613002761));
#17812=CARTESIAN_POINT('Ctrl Pts',(3.11618935672575,-1.4009369080848,-7.55896135121317));
#17813=CARTESIAN_POINT('Ctrl Pts',(3.16905364205286,-1.41691123325669,-7.55595954512955));
#17814=CARTESIAN_POINT('Ctrl Pts',(3.22288303313078,-1.429907185546,-7.55295773904593));
#17815=CARTESIAN_POINT('Ctrl Pts',(3.27731123190228,-1.43981919347764,-7.54995593296231));
#17816=CARTESIAN_POINT('Ctrl Pts',(3.33170708081012,-1.44972531012293,-7.54695591102771));
#17817=CARTESIAN_POINT('Ctrl Pts',(3.3867005134482,-1.45655102104369,-7.5439558890931));
#17818=CARTESIAN_POINT('Ctrl Pts',(3.44191384441607,-1.46024158061615,-7.5409558671585));
#17819=CARTESIAN_POINT('Ctrl Pts',(3.49711616551202,-1.46393140426872,-7.53795644344641));
#17820=CARTESIAN_POINT('Ctrl Pts',(3.55253777121056,-1.46448728292818,-7.53495701973431));
#17821=CARTESIAN_POINT('Ctrl Pts',(3.60779696129584,-1.46190641864889,-7.53195759602222));
#17822=CARTESIAN_POINT('Ctrl Pts',(3.66310695420265,-1.45932318163872,-7.52895541477446));
#17823=CARTESIAN_POINT('Ctrl Pts',(3.71825370450435,-1.45359746496207,-7.5259532335267));
#17824=CARTESIAN_POINT('Ctrl Pts',(3.77285813507016,-1.44477857181508,-7.52295105227893));
#17825=CARTESIAN_POINT('Ctrl Pts',(3.82748742036061,-1.43595566450369,-7.51994750450491));
#17826=CARTESIAN_POINT('Ctrl Pts',(3.88157337719182,-1.42403688793093,-7.51694395673089));
#17827=CARTESIAN_POINT('Ctrl Pts',(3.9347479329469,-1.40912255691934,-7.51394040895687));
#17828=CARTESIAN_POINT('Ctrl Pts',(3.98802284672706,-1.39418007761795,-7.51093119249191));
#17829=CARTESIAN_POINT('Ctrl Pts',(4.0403824224292,-1.37623092160211,-7.50792197602694));
#17830=CARTESIAN_POINT('Ctrl Pts',(4.09147565770711,-1.3554247133926,-7.50491275956197));
#17831=CARTESIAN_POINT('Ctrl Pts',(4.13056407666066,-1.33950711140665,-7.50261058563885));
#17832=CARTESIAN_POINT('Ctrl Pts',(4.16891166197947,-1.32191834261424,-7.50030841171573));
#17833=CARTESIAN_POINT('Ctrl Pts',(4.20637141150496,-1.30274332795045,-7.49800623779262));
#17834=CARTESIAN_POINT('Ctrl Pts',(4.25535062396027,-1.27767169429169,-7.49499610913138));
#17835=CARTESIAN_POINT('Ctrl Pts',(4.30301685460356,-1.24978133638674,-7.49198598047014));
#17836=CARTESIAN_POINT('Ctrl Pts',(4.34902626059857,-1.21923349965203,-7.4889758518089));
#17837=CARTESIAN_POINT('Ctrl Pts',(4.39495389491509,-1.18873995503065,-7.48597107299446));
#17838=CARTESIAN_POINT('Ctrl Pts',(4.43923011183765,-1.1555985943354,-7.48296629418001));
#17839=CARTESIAN_POINT('Ctrl Pts',(4.48153573146479,-1.12001643855748,-7.47996151536556));
#17840=CARTESIAN_POINT('Ctrl Pts',(4.52379949669023,-1.08446948542769,-7.47695970928195));
#17841=CARTESIAN_POINT('Ctrl Pts',(4.56409612446335,-1.04648685900667,-7.47395790319833));
#17842=CARTESIAN_POINT('Ctrl Pts',(4.60213705201202,-1.00631765993594,-7.47095609711471));
#17843=CARTESIAN_POINT('Ctrl Pts',(4.6401553696113,-0.966172335770903,-7.46795607518011));
#17844=CARTESIAN_POINT('Ctrl Pts',(4.67592028191785,-0.923843397553667,
-7.46495605324551));
#17845=CARTESIAN_POINT('Ctrl Pts',(4.70917957217821,-0.879617254177804,
-7.46195603131091));
#17846=CARTESIAN_POINT('Ctrl Pts',(4.74243223033506,-0.835399929762271,
-7.45895660759882));
#17847=CARTESIAN_POINT('Ctrl Pts',(4.77317994146253,-0.789286573348888,
-7.45595718388673));
#17848=CARTESIAN_POINT('Ctrl Pts',(4.80121180270633,-0.74159534035462,-7.45295776017464));
#17849=CARTESIAN_POINT('Ctrl Pts',(4.82926943518642,-0.693860262179192,
-7.44995557892688));
#17850=CARTESIAN_POINT('Ctrl Pts',(4.85460596125388,-0.644544865525292,
-7.44695339767913));
#17851=CARTESIAN_POINT('Ctrl Pts',(4.8770555474062,-0.593993576764832,-7.44395121643137));
#17852=CARTESIAN_POINT('Ctrl Pts',(4.89951535211179,-0.54341927817989,-7.44094766865735));
#17853=CARTESIAN_POINT('Ctrl Pts',(4.91908541045481,-0.491608460990895,
-7.43794412088333));
#17854=CARTESIAN_POINT('Ctrl Pts',(4.93564862536595,-0.438924207545657,
-7.43494057310931));
#17855=CARTESIAN_POINT('Ctrl Pts',(4.95224310055777,-0.38614052143844,-7.43193135664435));
#17856=CARTESIAN_POINT('Ctrl Pts',(4.96581926595016,-0.33248061925228,-7.42892214017938));
#17857=CARTESIAN_POINT('Ctrl Pts',(4.97631064980204,-0.278320229149412,
-7.42591292371442));
#17858=CARTESIAN_POINT('Ctrl Pts',(4.98433698841955,-0.236885311052895,
-7.4236107497913));
#17859=CARTESIAN_POINT('Ctrl Pts',(4.99055889127085,-0.19515774208079,-7.42130857586819));
#17860=CARTESIAN_POINT('Ctrl Pts',(4.99496716052216,-0.153307040962731,
-7.41900640194507));
#17861=CARTESIAN_POINT('Ctrl Pts',(5.00073104199375,-0.0985865901473312,
-7.41599627328384));
#17862=CARTESIAN_POINT('Ctrl Pts',(5.00341675794117,-0.043425657072795,
-7.4129861446226));
#17863=CARTESIAN_POINT('Ctrl Pts',(5.00297148136434,0.0117996767691311,
-7.40997601596136));
#17864=CARTESIAN_POINT('Ctrl Pts',(5.00252699616945,0.0669268596320173,
-7.40697123714692));
#17865=CARTESIAN_POINT('Ctrl Pts',(4.99896256577096,0.122117692291433,-7.40396645833247));
#17866=CARTESIAN_POINT('Ctrl Pts',(4.99227717717537,0.176991737532915,-7.40096167951803));
#17867=CARTESIAN_POINT('Ctrl Pts',(4.9855984026642,0.231811493997805,-7.39795987343441));
#17868=CARTESIAN_POINT('Ctrl Pts',(4.97580485003877,0.286314562229754,-7.39495806735079));
#17869=CARTESIAN_POINT('Ctrl Pts',(4.96294747822448,0.340123155528362,-7.39195626126717));
#17870=CARTESIAN_POINT('Ctrl Pts',(4.95009774829868,0.393899767231109,-7.38895623933257));
#17871=CARTESIAN_POINT('Ctrl Pts',(4.93418793103073,0.446982209501532,-7.38595621739797));
#17872=CARTESIAN_POINT('Ctrl Pts',(4.91532009133315,0.49900275132561,-7.38295619546338));
#17873=CARTESIAN_POINT('Ctrl Pts',(4.89645601399685,0.551012919939193,-7.37995677175128));
#17874=CARTESIAN_POINT('Ctrl Pts',(4.87463526561117,0.601961112440734,-7.37695734803919));
#17875=CARTESIAN_POINT('Ctrl Pts',(4.85000907340865,0.65149685314286,-7.3739579243271));
#17876=CARTESIAN_POINT('Ctrl Pts',(4.82536024098924,0.701078134783833,-7.37095574307934));
#17877=CARTESIAN_POINT('Ctrl Pts',(4.79790104745124,0.749243896384174,-7.36795356183158));
#17878=CARTESIAN_POINT('Ctrl Pts',(4.7678293483759,0.795667054704943,-7.36495138058382));
#17879=CARTESIAN_POINT('Ctrl Pts',(4.73774396133068,0.842111343816857,-7.3619478328098));
#17880=CARTESIAN_POINT('Ctrl Pts',(4.70504401060774,0.88681102148971,-7.35894428503578));
#17881=CARTESIAN_POINT('Ctrl Pts',(4.66996960606598,0.92946962900702,-7.35594073726176));
#17882=CARTESIAN_POINT('Ctrl Pts',(4.63482900448844,0.972208747466868,-7.3529315207968));
#17883=CARTESIAN_POINT('Ctrl Pts',(4.59730535573755,1.01289871126396,-7.34992230433183));
#17884=CARTESIAN_POINT('Ctrl Pts',(4.55767702236274,1.05127855213332,-7.34691308786687));
#17885=CARTESIAN_POINT('Ctrl Pts',(4.52735972323377,1.08064070332837,-7.34461091394374));
#17886=CARTESIAN_POINT('Ctrl Pts',(4.49581138450125,1.10865149429612,-7.34230874002062));
#17887=CARTESIAN_POINT('Ctrl Pts',(4.46316895700323,1.13521059723485,-7.3400065660975));
#17888=CARTESIAN_POINT('Ctrl Pts',(4.42048846896653,1.16993704260448,-7.33699643743626));
#17889=CARTESIAN_POINT('Ctrl Pts',(4.37575716762441,1.20232611928238,-7.33398630877503));
#17890=CARTESIAN_POINT('Ctrl Pts',(4.3292611668822,1.23212809378349,-7.33097618011379));
#17891=CARTESIAN_POINT('Ctrl Pts',(4.28284780263447,1.26187710177862,-7.32797140129934));
#17892=CARTESIAN_POINT('Ctrl Pts',(4.2346764041576,1.28904784969781,-7.3249666224849));
#17893=CARTESIAN_POINT('Ctrl Pts',(4.1850650443617,1.31343161973118,-7.32196184367045));
#17894=CARTESIAN_POINT('Ctrl Pts',(4.13550276678703,1.33779126606386,-7.31896003758683));
#17895=CARTESIAN_POINT('Ctrl Pts',(4.08450382159625,1.35936916469073,-7.31595823150321));
#17896=CARTESIAN_POINT('Ctrl Pts',(4.03241245907508,1.37800157391323,-7.31295642541959));
#17897=CARTESIAN_POINT('Ctrl Pts',(3.98035205749902,1.39662290880456,-7.309956403485));
#17898=CARTESIAN_POINT('Ctrl Pts',(3.92720102179366,1.41230204673812,-7.3069563815504));
#17899=CARTESIAN_POINT('Ctrl Pts',(3.87332310444746,1.42492354304251,-7.3039563596158));
#17900=CARTESIAN_POINT('Ctrl Pts',(3.81945593068366,1.43754252254425,-7.3009569359037));
#17901=CARTESIAN_POINT('Ctrl Pts',(3.76486267703996,1.44710495089072,-7.29795751219161));
#17902=CARTESIAN_POINT('Ctrl Pts',(3.70991950630306,1.45354598641937,-7.29495808847952));
#17903=CARTESIAN_POINT('Ctrl Pts',(3.65492582327863,1.45999294354728,-7.29195590723176));
#17904=CARTESIAN_POINT('Ctrl Pts',(3.59958210610123,1.46331271300988,-7.288953725984));
#17905=CARTESIAN_POINT('Ctrl Pts',(3.54427040329912,1.46349228718359,-7.28595154473625));
#17906=CARTESIAN_POINT('Ctrl Pts',(3.48893352383772,1.46367194309547,-7.28294799696223));
#17907=CARTESIAN_POINT('Ctrl Pts',(3.43362921607942,1.46070858272003,-7.27994444918821));
#17908=CARTESIAN_POINT('Ctrl Pts',(3.37873696726217,1.45464132064728,-7.27694090141419));
#17909=CARTESIAN_POINT('Ctrl Pts',(3.32374111856326,1.44856260763845,-7.27393168494922));
#17910=CARTESIAN_POINT('Ctrl Pts',(3.26915940442258,1.43936837842359,-7.27092246848426));
#17911=CARTESIAN_POINT('Ctrl Pts',(3.21536248898975,1.42714917709389,-7.26791325201929));
#17912=CARTESIAN_POINT('Ctrl Pts',(3.17420564391213,1.41780098729431,-7.26561107809617));
#17913=CARTESIAN_POINT('Ctrl Pts',(3.13350796418715,1.40668339077259,-7.26330890417305));
#17914=CARTESIAN_POINT('Ctrl Pts',(3.09342830644917,1.39385626882433,-7.26100673024994));
#17915=CARTESIAN_POINT('Ctrl Pts',(3.04102352274529,1.37708460486362,-7.2579966015887));
#17916=CARTESIAN_POINT('Ctrl Pts',(2.98945579188682,1.35731820048865,-7.25498647292746));
#17917=CARTESIAN_POINT('Ctrl Pts',(2.93909060390324,1.33466023039944,-7.25197634426622));
#17918=CARTESIAN_POINT('Ctrl Pts',(2.88881492905009,1.3120425299074,-7.24897156545178));
#17919=CARTESIAN_POINT('Ctrl Pts',(2.83973803339766,1.28654367725034,-7.24596678663733));
#17920=CARTESIAN_POINT('Ctrl Pts',(2.79220851751837,1.25831602445881,-7.24296200782289));
#17921=CARTESIAN_POINT('Ctrl Pts',(2.74472602422066,1.23011629825313,-7.23996020173927));
#17922=CARTESIAN_POINT('Ctrl Pts',(2.69878832994593,1.19919338822763,-7.23695839565565));
#17923=CARTESIAN_POINT('Ctrl Pts',(2.65472066977822,1.16574614544007,-7.23395658957203));
#17924=CARTESIAN_POINT('Ctrl Pts',(2.6106792015998,1.13231878230625,-7.23095656763743));
#17925=CARTESIAN_POINT('Ctrl Pts',(2.56850598434983,1.09637037886917,-7.22795654570284));
#17926=CARTESIAN_POINT('Ctrl Pts',(2.52849645897932,1.05814250911232,-7.22495652376824));
#17927=CARTESIAN_POINT('Ctrl Pts',(2.48849491174998,1.01992226222375,-7.22195710005615));
#17928=CARTESIAN_POINT('Ctrl Pts',(2.45065658117789,0.979423816342425,-7.21895767634406));
#17929=CARTESIAN_POINT('Ctrl Pts',(2.41524130777047,0.936926788695978,-7.21595825263197));
#17930=CARTESIAN_POINT('Ctrl Pts',(2.37979347514869,0.894390691187862,-7.21295607138421));
#17931=CARTESIAN_POINT('Ctrl Pts',(2.34677348907133,0.849852747591995,-7.20995389013645));
#17932=CARTESIAN_POINT('Ctrl Pts',(2.31640099358928,0.803625826518375,-7.20695170888869));
#17933=CARTESIAN_POINT('Ctrl Pts',(2.28601467322152,0.757377863976449,-7.20394816111467));
#17934=CARTESIAN_POINT('Ctrl Pts',(2.25827851063289,0.70943984935134,-7.20094461334065));
#17935=CARTESIAN_POINT('Ctrl Pts',(2.23336709663869,0.660150985476387,-7.19794106556663));
#17936=CARTESIAN_POINT('Ctrl Pts',(2.20840866654298,0.610769097165842,-7.19493184910167));
#17937=CARTESIAN_POINT('Ctrl Pts',(2.1862858466144,0.560031751868736,-7.1919226326367));
#17938=CARTESIAN_POINT('Ctrl Pts',(2.16712533317604,0.508298863722015,-7.18891341617174));
#17939=CARTESIAN_POINT('Ctrl Pts',(2.1524667551359,0.468721084108749,-7.18661124224862));
#17940=CARTESIAN_POINT('Ctrl Pts',(2.13954098899165,0.428561070948839,-7.1843090683255));
#17941=CARTESIAN_POINT('Ctrl Pts',(2.12838468118806,0.387984589853703,-7.18200689440238));
#17942=CARTESIAN_POINT('Ctrl Pts',(2.11011855844064,0.321549081136019,-7.17823756567768));
#17943=CARTESIAN_POINT('Ctrl Pts',(2.09653491201419,0.253774759083523,-7.17446823695298));
#17944=CARTESIAN_POINT('Ctrl Pts',(2.0877904184246,0.185246400872139,-7.17069890822829));
#17945=CARTESIAN_POINT('Ctrl Pts',(2.08002348789786,0.124378954188602,-7.16735095971221));
#17946=CARTESIAN_POINT('Ctrl Pts',(2.07607370014426,0.0629167803784564,
-7.16400301119612));
#17947=CARTESIAN_POINT('Ctrl Pts',(2.0760196139518,0.00128430857734538,
-7.16065506268004));
#17948=CARTESIAN_POINT('Ctrl Pts',(2.07601962331082,0.00129492948150936,
-7.08934495420699));
#17949=CARTESIAN_POINT('Ctrl Pts',(2.07608179175475,0.0715562706402045,
-7.0931627932276));
#17950=CARTESIAN_POINT('Ctrl Pts',(2.0812075995991,0.141595414252205,-7.09698063224821));
#17951=CARTESIAN_POINT('Ctrl Pts',(2.09127877754473,0.210789852728969,-7.10079847126883));
#17952=CARTESIAN_POINT('Ctrl Pts',(2.09935677175096,0.266290041101816,-7.10386072293943));
#17953=CARTESIAN_POINT('Ctrl Pts',(2.11061538540839,0.321247370894252,-7.10692297461003));
#17954=CARTESIAN_POINT('Ctrl Pts',(2.12497181061545,0.375350977556833,-7.10998522628063));
#17955=CARTESIAN_POINT('Ctrl Pts',(2.13908387312279,0.428533679244935,-7.11299535494186));
#17956=CARTESIAN_POINT('Ctrl Pts',(2.15622901998243,0.481031160584161,-7.1160054836031));
#17957=CARTESIAN_POINT('Ctrl Pts',(2.17632260802631,0.532473200674955,-7.11901561226434));
#17958=CARTESIAN_POINT('Ctrl Pts',(2.19638048410248,0.583823813765733,-7.12202039107878));
#17959=CARTESIAN_POINT('Ctrl Pts',(2.21937621153617,0.634122220236513,-7.12502516989323));
#17960=CARTESIAN_POINT('Ctrl Pts',(2.24517518188764,0.68301259138096,-7.12802994870767));
#17961=CARTESIAN_POINT('Ctrl Pts',(2.27094862843214,0.731854593602992,-7.13103175479129));
#17962=CARTESIAN_POINT('Ctrl Pts',(2.29951957877341,0.779290855221282,-7.13403356087491));
#17963=CARTESIAN_POINT('Ctrl Pts',(2.33070580806938,0.824986542381488,-7.13703536695852));
#17964=CARTESIAN_POINT('Ctrl Pts',(2.36187350156428,0.870655069920728,-7.14003538889312));
#17965=CARTESIAN_POINT('Ctrl Pts',(2.39565309595574,0.914584638159451,-7.14303541082772));
#17966=CARTESIAN_POINT('Ctrl Pts',(2.43181819766048,0.956468018696495,-7.14603543276232));
#17967=CARTESIAN_POINT('Ctrl Pts',(2.46797608782533,0.998343047434297,-7.14903485647441));
#17968=CARTESIAN_POINT('Ctrl Pts',(2.5065181956584,1.03817229928607,-7.1520342801865));
#17969=CARTESIAN_POINT('Ctrl Pts',(2.54717834026204,1.07568218585104,-7.15503370389859));
#17970=CARTESIAN_POINT('Ctrl Pts',(2.58787586597944,1.11322655732377,-7.15803588514635));
#17971=CARTESIAN_POINT('Ctrl Pts',(2.63069492977307,1.1484469445467,-7.16103806639411));
#17972=CARTESIAN_POINT('Ctrl Pts',(2.67533411782859,1.18110823055163,-7.16404024764187));
#17973=CARTESIAN_POINT('Ctrl Pts',(2.71999362465158,1.21378438324892,-7.16704379541588));
#17974=CARTESIAN_POINT('Ctrl Pts',(2.76647446325922,1.24389882502802,-7.1700473431899));
#17975=CARTESIAN_POINT('Ctrl Pts',(2.81444665079178,1.2712601092196,-7.17305089096391));
#17976=CARTESIAN_POINT('Ctrl Pts',(2.86250937775492,1.29867303323039,-7.17606010742888));
#17977=CARTESIAN_POINT('Ctrl Pts',(2.91206860236527,1.32332218383257,-7.17906932389384));
#17978=CARTESIAN_POINT('Ctrl Pts',(2.96277124546302,1.34506290539657,-7.18207854035881));
#17979=CARTESIAN_POINT('Ctrl Pts',(3.00156084539114,1.36169544839813,-7.18438071428193));
#17980=CARTESIAN_POINT('Ctrl Pts',(3.04101917939818,1.37662668963308,-7.18668288820506));
#17981=CARTESIAN_POINT('Ctrl Pts',(3.08098253705965,1.38981168361494,-7.18898506212818));
#17982=CARTESIAN_POINT('Ctrl Pts',(3.13323525658173,1.40705127089563,-7.19199519078942));
#17983=CARTESIAN_POINT('Ctrl Pts',(3.18657135100372,1.42137616669333,-7.19500531945066));
#17984=CARTESIAN_POINT('Ctrl Pts',(3.24063450166375,1.43265497469314,-7.19801544811189));
#17985=CARTESIAN_POINT('Ctrl Pts',(3.2946015668717,1.4439137370731,-7.20102022692634));
#17986=CARTESIAN_POINT('Ctrl Pts',(3.34929261116631,1.45213704830831,-7.20402500574078));
#17987=CARTESIAN_POINT('Ctrl Pts',(3.40433606890657,1.45724322318147,-7.20702978455523));
#17988=CARTESIAN_POINT('Ctrl Pts',(3.45932507026464,1.46234434634056,-7.21003159063885));
#17989=CARTESIAN_POINT('Ctrl Pts',(3.51466527112711,1.46433439363332,-7.21303339672246));
#17990=CARTESIAN_POINT('Ctrl Pts',(3.56997667219122,1.4631830313656,-7.21603520280609));
#17991=CARTESIAN_POINT('Ctrl Pts',(3.62525519845288,1.46203235341985,-7.21903522474069));
#17992=CARTESIAN_POINT('Ctrl Pts',(3.68050443189642,1.45774397764399,-7.22203524667529));
#17993=CARTESIAN_POINT('Ctrl Pts',(3.73534335990227,1.45033964636459,-7.22503526860989));
#17994=CARTESIAN_POINT('Ctrl Pts',(3.79017135269438,1.44293679155361,-7.22803469232198));
#17995=CARTESIAN_POINT('Ctrl Pts',(3.84458867946096,1.4324192858196,-7.23103411603407));
#17996=CARTESIAN_POINT('Ctrl Pts',(3.89822076235576,1.41886057519987,-7.23403353974616));
#17997=CARTESIAN_POINT('Ctrl Pts',(3.95190215218274,1.40528939930955,-7.23703572099392));
#17998=CARTESIAN_POINT('Ctrl Pts',(4.00479634273179,1.38867156231254,-7.24003790224168));
#17999=CARTESIAN_POINT('Ctrl Pts',(4.05654172588942,1.36913103940183,-7.24304008348944));
#18000=CARTESIAN_POINT('Ctrl Pts',(4.10831066239682,1.34958162207885,-7.24604363126346));
#18001=CARTESIAN_POINT('Ctrl Pts',(4.15892926560436,1.32710708157942,-7.24904717903748));
#18002=CARTESIAN_POINT('Ctrl Pts',(4.2080568924349,1.30187918172081,-7.2520507268115));
#18003=CARTESIAN_POINT('Ctrl Pts',(4.25727723939323,1.27660366844691,-7.25505994327647));
#18004=CARTESIAN_POINT('Ctrl Pts',(4.30500053218034,1.24856468317737,-7.25806915974144));
#18005=CARTESIAN_POINT('Ctrl Pts',(4.3509126967465,1.21797889994279,-7.2610783762064));
#18006=CARTESIAN_POINT('Ctrl Pts',(4.38603738426848,1.1945795222641,-7.26338055012952));
#18007=CARTESIAN_POINT('Ctrl Pts',(4.42010257944943,1.1696904771901,-7.26568272405263));
#18008=CARTESIAN_POINT('Ctrl Pts',(4.45298118850154,1.14342431856987,-7.26798489797575));
#18009=CARTESIAN_POINT('Ctrl Pts',(4.49597048763992,1.10908090251015,-7.27099502663699));
#18010=CARTESIAN_POINT('Ctrl Pts',(4.53711060601078,1.07223755483061,-7.27400515529822));
#18011=CARTESIAN_POINT('Ctrl Pts',(4.57609680454605,1.03312090756948,-7.27701528395946));
#18012=CARTESIAN_POINT('Ctrl Pts',(4.61501371362141,0.994073781612415,-7.2800200627739));
#18013=CARTESIAN_POINT('Ctrl Pts',(4.65178393000102,0.952761745096384,-7.28302484158835));
#18014=CARTESIAN_POINT('Ctrl Pts',(4.68613601810939,0.909451361763591,-7.28602962040279));
#18015=CARTESIAN_POINT('Ctrl Pts',(4.7204541205178,0.866183826879724,-7.28903142648641));
#18016=CARTESIAN_POINT('Ctrl Pts',(4.7523585071905,0.82092227331864,-7.29203323257003));
#18017=CARTESIAN_POINT('Ctrl Pts',(4.78161614271498,0.773968386511875,-7.29503503865365));
#18018=CARTESIAN_POINT('Ctrl Pts',(4.81085638871451,0.727042407147772,-7.29803506058825));
#18019=CARTESIAN_POINT('Ctrl Pts',(4.83745272285583,0.678426535530215,-7.30103508252285));
#18020=CARTESIAN_POINT('Ctrl Pts',(4.86121517112297,0.628451759904153,-7.30403510445745));
#18021=CARTESIAN_POINT('Ctrl Pts',(4.88497288101429,0.578486949550428,-7.30703452816954));
#18022=CARTESIAN_POINT('Ctrl Pts',(4.90589760062895,0.527164250007887,-7.31003395188163));
#18023=CARTESIAN_POINT('Ctrl Pts',(4.92384617513506,0.474837510930213,-7.31303337559372));
#18024=CARTESIAN_POINT('Ctrl Pts',(4.94181125075578,0.422462664994939,-7.31603555684148));
#18025=CARTESIAN_POINT('Ctrl Pts',(4.95679454310981,0.369082435972092,-7.31903773808924));
#18026=CARTESIAN_POINT('Ctrl Pts',(4.96870230350416,0.315067419947433,-7.322039919337));
#18027=CARTESIAN_POINT('Ctrl Pts',(4.98061548404671,0.261027817486531,-7.32504346711102));
#18028=CARTESIAN_POINT('Ctrl Pts',(4.98945025760604,0.206353374302396,-7.32804701488504));
#18029=CARTESIAN_POINT('Ctrl Pts',(4.99516435496168,0.151423239215319,-7.33105056265906));
#18030=CARTESIAN_POINT('Ctrl Pts',(5.00088923671444,0.0963894327426314,
-7.33405977912402));
#18031=CARTESIAN_POINT('Ctrl Pts',(5.0034816517754,0.0410994991783652,-7.33706899558899));
#18032=CARTESIAN_POINT('Ctrl Pts',(5.00295146164869,-0.0140651261684224,
-7.34007821205395));
#18033=CARTESIAN_POINT('Ctrl Pts',(5.00254584447285,-0.0562683253834388,
-7.34238038597707));
#18034=CARTESIAN_POINT('Ctrl Pts',(5.00031368830613,-0.0983981196657256,
-7.3446825599002));
#18035=CARTESIAN_POINT('Ctrl Pts',(4.99627981647953,-0.140286565566228,
-7.34698473382331));
#18036=CARTESIAN_POINT('Ctrl Pts',(4.99100546553712,-0.195056368279009,
-7.34999486248455));
#18037=CARTESIAN_POINT('Ctrl Pts',(4.98262696947039,-0.249643385155416,
-7.35300499114579));
#18038=CARTESIAN_POINT('Ctrl Pts',(4.97116763048022,-0.303668558168483,
-7.35601511980703));
#18039=CARTESIAN_POINT('Ctrl Pts',(4.95972865796432,-0.357597713226465,
-7.35901989862147));
#18040=CARTESIAN_POINT('Ctrl Pts',(4.94521981743802,-0.410966493616206,
-7.36202467743592));
#18041=CARTESIAN_POINT('Ctrl Pts',(4.92771605187653,-0.463401915355784,
-7.36502945625036));
#18042=CARTESIAN_POINT('Ctrl Pts',(4.91022960339115,-0.51578546093271,-7.36803126233398));
#18043=CARTESIAN_POINT('Ctrl Pts',(4.88975426579602,-0.567236978598274,
-7.3710330684176));
#18044=CARTESIAN_POINT('Ctrl Pts',(4.86641537912471,-0.61739645518735,-7.37403487450122));
#18045=CARTESIAN_POINT('Ctrl Pts',(4.84309036411953,-0.667526119064172,
-7.37703489643582));
#18046=CARTESIAN_POINT('Ctrl Pts',(4.81690539581176,-0.716364786097724,
-7.38003491837042));
#18047=CARTESIAN_POINT('Ctrl Pts',(4.78803388470787,-0.763572497259173,
-7.38303494030502));
#18048=CARTESIAN_POINT('Ctrl Pts',(4.75916813075781,-0.810770794917652,
-7.38603436401711));
#18049=CARTESIAN_POINT('Ctrl Pts',(4.72761717330138,-0.856338332297551,
-7.3890337877292));
#18050=CARTESIAN_POINT('Ctrl Pts',(4.69359915170852,-0.89996187131277,-7.39203321144129));
#18051=CARTESIAN_POINT('Ctrl Pts',(4.65954985547196,-0.943625515853699,
-7.39503539268905));
#18052=CARTESIAN_POINT('Ctrl Pts',(4.62302928917016,-0.985341174032534,
-7.39803757393681));
#18053=CARTESIAN_POINT('Ctrl Pts',(4.58429661308093,-1.0248278365494,-7.40103975518456));
#18054=CARTESIAN_POINT('Ctrl Pts',(4.54554630673736,-1.0643324725185,-7.40404330295858));
#18055=CARTESIAN_POINT('Ctrl Pts',(4.50458227471166,-1.10160573426922,-7.4070468507326));
#18056=CARTESIAN_POINT('Ctrl Pts',(4.46169896860869,-1.13640505476481,-7.41005039850662));
#18057=CARTESIAN_POINT('Ctrl Pts',(4.41873472748243,-1.17127005312134,-7.41305961497159));
#18058=CARTESIAN_POINT('Ctrl Pts',(4.37384440552029,-1.20365147315699,-7.41606883143655));
#18059=CARTESIAN_POINT('Ctrl Pts',(4.32735285334631,-1.23334915939136,-7.41907804790152));
#18060=CARTESIAN_POINT('Ctrl Pts',(4.2917849105591,-1.25606910646785,-7.42138022182464));
#18061=CARTESIAN_POINT('Ctrl Pts',(4.25528043264427,-1.27721916981486,-7.42368239574776));
#18062=CARTESIAN_POINT('Ctrl Pts',(4.21799364013086,-1.2967283759989,-7.42598456967087));
#18063=CARTESIAN_POINT('Ctrl Pts',(4.16924057169274,-1.32223697033352,-7.42899469833211));
#18064=CARTESIAN_POINT('Ctrl Pts',(4.11894449860163,-1.34504588612142,-7.43200482699335));
#18065=CARTESIAN_POINT('Ctrl Pts',(4.06743562438777,-1.36496752376505,-7.43501495565459));
#18066=CARTESIAN_POINT('Ctrl Pts',(4.01601829595701,-1.38485375504527,-7.43801973446903));
#18067=CARTESIAN_POINT('Ctrl Pts',(3.96339293256247,-1.40186270272871,-7.44102451328347));
#18068=CARTESIAN_POINT('Ctrl Pts',(3.90991286687456,-1.4158533365905,-7.44402929209792));
#18069=CARTESIAN_POINT('Ctrl Pts',(3.8564857108514,-1.42983012903796,-7.44703109818154));
#18070=CARTESIAN_POINT('Ctrl Pts',(3.80220603601128,-1.44079439002423,-7.45003290426516));
#18071=CARTESIAN_POINT('Ctrl Pts',(3.7474438483713,-1.44865438542054,-7.45303471034878));
#18072=CARTESIAN_POINT('Ctrl Pts',(3.6927142091041,-1.45650970916162,-7.45603473228338));
#18073=CARTESIAN_POINT('Ctrl Pts',(3.6375031471802,-1.46126434943483,-7.45903475421797));
#18074=CARTESIAN_POINT('Ctrl Pts',(3.58219013825552,-1.46287778992751,-7.46203477615257));
#18075=CARTESIAN_POINT('Ctrl Pts',(3.52688815907917,-1.4644909086904,-7.46503419986466));
#18076=CARTESIAN_POINT('Ctrl Pts',(3.47148480086988,-1.46296405623551,-7.46803362357676));
#18077=CARTESIAN_POINT('Ctrl Pts',(3.41636159945032,-1.45830877809534,-7.47103304728885));
#18078=CARTESIAN_POINT('Ctrl Pts',(3.36118772023106,-1.45364922010118,-7.4740352285366));
#18079=CARTESIAN_POINT('Ctrl Pts',(3.3062950397537,-1.44585553481704,-7.47703740978436));
#18080=CARTESIAN_POINT('Ctrl Pts',(3.25206051502811,-1.43499123357205,-7.48003959103212));
#18081=CARTESIAN_POINT('Ctrl Pts',(3.19780130395077,-1.42412198713829,-7.48304313880614));
#18082=CARTESIAN_POINT('Ctrl Pts',(3.14420135781168,-1.41017947175448,-7.48604668658016));
#18083=CARTESIAN_POINT('Ctrl Pts',(3.09162472023332,-1.39327776088759,-7.48905023435418));
#18084=CARTESIAN_POINT('Ctrl Pts',(3.0389488530998,-1.37634415088588,-7.49205945081915));
#18085=CARTESIAN_POINT('Ctrl Pts',(2.98730064664274,-1.35644037890267,-7.49506866728411));
#18086=CARTESIAN_POINT('Ctrl Pts',(2.93702523356946,-1.33372915190951,-7.49807788374908));
#18087=CARTESIAN_POINT('Ctrl Pts',(2.89856248211946,-1.31635413248025,-7.5003800576722));
#18088=CARTESIAN_POINT('Ctrl Pts',(2.86090283142582,-1.29733696136966,-7.50268223159532));
#18089=CARTESIAN_POINT('Ctrl Pts',(2.82418998914086,-1.2767680228159,-7.50498440551843));
#18090=CARTESIAN_POINT('Ctrl Pts',(2.77618736966552,-1.24987381171822,-7.50799453417967));
#18091=CARTESIAN_POINT('Ctrl Pts',(2.72960271194419,-1.22021219893684,-7.51100466284091));
#18092=CARTESIAN_POINT('Ctrl Pts',(2.68477355760134,-1.18795723513141,-7.51401479150215));
#18093=CARTESIAN_POINT('Ctrl Pts',(2.64002407729726,-1.15575959748514,-7.51701957031659));
#18094=CARTESIAN_POINT('Ctrl Pts',(2.59702433387971,-1.12097806158276,-7.52002434913103));
#18095=CARTESIAN_POINT('Ctrl Pts',(2.55608550354162,-1.08383149468371,-7.52302912794548));
#18096=CARTESIAN_POINT('Ctrl Pts',(2.51518717539366,-1.0467216781584,-7.52603093402909));
#18097=CARTESIAN_POINT('Ctrl Pts',(2.47634611048559,-1.00725181881574,-7.52903274011271));
#18098=CARTESIAN_POINT('Ctrl Pts',(2.43984130845434,-0.965681683485155,
-7.53203454619633));
#18099=CARTESIAN_POINT('Ctrl Pts',(2.40335820336318,-0.924136255718675,
-7.53503456813093));
#18100=CARTESIAN_POINT('Ctrl Pts',(2.36920895667512,-0.88049342224595,-7.53803459006553));
#18101=CARTESIAN_POINT('Ctrl Pts',(2.33763484590116,-0.835048866187434,
-7.54103461200013));
#18102=CARTESIAN_POINT('Ctrl Pts',(2.30606703119571,-0.789613372048069,
-7.54403403571222));
#18103=CARTESIAN_POINT('Ctrl Pts',(2.27707363378539,-0.742377302293122,
-7.54703345942431));
#18104=CARTESIAN_POINT('Ctrl Pts',(2.25085345365173,-0.69366651187596,-7.5500328831364));
#18105=CARTESIAN_POINT('Ctrl Pts',(2.22460916786017,-0.64491093894229,-7.55303506438416));
#18106=CARTESIAN_POINT('Ctrl Pts',(2.20114344391124,-0.594678402674966,
-7.55603724563191));
#18107=CARTESIAN_POINT('Ctrl Pts',(2.18060905718792,-0.543319317055689,
-7.55903942687967));
#18108=CARTESIAN_POINT('Ctrl Pts',(2.16006532366759,-0.491936853920719,
-7.56204297465369));
#18109=CARTESIAN_POINT('Ctrl Pts',(2.14245575537787,-0.439427320824445,
-7.56504652242771));
#18110=CARTESIAN_POINT('Ctrl Pts',(2.12788372472633,-0.386157943392716,
-7.56805007020173));
#18111=CARTESIAN_POINT('Ctrl Pts',(2.11328419181931,-0.332788028975963,
-7.5710592866667));
#18112=CARTESIAN_POINT('Ctrl Pts',(2.101733759267,-0.278655923186127,-7.57406850313166));
#18113=CARTESIAN_POINT('Ctrl Pts',(2.09328473475822,-0.224139586404663,
-7.57707771959663));
#18114=CARTESIAN_POINT('Ctrl Pts',(2.08682088474065,-0.182432354511015,
-7.57937989351975));
#18115=CARTESIAN_POINT('Ctrl Pts',(2.08217119205194,-0.140500475882394,
-7.58168206744287));
#18116=CARTESIAN_POINT('Ctrl Pts',(2.0793384787572,-0.0985136951381293,
-7.583984241366));
#18117=CARTESIAN_POINT('Ctrl Pts',(2.07713977977388,-0.0659243426234165,
-7.58577114562969));
#18118=CARTESIAN_POINT('Ctrl Pts',(2.07603198051246,-0.0332605710567609,
-7.58755804989339));
#18119=CARTESIAN_POINT('Ctrl Pts',(2.07601916294366,-0.000573888477519203,
-7.58934495415709));
#18120=CARTESIAN_POINT('Origin',(3.53951905042299,8.32667268468867E-16,
0.));
#18121=CARTESIAN_POINT('',(2.07789371708856,-0.000813024483110047,-8.16065504584291));
#18122=CARTESIAN_POINT('',(2.07796531875306,-0.000756418292827756,-8.08934495415709));
#18123=CARTESIAN_POINT('',(2.07601905042299,1.01189432752408E-15,0.));
#18124=CARTESIAN_POINT('Ctrl Pts',(2.07789371708856,-0.000813024483110047,
-8.16065504584291));
#18125=CARTESIAN_POINT('Ctrl Pts',(2.07693198018494,-0.18926297634554,-8.15043833875298));
#18126=CARTESIAN_POINT('Ctrl Pts',(2.19803679261536,-0.862248877409424,
-8.11388835304717));
#18127=CARTESIAN_POINT('Ctrl Pts',(3.20845871698005,-1.69493867564852,-8.05100508872559));
#18128=CARTESIAN_POINT('Ctrl Pts',(4.77818574047571,-1.20337977775244,-7.97200525287798));
#18129=CARTESIAN_POINT('Ctrl Pts',(5.22418461769582,0.379894702512827,-7.89300541703046));
#18130=CARTESIAN_POINT('Ctrl Pts',(4.14184166559634,1.61852572602733,-7.81400558118286));
#18131=CARTESIAN_POINT('Ctrl Pts',(2.54502163675168,1.39332412042453,-7.73655563325641));
#18132=CARTESIAN_POINT('Ctrl Pts',(2.07592938050414,0.453437848859226,-7.68543896394578));
#18133=CARTESIAN_POINT('Ctrl Pts',(2.07388874310075,-0.000493743824116852,
-7.66065557325101));
#18134=CARTESIAN_POINT('Ctrl Pts',(2.07395567091487,-0.000564195093096354,
-7.58934552749836));
#18135=CARTESIAN_POINT('Ctrl Pts',(2.07622157562037,0.449077329977556,-7.61389171073677));
#18136=CARTESIAN_POINT('Ctrl Pts',(2.53748680820253,1.38510922610061,-7.66477117259103));
#18137=CARTESIAN_POINT('Ctrl Pts',(4.1273450240176,1.62384686131859,-7.74198391306112));
#18138=CARTESIAN_POINT('Ctrl Pts',(5.22072030366117,0.394943477419077,-7.82098374890869));
#18139=CARTESIAN_POINT('Ctrl Pts',(4.7888966068738,-1.19225572998487,-7.89998358475626));
#18140=CARTESIAN_POINT('Ctrl Pts',(3.22362778172652,-1.69783117847794,-7.97898342060381));
#18141=CARTESIAN_POINT('Ctrl Pts',(2.20196131736979,-0.871103028593394,
-8.04210387707076));
#18142=CARTESIAN_POINT('Ctrl Pts',(2.0770525139401,-0.193605137899811,-8.07889105492185));
#18143=CARTESIAN_POINT('Ctrl Pts',(2.07796531875306,-0.000756418292827756,
-8.08934495415709));
#18144=CARTESIAN_POINT('Origin',(3.53951905042299,8.32667268468867E-16,
0.));
#18145=CARTESIAN_POINT('',(2.07672228599458,0.00126145580453749,-8.66065504584291));
#18146=CARTESIAN_POINT('',(2.07601960916399,0.00127884111782682,-8.58934497249013));
#18147=CARTESIAN_POINT('',(2.07601905042299,1.01189432752408E-15,0.));
#18148=CARTESIAN_POINT('Ctrl Pts',(2.07672228599458,0.00126145580453749,
-8.66065504584291));
#18149=CARTESIAN_POINT('Ctrl Pts',(2.07963777649526,-0.346349860195879,
-8.64177134378144));
#18150=CARTESIAN_POINT('Ctrl Pts',(2.37702178386745,-1.18318906413124,-8.59655436310413));
#18151=CARTESIAN_POINT('Ctrl Pts',(3.7699732897758,-1.71152239351114,-8.52500410381095));
#18152=CARTESIAN_POINT('Ctrl Pts',(5.09888440860025,-0.742157488805154,
-8.44600426796337));
#18153=CARTESIAN_POINT('Ctrl Pts',(5.01312703127878,0.900498515814794,-8.36700443211582));
#18154=CARTESIAN_POINT('Ctrl Pts',(3.59050092423819,1.72621519727753,-8.28800459626826));
#18155=CARTESIAN_POINT('Ctrl Pts',(2.3115872043854,1.08163819160217,-8.21922146751061));
#18156=CARTESIAN_POINT('Ctrl Pts',(2.07941083032865,0.296461537811273,-8.17677161736884));
#18157=CARTESIAN_POINT('Ctrl Pts',(2.07789371708856,-0.000813024483110047,
-8.16065504584291));
#18158=CARTESIAN_POINT('Ctrl Pts',(2.07796531875306,-0.000756418292827756,
-8.08934495415709));
#18159=CARTESIAN_POINT('Ctrl Pts',(2.07935186109475,0.292179060880606,-8.1052243335377));
#18160=CARTESIAN_POINT('Ctrl Pts',(2.30635466103924,1.07287711057751,-8.14743699153416));
#18161=CARTESIAN_POINT('Ctrl Pts',(3.57506339039297,1.72660203989655,-8.21598292814651));
#18162=CARTESIAN_POINT('Ctrl Pts',(5.00501601458435,0.913639235277645,-8.29498276399406));
#18163=CARTESIAN_POINT('Ctrl Pts',(5.10545828694895,-0.728184256712089,
-8.37398259984163));
#18164=CARTESIAN_POINT('Ctrl Pts',(3.78526818937201,-1.70939327399081,-8.45298243568918));
#18165=CARTESIAN_POINT('Ctrl Pts',(2.3830149561948,-1.19182649892971,-8.52476988712768));
#18166=CARTESIAN_POINT('Ctrl Pts',(2.07961074474305,-0.350624743640976,
-8.57022405995031));
#18167=CARTESIAN_POINT('Ctrl Pts',(2.07659996625117,0.00127799658744232,
-8.58934495415709));
#18168=CARTESIAN_POINT('Origin',(3.53951905042299,8.32667268468867E-16,
0.));
#18169=CARTESIAN_POINT('',(2.07585468749027,-0.000399586479062222,-9.16065504584292));
#18170=CARTESIAN_POINT('',(2.07601912703111,-0.000473531363087066,-9.08934495420967));
#18171=CARTESIAN_POINT('',(2.07601905042299,1.01189432752408E-15,0.));
#18172=CARTESIAN_POINT('Ctrl Pts',(2.0738084935334,-0.000400145098551985,
-9.16065504584292));
#18173=CARTESIAN_POINT('Ctrl Pts',(2.07372679669453,-0.0226950761968628,
-9.15943762742576));
#18174=CARTESIAN_POINT('Ctrl Pts',(2.08425249274981,-0.527160066346179,
-9.13188693039255));
#18175=CARTESIAN_POINT('Ctrl Pts',(2.66326349110611,-1.48815124140486,-9.07800295474405));
#18176=CARTESIAN_POINT('Ctrl Pts',(4.30710318516207,-1.54700766169977,-8.99900311889623));
#18177=CARTESIAN_POINT('Ctrl Pts',(5.25458455049922,-0.202406515394875,
-8.92000328304879));
#18178=CARTESIAN_POINT('Ctrl Pts',(4.64614501576207,1.32581937401458,-8.84100344720118));
#18179=CARTESIAN_POINT('Ctrl Pts',(3.03376572375074,1.65125153735703,-8.76200361135363));
#18180=CARTESIAN_POINT('Ctrl Pts',(2.15594970700447,0.758946513770955,-8.70188747756755));
#18181=CARTESIAN_POINT('Ctrl Pts',(2.07557213177123,0.138393311691988,-8.6681046223973));
#18182=CARTESIAN_POINT('Ctrl Pts',(2.07672228599458,0.00126145580453749,
-8.66065504584291));
#18183=CARTESIAN_POINT('Ctrl Pts',(2.07601960916399,0.00127884111782682,
-8.58934497249013));
#18184=CARTESIAN_POINT('Ctrl Pts',(2.07607995389544,0.0703370528976135,
-8.59309584414968));
#18185=CARTESIAN_POINT('Ctrl Pts',(2.08103218347023,0.139181342753791,-8.59684671580924));
#18186=CARTESIAN_POINT('Ctrl Pts',(2.09076283215383,0.207214068119058,-8.6005975874688));
#18187=CARTESIAN_POINT('Ctrl Pts',(2.09974279949806,0.269998335847097,-8.60405909410731));
#18188=CARTESIAN_POINT('Ctrl Pts',(2.11279171882277,0.332091823618981,-8.60752060074581));
#18189=CARTESIAN_POINT('Ctrl Pts',(2.12978476702327,0.393041346689484,-8.61098210738432));
#18190=CARTESIAN_POINT('Ctrl Pts',(2.14456193393777,0.44604309570737,-8.61399223604218));
#18191=CARTESIAN_POINT('Ctrl Pts',(2.16236336355835,0.498321683152169,-8.61700236470005));
#18192=CARTESIAN_POINT('Ctrl Pts',(2.18309978165723,0.549507977486184,-8.62001249335791));
#18193=CARTESIAN_POINT('Ctrl Pts',(2.20379934529848,0.600603299352993,-8.62301727216902));
#18194=CARTESIAN_POINT('Ctrl Pts',(2.22742334894202,0.650609695140782,-8.62602205098014));
#18195=CARTESIAN_POINT('Ctrl Pts',(2.25383273729771,0.699173050283212,-8.62902682979125));
#18196=CARTESIAN_POINT('Ctrl Pts',(2.28021599793915,0.747688360031737,-8.63202863587156));
#18197=CARTESIAN_POINT('Ctrl Pts',(2.30937893336773,0.794762995570515,-8.63503044195187));
#18198=CARTESIAN_POINT('Ctrl Pts',(2.34113513862651,0.840064432021361,-8.63803224803218));
#18199=CARTESIAN_POINT('Ctrl Pts',(2.37287246931444,0.885338943177917,-8.6410322699635));
#18200=CARTESIAN_POINT('Ctrl Pts',(2.40719971227237,0.928841912593762,-8.64403229189482));
#18201=CARTESIAN_POINT('Ctrl Pts',(2.44388664307717,0.970268971973029,-8.64703231382614));
#18202=CARTESIAN_POINT('Ctrl Pts',(2.48056625828663,1.01168777054673,-8.65003173753498));
#18203=CARTESIAN_POINT('Ctrl Pts',(2.51960427694535,1.0510310860224,-8.65303116124383));
#18204=CARTESIAN_POINT('Ctrl Pts',(2.56073111184097,1.08802868587476,-8.65603058495268));
#18205=CARTESIAN_POINT('Ctrl Pts',(2.60189575690564,1.12506029966251,-8.65903276619728));
#18206=CARTESIAN_POINT('Ctrl Pts',(2.64515266137718,1.15974153536591,-8.66203494744187));
#18207=CARTESIAN_POINT('Ctrl Pts',(2.69019748981689,1.1918410702311,-8.66503712868647));
#18208=CARTESIAN_POINT('Ctrl Pts',(2.73526282166318,1.22395521609243,-8.66804067645736));
#18209=CARTESIAN_POINT('Ctrl Pts',(2.78211725221439,1.25348503649361,-8.67104422422826));
#18210=CARTESIAN_POINT('Ctrl Pts',(2.83042842627935,1.28024323343323,-8.67404777199916));
#18211=CARTESIAN_POINT('Ctrl Pts',(2.87883077955668,1.30705193196735,-8.6770569884611));
#18212=CARTESIAN_POINT('Ctrl Pts',(2.92869489168338,1.33107832755431,-8.68006620492305));
#18213=CARTESIAN_POINT('Ctrl Pts',(2.9796658991248,1.352182198885,-8.683075421385));
#18214=CARTESIAN_POINT('Ctrl Pts',(3.01866080925094,1.36832752555526,-8.68537759533396));
#18215=CARTESIAN_POINT('Ctrl Pts',(3.05830308904755,1.3827633067805,-8.68767976928291));
#18216=CARTESIAN_POINT('Ctrl Pts',(3.09842847790439,1.39544665137554,-8.68998194323187));
#18217=CARTESIAN_POINT('Ctrl Pts',(3.15089305509941,1.41203032397176,-8.69299207188863));
#18218=CARTESIAN_POINT('Ctrl Pts',(3.20440441028564,1.42568596251956,-8.69600220054538));
#18219=CARTESIAN_POINT('Ctrl Pts',(3.25860460677885,1.43628664456372,-8.69901232920214));
#18220=CARTESIAN_POINT('Ctrl Pts',(3.31270847424938,1.44686848620863,-8.70201710801203));
#18221=CARTESIAN_POINT('Ctrl Pts',(3.36749823936066,1.45440604571561,-8.70502188682191));
#18222=CARTESIAN_POINT('Ctrl Pts',(3.42260134236897,1.45882229882306,-8.7080266656318));
#18223=CARTESIAN_POINT('Ctrl Pts',(3.47764992998511,1.46323418277965,-8.71102847171082));
#18224=CARTESIAN_POINT('Ctrl Pts',(3.53301071757116,1.46453083556383,-8.71403027778983));
#18225=CARTESIAN_POINT('Ctrl Pts',(3.58830335565611,1.46268668605513,-8.71703208386885));
#18226=CARTESIAN_POINT('Ctrl Pts',(3.64356313008982,1.46084363263241,-8.72003210579881));
#18227=CARTESIAN_POINT('Ctrl Pts',(3.69875430853763,1.45586349453199,-8.72303212772878));
#18228=CARTESIAN_POINT('Ctrl Pts',(3.75349618063956,1.44777278526165,-8.72603214965874));
#18229=CARTESIAN_POINT('Ctrl Pts',(3.8082271368808,1.43968368932773,-8.72903157336616));
#18230=CARTESIAN_POINT('Ctrl Pts',(3.86250844255891,1.42848533121913,-8.73203099707359));
#18231=CARTESIAN_POINT('Ctrl Pts',(3.91596646926689,1.41425584349005,-8.73503042078102));
#18232=CARTESIAN_POINT('Ctrl Pts',(3.96947364288763,1.400013273808,-8.73803260202411));
#18233=CARTESIAN_POINT('Ctrl Pts',(4.02215551393625,1.38273414320771,-8.7410347832672));
#18234=CARTESIAN_POINT('Ctrl Pts',(4.07365205569197,1.36254694696452,-8.7440369645103));
#18235=CARTESIAN_POINT('Ctrl Pts',(4.12517203753024,1.34235056195776,-8.74704051227964));
#18236=CARTESIAN_POINT('Ctrl Pts',(4.17550513375568,1.31924369335141,-8.75004406004898));
#18237=CARTESIAN_POINT('Ctrl Pts',(4.22431287967973,1.29340235866953,-8.75304760781833));
#18238=CARTESIAN_POINT('Ctrl Pts',(4.27321274201106,1.26751225281689,-8.75605682427866));
#18239=CARTESIAN_POINT('Ctrl Pts',(4.32058105004415,1.23887764518127,-8.759066040739));
#18240=CARTESIAN_POINT('Ctrl Pts',(4.36610646861661,1.20771912715002,-8.76207525719933));
#18241=CARTESIAN_POINT('Ctrl Pts',(4.4009352802155,1.18388158346036,-8.76437743115937));
#18242=CARTESIAN_POINT('Ctrl Pts',(4.43468602173213,1.15856776131379,-8.76667960511941));
#18243=CARTESIAN_POINT('Ctrl Pts',(4.46723301928997,1.13189179781862,-8.76898177907944));
#18244=CARTESIAN_POINT('Ctrl Pts',(4.5097887307986,1.09701255574114,-8.77199190776219));
#18245=CARTESIAN_POINT('Ctrl Pts',(4.550464090331,1.05965674258027,-8.77500203644493));
#18246=CARTESIAN_POINT('Ctrl Pts',(4.58895722171386,1.02005479001751,-8.77801216512767));
#18247=CARTESIAN_POINT('Ctrl Pts',(4.62738193995691,0.980523221282205,-8.78101694396365));
#18248=CARTESIAN_POINT('Ctrl Pts',(4.66363176171128,0.938753810976068,-8.78402172279962));
#18249=CARTESIAN_POINT('Ctrl Pts',(4.69743861190192,0.895016502163194,-8.7870265016356));
#18250=CARTESIAN_POINT('Ctrl Pts',(4.73121201581545,0.851322464170957,-8.79002830774075));
#18251=CARTESIAN_POINT('Ctrl Pts',(4.76254691457255,0.80566480019676,-8.79303011384591));
#18252=CARTESIAN_POINT('Ctrl Pts',(4.7912140702125,0.75834809120491,-8.79603191995106));
#18253=CARTESIAN_POINT('Ctrl Pts',(4.81986418728404,0.711059505302565,-8.79903194190715));
#18254=CARTESIAN_POINT('Ctrl Pts',(4.84584943088369,0.662114279615942,-8.80203196386324));
#18255=CARTESIAN_POINT('Ctrl Pts',(4.86898398814057,0.611845756199704,-8.80503198581934));
#18256=CARTESIAN_POINT('Ctrl Pts',(4.89211393222636,0.561587256632074,-8.80803140955285));
#18257=CARTESIAN_POINT('Ctrl Pts',(4.91239409820926,0.510006462855934,-8.81103083328636));
#18258=CARTESIAN_POINT('Ctrl Pts',(4.92968577511037,0.45745899004389,-8.81403025701987));
#18259=CARTESIAN_POINT('Ctrl Pts',(4.9469933492021,0.404863207446886,-8.81703243828877));
#18260=CARTESIAN_POINT('Ctrl Pts',(4.96130677966633,0.351299472995499,-8.82003461955766));
#18261=CARTESIAN_POINT('Ctrl Pts',(4.97253696756643,0.297139528077074,-8.82303680082656));
#18262=CARTESIAN_POINT('Ctrl Pts',(4.98377226719827,0.242954930756435,-8.82604034862159));
#18263=CARTESIAN_POINT('Ctrl Pts',(4.99192144879532,0.188174105266585,-8.82904389641662));
#18264=CARTESIAN_POINT('Ctrl Pts',(4.996946995993,0.133176700182812,-8.83204744421164));
#18265=CARTESIAN_POINT('Ctrl Pts',(5.0019820280644,0.0780754967619093,-8.83505666069715));
#18266=CARTESIAN_POINT('Ctrl Pts',(5.00388163072279,0.0227574262903489,
-8.83806587718266));
#18267=CARTESIAN_POINT('Ctrl Pts',(5.0026604428803,-0.0323962293808541,
-8.84107509366817));
#18268=CARTESIAN_POINT('Ctrl Pts',(5.001726184208,-0.0745910329373488,-8.84337726742111));
#18269=CARTESIAN_POINT('Ctrl Pts',(4.99896644966508,-0.11668955655156,-8.84567944117405));
#18270=CARTESIAN_POINT('Ctrl Pts',(4.9944081644295,-0.158524180948359,-8.84798161492699));
#18271=CARTESIAN_POINT('Ctrl Pts',(4.98844813431173,-0.213223614723226,
-8.85099174355975));
#18272=CARTESIAN_POINT('Ctrl Pts',(4.97938649241697,-0.267701391859348,
-8.8540018721925));
#18273=CARTESIAN_POINT('Ctrl Pts',(4.96725128751742,-0.321578775980827,
-8.85701200082525));
#18274=CARTESIAN_POINT('Ctrl Pts',(4.95513765029562,-0.375360404812791,
-8.86001677961143));
#18275=CARTESIAN_POINT('Ctrl Pts',(4.93996140571602,-0.428543247190867,
-8.86302155839762));
#18276=CARTESIAN_POINT('Ctrl Pts',(4.92180216318462,-0.480755287203381,
-8.8660263371838));
#18277=CARTESIAN_POINT('Ctrl Pts',(4.90366088621443,-0.532915672054686,
-8.86902814323931));
#18278=CARTESIAN_POINT('Ctrl Pts',(4.88254263007397,-0.584106660785801,
-8.87202994929483));
#18279=CARTESIAN_POINT('Ctrl Pts',(4.85857723478985,-0.633969838600237,
-8.87503175535034));
#18280=CARTESIAN_POINT('Ctrl Pts',(4.8346260835411,-0.683803379813211,-8.87803177725704));
#18281=CARTESIAN_POINT('Ctrl Pts',(4.80783137555879,-0.732310199304294,
-8.88103179916373));
#18282=CARTESIAN_POINT('Ctrl Pts',(4.77837076635551,-0.779152537011243,
-8.88403182107043));
#18283=CARTESIAN_POINT('Ctrl Pts',(4.74891603177336,-0.825985534076756,
-8.88703124475487));
#18284=CARTESIAN_POINT('Ctrl Pts',(4.71679673270429,-0.871154261713097,
-8.89003066843931));
#18285=CARTESIAN_POINT('Ctrl Pts',(4.68223491528552,-0.914348239015901,
-8.89303009212375));
#18286=CARTESIAN_POINT('Ctrl Pts',(4.6476413232743,-0.957581926933696,-8.89603227334446));
#18287=CARTESIAN_POINT('Ctrl Pts',(4.61060105727068,-0.998836824145652,
-8.89903445456518));
#18288=CARTESIAN_POINT('Ctrl Pts',(4.5713767773759,-1.03783518986763,-8.90203663578589));
#18289=CARTESIAN_POINT('Ctrl Pts',(4.53213464345563,-1.07685130678395,-8.90504018353316));
#18290=CARTESIAN_POINT('Ctrl Pts',(4.4907069096717,-1.11360849359802,-8.90804373128042));
#18291=CARTESIAN_POINT('Ctrl Pts',(4.44739104312258,-1.14786789086187,-8.91104727902769));
#18292=CARTESIAN_POINT('Ctrl Pts',(4.40399342515271,-1.18219194698225,-8.91405649546671));
#18293=CARTESIAN_POINT('Ctrl Pts',(4.35870098891423,-1.21400849197432,-8.91706571190573));
#18294=CARTESIAN_POINT('Ctrl Pts',(4.31184106685614,-1.24312145542285,-8.92007492834476));
#18295=CARTESIAN_POINT('Ctrl Pts',(4.27599130227328,-1.26539406792625,-8.92237710248803));
#18296=CARTESIAN_POINT('Ctrl Pts',(4.23922474156701,-1.28608518774481,-8.9246792766313));
#18297=CARTESIAN_POINT('Ctrl Pts',(4.20169648228609,-1.30512577889305,-8.92698145077457));
#18298=CARTESIAN_POINT('Ctrl Pts',(4.15262769724198,-1.3300216491537,-8.92999157941722));
#18299=CARTESIAN_POINT('Ctrl Pts',(4.10204984709073,-1.35219872375596,-8.93300170805987));
#18300=CARTESIAN_POINT('Ctrl Pts',(4.05029545947883,-1.37147355422991,-8.93601183670252));
#18301=CARTESIAN_POINT('Ctrl Pts',(3.99863305400672,-1.39071412789525,-8.93901661549781));
#18302=CARTESIAN_POINT('Ctrl Pts',(3.94579875165924,-1.40706251090148,-8.94202139429311));
#18303=CARTESIAN_POINT('Ctrl Pts',(3.8921476240414,-1.42038211023226,-8.9450261730884));
#18304=CARTESIAN_POINT('Ctrl Pts',(3.83854957533194,-1.43368853202467,-8.94802797915254));
#18305=CARTESIAN_POINT('Ctrl Pts',(3.78413681222264,-1.44397197940106,-8.95102978521668));
#18306=CARTESIAN_POINT('Ctrl Pts',(3.72928046083283,-1.4511453604375,-8.95403159128083));
#18307=CARTESIAN_POINT('Ctrl Pts',(3.67445671378833,-1.45831447791307,-8.95703161319566));
#18308=CARTESIAN_POINT('Ctrl Pts',(3.61919042364834,-1.46237712454633,-8.9600316351105));
#18309=CARTESIAN_POINT('Ctrl Pts',(3.56386154383068,-1.46329754083532,-8.96303165702533));
#18310=CARTESIAN_POINT('Ctrl Pts',(3.50854369693081,-1.46421777358765,-8.9660310807174));
#18311=CARTESIAN_POINT('Ctrl Pts',(3.45316381288654,-1.46199701157743,-8.96903050440947));
#18312=CARTESIAN_POINT('Ctrl Pts',(3.39810325295033,-1.45665157887024,-8.97202992810155));
#18313=CARTESIAN_POINT('Ctrl Pts',(3.34299207280798,-1.45130123181228,-8.97503210932907));
#18314=CARTESIAN_POINT('Ctrl Pts',(3.28820133006719,-1.44282052595289,-8.97803429055658));
#18315=CARTESIAN_POINT('Ctrl Pts',(3.23410715655957,-1.43127768971879,-8.9810364717841));
#18316=CARTESIAN_POINT('Ctrl Pts',(3.17998836058761,-1.41972959944244,-8.98404001953772));
#18317=CARTESIAN_POINT('Ctrl Pts',(3.12656727618178,-1.40511673990528,-8.98704356729135));
#18318=CARTESIAN_POINT('Ctrl Pts',(3.07420648941548,-1.38755773594061,-8.99004711504497));
#18319=CARTESIAN_POINT('Ctrl Pts',(3.02174688047532,-1.36996559231074,-8.99305633148955));
#18320=CARTESIAN_POINT('Ctrl Pts',(2.97035205832455,-1.34941639313374,-8.99606554793413));
#18321=CARTESIAN_POINT('Ctrl Pts',(2.92036509038084,-1.32607715603735,-8.99907476437871));
#18322=CARTESIAN_POINT('Ctrl Pts',(2.88212300839229,-1.30822168179465,-9.00137693845985));
#18323=CARTESIAN_POINT('Ctrl Pts',(2.8447045352404,-1.28873424481411,-9.00367911254098));
#18324=CARTESIAN_POINT('Ctrl Pts',(2.80825223510219,-1.26770702246638,-9.00598128662213));
#18325=CARTESIAN_POINT('Ctrl Pts',(2.76059027961522,-1.24021359868372,-9.00899141542504));
#18326=CARTESIAN_POINT('Ctrl Pts',(2.7143808416501,-1.20997075273178,-9.01200154422795));
#18327=CARTESIAN_POINT('Ctrl Pts',(2.6699592560569,-1.17715674997938,-9.01501167303087));
#18328=CARTESIAN_POINT('Ctrl Pts',(2.62561662012888,-1.14440106694914,-9.01801645198736));
#18329=CARTESIAN_POINT('Ctrl Pts',(2.58305595211978,-1.10908360690832,-9.02102123094385));
#18330=CARTESIAN_POINT('Ctrl Pts',(2.54258566210338,-1.07142711803163,-9.02402600990033));
#18331=CARTESIAN_POINT('Ctrl Pts',(2.50215541073065,-1.03380788400882,-9.02702781612611));
#18332=CARTESIAN_POINT('Ctrl Pts',(2.46381182531109,-0.993854563216969,
-9.03002962235189));
#18333=CARTESIAN_POINT('Ctrl Pts',(2.42783062954249,-0.951830397119265,
-9.03303142857766));
#18334=CARTESIAN_POINT('Ctrl Pts',(2.39187081950476,-0.909831208443431,
-9.03603145065428));
#18335=CARTESIAN_POINT('Ctrl Pts',(2.35827095887694,-0.865764014397917,
-9.0390314727309));
#18336=CARTESIAN_POINT('Ctrl Pts',(2.32726860227162,-0.819927497378155,
-9.04203149480753));
#18337=CARTESIAN_POINT('Ctrl Pts',(2.29627242772731,-0.774100120442426,
-9.04503091866125));
#18338=CARTESIAN_POINT('Ctrl Pts',(2.26787302427423,-0.726504558411053,
-9.04803034251498));
#18339=CARTESIAN_POINT('Ctrl Pts',(2.24226509436996,-0.677469131034583,
-9.05102976636871));
#18340=CARTESIAN_POINT('Ctrl Pts',(2.21663362169899,-0.628388622715184,
-9.05403194775638));
#18341=CARTESIAN_POINT('Ctrl Pts',(2.19379899481406,-0.577866073507391,
-9.05703412914405));
#18342=CARTESIAN_POINT('Ctrl Pts',(2.17390958753799,-0.526253783719348,
-9.06003631053172));
#18343=CARTESIAN_POINT('Ctrl Pts',(2.15401112705056,-0.474618001176516,
-9.06303985844492));
#18344=CARTESIAN_POINT('Ctrl Pts',(2.13706072047535,-0.421891992911413,
-9.06604340635811));
#18345=CARTESIAN_POINT('Ctrl Pts',(2.12315713193944,-0.368444250694168,
-9.06904695427131));
#18346=CARTESIAN_POINT('Ctrl Pts',(2.10922730273489,-0.314895634915433,
-9.0720561708725));
#18347=CARTESIAN_POINT('Ctrl Pts',(2.09835588277445,-0.260623083176926,
-9.0750653874737));
#18348=CARTESIAN_POINT('Ctrl Pts',(2.09059044100075,-0.206005181482704,
-9.0780746040749));
#18349=CARTESIAN_POINT('Ctrl Pts',(2.08464956296263,-0.164220270576309,
-9.08037677687317));
#18350=CARTESIAN_POINT('Ctrl Pts',(2.08052551225042,-0.122233456462208,
-9.08267894967144));
#18351=CARTESIAN_POINT('Ctrl Pts',(2.07821898435105,-0.0802145055345787,
-9.08498112246972));
#18352=CARTESIAN_POINT('Ctrl Pts',(2.07676162205074,-0.0536651475157462,
-9.08643573303217));
#18353=CARTESIAN_POINT('Ctrl Pts',(2.07602773447542,-0.0270757155095218,
-9.08789034359462));
#18354=CARTESIAN_POINT('Ctrl Pts',(2.07601912703142,-0.000473532324670548,
-9.08934495415709));
#18355=CARTESIAN_POINT('Origin',(3.53951905042299,8.32667268468867E-16,
0.));
#18356=CARTESIAN_POINT('',(2.07601932070519,-0.000889446977639352,-9.66065500905984));
#18357=CARTESIAN_POINT('',(2.07601928958954,-0.000836684188483706,-9.58934491816123));
#18358=CARTESIAN_POINT('',(2.07601905042299,1.01189432752408E-15,0.));
#18359=CARTESIAN_POINT('Ctrl Pts',(2.07601932070519,-0.000889446977639352,
-9.66065500905984));
#18360=CARTESIAN_POINT('Ctrl Pts',(2.07605714525543,-0.0631261181238673,
-9.65728432050564));
#18361=CARTESIAN_POINT('Ctrl Pts',(2.08006908018252,-0.125215714240401,
-9.65391363195144));
#18362=CARTESIAN_POINT('Ctrl Pts',(2.08797468161632,-0.186684748669116,
-9.65054294339725));
#18363=CARTESIAN_POINT('Ctrl Pts',(2.09594128600493,-0.248628104091767,
-9.6471462451886));
#18364=CARTESIAN_POINT('Ctrl Pts',(2.10786175311519,-0.309941017617402,
-9.64374954697994));
#18365=CARTESIAN_POINT('Ctrl Pts',(2.12360383412636,-0.370157196687643,
-9.64035284877129));
#18366=CARTESIAN_POINT('Ctrl Pts',(2.13804971351566,-0.425415180655378,
-9.63723583440646));
#18367=CARTESIAN_POINT('Ctrl Pts',(2.1557131111941,-0.479749678775611,-9.63411882004164));
#18368=CARTESIAN_POINT('Ctrl Pts',(2.17645673853775,-0.532816463632704,
-9.63100180567681));
#18369=CARTESIAN_POINT('Ctrl Pts',(2.19648926087477,-0.584064084667966,
-9.62799164458715));
#18370=CARTESIAN_POINT('Ctrl Pts',(2.21945805143587,-0.634288035178362,
-9.62498148349749));
#18371=CARTESIAN_POINT('Ctrl Pts',(2.24523715874897,-0.683130027801967,
-9.62197132240783));
#18372=CARTESIAN_POINT('Ctrl Pts',(2.27097045388209,-0.731885223077252,
-9.61896651069043));
#18373=CARTESIAN_POINT('Ctrl Pts',(2.29950391016743,-0.77926287092397,-9.61596169897304));
#18374=CARTESIAN_POINT('Ctrl Pts',(2.33066355794073,-0.82492463188795,-9.61295688725564));
#18375=CARTESIAN_POINT('Ctrl Pts',(2.36179238148982,-0.87054122262511,-9.60995504800413));
#18376=CARTESIAN_POINT('Ctrl Pts',(2.39554195395406,-0.914444854911577,
-9.60695320875262));
#18377=CARTESIAN_POINT('Ctrl Pts',(2.43169336758349,-0.956323431921016,
-9.60395136950111));
#18378=CARTESIAN_POINT('Ctrl Pts',(2.46782329701041,-0.99817712116705,-9.60095131419429));
#18379=CARTESIAN_POINT('Ctrl Pts',(2.50635189404797,-1.03800774151046,-9.59795125888746));
#18380=CARTESIAN_POINT('Ctrl Pts',(2.5470194855512,-1.07553561713656,-9.59495120358064));
#18381=CARTESIAN_POINT('Ctrl Pts',(2.58767896973404,-1.11305601136284,-9.59195174635226));
#18382=CARTESIAN_POINT('Ctrl Pts',(2.63047621363907,-1.14827421461551,-9.58895228912388));
#18383=CARTESIAN_POINT('Ctrl Pts',(2.67511581404292,-1.18094847259974,-9.58595283189549));
#18384=CARTESIAN_POINT('Ctrl Pts',(2.71979645295554,-1.21365276899853,-9.58295061717711));
#18385=CARTESIAN_POINT('Ctrl Pts',(2.76632240516495,-1.2438081350728,-9.57994840245873));
#18386=CARTESIAN_POINT('Ctrl Pts',(2.81436760856459,-1.27121502365677,-9.57694618774034));
#18387=CARTESIAN_POINT('Ctrl Pts',(2.86243468124854,-1.29863438734743,-9.57394260646957));
#18388=CARTESIAN_POINT('Ctrl Pts',(2.91202190999988,-1.3233025440241,-9.5709390251988));
#18389=CARTESIAN_POINT('Ctrl Pts',(2.96277978240611,-1.34506656590941,-9.56793544392803));
#18390=CARTESIAN_POINT('Ctrl Pts',(3.0136334443206,-1.36687166053588,-9.56492619434299));
#18391=CARTESIAN_POINT('Ctrl Pts',(3.06566166553807,-1.38576149126953,-9.56191694475794));
#18392=CARTESIAN_POINT('Ctrl Pts',(3.1184972736761,-1.4016322319014,-9.55890769517289));
#18393=CARTESIAN_POINT('Ctrl Pts',(3.15891357324997,-1.41377246517289,-9.55660578672501));
#18394=CARTESIAN_POINT('Ctrl Pts',(3.19980192479155,-1.42414712434995,-9.55430387827713));
#18395=CARTESIAN_POINT('Ctrl Pts',(3.24099464769623,-1.43273006214591,-9.55200196982925));
#18396=CARTESIAN_POINT('Ctrl Pts',(3.29486108501997,-1.44395370186281,-9.54899183603887));
#18397=CARTESIAN_POINT('Ctrl Pts',(3.34947453901964,-1.45215886917043,-9.5459817022485));
#18398=CARTESIAN_POINT('Ctrl Pts',(3.4044661220345,-1.45725528186852,-9.54297156845813));
#18399=CARTESIAN_POINT('Ctrl Pts',(3.45935997522778,-1.462342637335,-9.53996678421076));
#18400=CARTESIAN_POINT('Ctrl Pts',(3.51463010223504,-1.46433215387418,-9.5369619999634));
#18401=CARTESIAN_POINT('Ctrl Pts',(3.56989808465953,-1.46318466513248,-9.53395721571603));
#18402=CARTESIAN_POINT('Ctrl Pts',(3.62511139201718,-1.46203831156926,-9.53095540401755));
#18403=CARTESIAN_POINT('Ctrl Pts',(3.68032203359013,-1.4577611112248,-9.52795359231907));
#18404=CARTESIAN_POINT('Ctrl Pts',(3.73514901532542,-1.45036587343755,-9.52495178062059));
#18405=CARTESIAN_POINT('Ctrl Pts',(3.78994341337512,-1.44297503064152,-9.52195175289937));
#18406=CARTESIAN_POINT('Ctrl Pts',(3.84435408118658,-1.43246989372409,-9.51895172517814));
#18407=CARTESIAN_POINT('Ctrl Pts',(3.8980049037048,-1.41891512889137,-9.51595169745692));
#18408=CARTESIAN_POINT('Ctrl Pts',(3.9516450308391,-1.40536306622437,-9.5129522677964));
#18409=CARTESIAN_POINT('Ctrl Pts',(4.00452510176795,-1.38876271229221,-9.50995283813587));
#18410=CARTESIAN_POINT('Ctrl Pts',(4.05628123869077,-1.36922937843763,-9.50695340847535));
#18411=CARTESIAN_POINT('Ctrl Pts',(4.10808496132246,-1.34967808521449,-9.50395122107448));
#18412=CARTESIAN_POINT('Ctrl Pts',(4.15876219025388,-1.32718861140194,-9.50094903367362));
#18413=CARTESIAN_POINT('Ctrl Pts',(4.20796764522582,-1.3019250078657,-9.49794684627275));
#18414=CARTESIAN_POINT('Ctrl Pts',(4.25719549940164,-1.27664990388493,-9.49494329222245));
#18415=CARTESIAN_POINT('Ctrl Pts',(4.30494978790693,-1.24859842076241,-9.49193973817214));
#18416=CARTESIAN_POINT('Ctrl Pts',(4.35091146235571,-1.21797972226881,-9.48893618412183));
#18417=CARTESIAN_POINT('Ctrl Pts',(4.39695988346231,-1.18730323498068,-9.48592696125552));
#18418=CARTESIAN_POINT('Ctrl Pts',(4.44120850857435,-1.15405017116868,-9.48291773838922));
#18419=CARTESIAN_POINT('Ctrl Pts',(4.48336976390905,-1.11847131418372,-9.47990851552291));
#18420=CARTESIAN_POINT('Ctrl Pts',(4.51562412863315,-1.09125264100738,-9.4776063883425));
#18421=CARTESIAN_POINT('Ctrl Pts',(4.54665747809227,-1.06267364596613,-9.4753042611621));
#18422=CARTESIAN_POINT('Ctrl Pts',(4.57635626090245,-1.03286051767176,-9.47300213398169));
#18423=CARTESIAN_POINT('Ctrl Pts',(4.61518852194012,-0.993878745668635,
-9.46999201723103));
#18424=CARTESIAN_POINT('Ctrl Pts',(4.65190093845684,-0.952622063388328,
-9.46698190048036));
#18425=CARTESIAN_POINT('Ctrl Pts',(4.68621633738463,-0.909350087741141,
-9.46397178372969));
#18426=CARTESIAN_POINT('Ctrl Pts',(4.72047074445351,-0.866155023285883,
-9.46096701713148));
#18427=CARTESIAN_POINT('Ctrl Pts',(4.75233626330003,-0.820952184343345,
-9.45796225053327));
#18428=CARTESIAN_POINT('Ctrl Pts',(4.781573323665,-0.774037100093561,-9.45495748393507));
#18429=CARTESIAN_POINT('Ctrl Pts',(4.81078145695544,-0.727168433511017,
-9.45195569024543));
#18430=CARTESIAN_POINT('Ctrl Pts',(4.83736600545975,-0.678591323539135,
-9.4489538965558));
#18431=CARTESIAN_POINT('Ctrl Pts',(4.86112952218744,-0.628631856433107,
-9.44595210286616));
#18432=CARTESIAN_POINT('Ctrl Pts',(4.88487891357995,-0.57870208586682,-9.4429520934807));
#18433=CARTESIAN_POINT('Ctrl Pts',(4.90581037043906,-0.527392062776655,
-9.43995208409524));
#18434=CARTESIAN_POINT('Ctrl Pts',(4.92377254285713,-0.475052122070712,
-9.43695207470978));
#18435=CARTESIAN_POINT('Ctrl Pts',(4.94173113269943,-0.422722620625602,
-9.43395266367961));
#18436=CARTESIAN_POINT('Ctrl Pts',(4.95672144290561,-0.369364108760113,
-9.43095325264944));
#18437=CARTESIAN_POINT('Ctrl Pts',(4.96864122643677,-0.315344345161995,
-9.42795384161927));
#18438=CARTESIAN_POINT('Ctrl Pts',(4.98057196811161,-0.261274919895944,
-9.42495167315839));
#18439=CARTESIAN_POINT('Ctrl Pts',(4.98942642946449,-0.206543545206128,
-9.42194950469752));
#18440=CARTESIAN_POINT('Ctrl Pts',(4.99515334565316,-0.151529035335643,
-9.41894733623665));
#18441=CARTESIAN_POINT('Ctrl Pts',(5.00088286846927,-0.0964894854041399,
-9.41594380132752));
#18442=CARTESIAN_POINT('Ctrl Pts',(5.00348198361674,-0.0411670718573775,
-9.41294026641838));
#18443=CARTESIAN_POINT('Ctrl Pts',(5.00295154250228,0.0140567110877411,
-9.40993673150925));
#18444=CARTESIAN_POINT('Ctrl Pts',(5.0024201002595,0.0693847206689516,-9.40692752787691));
#18445=CARTESIAN_POINT('Ctrl Pts',(4.99874733759426,0.124613199534061,-9.40391832424457));
#18446=CARTESIAN_POINT('Ctrl Pts',(4.99198616106228,0.179364273229523,-9.40090912061223));
#18447=CARTESIAN_POINT('Ctrl Pts',(4.98681333664813,0.22125309085957,-9.39860684645286));
#18448=CARTESIAN_POINT('Ctrl Pts',(4.97983381238854,0.262862521635656,-9.39630457229348));
#18449=CARTESIAN_POINT('Ctrl Pts',(4.97109123950477,0.304028481309916,-9.39400229813412));
#18450=CARTESIAN_POINT('Ctrl Pts',(4.95966066485512,0.357851375478105,-9.39099216404745));
#18451=CARTESIAN_POINT('Ctrl Pts',(4.94516648060807,0.411141823506292,-9.38798202996078));
#18452=CARTESIAN_POINT('Ctrl Pts',(4.92767468155269,0.46352582858229,-9.38497189587411));
#18453=CARTESIAN_POINT('Ctrl Pts',(4.91021396976422,0.515816734283992,-9.38196711154258));
#18454=CARTESIAN_POINT('Ctrl Pts',(4.8897663815523,0.567203897148697,-9.37896232721104));
#18455=CARTESIAN_POINT('Ctrl Pts',(4.86644853509855,0.617325192016863,-9.37595754287951));
#18456=CARTESIAN_POINT('Ctrl Pts',(4.84315375734608,0.667396901123263,-9.37295573122696));
#18457=CARTESIAN_POINT('Ctrl Pts',(4.81699456811533,0.716204746586315,-9.36995391957441));
#18458=CARTESIAN_POINT('Ctrl Pts',(4.78813619375466,0.763405186895047,-9.36695210792186));
#18459=CARTESIAN_POINT('Ctrl Pts',(4.75929497118225,0.81057757392719,-9.36395208037666));
#18460=CARTESIAN_POINT('Ctrl Pts',(4.72775801812582,0.856143999701005,-9.36095205283147));
#18461=CARTESIAN_POINT('Ctrl Pts',(4.69373605686976,0.899786281307431,-9.35795202528627));
#18462=CARTESIAN_POINT('Ctrl Pts',(4.65972087942777,0.943419860854571,-9.35495259593202));
#18463=CARTESIAN_POINT('Ctrl Pts',(4.62322200233724,0.985129641903256,-9.35195316657776));
#18464=CARTESIAN_POINT('Ctrl Pts',(4.58449157015024,1.02462904654069,-9.3489537372235));
#18465=CARTESIAN_POINT('Ctrl Pts',(4.54572553095928,1.06416476514049,-9.34595155032985));
#18466=CARTESIAN_POINT('Ctrl Pts',(4.50472420839937,1.10148566952206,-9.34294936343619));
#18467=CARTESIAN_POINT('Ctrl Pts',(4.46177686261144,1.13634184023003,-9.33994717654253));
#18468=CARTESIAN_POINT('Ctrl Pts',(4.41880996802786,1.17121387678829,-9.33694362311185));
#18469=CARTESIAN_POINT('Ctrl Pts',(4.37389571347937,1.20361863370915,-9.33394006968117));
#18470=CARTESIAN_POINT('Ctrl Pts',(4.32735407960895,1.2333483760834,-9.33093651625049));
#18471=CARTESIAN_POINT('Ctrl Pts',(4.28072460722553,1.26313422771178,-9.32792729418196));
#18472=CARTESIAN_POINT('Ctrl Pts',(4.23246208159446,1.2902347202587,-9.32491807211343));
#18473=CARTESIAN_POINT('Ctrl Pts',(4.18291189430237,1.31448769429189,-9.32190885004491));
#18474=CARTESIAN_POINT('Ctrl Pts',(4.14500477643329,1.33304181881886,-9.31960672079213));
#18475=CARTESIAN_POINT('Ctrl Pts',(4.1063445805378,1.34993033667301,-9.31730459153935));
#18476=CARTESIAN_POINT('Ctrl Pts',(4.06709255049389,1.3651001619013,-9.31500246228657));
#18477=CARTESIAN_POINT('Ctrl Pts',(4.01576890418584,1.38493533332302,-9.3119923334501));
#18478=CARTESIAN_POINT('Ctrl Pts',(3.9632172527145,1.401913734746,-9.30898220461363));
#18479=CARTESIAN_POINT('Ctrl Pts',(3.90978688627271,1.41588628771352,-9.30597207577716));
#18480=CARTESIAN_POINT('Ctrl Pts',(3.8564514800765,1.4298340076666,-9.30296729675565));
#18481=CARTESIAN_POINT('Ctrl Pts',(3.80224096494489,1.44078634827748,-9.29996251773414));
#18482=CARTESIAN_POINT('Ctrl Pts',(3.74752234880744,1.44864311611287,-9.29695773871262));
#18483=CARTESIAN_POINT('Ctrl Pts',(3.69285786731907,1.45649211102927,-9.29395593240258));
#18484=CARTESIAN_POINT('Ctrl Pts',(3.63768680079154,1.46125152521657,-9.29095412609254));
#18485=CARTESIAN_POINT('Ctrl Pts',(3.58238715228655,1.46287202989278,-9.2879523197825));
#18486=CARTESIAN_POINT('Ctrl Pts',(3.52712037124722,1.46449157141853,-9.28495229760253));
#18487=CARTESIAN_POINT('Ctrl Pts',(3.47172568654132,1.46297588577145,-9.28195227542256));
#18488=CARTESIAN_POINT('Ctrl Pts',(3.41658472162056,1.45832760407321,-9.27895225324259));
#18489=CARTESIAN_POINT('Ctrl Pts',(3.36145475179931,1.45368024924159,-9.27595282926656));
#18490=CARTESIAN_POINT('Ctrl Pts',(3.30657892724477,1.44590158320243,-9.27295340529053));
#18491=CARTESIAN_POINT('Ctrl Pts',(3.25233503441008,1.43504619819248,-9.2699539813145));
#18492=CARTESIAN_POINT('Ctrl Pts',(3.19804127169103,1.42418083313194,-9.26695179977593));
#18493=CARTESIAN_POINT('Ctrl Pts',(3.14438112036593,1.41023320173145,-9.26394961823736));
#18494=CARTESIAN_POINT('Ctrl Pts',(3.09172194430631,1.39330901158125,-9.26094743669879));
#18495=CARTESIAN_POINT('Ctrl Pts',(3.03903879869131,1.37637711782945,-9.25794388861859));
#18496=CARTESIAN_POINT('Ctrl Pts',(2.98735803026844,1.35646615466497,-9.25494034053838));
#18497=CARTESIAN_POINT('Ctrl Pts',(2.93702845779043,1.33373060840234,-9.25193679245818));
#18498=CARTESIAN_POINT('Ctrl Pts',(2.88660389636236,1.3109521524633,-9.24892757566543));
#18499=CARTESIAN_POINT('Ctrl Pts',(2.83753609454638,1.28533870902024,-9.24591835887269));
#18500=CARTESIAN_POINT('Ctrl Pts',(2.79014958485059,1.25709094900398,-9.24290914207994));
#18501=CARTESIAN_POINT('Ctrl Pts',(2.75389699899805,1.23548027643693,-9.24060697019963));
#18502=CARTESIAN_POINT('Ctrl Pts',(2.71862795991674,1.21232874178303,-9.23830479831931));
#18503=CARTESIAN_POINT('Ctrl Pts',(2.68447503902291,1.18774239150115,-9.236002626439));
#18504=CARTESIAN_POINT('Ctrl Pts',(2.63790054159497,1.15421387101162,-9.23286314391416));
#18505=CARTESIAN_POINT('Ctrl Pts',(2.59319110532703,1.11786235311868,-9.22972366138932));
#18506=CARTESIAN_POINT('Ctrl Pts',(2.55070897341634,1.07892858040285,-9.22658417886449));
#18507=CARTESIAN_POINT('Ctrl Pts',(2.51033977708129,1.04193125837264,-9.22360084491359));
#18508=CARTESIAN_POINT('Ctrl Pts',(2.47198205987822,1.00260285108754,-9.2206175109627));
#18509=CARTESIAN_POINT('Ctrl Pts',(2.43591635001457,0.961193700380545,-9.2176341770118));
#18510=CARTESIAN_POINT('Ctrl Pts',(2.39988516651582,0.919824191412278,-9.21465369906116));
#18511=CARTESIAN_POINT('Ctrl Pts',(2.36614199649358,0.876378285783741,-9.21167322111052));
#18512=CARTESIAN_POINT('Ctrl Pts',(2.33493064869678,0.831143208133652,-9.20869274315988));
#18513=CARTESIAN_POINT('Ctrl Pts',(2.30373639736095,0.785932908642596,-9.20571389780855));
#18514=CARTESIAN_POINT('Ctrl Pts',(2.27507152439762,0.73893581989652,-9.20273505245723));
#18515=CARTESIAN_POINT('Ctrl Pts',(2.24913812526181,0.690470359957754,-9.1997562071059));
#18516=CARTESIAN_POINT('Ctrl Pts',(2.22320831111068,0.642011599793678,-9.19677777354459));
#18517=CARTESIAN_POINT('Ctrl Pts',(2.2000094727482,0.592085344999108,-9.19379933998328));
#18518=CARTESIAN_POINT('Ctrl Pts',(2.17969790159473,0.541034835476783,-9.19082090642197));
#18519=CARTESIAN_POINT('Ctrl Pts',(2.15936755744828,0.489937142462359,-9.18783972004002));
#18520=CARTESIAN_POINT('Ctrl Pts',(2.14193000421592,0.437713620569443,-9.18485853365807));
#18521=CARTESIAN_POINT('Ctrl Pts',(2.1274928285188,0.384726134613917,-9.18187734727612));
#18522=CARTESIAN_POINT('Ctrl Pts',(2.11304788526616,0.331710140088062,-9.17889455694259));
#18523=CARTESIAN_POINT('Ctrl Pts',(2.10160664299598,0.27792988860327,-9.17591176660907));
#18524=CARTESIAN_POINT('Ctrl Pts',(2.09322560589289,0.223757731283741,-9.17292897627554));
#18525=CARTESIAN_POINT('Ctrl Pts',(2.08483022592481,0.16949286659056,-9.16994108135192));
#18526=CARTESIAN_POINT('Ctrl Pts',(2.07950554880692,0.114835291698482,-9.16695318642829));
#18527=CARTESIAN_POINT('Ctrl Pts',(2.07725611812157,0.0601611736690593,
-9.16396529150466));
#18528=CARTESIAN_POINT('Ctrl Pts',(2.07642541419144,0.0399702849170984,
-9.16286187628408));
#18529=CARTESIAN_POINT('Ctrl Pts',(2.076013596649,0.019777117921205,-9.1617584610635));
#18530=CARTESIAN_POINT('Ctrl Pts',(2.07601910496125,-0.000399541592406468,
-9.16065504584292));
#18531=CARTESIAN_POINT('Ctrl Pts',(2.07601912703111,-0.000473531363085116,
-9.08934495420967));
#18532=CARTESIAN_POINT('Ctrl Pts',(2.07600072508622,0.0563996707828281,
-9.09245478771415));
#18533=CARTESIAN_POINT('Ctrl Pts',(2.07930259651659,0.113405113069047,-9.09556462121863));
#18534=CARTESIAN_POINT('Ctrl Pts',(2.08594013758935,0.170119352706743,-9.09867445472312));
#18535=CARTESIAN_POINT('Ctrl Pts',(2.0922999035551,0.22446015257039,-9.10165414450043));
#18536=CARTESIAN_POINT('Ctrl Pts',(2.10172163808173,0.278533036092905,-9.10463383427774));
#18537=CARTESIAN_POINT('Ctrl Pts',(2.11416586932496,0.331964695613464,-9.10761352405505));
#18538=CARTESIAN_POINT('Ctrl Pts',(2.12659876553803,0.385347686039009,-9.11059049973352));
#18539=CARTESIAN_POINT('Ctrl Pts',(2.14204858610979,0.438090087384239,-9.11356747541199));
#18540=CARTESIAN_POINT('Ctrl Pts',(2.16042447852284,0.489826920202991,-9.11654445109047));
#18541=CARTESIAN_POINT('Ctrl Pts',(2.17879119649404,0.541537922626467,-9.11951994046887));
#18542=CARTESIAN_POINT('Ctrl Pts',(2.20008091182603,0.59224384532183,-9.12249542984727));
#18543=CARTESIAN_POINT('Ctrl Pts',(2.22415311018739,0.641595428029321,-9.12547091922567));
#18544=CARTESIAN_POINT('Ctrl Pts',(2.24822319763209,0.69094268304404,-9.12844614768024));
#18545=CARTESIAN_POINT('Ctrl Pts',(2.27507504589748,0.738935351725389,-9.13142137613481));
#18546=CARTESIAN_POINT('Ctrl Pts',(2.30452128333745,0.785246945421463,-9.13439660458939));
#18547=CARTESIAN_POINT('Ctrl Pts',(2.33399651661026,0.831604142337015,-9.13737476276382));
#18548=CARTESIAN_POINT('Ctrl Pts',(2.36607094607567,0.876276507662001,-9.14035292093826));
#18549=CARTESIAN_POINT('Ctrl Pts',(2.40051369859436,0.918966298895521,-9.1433310791127));
#18550=CARTESIAN_POINT('Ctrl Pts',(2.43497662413391,0.961681093416718,-9.1463109815858));
#18551=CARTESIAN_POINT('Ctrl Pts',(2.47181027029991,1.00241060609859,-9.1492908840589));
#18552=CARTESIAN_POINT('Ctrl Pts',(2.5107455181391,1.04089253492959,-9.152270786532));
#18553=CARTESIAN_POINT('Ctrl Pts',(2.54974830824503,1.07944121963979,-9.15525585834083));
#18554=CARTESIAN_POINT('Ctrl Pts',(2.59085956673665,1.11573419130838,-9.15824093014965));
#18555=CARTESIAN_POINT('Ctrl Pts',(2.63377688597688,1.14954920797001,-9.16122600195848));
#18556=CARTESIAN_POINT('Ctrl Pts',(2.64697984491329,1.1599519610851,-9.16214432074474));
#18557=CARTESIAN_POINT('Ctrl Pts',(2.66035352883006,1.1701205127387,-9.163062639531));
#18558=CARTESIAN_POINT('Ctrl Pts',(2.67388862910717,1.18004924629975,-9.16398095831725));
#18559=CARTESIAN_POINT('Ctrl Pts',(2.71825491382426,1.2125943335936,-9.16699108693825));
#18560=CARTESIAN_POINT('Ctrl Pts',(2.76455236415568,1.2427022655566,-9.17000121555925));
#18561=CARTESIAN_POINT('Ctrl Pts',(2.81248271675935,1.27013795295351,-9.17301134418025));
#18562=CARTESIAN_POINT('Ctrl Pts',(2.86032788355696,1.29752487936664,-9.17601612295049));
#18563=CARTESIAN_POINT('Ctrl Pts',(2.9097997386984,1.32224872606603,-9.17902090172074));
#18564=CARTESIAN_POINT('Ctrl Pts',(2.96057015433098,1.34411696876196,-9.18202568049099));
#18565=CARTESIAN_POINT('Ctrl Pts',(3.01129034100766,1.3659635764371,-9.18502748652803));
#18566=CARTESIAN_POINT('Ctrl Pts',(3.06330606057254,1.3849599687024,-9.18802929256507));
#18567=CARTESIAN_POINT('Ctrl Pts',(3.11626529340335,1.40095985209026,-9.19103109860211));
#18568=CARTESIAN_POINT('Ctrl Pts',(3.16919304942238,1.41695022579886,-9.19403112048786));
#18569=CARTESIAN_POINT('Ctrl Pts',(3.22306270265424,1.42994746826493,-9.19703114237362));
#18570=CARTESIAN_POINT('Ctrl Pts',(3.2775051748386,1.4398544992468,-9.20003116425937));
#18571=CARTESIAN_POINT('Ctrl Pts',(3.33193679082557,1.44975955469964,-9.20303058792045));
#18572=CARTESIAN_POINT('Ctrl Pts',(3.38694047962898,1.45657552793621,-9.20603001158154));
#18573=CARTESIAN_POINT('Ctrl Pts',(3.44213730285502,1.46025649981112,-9.20902943524262));
#18574=CARTESIAN_POINT('Ctrl Pts',(3.49738487151301,1.46394085580302,-9.21203161643648));
#18575=CARTESIAN_POINT('Ctrl Pts',(3.55282540125534,1.46448441700218,-9.21503379763035));
#18576=CARTESIAN_POINT('Ctrl Pts',(3.60807667158193,1.4618933280445,-9.21803597882421));
#18577=CARTESIAN_POINT('Ctrl Pts',(3.66335309102968,1.45930105968208,-9.22103952654265));
#18578=CARTESIAN_POINT('Ctrl Pts',(3.71843955313624,1.45357135162408,-9.22404307426108));
#18579=CARTESIAN_POINT('Ctrl Pts',(3.77295900615846,1.44476227700831,-9.22704662197952));
#18580=CARTESIAN_POINT('Ctrl Pts',(3.82758135543828,1.43593657675231,-9.23005583838688));
#18581=CARTESIAN_POINT('Ctrl Pts',(3.88163404087832,1.42402001397532,-9.23306505479425));
#18582=CARTESIAN_POINT('Ctrl Pts',(3.93475139873487,1.40912158483499,-9.23607427120162));
#18583=CARTESIAN_POINT('Ctrl Pts',(3.97538836221842,1.39772367376847,-9.23837644552268));
#18584=CARTESIAN_POINT('Ctrl Pts',(4.01547811093556,1.38458157483124,-9.24067861984375));
#18585=CARTESIAN_POINT('Ctrl Pts',(4.0548649868777,1.3697630509616,-9.24298079416481));
#18586=CARTESIAN_POINT('Ctrl Pts',(4.10636395406392,1.35038759514652,-9.24599092373162));
#18587=CARTESIAN_POINT('Ctrl Pts',(4.15687691820343,1.32806308232201,-9.24900105329842));
#18588=CARTESIAN_POINT('Ctrl Pts',(4.20604401566905,1.30291086445073,-9.25201118286523));
#18589=CARTESIAN_POINT('Ctrl Pts',(4.2551237294341,1.27780334911404,-9.25501596258886));
#18590=CARTESIAN_POINT('Ctrl Pts',(4.30286185706654,1.24987834069035,-9.25802074231249));
#18591=CARTESIAN_POINT('Ctrl Pts',(4.34891786639811,1.21930546078416,-9.26102552203612));
#18592=CARTESIAN_POINT('Ctrl Pts',(4.39492831097592,1.18876282765282,-9.26402732903046));
#18593=CARTESIAN_POINT('Ctrl Pts',(4.43925949607256,1.15557780303837,-9.26702913602479));
#18594=CARTESIAN_POINT('Ctrl Pts',(4.48159655472588,1.11996527887539,-9.27003094301913));
#18595=CARTESIAN_POINT('Ctrl Pts',(4.52390844999407,1.0843739213142,-9.27303096586436));
#18596=CARTESIAN_POINT('Ctrl Pts',(4.56422816467261,1.04635826321566,-9.27603098870958));
#18597=CARTESIAN_POINT('Ctrl Pts',(4.60227272843954,1.00617437348717,-9.2790310115548));
#18598=CARTESIAN_POINT('Ctrl Pts',(4.6403097058712,0.965998496689559,-9.28203043617582));
#18599=CARTESIAN_POINT('Ctrl Pts',(4.67607207049773,0.923655630197818,-9.28502986079683));
#18600=CARTESIAN_POINT('Ctrl Pts',(4.70931431326071,0.879438055261666,-9.28802928541785));
#18601=CARTESIAN_POINT('Ctrl Pts',(4.74258711733265,0.8351798288274,-9.29103146756468));
#18602=CARTESIAN_POINT('Ctrl Pts',(4.77333485268551,0.789043873624383,-9.29403364971151));
#18603=CARTESIAN_POINT('Ctrl Pts',(4.80135382175268,0.741353667194913,-9.29703583185834));
#18604=CARTESIAN_POINT('Ctrl Pts',(4.82938554439063,0.693641753313561,-9.30003938052734));
#18605=CARTESIAN_POINT('Ctrl Pts',(4.85468578308905,0.644374648546172,-9.30304292919634));
#18606=CARTESIAN_POINT('Ctrl Pts',(4.87709715598709,0.593899874992042,-9.30604647786535));
#18607=CARTESIAN_POINT('Ctrl Pts',(4.89955082643404,0.543329839125654,-9.30905569520745));
#18608=CARTESIAN_POINT('Ctrl Pts',(4.91910455238094,0.491548076564944,-9.31206491254955));
#18609=CARTESIAN_POINT('Ctrl Pts',(4.93564982372366,0.438920395792753,-9.31507412989166));
#18610=CARTESIAN_POINT('Ctrl Pts',(4.94830759101384,0.39865820108846,-9.31737629659856));
#18611=CARTESIAN_POINT('Ctrl Pts',(4.95920556962158,0.357901299559934,-9.31967846330547));
#18612=CARTESIAN_POINT('Ctrl Pts',(4.96831546214218,0.31681708264922,-9.32198063001237));
#18613=CARTESIAN_POINT('Ctrl Pts',(4.9802268205484,0.263098684615905,-9.32499075693701));
#18614=CARTESIAN_POINT('Ctrl Pts',(4.98912952154896,0.208594737591463,-9.32800088386164));
#18615=CARTESIAN_POINT('Ctrl Pts',(4.99492857241083,0.15367294266439,-9.33101101078628));
#18616=CARTESIAN_POINT('Ctrl Pts',(5.00071731673245,0.0988487591746224,
-9.33401578787091));
#18617=CARTESIAN_POINT('Ctrl Pts',(5.00341330256137,0.0436087224915531,
-9.33702056495555));
#18618=CARTESIAN_POINT('Ctrl Pts',(5.00297252691122,-0.0116692825189981,
-9.34002534204018));
#18619=CARTESIAN_POINT('Ctrl Pts',(5.00253218733501,-0.0668925991702068,
-9.34302714639943));
#18620=CARTESIAN_POINT('Ctrl Pts',(4.99896123796156,-0.122153284234078,
-9.34602895075867));
#18621=CARTESIAN_POINT('Ctrl Pts',(4.99226761429001,-0.17707021257766,-9.34903075511791));
#18622=CARTESIAN_POINT('Ctrl Pts',(4.98557796901429,-0.231954500711812,
-9.35203077533652));
#18623=CARTESIAN_POINT('Ctrl Pts',(4.97576939188507,-0.286494913898792,
-9.35503079555514));
#18624=CARTESIAN_POINT('Ctrl Pts',(4.96290173342562,-0.34031454234024,-9.35803081577376));
#18625=CARTESIAN_POINT('Ctrl Pts',(4.95003664080778,-0.394123439020127,
-9.36103023778123));
#18626=CARTESIAN_POINT('Ctrl Pts',(4.93411380100649,-0.447211323036412,
-9.3640296597887));
#18627=CARTESIAN_POINT('Ctrl Pts',(4.91524386204612,-0.499212873115784,
-9.36702908179617));
#18628=CARTESIAN_POINT('Ctrl Pts',(4.89635657470561,-0.551262231651783,
-9.37003126137023));
#18629=CARTESIAN_POINT('Ctrl Pts',(4.87451695558412,-0.602222763392148,
-9.37303344094428));
#18630=CARTESIAN_POINT('Ctrl Pts',(4.84988462607803,-0.651747119777476,
-9.37603562051834));
#18631=CARTESIAN_POINT('Ctrl Pts',(4.82524108435636,-0.701294018803769,
-9.37903916663325));
#18632=CARTESIAN_POINT('Ctrl Pts',(4.79780256031205,-0.749402979776172,
-9.38204271274816));
#18633=CARTESIAN_POINT('Ctrl Pts',(4.76777412001656,-0.795752306950904,
-9.38504625886307));
#18634=CARTESIAN_POINT('Ctrl Pts',(4.73768900561841,-0.842189111413878,
-9.38805547371333));
#18635=CARTESIAN_POINT('Ctrl Pts',(4.70500452290369,-0.886859220529012,
-9.39106468856358));
#18636=CARTESIAN_POINT('Ctrl Pts',(4.66996775660819,-0.929471878371908,
-9.39407390341384));
#18637=CARTESIAN_POINT('Ctrl Pts',(4.64316302222061,-0.96207251752321,-9.39637609089587));
#18638=CARTESIAN_POINT('Ctrl Pts',(4.61498239082923,-0.993469570782487,
-9.3986782783779));
#18639=CARTESIAN_POINT('Ctrl Pts',(4.58555059930908,-1.02354787320133,-9.40098046585993));
#18640=CARTESIAN_POINT('Ctrl Pts',(4.54706829075826,-1.06287550004913,-9.40399059485479));
#18641=CARTESIAN_POINT('Ctrl Pts',(4.5062841429003,-1.10011251335244,-9.40700072384964));
#18642=CARTESIAN_POINT('Ctrl Pts',(4.46345421198909,-1.13497844350535,-9.4100108528445));
#18643=CARTESIAN_POINT('Ctrl Pts',(4.42070040231218,-1.16978240676777,-9.41301563196533));
#18644=CARTESIAN_POINT('Ctrl Pts',(4.37590843140498,-1.20222331908433,-9.41602041108617));
#18645=CARTESIAN_POINT('Ctrl Pts',(4.32937074529078,-1.23205785177258,-9.41902519020701));
#18646=CARTESIAN_POINT('Ctrl Pts',(4.28287910076274,-1.26186286796954,-9.4220269965802));
#18647=CARTESIAN_POINT('Ctrl Pts',(4.23464560475323,-1.28906632898799,-9.4250288029534));
#18648=CARTESIAN_POINT('Ctrl Pts',(4.1849937960761,-1.313466635558,-9.42803060932659));
#18649=CARTESIAN_POINT('Ctrl Pts',(4.13537149865489,-1.33785243946011,-9.43103063153364));
#18650=CARTESIAN_POINT('Ctrl Pts',(4.08433303246491,-1.35943815876272,-9.43403065374068));
#18651=CARTESIAN_POINT('Ctrl Pts',(4.03222677203278,-1.37806797766514,-9.43703067594773));
#18652=CARTESIAN_POINT('Ctrl Pts',(3.98013090220608,-1.39669408156103,-9.44003009991482));
#18653=CARTESIAN_POINT('Ctrl Pts',(3.92696815801702,-1.41236527796435,-9.44302952388191));
#18654=CARTESIAN_POINT('Ctrl Pts',(3.87310496385929,-1.42497462726775,-9.446028947849));
#18655=CARTESIAN_POINT('Ctrl Pts',(3.81919225081428,-1.43759556892019,-9.44903112932313));
#18656=CARTESIAN_POINT('Ctrl Pts',(3.76457831657979,-1.44714891904127,-9.45203331079727));
#18657=CARTESIAN_POINT('Ctrl Pts',(3.70964129179006,-1.45357857475688,-9.4550354922714));
#18658=CARTESIAN_POINT('Ctrl Pts',(3.65467926117246,-1.46001115707553,-9.45803904025625));
#18659=CARTESIAN_POINT('Ctrl Pts',(3.59939437493514,-1.4633171791083,-9.4610425882411));
#18660=CARTESIAN_POINT('Ctrl Pts',(3.5441681096177,-1.46349261571373,-9.46404613622595));
#18661=CARTESIAN_POINT('Ctrl Pts',(3.48883761453575,-1.46366838342457,-9.46705535287403));
#18662=CARTESIAN_POINT('Ctrl Pts',(3.43356649003813,-1.46070179108835,-9.4700645695221));
#18663=CARTESIAN_POINT('Ctrl Pts',(3.37873325859932,-1.45464091072252,-9.47307378617018));
#18664=CARTESIAN_POINT('Ctrl Pts',(3.33678362971101,-1.45000409331432,-9.47537595801595));
#18665=CARTESIAN_POINT('Ctrl Pts',(3.2950902483301,-1.44355731500171,-9.47767812986172));
#18666=CARTESIAN_POINT('Ctrl Pts',(3.25381772053166,-1.43534211953051,-9.4799803017075));
#18667=CARTESIAN_POINT('Ctrl Pts',(3.19985309155182,-1.42460059243613,-9.48299043595737));
#18668=CARTESIAN_POINT('Ctrl Pts',(3.14638169686634,-1.41078889917564,-9.48600057020725));
#18669=CARTESIAN_POINT('Ctrl Pts',(3.09377834646457,-1.39396824742698,-9.48901070445713));
#18670=CARTESIAN_POINT('Ctrl Pts',(3.04126848630545,-1.37717749048163,-9.49201548889222));
#18671=CARTESIAN_POINT('Ctrl Pts',(2.98962410779196,-1.3573885471936,-9.49502027332732));
#18672=CARTESIAN_POINT('Ctrl Pts',(2.93920879747361,-1.33471339627796,-9.49802505776242));
#18673=CARTESIAN_POINT('Ctrl Pts',(2.88884336440228,-1.31206067851003,-9.501026869482));
#18674=CARTESIAN_POINT('Ctrl Pts',(2.83970507005814,-1.28652762509496,-9.50402868120157));
#18675=CARTESIAN_POINT('Ctrl Pts',(2.79213954034621,-1.25827505654264,-9.50703049292115));
#18676=CARTESIAN_POINT('Ctrl Pts',(2.74460228147621,-1.23003928006442,-9.51003052049693));
#18677=CARTESIAN_POINT('Ctrl Pts',(2.69863638759028,-1.19908746133809,-9.51303054807271));
#18678=CARTESIAN_POINT('Ctrl Pts',(2.65456270975754,-1.16562623731452,-9.51603057564849));
#18679=CARTESIAN_POINT('Ctrl Pts',(2.61049782053701,-1.13217168570262,-9.51903000499694));
#18680=CARTESIAN_POINT('Ctrl Pts',(2.56832481841323,-1.09620904171744,-9.52202943434538));
#18681=CARTESIAN_POINT('Ctrl Pts',(2.52833348165112,-1.05798676527993,-9.52502886369382));
#18682=CARTESIAN_POINT('Ctrl Pts',(2.48830537941433,-1.01972934972857,-9.52803105052558));
#18683=CARTESIAN_POINT('Ctrl Pts',(2.45046333223626,-0.979208517103823,
-9.53103323735734));
#18684=CARTESIAN_POINT('Ctrl Pts',(2.41506093746071,-0.93671030857641,-9.53403542418909));
#18685=CARTESIAN_POINT('Ctrl Pts',(2.37964242857244,-0.894192756133781,
-9.53703897752663));
#18686=CARTESIAN_POINT('Ctrl Pts',(2.346666100702,-0.849696458651381,-9.54004253086416));
#18687=CARTESIAN_POINT('Ctrl Pts',(2.31634376287682,-0.803538714646867,
-9.54304608420169));
#18688=CARTESIAN_POINT('Ctrl Pts',(2.28596419788774,-0.757293857412609,
-9.54605530612718));
#18689=CARTESIAN_POINT('Ctrl Pts',(2.25824889400525,-0.709381747993645,
-9.54906452805268));
#18690=CARTESIAN_POINT('Ctrl Pts',(2.23336441339684,-0.660145676479889,
-9.55207374997818));
#18691=CARTESIAN_POINT('Ctrl Pts',(2.21432717032797,-0.622478864143564,
-9.55437587917048));
#18692=CARTESIAN_POINT('Ctrl Pts',(2.19694576991218,-0.584037740428541,
-9.55667800836277));
#18693=CARTESIAN_POINT('Ctrl Pts',(2.18127535534639,-0.544982857330992,
-9.55898013755507));
#18694=CARTESIAN_POINT('Ctrl Pts',(2.15828431881751,-0.487683017549696,
-9.56235773398892));
#18695=CARTESIAN_POINT('Ctrl Pts',(2.1388962543463,-0.428859532790245,-9.56573533042276));
#18696=CARTESIAN_POINT('Ctrl Pts',(2.12328935970264,-0.368952182704129,
-9.56911292685661));
#18697=CARTESIAN_POINT('Ctrl Pts',(2.10770833125499,-0.309144120483749,
-9.57248492540738));
#18698=CARTESIAN_POINT('Ctrl Pts',(2.09589612654762,-0.24825603324965,-9.57585692395815));
#18699=CARTESIAN_POINT('Ctrl Pts',(2.08798271930862,-0.186747234129522,
-9.57922892250892));
#18700=CARTESIAN_POINT('Ctrl Pts',(2.08006931206962,-0.125238435009388,
-9.5826009210597));
#18701=CARTESIAN_POINT('Ctrl Pts',(2.07605489084021,-0.0631091910183387,
-9.58597291961046));
#18702=CARTESIAN_POINT('Ctrl Pts',(2.07601928958954,-0.000836684188483706,
-9.58934491816123));
#18703=CARTESIAN_POINT('Origin',(3.53951905042299,8.32667268468867E-16,
0.));
#18704=CARTESIAN_POINT('',(2.07692213061801,0.00132420044191561,-10.1606550458429));
#18705=CARTESIAN_POINT('',(2.07677307172911,0.00126791318965598,-10.0893449541571));
#18706=CARTESIAN_POINT('',(2.07601905042299,1.01189432752408E-15,0.));
#18707=CARTESIAN_POINT('Ctrl Pts',(2.07692213061801,0.00132420044191561,
-10.1606550458429));
#18708=CARTESIAN_POINT('Ctrl Pts',(2.07968635796469,-0.340292586538367,
-10.1421036374827));
#18709=CARTESIAN_POINT('Ctrl Pts',(2.3686807329946,-1.17120535538033,-10.0972189505064));
#18710=CARTESIAN_POINT('Ctrl Pts',(3.74854525128539,-1.71419019754643,-10.0260009849147));
#18711=CARTESIAN_POINT('Ctrl Pts',(5.08944937204478,-0.761677757650357,
-9.94700114906702));
#18712=CARTESIAN_POINT('Ctrl Pts',(5.02430011578218,0.881991624007174,-9.86800131321952));
#18713=CARTESIAN_POINT('Ctrl Pts',(3.6121165985489,1.72542879024637,-9.78900147737193));
#18714=CARTESIAN_POINT('Ctrl Pts',(2.31901753288414,1.09390323182268,-9.71988605491308));
#18715=CARTESIAN_POINT('Ctrl Pts',(2.07948494644385,0.302460268914583,-9.67710391107006));
#18716=CARTESIAN_POINT('Ctrl Pts',(2.07778482844489,-0.000887695637598399,
-9.66065504584291));
#18717=CARTESIAN_POINT('Ctrl Pts',(2.07786355472798,-0.00083496590290807,
-9.5893449541571));
#18718=CARTESIAN_POINT('Ctrl Pts',(2.07943303720893,0.298178416615211,-9.60555662723894));
#18719=CARTESIAN_POINT('Ctrl Pts',(2.31370169398425,1.08514940936176,-9.64810157893662));
#18720=CARTESIAN_POINT('Ctrl Pts',(3.5966891679774,1.72601943169721,-9.71697980925019));
#18721=CARTESIAN_POINT('Ctrl Pts',(5.01634665164319,0.895213050221392,-9.79597964509776));
#18722=CARTESIAN_POINT('Ctrl Pts',(5.09621241255259,-0.747750182775267,
-9.8749794809453));
#18723=CARTESIAN_POINT('Ctrl Pts',(3.76383778077046,-1.71232472144846,-9.95397931679288));
#18724=CARTESIAN_POINT('Ctrl Pts',(2.37463262236157,-1.17974343592703,-10.0254344745302));
#18725=CARTESIAN_POINT('Ctrl Pts',(2.07964814994376,-0.344625173506082,
-10.0705563536515));
#18726=CARTESIAN_POINT('Ctrl Pts',(2.07677307172911,0.00126791318965598,
-10.0893449541571));
#18727=CARTESIAN_POINT('Origin',(3.53951905042299,8.32667268468867E-16,
0.));
#18728=CARTESIAN_POINT('',(2.904562511392,-1.32104332876118,-10.4999647974346));
#18729=CARTESIAN_POINT('Ctrl Pts',(2.07677307172911,0.00126791318965598,
-10.0893449541571));
#18730=CARTESIAN_POINT('Ctrl Pts',(2.0756185663861,0.140163409899335,-10.0968896322674));
#18731=CARTESIAN_POINT('Ctrl Pts',(2.15728834009292,0.762509891316419,-10.1307675889936));
#18732=CARTESIAN_POINT('Ctrl Pts',(3.03967406104186,1.65296546888283,-10.1909788243355));
#18733=CARTESIAN_POINT('Ctrl Pts',(4.65091988412873,1.3220120331683,-10.2699786601832));
#18734=CARTESIAN_POINT('Ctrl Pts',(5.25379341461138,-0.208875272215984,
-10.3489784960306));
#18735=CARTESIAN_POINT('Ctrl Pts',(4.32983134761648,-1.5094750881873,-10.4256405417812));
#18736=CARTESIAN_POINT('Ctrl Pts',(3.3020958806422,-1.50905208505225,-10.4759693089158));
#18737=CARTESIAN_POINT('Ctrl Pts',(2.904562511392,-1.32104332876118,-10.4999647974346));
#18738=CARTESIAN_POINT('',(4.1735261449982,-1.31904027763685,-10.5));
#18739=CARTESIAN_POINT('Origin',(3.53951905042299,8.32667268468867E-16,
-10.5));
#18740=CARTESIAN_POINT('Ctrl Pts',(4.1735261449982,-1.31904027763685,-10.5));
#18741=CARTESIAN_POINT('Ctrl Pts',(4.61001469460598,-1.10923861968599,-10.4736667213841));
#18742=CARTESIAN_POINT('Ctrl Pts',(5.25113005292935,-0.226200379926371,
-10.4210001641525));
#18743=CARTESIAN_POINT('Ctrl Pts',(4.66306375306162,1.31298734088882,-10.3420003283048));
#18744=CARTESIAN_POINT('Ctrl Pts',(3.05428328236686,1.65687129011178,-10.2630004924574));
#18745=CARTESIAN_POINT('Ctrl Pts',(2.16068644613406,0.771444902797137,-10.20255206497));
#18746=CARTESIAN_POINT('Ctrl Pts',(2.07576260363487,0.14462423792681,-10.1684369160985));
#18747=CARTESIAN_POINT('Ctrl Pts',(2.07692213061801,0.00132420044191561,
-10.1606550458429));
#18748=CARTESIAN_POINT('Origin',(3.53951905042299,8.32667268468867E-16,
0.924367114736157));
#18749=CARTESIAN_POINT('',(4.21285985862019,0.966285267670136,-10.5));
#18750=CARTESIAN_POINT('Ctrl Pts',(4.21285985862019,0.966285267670136,-10.5));
#18751=CARTESIAN_POINT('Ctrl Pts',(4.12691296029429,1.02617602241623,-10.4924697639478));
#18752=CARTESIAN_POINT('Ctrl Pts',(4.03333366517216,1.07435164214843,-10.4846304956294));
#18753=CARTESIAN_POINT('Ctrl Pts',(3.8990102589921,1.12217937116524,-10.47446765702));
#18754=CARTESIAN_POINT('Ctrl Pts',(3.86285169382147,1.13312709505302,-10.4718237382524));
#18755=CARTESIAN_POINT('Ctrl Pts',(3.81653974099716,1.14475077295999,-10.4685493303852));
#18756=CARTESIAN_POINT('Ctrl Pts',(3.8068227682405,1.14705864197507,-10.4678683481899));
#18757=CARTESIAN_POINT('Ctrl Pts',(3.79111786242873,1.15057828923006,-10.4667771191176));
#18758=CARTESIAN_POINT('Ctrl Pts',(3.78514797849336,1.15186752446851,-10.466364484865));
#18759=CARTESIAN_POINT('Ctrl Pts',(3.77371953385572,1.15424268105789,-10.4655785992848));
#18760=CARTESIAN_POINT('Ctrl Pts',(3.76826279376341,1.1553364595976,-10.4652051148072));
#18761=CARTESIAN_POINT('Ctrl Pts',(3.7558197159075,1.15773900456352,-10.4643573277347));
#18762=CARTESIAN_POINT('Ctrl Pts',(3.74882882859123,1.15902329612631,-10.463883787959));
#18763=CARTESIAN_POINT('Ctrl Pts',(3.72680360950976,1.16286375339913,-10.4624002136484));
#18764=CARTESIAN_POINT('Ctrl Pts',(3.71173062999975,1.16519132362581,-10.461397137812));
#18765=CARTESIAN_POINT('Ctrl Pts',(3.61932276551113,1.17762851309365,-10.4553134950841));
#18766=CARTESIAN_POINT('Ctrl Pts',(3.54118478086041,1.18032900442303,-10.4504671690847));
#18767=CARTESIAN_POINT('Ctrl Pts',(3.43590521451579,1.17350560927382,-10.4439098990448));
#18768=CARTESIAN_POINT('Ctrl Pts',(3.40853530504769,1.17076660427417,-10.4422007519744));
#18769=CARTESIAN_POINT('Ctrl Pts',(3.35005555590813,1.16283789793965,-10.4384979914452));
#18770=CARTESIAN_POINT('Ctrl Pts',(3.31900877578698,1.15735186523851,-10.4365008725666));
#18771=CARTESIAN_POINT('Ctrl Pts',(3.27663502097098,1.1480974274304,-10.433687591134));
#18772=CARTESIAN_POINT('Ctrl Pts',(3.26508774453619,1.14539213879608,-10.4329118325623));
#18773=CARTESIAN_POINT('Ctrl Pts',(3.24513042288521,1.14039744528032,-10.4315521241759));
#18774=CARTESIAN_POINT('Ctrl Pts',(3.23670111984714,1.13818815997004,-10.4309719066595));
#18775=CARTESIAN_POINT('Ctrl Pts',(3.22452608118542,1.13485231746078,-10.4301242189358));
#18776=CARTESIAN_POINT('Ctrl Pts',(3.22075999106738,1.13380025318935,-10.4298606607323));
#18777=CARTESIAN_POINT('Ctrl Pts',(3.21697597771734,1.13272283871051,-10.429594429032));
#18778=CARTESIAN_POINT('Ctrl Pts',(3.21695268015998,1.132716204467,-10.4295927898323));
#18779=CARTESIAN_POINT('Ctrl Pts',(3.21690580728414,1.13270285532099,-10.4295894917808));
#18780=CARTESIAN_POINT('Ctrl Pts',(3.21688223196395,1.13269614039932,-10.4295878329275));
#18781=CARTESIAN_POINT('Ctrl Pts',(3.21683479462963,1.13268262729623,-10.4295844949363));
#18782=CARTESIAN_POINT('Ctrl Pts',(3.21681093261599,1.13267582909545,-10.429582815797));
#18783=CARTESIAN_POINT('Ctrl Pts',(3.21676291263406,1.13266214673687,-10.4295794365779));
#18784=CARTESIAN_POINT('Ctrl Pts',(3.21673875466121,1.13265526255739,-10.4295777364964));
#18785=CARTESIAN_POINT('Ctrl Pts',(3.21669013313684,1.13264140543728,-10.4295743147112));
#18786=CARTESIAN_POINT('Ctrl Pts',(3.21666566960863,1.132634432482,-10.4295725930078));
#18787=CARTESIAN_POINT('Ctrl Pts',(3.21661642702002,1.13262039490881,-10.4295691272736));
#18788=CARTESIAN_POINT('Ctrl Pts',(3.21659164794706,1.13261333026504,-10.4295673832405));
#18789=CARTESIAN_POINT('Ctrl Pts',(3.21654176391438,1.13259910629536,-10.4295638721137));
#18790=CARTESIAN_POINT('Ctrl Pts',(3.21651665897117,1.13259194695085,-10.4295621050194));
#18791=CARTESIAN_POINT('Ctrl Pts',(3.21646611244882,1.13257753044381,-10.4295585470087));
#18792=CARTESIAN_POINT('Ctrl Pts',(3.21644067087711,1.13257027325899,-10.429556756091));
#18793=CARTESIAN_POINT('Ctrl Pts',(3.21638943993205,1.13255565781255,-10.4295531496421));
#18794=CARTESIAN_POINT('Ctrl Pts',(3.21636365057277,1.13254829952938,-10.4295513341101));
#18795=CARTESIAN_POINT('Ctrl Pts',(3.21631171245287,1.1325334784993,-10.4295476776107));
#18796=CARTESIAN_POINT('Ctrl Pts',(3.21628556369563,1.13252601572658,-10.4295458366416));
#18797=CARTESIAN_POINT('Ctrl Pts',(3.21623289471368,1.13251098219282,-10.4295421284127));
#18798=CARTESIAN_POINT('Ctrl Pts',(3.21620637449497,1.13250341140542,-10.4295402611513));
#18799=CARTESIAN_POINT('Ctrl Pts',(3.21615295003582,1.13248815817352,-10.429536499448));
#18800=CARTESIAN_POINT('Ctrl Pts',(3.21612604579817,1.13248047570039,-10.4295346050041));
#18801=CARTESIAN_POINT('Ctrl Pts',(3.21607184022346,1.13246499527372,-10.4295307880087));
#18802=CARTESIAN_POINT('Ctrl Pts',(3.21604453890365,1.13245719729423,-10.4295288654561));
#18803=CARTESIAN_POINT('Ctrl Pts',(3.21598952556157,1.13244148187604,-10.4295249912787));
#18804=CARTESIAN_POINT('Ctrl Pts',(3.21596181353872,1.13243356440476,-10.4295230396515));
#18805=CARTESIAN_POINT('Ctrl Pts',(3.2159059646182,1.13241760585583,-10.4295191063199));
#18806=CARTESIAN_POINT('Ctrl Pts',(3.21587782771689,1.1324095647431,-10.4295171246129));
#18807=CARTESIAN_POINT('Ctrl Pts',(3.21582111424197,1.13239335457936,-10.4295131300719));
#18808=CARTESIAN_POINT('Ctrl Pts',(3.21579253768988,1.13238518549874,-10.4295111172371));
#18809=CARTESIAN_POINT('Ctrl Pts',(3.21573492949764,1.13236871488414,-10.4295070593472));
#18810=CARTESIAN_POINT('Ctrl Pts',(3.2157058978657,1.13236041331489,-10.42950501429));
#18811=CARTESIAN_POINT('Ctrl Pts',(3.21564736342919,1.13234367300984,-10.4295008908144));
#18812=CARTESIAN_POINT('Ctrl Pts',(3.21561786063733,1.13233523423811,-10.4294988123941));
#18813=CARTESIAN_POINT('Ctrl Pts',(3.21555836708481,1.13231821460407,-10.4294946210004));
#18814=CARTESIAN_POINT('Ctrl Pts',(3.21552837633875,1.13230963370428,-10.4294925080251));
#18815=CARTESIAN_POINT('Ctrl Pts',(3.21546788933872,1.1322923246698,-10.429488246277));
#18816=CARTESIAN_POINT('Ctrl Pts',(3.21543739309562,1.13228359649434,-10.4294860975017));
#18817=CARTESIAN_POINT('Ctrl Pts',(3.21537587676924,1.1322659875289,-10.4294817628525));
#18818=CARTESIAN_POINT('Ctrl Pts',(3.21534485670016,1.13225710669674,-10.4294795769763));
#18819=CARTESIAN_POINT('Ctrl Pts',(3.21528227355241,1.13223918678984,-10.4294751667644));
#18820=CARTESIAN_POINT('Ctrl Pts',(3.21525071048926,1.13223014767076,-10.4294729424264));
#18821=CARTESIAN_POINT('Ctrl Pts',(3.21518702130536,1.13221190530096,-10.4294684538676));
#18822=CARTESIAN_POINT('Ctrl Pts',(3.21515489519293,1.13220270200114,-10.4294661896438));
#18823=CARTESIAN_POINT('Ctrl Pts',(3.2150900589162,1.13218412509967,-10.4294616198228));
#18824=CARTESIAN_POINT('Ctrl Pts',(3.21505734877094,1.13217475144912,-10.4294593142232));
#18825=CARTESIAN_POINT('Ctrl Pts',(3.2149913224468,1.13215582738234,-10.4294546600893));
#18826=CARTESIAN_POINT('Ctrl Pts',(3.21495800628006,1.13214627691214,-10.4294523115519));
#18827=CARTESIAN_POINT('Ctrl Pts',(3.21489074487493,1.13212699242798,-10.4294475699064));
#18828=CARTESIAN_POINT('Ctrl Pts',(3.21485679965562,1.13211725835873,-10.4294451767953));
#18829=CARTESIAN_POINT('Ctrl Pts',(3.21478825600129,1.13209759956896,-10.429440344287));
#18830=CARTESIAN_POINT('Ctrl Pts',(3.21475365756872,1.13208767478485,-10.4294379048856));
#18831=CARTESIAN_POINT('Ctrl Pts',(3.21468378213638,1.13206762709836,-10.4294329779954));
#18832=CARTESIAN_POINT('Ctrl Pts',(3.21464850516653,1.13205750413648,-10.429430490504));
#18833=CARTESIAN_POINT('Ctrl Pts',(3.21457724606094,1.13203705225551,-10.4294254655438));
#18834=CARTESIAN_POINT('Ctrl Pts',(3.2145412639418,1.13202672326902,-10.4294229280711));
#18835=CARTESIAN_POINT('Ctrl Pts',(3.21447950250827,1.13200899091429,-10.4294185724067));
#18836=CARTESIAN_POINT('Ctrl Pts',(3.21445372294447,1.13200158837816,-10.4294167542611));
#18837=CARTESIAN_POINT('Ctrl Pts',(3.21439966149649,1.13198606277194,-10.4294129413488));
#18838=CARTESIAN_POINT('Ctrl Pts',(3.21437137966856,1.13197793952392,-10.4294109465724));
#18839=CARTESIAN_POINT('Ctrl Pts',(3.21431203566975,1.13196089203638,-10.4294067607464));
#18840=CARTESIAN_POINT('Ctrl Pts',(3.21428097357151,1.13195196758098,-10.4294045696853));
#18841=CARTESIAN_POINT('Ctrl Pts',(3.21421575320059,1.1319332262017,-10.4293999689597));
#18842=CARTESIAN_POINT('Ctrl Pts',(3.21418159499902,1.1319234090085,-10.4293975592799));
#18843=CARTESIAN_POINT('Ctrl Pts',(3.21410982221765,1.13190277772899,-10.4293924958429));
#18844=CARTESIAN_POINT('Ctrl Pts',(3.21407220772992,1.13189196331316,-10.4293898420671));
#18845=CARTESIAN_POINT('Ctrl Pts',(3.21399310983144,1.13186921787157,-10.429384261254));
#18846=CARTESIAN_POINT('Ctrl Pts',(3.21395162654273,1.13185728644171,-10.4293813341944));
#18847=CARTESIAN_POINT('Ctrl Pts',(3.21386431640998,1.13183216909085,-10.4293751732267));
#18848=CARTESIAN_POINT('Ctrl Pts',(3.21381848970678,1.13181898266601,-10.4293719392903));
#18849=CARTESIAN_POINT('Ctrl Pts',(3.21372194394328,1.1317911957137,-10.4293651257208));
#18850=CARTESIAN_POINT('Ctrl Pts',(3.2136712250741,1.13177659456317,-10.4293615460533));
#18851=CARTESIAN_POINT('Ctrl Pts',(3.21356425701046,1.13174579238354,-10.4293539958449));
#18852=CARTESIAN_POINT('Ctrl Pts',(3.21350800804115,1.13172959056992,-10.4293500252599));
#18853=CARTESIAN_POINT('Ctrl Pts',(3.21338923377783,1.13169536953595,-10.4293416403688));
#18854=CARTESIAN_POINT('Ctrl Pts',(3.21332670877271,1.13167734932834,-10.4293372260073));
#18855=CARTESIAN_POINT('Ctrl Pts',(3.21319450451768,1.13163923513577,-10.4293278913432));
#18856=CARTESIAN_POINT('Ctrl Pts',(3.21312482563956,1.13161913989954,-10.4293229709707));
#18857=CARTESIAN_POINT('Ctrl Pts',(3.21297778778636,1.13157671979344,-10.4293125868531));
#18858=CARTESIAN_POINT('Ctrl Pts',(3.21290042924635,1.13155439342679,-10.4293071230237));
#18859=CARTESIAN_POINT('Ctrl Pts',(3.21268346681041,1.13149175202437,-10.429291797269));
#18860=CARTESIAN_POINT('Ctrl Pts',(3.21254386815168,1.1314514191043,-10.4292819343375));
#18861=CARTESIAN_POINT('Ctrl Pts',(3.20946721188047,1.13056189295936,-10.4290645184194));
#18862=CARTESIAN_POINT('Ctrl Pts',(3.20653357160968,1.12970132343361,-10.4288563207278));
#18863=CARTESIAN_POINT('Ctrl Pts',(3.19957106784925,1.12762942957046,-10.4283600901626));
#18864=CARTESIAN_POINT('Ctrl Pts',(3.19554535715557,1.12640794487554,-10.4280714987364));
#18865=CARTESIAN_POINT('Ctrl Pts',(3.18253528599118,1.12238417060919,-10.4271336143682));
#18866=CARTESIAN_POINT('Ctrl Pts',(3.17357821558417,1.11949583571058,-10.4264798085899));
#18867=CARTESIAN_POINT('Ctrl Pts',(3.09149691085084,1.09193726525416,-10.4204195290882));
#18868=CARTESIAN_POINT('Ctrl Pts',(3.02093453246352,1.06024479488837,-10.4147173204694));
#18869=CARTESIAN_POINT('Ctrl Pts',(2.88642961043058,0.983174122961987,-10.403369426687));
#18870=CARTESIAN_POINT('Ctrl Pts',(2.8228683152307,0.93785552016733,-10.3977556629365));
#18871=CARTESIAN_POINT('Ctrl Pts',(2.75434645728467,0.877936049323524,-10.3914726025992));
#18872=CARTESIAN_POINT('Ctrl Pts',(2.7446004613044,0.86912149234229,-10.3905723030498));
#18873=CARTESIAN_POINT('Ctrl Pts',(2.73009293144841,0.855552238370565,-10.389221445348));
#18874=CARTESIAN_POINT('Ctrl Pts',(2.72522153716476,0.850917056936007,-10.3887659629644));
#18875=CARTESIAN_POINT('Ctrl Pts',(2.71647260729152,0.842448419557565,-10.3879443656035));
#18876=CARTESIAN_POINT('Ctrl Pts',(2.71258151907054,0.83862930315528,-10.3875776567349));
#18877=CARTESIAN_POINT('Ctrl Pts',(2.70426746309748,0.830354898431243,-10.3867912024319));
#18878=CARTESIAN_POINT('Ctrl Pts',(2.69985329798885,0.825890972362758,-10.3863718461832));
#18879=CARTESIAN_POINT('Ctrl Pts',(2.68800218394732,0.813713030465413,-10.3852408418027));
#18880=CARTESIAN_POINT('Ctrl Pts',(2.68063435032583,0.805932350826788,-10.3845321458456));
#18881=CARTESIAN_POINT('Ctrl Pts',(2.64243016607699,0.76446840655799,-10.3808255239602));
#18882=CARTESIAN_POINT('Ctrl Pts',(2.61346400703542,0.729111240885981,-10.3779057225038));
#18883=CARTESIAN_POINT('Ctrl Pts',(2.53978414887236,0.627675753345193,-10.3700228969018));
#18884=CARTESIAN_POINT('Ctrl Pts',(2.49961464066712,0.558609729728254,-10.3651888901604));
#18885=CARTESIAN_POINT('Ctrl Pts',(2.45017983010922,0.449492132932587,-10.3576570484934));
#18886=CARTESIAN_POINT('Ctrl Pts',(2.4355098468213,0.412148085575772,-10.355093007927));
#18887=CARTESIAN_POINT('Ctrl Pts',(2.42066117638748,0.367826539462877,-10.3519864476286));
#18888=CARTESIAN_POINT('Ctrl Pts',(2.41860172422818,0.361501933869866,-10.3515416665765));
#18889=CARTESIAN_POINT('Ctrl Pts',(2.41551103640892,0.351729998438064,-10.3508516866609));
#18890=CARTESIAN_POINT('Ctrl Pts',(2.41444180320891,0.34829469462588,-10.3506086022224));
#18891=CARTESIAN_POINT('Ctrl Pts',(2.41249932019603,0.341951471292379,-10.3501586951136));
#18892=CARTESIAN_POINT('Ctrl Pts',(2.41162155800402,0.339045022177699,-10.3499521345814));
#18893=CARTESIAN_POINT('Ctrl Pts',(2.40964757276049,0.332416250311918,-10.3494800816322));
#18894=CARTESIAN_POINT('Ctrl Pts',(2.40855851318749,0.328691925112741,-10.349214193736));
#18895=CARTESIAN_POINT('Ctrl Pts',(2.40575315599553,0.318919249303073,-10.3485148743054));
#18896=CARTESIAN_POINT('Ctrl Pts',(2.40406687890954,0.312862514262297,-10.3480798356185));
#18897=CARTESIAN_POINT('Ctrl Pts',(2.39162515800205,0.266748794412219,-10.3447567741295));
#18898=CARTESIAN_POINT('Ctrl Pts',(2.38294509815073,0.226166371157745,-10.3417712626954));
#18899=CARTESIAN_POINT('Ctrl Pts',(2.36526271536538,0.115126766491998,-10.333576132822));
#18900=CARTESIAN_POINT('Ctrl Pts',(2.36045907240003,0.0441668277872275,
-10.3283200339461));
#18901=CARTESIAN_POINT('Ctrl Pts',(2.36324626146657,-0.0783134036235878,
-10.3194747209279));
#18902=CARTESIAN_POINT('Ctrl Pts',(2.36779877002687,-0.129705798184287,
-10.3158297201827));
#18903=CARTESIAN_POINT('Ctrl Pts',(2.37734497666333,-0.191208906323424,
-10.311553974777));
#18904=CARTESIAN_POINT('Ctrl Pts',(2.37912909944433,-0.201753806456629,
-10.3108238314908));
#18905=CARTESIAN_POINT('Ctrl Pts',(2.38216761299106,-0.218336223749617,
-10.3096799713337));
#18906=CARTESIAN_POINT('Ctrl Pts',(2.38332617151421,-0.22439047573263,-10.3092632600904));
#18907=CARTESIAN_POINT('Ctrl Pts',(2.38558646377435,-0.235719495316486,
-10.3084851040733));
#18908=CARTESIAN_POINT('Ctrl Pts',(2.38667696508284,-0.240996313106781,
-10.3081233147359));
#18909=CARTESIAN_POINT('Ctrl Pts',(2.3892023845812,-0.252806997371728,-10.3073149382348));
#18910=CARTESIAN_POINT('Ctrl Pts',(2.39065684135969,-0.259336532989567,
-10.3068689834752));
#18911=CARTESIAN_POINT('Ctrl Pts',(2.39450494226832,-0.275943904992911,
-10.3057369432805));
#18912=CARTESIAN_POINT('Ctrl Pts',(2.39697607705039,-0.286003342217437,
-10.3050533305825));
#18913=CARTESIAN_POINT('Ctrl Pts',(2.41612685914796,-0.359748551490968,
-10.3000543016118));
#18914=CARTESIAN_POINT('Ctrl Pts',(2.43798835149292,-0.421972621601104,
-10.295914200806));
#18915=CARTESIAN_POINT('Ctrl Pts',(2.50133953419122,-0.563194112899108,
-10.2863123921748));
#18916=CARTESIAN_POINT('Ctrl Pts',(2.54680839404966,-0.63994180278262,-10.2809323599877));
#18917=CARTESIAN_POINT('Ctrl Pts',(2.60825253629757,-0.721113044748076,
-10.2742771728897));
#18918=CARTESIAN_POINT('Ctrl Pts',(2.61620325781039,-0.731265517311831,
-10.2734252352242));
#18919=CARTESIAN_POINT('Ctrl Pts',(2.62724940399224,-0.744903239726535,
-10.2722507364804));
#18920=CARTESIAN_POINT('Ctrl Pts',(2.63020153461821,-0.74850410685098,-10.2719377025984));
#18921=CARTESIAN_POINT('Ctrl Pts',(2.6351842922247,-0.754508853025449,-10.2714105875542));
#18922=CARTESIAN_POINT('Ctrl Pts',(2.63720338307405,-0.756922321241501,
-10.2711973265075));
#18923=CARTESIAN_POINT('Ctrl Pts',(2.64107454456425,-0.761512113330287,
-10.270789022964));
#18924=CARTESIAN_POINT('Ctrl Pts',(2.64292489092453,-0.763689820257783,
-10.2705941150436));
#18925=CARTESIAN_POINT('Ctrl Pts',(2.64734500091451,-0.768853724101917,
-10.2701291644115));
#18926=CARTESIAN_POINT('Ctrl Pts',(2.64992183856594,-0.771833779529966,
-10.2698586210713));
#18927=CARTESIAN_POINT('Ctrl Pts',(2.65911808138479,-0.78236179932678,-10.2688950874734));
#18928=CARTESIAN_POINT('Ctrl Pts',(2.66581876783266,-0.789837737037588,
-10.2681966373822));
#18929=CARTESIAN_POINT('Ctrl Pts',(2.71604221672672,-0.844450760888732,
-10.2629936637172));
#18930=CARTESIAN_POINT('Ctrl Pts',(2.76325243813557,-0.888042645332946,
-10.2582838914359));
#18931=CARTESIAN_POINT('Ctrl Pts',(2.86230090177843,-0.965540015174516,
-10.2490537663441));
#18932=CARTESIAN_POINT('Ctrl Pts',(2.91374024413245,-0.999647077829176,
-10.2445477290543));
#18933=CARTESIAN_POINT('Ctrl Pts',(2.99853794554455,-1.04675002924201,-10.2376490200572));
#18934=CARTESIAN_POINT('Ctrl Pts',(3.03021947955894,-1.06252556601585,-10.235175725431));
#18935=CARTESIAN_POINT('Ctrl Pts',(3.07142952627252,-1.08077806658095,-10.2320862223871));
#18936=CARTESIAN_POINT('Ctrl Pts',(3.08034118993985,-1.08459427159758,-10.2314254271313));
#18937=CARTESIAN_POINT('Ctrl Pts',(3.09482989261593,-1.09058811613258,-10.2303625889635));
#18938=CARTESIAN_POINT('Ctrl Pts',(3.10037804191978,-1.09283395950394,-10.2299582902402));
#18939=CARTESIAN_POINT('Ctrl Pts',(3.11104761559829,-1.09705853641024,-10.2291858406323));
#18940=CARTESIAN_POINT('Ctrl Pts',(3.11616621260847,-1.0990439387123,-10.2288174774336));
#18941=CARTESIAN_POINT('Ctrl Pts',(3.12789786117898,-1.10350029159658,-10.2279781377109));
#18942=CARTESIAN_POINT('Ctrl Pts',(3.13451966402631,-1.10594773729313,-10.2275079426231));
#18943=CARTESIAN_POINT('Ctrl Pts',(3.15558235257554,-1.11351804882051,-10.2260232491265));
#18944=CARTESIAN_POINT('Ctrl Pts',(3.17010177858657,-1.118418860395,-10.2250159613216));
#18945=CARTESIAN_POINT('Ctrl Pts',(3.26358518269553,-1.14795351306181,-10.2186245553719));
#18946=CARTESIAN_POINT('Ctrl Pts',(3.34486469702706,-1.16449494768915,-10.2135142232708));
#18947=CARTESIAN_POINT('Ctrl Pts',(3.45198811315878,-1.17475646615739,-10.2068518494481));
#18948=CARTESIAN_POINT('Ctrl Pts',(3.4768301435026,-1.17634368906135,-10.2053100587526));
#18949=CARTESIAN_POINT('Ctrl Pts',(3.54582105443965,-1.1785600256522,-10.2009971443494));
#18950=CARTESIAN_POINT('Ctrl Pts',(3.58997887832675,-1.17749581089715,-10.1982018206856));
#18951=CARTESIAN_POINT('Ctrl Pts',(3.64349202072682,-1.17319051698836,-10.1946631559371));
#18952=CARTESIAN_POINT('Ctrl Pts',(3.65300657211122,-1.17230837916763,-10.19402811157));
#18953=CARTESIAN_POINT('Ctrl Pts',(3.66665642796826,-1.17087511753538,-10.1931072544528));
#18954=CARTESIAN_POINT('Ctrl Pts',(3.67080147375498,-1.17041760822355,-10.1928263162972));
#18955=CARTESIAN_POINT('Ctrl Pts',(3.67800869530667,-1.16958334437505,-10.1923354305104));
#18956=CARTESIAN_POINT('Ctrl Pts',(3.68107196558551,-1.16921655529465,-10.1921260317118));
#18957=CARTESIAN_POINT('Ctrl Pts',(3.68755939112151,-1.16841389678158,-10.1916809044332));
#18958=CARTESIAN_POINT('Ctrl Pts',(3.69098302676092,-1.16797501675569,-10.1914450236572));
#18959=CARTESIAN_POINT('Ctrl Pts',(3.70032082580992,-1.16673624651299,-10.1907991060319));
#18960=CARTESIAN_POINT('Ctrl Pts',(3.70623081811424,-1.16590645536315,-10.1903874871926));
#18961=CARTESIAN_POINT('Ctrl Pts',(3.73466520507534,-1.16169352071419,-10.188394344782));
#18962=CARTESIAN_POINT('Ctrl Pts',(3.75709300669732,-1.15770258127492,-10.1867837182827));
#18963=CARTESIAN_POINT('Ctrl Pts',(3.80078763369272,-1.14861285962786,-10.1835872535575));
#18964=CARTESIAN_POINT('Ctrl Pts',(3.8220571347356,-1.14356675299423,-10.1820036044542));
#18965=CARTESIAN_POINT('Ctrl Pts',(3.92442490187191,-1.11625021341218,-10.1742799219596));
#18966=CARTESIAN_POINT('Ctrl Pts',(4.00313175086993,-1.08592497142648,-10.1680515336758));
#18967=CARTESIAN_POINT('Ctrl Pts',(4.07801580972292,-1.04743320081398,-10.1620447146955));
#18968=CARTESIAN_POINT('Ctrl Pts',(4.07809254084581,-1.04739374895876,-10.1620385595981));
#18969=CARTESIAN_POINT('Ctrl Pts',(4.07816926754606,-1.0473542887167,-10.1620324047393));
#18970=CARTESIAN_POINT('',(2.85485462588355,0.95829519891841,-10.5));
#18971=CARTESIAN_POINT('Origin',(3.53951905042299,8.32667268468867E-16,
-10.5));
#18972=CARTESIAN_POINT('',(2.36176905131988,-4.59633220793995E-5,-10.4243671147817));
#18973=CARTESIAN_POINT('Ctrl Pts',(2.36176905131988,-4.59633220629141E-5,
-10.4243671147817));
#18974=CARTESIAN_POINT('Ctrl Pts',(2.36176719489522,0.0475224899499069,
-10.4276061092289));
#18975=CARTESIAN_POINT('Ctrl Pts',(2.36465152554336,0.0951870191939661,
-10.4308451036761));
#18976=CARTESIAN_POINT('Ctrl Pts',(2.37043099647105,0.14257694276026,-10.4340840981233));
#18977=CARTESIAN_POINT('Ctrl Pts',(2.3762006347751,0.189886241769647,-10.4373175820638));
#18978=CARTESIAN_POINT('Ctrl Pts',(2.38485558852686,0.236921338236482,-10.4405510660043));
#18979=CARTESIAN_POINT('Ctrl Pts',(2.39635290126212,0.283312932837025,-10.4437845499448));
#18980=CARTESIAN_POINT('Ctrl Pts',(2.40783503551282,0.329643282334564,-10.4470137651151));
#18981=CARTESIAN_POINT('Ctrl Pts',(2.42215196230261,0.375331301165948,-10.4502429802854));
#18982=CARTESIAN_POINT('Ctrl Pts',(2.43920948510574,0.420016574638867,-10.4534721954557));
#18983=CARTESIAN_POINT('Ctrl Pts',(2.45625098279648,0.464659867424579,-10.4566983768598));
#18984=CARTESIAN_POINT('Ctrl Pts',(2.47602778023458,0.508301788416858,-10.4599245582639));
#18985=CARTESIAN_POINT('Ctrl Pts',(2.4983962137101,0.550598130558847,-10.463150739668));
#18986=CARTESIAN_POINT('Ctrl Pts',(2.52075937488268,0.592884503333545,-10.466376160652));
#18987=CARTESIAN_POINT('Ctrl Pts',(2.54571272466943,0.633825450117072,-10.469601581636));
#18988=CARTESIAN_POINT('Ctrl Pts',(2.57306577657067,0.673099644896752,-10.47282700262));
#18989=CARTESIAN_POINT('Ctrl Pts',(2.60041300765289,0.712365481999164,-10.4760517372239));
#18990=CARTESIAN_POINT('Ctrl Pts',(2.63015861772617,0.749964838514729,-10.4792764718278));
#18991=CARTESIAN_POINT('Ctrl Pts',(2.66206929628169,0.785606129976958,-10.4825012064317));
#18992=CARTESIAN_POINT('Ctrl Pts',(2.69400664615116,0.821277210842526,-10.485728636306));
#18993=CARTESIAN_POINT('Ctrl Pts',(2.72811232122637,0.854986562867321,-10.4889560661803));
#18994=CARTESIAN_POINT('Ctrl Pts',(2.76411439808519,0.886477685919338,-10.4921834960547));
#18995=CARTESIAN_POINT('Ctrl Pts',(2.79317884324904,0.911900442019834,-10.4947889973698));
#18996=CARTESIAN_POINT('Ctrl Pts',(2.82347841660538,0.935878125041895,-10.4973944986849));
#18997=CARTESIAN_POINT('Ctrl Pts',(2.85485462588355,0.958295198918412,-10.5));
#18998=CARTESIAN_POINT('Ctrl Pts',(4.07816926754758,-1.04735428871592,-10.2615635160918));
#18999=CARTESIAN_POINT('Ctrl Pts',(4.07189768950143,-1.05057973679272,-10.2620425082136));
#19000=CARTESIAN_POINT('Ctrl Pts',(4.06559906735751,-1.05374785987524,-10.2625215003355));
#19001=CARTESIAN_POINT('Ctrl Pts',(4.0592745442172,-1.05685821621007,-10.2630004924573));
#19002=CARTESIAN_POINT('Ctrl Pts',(4.01581207835197,-1.0782327535518,-10.2662921522843));
#19003=CARTESIAN_POINT('Ctrl Pts',(3.97093229426151,-1.09696933473833,-10.2695838121113));
#19004=CARTESIAN_POINT('Ctrl Pts',(3.92498877417435,-1.11288281259576,-10.2728754719383));
#19005=CARTESIAN_POINT('Ctrl Pts',(3.88064510817398,-1.12824214826868,-10.2760525089541));
#19006=CARTESIAN_POINT('Ctrl Pts',(3.83531115241496,-1.14097157503757,-10.2792295459699));
#19007=CARTESIAN_POINT('Ctrl Pts',(3.7893282018029,-1.1509519757083,-10.2824065829858));
#19008=CARTESIAN_POINT('Ctrl Pts',(3.74338991283836,-1.16092268276149,-10.2855805342556));
#19009=CARTESIAN_POINT('Ctrl Pts',(3.69680441740098,-1.16814953187371,-10.2887544855254));
#19010=CARTESIAN_POINT('Ctrl Pts',(3.64992723619355,-1.17256347163591,-10.2919284367952));
#19011=CARTESIAN_POINT('Ctrl Pts',(3.60307513846398,-1.17697504954619,-10.2951006897176));
#19012=CARTESIAN_POINT('Ctrl Pts',(3.55593221637032,-1.17857664819459,-10.2982729426401));
#19013=CARTESIAN_POINT('Ctrl Pts',(3.50886054014208,-1.17735089002699,-10.3014451955625));
#19014=CARTESIAN_POINT('Ctrl Pts',(3.46179352166238,-1.17612525314832,-10.3046171345901));
#19015=CARTESIAN_POINT('Ctrl Pts',(3.41479828999723,-1.17207283170602,-10.3077890736177));
#19016=CARTESIAN_POINT('Ctrl Pts',(3.36823563163836,-1.16522832653066,-10.3109610126454));
#19017=CARTESIAN_POINT('Ctrl Pts',(3.321625526321,-1.15837684686192,-10.3141361838522));
#19018=CARTESIAN_POINT('Ctrl Pts',(3.27544942398851,-1.14872768936456,-10.3173113550591));
#19019=CARTESIAN_POINT('Ctrl Pts',(3.2300597421721,-1.13636701775301,-10.320486526266));
#19020=CARTESIAN_POINT('Ctrl Pts',(3.18464214351442,-1.12399874373287,-10.3236636503562));
#19021=CARTESIAN_POINT('Ctrl Pts',(3.14001245434683,-1.10891581454595,-10.3268407744463));
#19022=CARTESIAN_POINT('Ctrl Pts',(3.09650622236022,-1.09125372699104,-10.3300178985365));
#19023=CARTESIAN_POINT('Ctrl Pts',(3.05292222210614,-1.07356006809826,-10.3332007018001));
#19024=CARTESIAN_POINT('Ctrl Pts',(3.01046618442413,-1.05327829596091,-10.3363835050637));
#19025=CARTESIAN_POINT('Ctrl Pts',(2.96945029737604,-1.0305904517797,-10.3395663083272));
#19026=CARTESIAN_POINT('Ctrl Pts',(2.95899478795995,-1.02480701064166,-10.3403776483198));
#19027=CARTESIAN_POINT('Ctrl Pts',(2.94863271329714,-1.01886743979341,-10.3411889883123));
#19028=CARTESIAN_POINT('Ctrl Pts',(2.93836892723928,-1.01277519316787,-10.3420003283049));
#19029=CARTESIAN_POINT('Ctrl Pts',(2.8967280706936,-0.988058547054513,-10.3452919881319));
#19030=CARTESIAN_POINT('Ctrl Pts',(2.85650517515445,-0.960704585188008,
-10.3485836479588));
#19031=CARTESIAN_POINT('Ctrl Pts',(2.81805680175141,-0.930906701147725,
-10.3518753077858));
#19032=CARTESIAN_POINT('Ctrl Pts',(2.78140908255892,-0.902504342603417,
-10.3550128091764));
#19033=CARTESIAN_POINT('Ctrl Pts',(2.74637389179197,-0.871882272761917,
-10.3581503105669));
#19034=CARTESIAN_POINT('Ctrl Pts',(2.71323359960642,-0.83925408326016,-10.3612878119575));
#19035=CARTESIAN_POINT('Ctrl Pts',(2.68012580534745,-0.806657889508507,
-10.3644222366615));
#19036=CARTESIAN_POINT('Ctrl Pts',(2.64890964063671,-0.772059864136999,
-10.3675566613655));
#19037=CARTESIAN_POINT('Ctrl Pts',(2.61983368595614,-0.735713186564894,
-10.3706910860696));
#19038=CARTESIAN_POINT('Ctrl Pts',(2.5907727637071,-0.699385300428803,-10.3738238902585));
#19039=CARTESIAN_POINT('Ctrl Pts',(2.56385021773247,-0.661310996241715,
-10.3769566944474));
#19040=CARTESIAN_POINT('Ctrl Pts',(2.53927510798554,-0.62177738630251,-10.3800894986363));
#19041=CARTESIAN_POINT('Ctrl Pts',(2.51470131136347,-0.582245888767549,
-10.3832221354297));
#19042=CARTESIAN_POINT('Ctrl Pts',(2.4924750007092,-0.541255726359354,-10.3863547722231));
#19043=CARTESIAN_POINT('Ctrl Pts',(2.47276095243106,-0.499121451020331,
-10.3894874090164));
#19044=CARTESIAN_POINT('Ctrl Pts',(2.45302344007767,-0.456937026579845,
-10.3926237743401));
#19045=CARTESIAN_POINT('Ctrl Pts',(2.43580439438563,-0.413606292013472,
-10.3957601396637));
#19046=CARTESIAN_POINT('Ctrl Pts',(2.42122088960644,-0.369464864384054,
-10.3988965049874));
#19047=CARTESIAN_POINT('Ctrl Pts',(2.40662720568347,-0.325292626469616,
-10.4020350594634));
#19048=CARTESIAN_POINT('Ctrl Pts',(2.39467286227741,-0.280309123097656,
-10.4051736139393));
#19049=CARTESIAN_POINT('Ctrl Pts',(2.38542429928129,-0.234862444607861,
-10.4083121684153));
#19050=CARTESIAN_POINT('Ctrl Pts',(2.37615682954507,-0.18932285995102,-10.4114571390052));
#19051=CARTESIAN_POINT('Ctrl Pts',(2.36960624399691,-0.14331877673319,-10.4146021095951));
#19052=CARTESIAN_POINT('Ctrl Pts',(2.36578718165589,-0.0972037177298007,
-10.417747080185));
#19053=CARTESIAN_POINT('Ctrl Pts',(2.36447039875689,-0.0813036051734252,
-10.4188314415075));
#19054=CARTESIAN_POINT('Ctrl Pts',(2.36347788782083,-0.0653902887482771,
-10.4199158028299));
#19055=CARTESIAN_POINT('Ctrl Pts',(2.36280881668566,-0.0494781600085864,
-10.4210001641524));
#19056=CARTESIAN_POINT('Ctrl Pts',(2.36211632627601,-0.0330090643176043,
-10.4221224810136));
#19057=CARTESIAN_POINT('Ctrl Pts',(2.36176969458343,-0.0165285106694148,
-10.4232447978749));
#19058=CARTESIAN_POINT('Ctrl Pts',(2.36176905131991,-4.59639904046127E-5,
-10.4243671147362));
#19059=CARTESIAN_POINT('Ctrl Pts',(3.03016972909157,-1.05969203810452,0.166133550473327));
#19060=CARTESIAN_POINT('Ctrl Pts',(2.67950307502106,-0.891141349940568,
0.139800271857472));
#19061=CARTESIAN_POINT('Ctrl Pts',(2.16444303486989,-0.1817253130263,0.0871337146257638));
#19062=CARTESIAN_POINT('Ctrl Pts',(2.63688451788926,1.05482934048912,0.00813387877820125));
#19063=CARTESIAN_POINT('Ctrl Pts',(3.92934827499653,1.33109899959936,-0.0708659570693613));
#19064=CARTESIAN_POINT('Ctrl Pts',(4.86756771448359,0.401458164283287,-0.149865792916923));
#19065=CARTESIAN_POINT('Ctrl Pts',(4.60127863509294,-0.893258821518505,
-0.228865628764486));
#19066=CARTESIAN_POINT('Ctrl Pts',(3.37159135201681,-1.37714798759902,-0.307865464612048));
#19067=CARTESIAN_POINT('Ctrl Pts',(2.29433432465055,-0.611917524973032,
-0.386865300459611));
#19068=CARTESIAN_POINT('Ctrl Pts',(2.34667400544937,0.708575406788336,-0.465865136307173));
#19069=CARTESIAN_POINT('Ctrl Pts',(3.48119555264166,1.38617687493562,-0.544864972154736));
#19070=CARTESIAN_POINT('Ctrl Pts',(4.66861629168543,0.806262653193108,-0.623864808002299));
#19071=CARTESIAN_POINT('Ctrl Pts',(4.83171763843987,-0.505117703190085,
-0.702864643849861));
#19072=CARTESIAN_POINT('Ctrl Pts',(3.82252286862625,-1.35824167832699,-0.781864479697424));
#19073=CARTESIAN_POINT('Ctrl Pts',(2.55658660705165,-0.979163204938215,
-0.860864315544985));
#19074=CARTESIAN_POINT('Ctrl Pts',(2.18237343206576,0.288222479142872,-0.93986415139255));
#19075=CARTESIAN_POINT('Ctrl Pts',(3.03937391325844,1.29412906681933,-1.01886398724011));
#19076=CARTESIAN_POINT('Ctrl Pts',(4.35010972888344,1.12599234088644,-1.09786382308768));
#19077=CARTESIAN_POINT('Ctrl Pts',(4.92547145397695,-0.0636538642554802,
-1.17686365893524));
#19078=CARTESIAN_POINT('Ctrl Pts',(4.24348620505496,-1.19555258043752,-1.2558634947828));
#19079=CARTESIAN_POINT('Ctrl Pts',(2.9228564643445,-1.24283671611121,-1.33486333063036));
#19080=CARTESIAN_POINT('Ctrl Pts',(2.16166784335581,-0.16260956886651,-1.41386316647793));
#19081=CARTESIAN_POINT('Ctrl Pts',(2.65047666571883,1.06513822635395,-1.49286300232549));
#19082=CARTESIAN_POINT('Ctrl Pts',(3.94583171405088,1.3265842755385,-1.57186283817305));
#19083=CARTESIAN_POINT('Ctrl Pts',(4.87257672678285,0.384542646461178,-1.65086267402061));
#19084=CARTESIAN_POINT('Ctrl Pts',(4.58996134785928,-0.90635908631751,-1.72986250986818));
#19085=CARTESIAN_POINT('Ctrl Pts',(3.35437647024072,-1.37500474221842,-1.80886234571574));
#19086=CARTESIAN_POINT('Ctrl Pts',(2.28675439453907,-0.596235299315049,
-1.8878621815633));
#19087=CARTESIAN_POINT('Ctrl Pts',(2.35565025061696,0.723443487680916,-1.96686201741086));
#19088=CARTESIAN_POINT('Ctrl Pts',(3.49856117658577,1.38680866306196,-2.04586185325842));
#19089=CARTESIAN_POINT('Ctrl Pts',(4.67862940733048,0.792050130990127,-2.12486168910599));
#19090=CARTESIAN_POINT('Ctrl Pts',(4.825287778842,-0.521262498390872,-2.20386152495355));
#19091=CARTESIAN_POINT('Ctrl Pts',(3.80548666508593,-1.36168169672898,-2.28286136080111));
#19092=CARTESIAN_POINT('Ctrl Pts',(2.5443976431265,-0.966772568896671,-2.36186119664867));
#19093=CARTESIAN_POINT('Ctrl Pts',(2.18609057479567,0.305200223776868,-2.44086103249624));
#19094=CARTESIAN_POINT('Ctrl Pts',(3.05562444562635,1.30029297725059,-2.5198608683438));
#19095=CARTESIAN_POINT('Ctrl Pts',(4.36415130109645,1.11574973286296,-2.59886070419136));
#19096=CARTESIAN_POINT('Ctrl Pts',(4.92456530437952,-0.0810104291810054,
-2.67786054003893));
#19097=CARTESIAN_POINT('Ctrl Pts',(4.22845447176036,-1.20427729384166,-2.75686037588648));
#19098=CARTESIAN_POINT('Ctrl Pts',(2.90733601591503,-1.23501434247363,-2.83586021173405));
#19099=CARTESIAN_POINT('Ctrl Pts',(2.15973897238825,-0.14533668323525,-2.91486004758161));
#19100=CARTESIAN_POINT('Ctrl Pts',(2.66388924862181,1.07619155610565,-2.99385988342918));
#19101=CARTESIAN_POINT('Ctrl Pts',(3.9624177558182,1.32139036632271,-3.07285971927674));
#19102=CARTESIAN_POINT('Ctrl Pts',(4.87728923720612,0.36781346167547,-3.1518595551243));
#19103=CARTESIAN_POINT('Ctrl Pts',(4.57852510200631,-0.919446703190933,
-3.23085939097186));
#19104=CARTESIAN_POINT('Ctrl Pts',(3.33716651933725,-1.37257760013728,-3.30985922681943));
#19105=CARTESIAN_POINT('Ctrl Pts',(2.27938374158492,-0.5804953218201,-3.38885906266698));
#19106=CARTESIAN_POINT('Ctrl Pts',(2.36480560961949,0.73821687005311,-3.46785889851455));
#19107=CARTESIAN_POINT('Ctrl Pts',(3.51593673409344,1.38721292150555,-3.54685873436211));
#19108=CARTESIAN_POINT('Ctrl Pts',(4.6884619210917,0.777718519243937,-3.62585857020968));
#19109=CARTESIAN_POINT('Ctrl Pts',(4.81865711520746,-0.537328229720796,
-3.70485840605724));
#19110=CARTESIAN_POINT('Ctrl Pts',(3.78840821414682,-1.36490658999665,-3.7838582419048));
#19111=CARTESIAN_POINT('Ctrl Pts',(2.53236510967047,-0.954230975635406,
-3.86285807775236));
#19112=CARTESIAN_POINT('Ctrl Pts',(2.19001996763953,0.322130471706748,-3.94185791359992));
#19113=CARTESIAN_POINT('Ctrl Pts',(3.07195098873404,1.30625262599693,-4.02085774944749));
#19114=CARTESIAN_POINT('Ctrl Pts',(4.37806342637599,1.10533214229617,-4.09985758529504));
#19115=CARTESIAN_POINT('Ctrl Pts',(4.92344182255072,-0.0983543391097721,
-4.17885742114262));
#19116=CARTESIAN_POINT('Ctrl Pts',(4.21331461435868,-1.21281299187304,-4.25785725699017));
#19117=CARTESIAN_POINT('Ctrl Pts',(2.89191478044192,-1.22699817633838,-4.33685709283774));
#19118=CARTESIAN_POINT('Ctrl Pts',(2.15802662474044,-0.128040981787732,
-4.41585692868529));
#19119=CARTESIAN_POINT('Ctrl Pts',(2.67743924402949,1.08707599671962,-4.49485676453287));
#19120=CARTESIAN_POINT('Ctrl Pts',(3.9789374320634,1.31598909612198,-4.57385660038042));
#19121=CARTESIAN_POINT('Ctrl Pts',(4.88179181429946,0.351026555392716,-4.65285643622799));
#19122=CARTESIAN_POINT('Ctrl Pts',(4.56692580665797,-0.93239003237817,-4.73185627207555));
#19123=CARTESIAN_POINT('Ctrl Pts',(3.31998832335595,-1.36993506236933,-4.81085610792312));
#19124=CARTESIAN_POINT('Ctrl Pts',(2.27221083923482,-0.564664248107207,
-4.88985594377067));
#19125=CARTESIAN_POINT('Ctrl Pts',(2.37414531422868,0.752874405345241,-4.96885577961824));
#19126=CARTESIAN_POINT('Ctrl Pts',(3.53331599231234,1.38739948728025,-5.0478556154658));
#19127=CARTESIAN_POINT('Ctrl Pts',(4.6981141334156,0.763264861565624,-5.12685545131336));
#19128=CARTESIAN_POINT('Ctrl Pts',(4.8118257188344,-0.553309639127398,-5.20585528716093));
#19129=CARTESIAN_POINT('Ctrl Pts',(3.77129070550129,-1.3679172910442,-5.28485512300849));
#19130=CARTESIAN_POINT('Ctrl Pts',(2.52049062698915,-0.941539636695861,
-5.36385495885605));
#19131=CARTESIAN_POINT('Ctrl Pts',(2.19416113484018,0.339010168304841,-5.44285479470361));
#19132=CARTESIAN_POINT('Ctrl Pts',(3.08835090641897,1.31200728697343,-5.52185463055117));
#19133=CARTESIAN_POINT('Ctrl Pts',(4.39184396046197,1.09474109403205,-5.60085446639874));
#19134=CARTESIAN_POINT('Ctrl Pts',(4.92210116432083,-0.115682814476576,
-5.6798543022463));
#19135=CARTESIAN_POINT('Ctrl Pts',(4.19806901948488,-1.22115836543997,-5.75885413809386));
#19136=CARTESIAN_POINT('Ctrl Pts',(2.87659517229037,-1.21878945968409,-5.83785397394143));
#19137=CARTESIAN_POINT('Ctrl Pts',(2.15653107210394,-0.110725187109488,
-5.91685380978898));
#19138=CARTESIAN_POINT('Ctrl Pts',(2.69112452400181,1.09778984453947,-5.99585364563655));
#19139=CARTESIAN_POINT('Ctrl Pts',(3.99538815120739,1.31038131022442,-6.07485348148411));
#19140=CARTESIAN_POINT('Ctrl Pts',(4.88608375104936,0.334184563172007,-6.15385331733167));
#19141=CARTESIAN_POINT('Ctrl Pts',(4.55516528229729,-0.945187043349074,
-6.23285315317924));
#19142=CARTESIAN_POINT('Ctrl Pts',(3.30284457791926,-1.36707754326538,-6.3118529890268));
#19143=CARTESIAN_POINT('Ctrl Pts',(2.26523681318173,-0.548744562694544,
-6.39085282487436));
#19144=CARTESIAN_POINT('Ctrl Pts',(2.38366789874921,0.76741379347118,-6.46985266072193));
#19145=CARTESIAN_POINT('Ctrl Pts',(3.55069622396548,1.38736833105958,-6.54885249656949));
#19146=CARTESIAN_POINT('Ctrl Pts',(4.70758452958949,0.748691426166348,-6.62785233241704));
#19147=CARTESIAN_POINT('Ctrl Pts',(4.80479466176584,-0.569204218691696,
-6.70685216826462));
#19148=CARTESIAN_POINT('Ctrl Pts',(3.7541368253653,-1.37071332740082,-6.78585200411217));
#19149=CARTESIAN_POINT('Ctrl Pts',(2.50877605852413,-0.928700543709767,
-6.86485183995974));
#19150=CARTESIAN_POINT('Ctrl Pts',(2.19851342653132,0.355836664674037,-6.9438516758073));
#19151=CARTESIAN_POINT('Ctrl Pts',(3.10482162507327,1.31755605711095,-7.02285151165486));
#19152=CARTESIAN_POINT('Ctrl Pts',(4.40549074080085,1.08397825010448,-7.10185134750243));
#19153=CARTESIAN_POINT('Ctrl Pts',(4.92054354007692,-0.132993135956621,
-7.18085118334998));
#19154=CARTESIAN_POINT('Ctrl Pts',(4.1827200796015,-1.22931210491848,-7.25985101919756));
#19155=CARTESIAN_POINT('Ctrl Pts',(2.86137959553775,-1.21038948068935,-7.3388508550451));
#19156=CARTESIAN_POINT('Ctrl Pts',(2.15525254917303,-0.0933920165355914,
-7.41785069089267));
#19157=CARTESIAN_POINT('Ctrl Pts',(2.70494294093347,1.10833141826107,-7.49685052674024));
#19158=CARTESIAN_POINT('Ctrl Pts',(4.01176733166974,1.30456788864948,-7.5758503625878));
#19159=CARTESIAN_POINT('Ctrl Pts',(4.89016437393018,0.31729012799526,-7.65485019843536));
#19160=CARTESIAN_POINT('Ctrl Pts',(4.5432453744814,-0.957835727892178,-7.73385003428293));
#19161=CARTESIAN_POINT('Ctrl Pts',(3.28573797336276,-1.36400549125164,-7.81284987013048));
#19162=CARTESIAN_POINT('Ctrl Pts',(2.25846275784679,-0.532738763826387,
-7.89184970597805));
#19163=CARTESIAN_POINT('Ctrl Pts',(2.39337186881909,0.781832752788139,-7.97084954182562));
#19164=CARTESIAN_POINT('Ctrl Pts',(3.56807470160707,1.38711945774027,-8.04984937767317));
#19165=CARTESIAN_POINT('Ctrl Pts',(4.71687162343945,0.734000500013747,-8.12884921352074));
#19166=CARTESIAN_POINT('Ctrl Pts',(4.79756504737693,-0.585009474080196,
-8.2078490493683));
#19167=CARTESIAN_POINT('Ctrl Pts',(3.73694926565633,-1.37329426034113,-8.28684888521586));
#19168=CARTESIAN_POINT('Ctrl Pts',(2.49722324263719,-0.915715711394235,
-8.36584872106343));
#19169=CARTESIAN_POINT('Ctrl Pts',(2.20307615968452,0.372607320078181,-8.44484855691098));
#19170=CARTESIAN_POINT('Ctrl Pts',(3.12136056003786,1.32289806600452,-8.52384839275855));
#19171=CARTESIAN_POINT('Ctrl Pts',(4.4190016257151,1.07304529883463,-8.60284822860612));
#19172=CARTESIAN_POINT('Ctrl Pts',(4.91876919447073,-0.150282585796148,
-8.68184806445366));
#19173=CARTESIAN_POINT('Ctrl Pts',(4.16727020297665,-1.23727293318732,-8.76084790030125));
#19174=CARTESIAN_POINT('Ctrl Pts',(2.84627043871991,-1.2017995529258,-8.83984773614879));
#19175=CARTESIAN_POINT('Ctrl Pts',(2.15419125509278,-0.0760441989173671,
-8.91884757199636));
#19176=CARTESIAN_POINT('Ctrl Pts',(2.71889232916227,1.11869908033215,-8.99784740784393));
#19177=CARTESIAN_POINT('Ctrl Pts',(4.02807239770252,1.29854971189147,-9.07684724369149));
#19178=CARTESIAN_POINT('Ctrl Pts',(4.89403305283643,0.300345961546974,-9.15584707953904));
#19179=CARTESIAN_POINT('Ctrl Pts',(4.53116793426698,-0.970334216088902,
-9.23484691538663));
#19180=CARTESIAN_POINT('Ctrl Pts',(3.2686712313047,-1.36071916966539,-9.31384675123416));
#19181=CARTESIAN_POINT('Ctrl Pts',(2.25188966568679,-0.516649779321854,
-9.39284658708175));
#19182=CARTESIAN_POINT('Ctrl Pts',(2.4032558358579,0.796129811879359,-9.4718464229293));
#19183=CARTESIAN_POINT('Ctrl Pts',(3.58544844273731,1.38665140132039,-9.55084625877686));
#19184=CARTESIAN_POINT('Ctrl Pts',(4.72597444318006,0.719197251069897,-9.62984609462442));
#19185=CARTESIAN_POINT('Ctrl Pts',(4.79013708657144,-0.600728369415522,
-9.70884593047199));
#19186=CARTESIAN_POINT('Ctrl Pts',(3.71973248027576,-1.37564932984407,-9.78784576631954));
#19187=CARTESIAN_POINT('Ctrl Pts',(2.48583065115498,-0.902606872160507,
-9.86684560216712));
#19188=CARTESIAN_POINT('Ctrl Pts',(2.20785497294659,0.389356961444151,-9.94584543801465));
#19189=CARTESIAN_POINT('Ctrl Pts',(3.13795302964717,1.32796122782191,-10.0248452738622));
#19190=CARTESIAN_POINT('Ctrl Pts',(4.43239748225584,1.06207949035224,-10.1038451097098));
#19191=CARTESIAN_POINT('Ctrl Pts',(4.91673468640922,-0.167806447366913,
-10.1828449455574));
#19192=CARTESIAN_POINT('Ctrl Pts',(4.15180495687604,-1.24454704202974,-10.2618447814049));
#19193=CARTESIAN_POINT('Ctrl Pts',(2.83111201811591,-1.1939738328192,-10.3408446172525));
#19194=CARTESIAN_POINT('Ctrl Pts',(2.15359519437813,-0.0566474417221517,
-10.4198505843376));
#19195=CARTESIAN_POINT('Ctrl Pts',(2.53953407659744,0.730669948020605,-10.4725232728068));
#19196=CARTESIAN_POINT('Ctrl Pts',(2.85623945459991,0.956824401315803,-10.4988626826603));
#19197=CARTESIAN_POINT('Ctrl Pts',(2.98834871728712,-1.14669989573515,0.110397971418231));
#19198=CARTESIAN_POINT('Ctrl Pts',(2.60888996776239,-0.964310060203871,
0.0840646928023764));
#19199=CARTESIAN_POINT('Ctrl Pts',(2.05154002730692,-0.196646185879096,
0.0313981355706681));
#19200=CARTESIAN_POINT('Ctrl Pts',(2.56277213988209,1.14143793787563,-0.0476017002768946));
#19201=CARTESIAN_POINT('Ctrl Pts',(3.961355881407,1.44039119778986,-0.126601536124457));
#19202=CARTESIAN_POINT('Ctrl Pts',(4.97660945957003,0.434420585011763,-0.205601371972019));
#19203=CARTESIAN_POINT('Ctrl Pts',(4.68845625222988,-0.966601390468067,
-0.284601207819581));
#19204=CARTESIAN_POINT('Ctrl Pts',(3.35780335630695,-1.49022111803005,-0.363601043667145));
#19205=CARTESIAN_POINT('Ctrl Pts',(2.19209626732059,-0.662160077507238,
-0.442600879514707));
#19206=CARTESIAN_POINT('Ctrl Pts',(2.24873338863196,0.766754222800465,-0.521600715362269));
#19207=CARTESIAN_POINT('Ctrl Pts',(3.47640680042968,1.49999133786299,-0.600600551209832));
#19208=CARTESIAN_POINT('Ctrl Pts',(4.76132278421946,0.872462250452896,-0.679600387057394));
#19209=CARTESIAN_POINT('Ctrl Pts',(4.9378158506882,-0.546591270628113,-0.758600222904958));
#19210=CARTESIAN_POINT('Ctrl Pts',(3.8457593892735,-1.4697624733565,-0.837600058752518));
#19211=CARTESIAN_POINT('Ctrl Pts',(2.47588122943425,-1.05955910267923,-0.916599894600083));
#19212=CARTESIAN_POINT('Ctrl Pts',(2.07094263094616,0.31188748702201,-0.995599730447643));
#19213=CARTESIAN_POINT('Ctrl Pts',(2.99830862700141,1.4003857843869,-1.0745995662952));
#19214=CARTESIAN_POINT('Ctrl Pts',(4.41666468618437,1.21844390017556,-1.15359940214277));
#19215=CARTESIAN_POINT('Ctrl Pts',(5.03926748629117,-0.0688802754764985,
-1.23259923799033));
#19216=CARTESIAN_POINT('Ctrl Pts',(4.30128665250989,-1.29371550416271,-1.31159907383789));
#19217=CARTESIAN_POINT('Ctrl Pts',(2.87222431031641,-1.34488198602467,-1.39059890968545));
#19218=CARTESIAN_POINT('Ctrl Pts',(2.04853697386742,-0.175960910302112,
-1.46959874553302));
#19219=CARTESIAN_POINT('Ctrl Pts',(2.57748029464644,1.15259325274191,-1.54859858138058));
#19220=CARTESIAN_POINT('Ctrl Pts',(3.97919272189017,1.43550578445872,-1.62759841722814));
#19221=CARTESIAN_POINT('Ctrl Pts',(4.98202974553497,0.416116189182186,-1.70659825307571));
#19222=CARTESIAN_POINT('Ctrl Pts',(4.67620973944672,-0.980777275290219,
-1.78559808892326));
#19223=CARTESIAN_POINT('Ctrl Pts',(3.33917501672534,-1.4879018977603,-1.86459792477083));
#19224=CARTESIAN_POINT('Ctrl Pts',(2.18389397386554,-0.645190235439661,
-1.94359776061839));
#19225=CARTESIAN_POINT('Ctrl Pts',(2.25844664401903,0.782843073330851,-2.02259759646596));
#19226=CARTESIAN_POINT('Ctrl Pts',(3.49519825912716,1.50067500005214,-2.10159743231351));
#19227=CARTESIAN_POINT('Ctrl Pts',(4.7721580441377,0.857082784398361,-2.18059726816108));
#19228=CARTESIAN_POINT('Ctrl Pts',(4.9308580562863,-0.564061662315234,-2.25959710400864));
#19229=CARTESIAN_POINT('Ctrl Pts',(3.82732439861496,-1.47348494045169,-2.3385969398562));
#19230=CARTESIAN_POINT('Ctrl Pts',(2.46269146942899,-1.04615111191774,-2.41759677570377));
#19231=CARTESIAN_POINT('Ctrl Pts',(2.07496497614415,0.330259218904082,-2.49659661155133));
#19232=CARTESIAN_POINT('Ctrl Pts',(3.01589343758964,1.40705579340337,-2.5755964473989));
#19233=CARTESIAN_POINT('Ctrl Pts',(4.43185916610274,1.20736030500805,-2.65459628324645));
#19234=CARTESIAN_POINT('Ctrl Pts',(5.03828693570521,-0.0876619313489172,
-2.73359611909402));
#19235=CARTESIAN_POINT('Ctrl Pts',(4.28502071261241,-1.30315657533346,-2.81259595494158));
#19236=CARTESIAN_POINT('Ctrl Pts',(2.85542952847803,-1.3364173427962,-2.89159579078914));
#19237=CARTESIAN_POINT('Ctrl Pts',(2.04644972959469,-0.157269804357935,
-2.9705956266367));
#19238=CARTESIAN_POINT('Ctrl Pts',(2.59199414099363,1.16455413535502,-3.04959546248426));
#19239=CARTESIAN_POINT('Ctrl Pts',(3.99714058946054,1.42988542029437,-3.12859529833183));
#19240=CARTESIAN_POINT('Ctrl Pts',(4.98712918482176,0.398013425587001,-3.20759513417939));
#19241=CARTESIAN_POINT('Ctrl Pts',(4.66383450073996,-0.994939473706866,
-3.28659497002696));
#19242=CARTESIAN_POINT('Ctrl Pts',(3.32055201287423,-1.4852754709577,-3.36559480587451));
#19243=CARTESIAN_POINT('Ctrl Pts',(2.17591814063276,-0.628157899720108,
-3.44459464172208));
#19244=CARTESIAN_POINT('Ctrl Pts',(2.26835371969396,0.798829449954148,-3.52359447756964));
#19245=CARTESIAN_POINT('Ctrl Pts',(3.51400046700072,1.50111245083826,-3.6025943134172));
#19246=CARTESIAN_POINT('Ctrl Pts',(4.78279787354038,0.841574450746565,-3.68159414926477));
#19247=CARTESIAN_POINT('Ctrl Pts',(4.92368297048308,-0.581446498454876,
-3.76059398511233));
#19248=CARTESIAN_POINT('Ctrl Pts',(3.80884369176145,-1.47697461918932,-3.83959382095989));
#19249=CARTESIAN_POINT('Ctrl Pts',(2.44967098388855,-1.03257976933148,-3.91859365680745));
#19250=CARTESIAN_POINT('Ctrl Pts',(2.0792169986208,0.348579554282547,-3.99759349265502));
#19251=CARTESIAN_POINT('Ctrl Pts',(3.03356049991161,1.41350476947407,-4.07659332850258));
#19252=CARTESIAN_POINT('Ctrl Pts',(4.44691357062203,1.19608736005122,-4.15559316435014));
#19253=CARTESIAN_POINT('Ctrl Pts',(5.03707120844708,-0.106429893164062,
-4.2345930001977));
#19254=CARTESIAN_POINT('Ctrl Pts',(4.26863777089002,-1.3123931116956,-4.31359283604526));
#19255=CARTESIAN_POINT('Ctrl Pts',(2.83874210564833,-1.32774299540001,-4.39259267189283));
#19256=CARTESIAN_POINT('Ctrl Pts',(2.04459678666542,-0.13855400926523,-4.47159250774039));
#19257=CARTESIAN_POINT('Ctrl Pts',(2.60665668233817,1.17633226189402,-4.55059234358796));
#19258=CARTESIAN_POINT('Ctrl Pts',(4.01501664245213,1.42404066941082,-4.62959217943551));
#19259=CARTESIAN_POINT('Ctrl Pts',(4.9920014538375,0.379848201170875,-4.70859201528308));
#19260=CARTESIAN_POINT('Ctrl Pts',(4.65128282507545,-1.00894553744593,-4.78759185113064));
#19261=CARTESIAN_POINT('Ctrl Pts',(3.30196337123839,-1.48241596303085,-4.8665916869782));
#19262=CARTESIAN_POINT('Ctrl Pts',(2.16815629466128,-0.611026988169218,
-4.94559152282576));
#19263=CARTESIAN_POINT('Ctrl Pts',(2.27846027699217,0.814690467671415,-5.02459135867333));
#19264=CARTESIAN_POINT('Ctrl Pts',(3.53280667943882,1.50131433492034,-5.1035911945209));
#19265=CARTESIAN_POINT('Ctrl Pts',(4.79324259754267,0.825934050369154,-5.18259103036845));
#19266=CARTESIAN_POINT('Ctrl Pts',(4.91629067043077,-0.598740089273046,
-5.26159086621601));
#19267=CARTESIAN_POINT('Ctrl Pts',(3.79032072030063,-1.48023251908209,-5.34059070206358));
#19268=CARTESIAN_POINT('Ctrl Pts',(2.43682152615653,-1.01884638593762,-5.41959053791113));
#19269=CARTESIAN_POINT('Ctrl Pts',(2.08369818355609,0.366845187724217,-5.49859037375871));
#19270=CARTESIAN_POINT('Ctrl Pts',(3.05130696135811,1.41973192689762,-5.57759020960626));
#19271=CARTESIAN_POINT('Ctrl Pts',(4.46182557942397,1.18462671535117,-5.65659004545384));
#19272=CARTESIAN_POINT('Ctrl Pts',(5.03562047314177,-0.125181153135692,
-5.73558988130139));
#19273=CARTESIAN_POINT('Ctrl Pts',(4.25214040993648,-1.32142369667214,-5.81458971714896));
#19274=CARTESIAN_POINT('Ctrl Pts',(2.82216465442814,-1.31886028778958,-5.89358955299651));
#19275=CARTESIAN_POINT('Ctrl Pts',(2.0429784390789,-0.119816471152147,-5.97258938884408));
#19276=CARTESIAN_POINT('Ctrl Pts',(2.6214656160218,1.18792578882087,-6.05158922469164));
#19277=CARTESIAN_POINT('Ctrl Pts',(4.03281807649984,1.41797244649999,-6.1305890605392));
#19278=CARTESIAN_POINT('Ctrl Pts',(4.99664578751808,0.361623367890064,-6.20958889638677));
#19279=CARTESIAN_POINT('Ctrl Pts',(4.63855668241017,-1.02279326925705,-6.28858873223433));
#19280=CARTESIAN_POINT('Ctrl Pts',(3.28341200876903,-1.47932382235155,-6.36758856808189));
#19281=CARTESIAN_POINT('Ctrl Pts',(2.16060965407101,-0.593800189300851,
-6.44658840392945));
#19282=CARTESIAN_POINT('Ctrl Pts',(2.28876472987488,0.830423637543947,-6.52558823977702));
#19283=CARTESIAN_POINT('Ctrl Pts',(3.55161394523668,1.50128062056398,-6.60458807562458));
#19284=CARTESIAN_POINT('Ctrl Pts',(4.80349057706377,0.810164037712699,-6.68358791147214));
#19285=CARTESIAN_POINT('Ctrl Pts',(4.90868231619433,-0.615939720933709,
-6.7625877473197));
#19286=CARTESIAN_POINT('Ctrl Pts',(3.77175839100488,-1.48325812886618,-6.84158758316727));
#19287=CARTESIAN_POINT('Ctrl Pts',(2.42414511267564,-1.00495311689426,-6.92058741901482));
#19288=CARTESIAN_POINT('Ctrl Pts',(2.08840782772533,0.385053252839684,-6.9995872548624));
#19289=CARTESIAN_POINT('Ctrl Pts',(3.06913003701067,1.42573628845678,-7.07858709070995));
#19290=CARTESIAN_POINT('Ctrl Pts',(4.47659285239482,1.17298016940594,-7.15758692655752));
#19291=CARTESIAN_POINT('Ctrl Pts',(5.03393495745053,-0.143912768664118,
-7.23658676240507));
#19292=CARTESIAN_POINT('Ctrl Pts',(4.23553121865162,-1.33024691311019,-7.31558659825265));
#19293=CARTESIAN_POINT('Ctrl Pts',(2.80569977628582,-1.3097706139116,-7.39458643410019));
#19294=CARTESIAN_POINT('Ctrl Pts',(2.04159494079934,-0.101060130465283,
-7.47358626994778));
#19295=CARTESIAN_POINT('Ctrl Pts',(2.63641861810635,1.19933289678506,-7.55258610579532));
#19296=CARTESIAN_POINT('Ctrl Pts',(4.05054209805801,1.4116817038369,-7.6315859416429));
#19297=CARTESIAN_POINT('Ctrl Pts',(5.0010614570369,0.343341785733108,-7.71058577749045));
#19298=CARTESIAN_POINT('Ctrl Pts',(4.6256580698339,-1.03648049604108,-7.78958561333802));
#19299=CARTESIAN_POINT('Ctrl Pts',(3.26490083669646,-1.47599953416481,-7.86858544918558));
#19300=CARTESIAN_POINT('Ctrl Pts',(2.15327940314247,-0.576480206481971,
-7.94758528503314));
#19301=CARTESIAN_POINT('Ctrl Pts',(2.2992654612829,0.846026490590706,-8.02658512088071));
#19302=CARTESIAN_POINT('Ctrl Pts',(3.57041931300681,1.50101131306799,-8.10558495672826));
#19303=CARTESIAN_POINT('Ctrl Pts',(4.81354020390489,0.794266887520294,-8.18458479257583));
#19304=CARTESIAN_POINT('Ctrl Pts',(4.90085910174346,-0.633042694301782,
-8.26358462842339));
#19305=CARTESIAN_POINT('Ctrl Pts',(3.75315961681622,-1.48605097379388,-8.34258446427096));
#19306=CARTESIAN_POINT('Ctrl Pts',(2.41164373274955,-0.990902142340378,
-8.4215843001185));
#19307=CARTESIAN_POINT('Ctrl Pts',(2.09334519201882,0.403200892070548,-8.5005841359661));
#19308=CARTESIAN_POINT('Ctrl Pts',(3.08702692999233,1.4315169122805,-8.57958397181362));
#19309=CARTESIAN_POINT('Ctrl Pts',(4.49121307201085,1.1611495491593,-8.65858380766123));
#19310=CARTESIAN_POINT('Ctrl Pts',(5.03201492611272,-0.162621798849685,
-8.73758364350875));
#19311=CARTESIAN_POINT('Ctrl Pts',(4.2188128030386,-1.3388613790282,-8.81658347935634));
#19312=CARTESIAN_POINT('Ctrl Pts',(2.7893500558721,-1.30047539519085,-8.89558331520388));
#19313=CARTESIAN_POINT('Ctrl Pts',(2.04044650732301,-0.0822879401130431,
-8.97458315105147));
#19314=CARTESIAN_POINT('Ctrl Pts',(2.65151334511416,1.21055181378021,-9.053582986899));
#19315=CARTESIAN_POINT('Ctrl Pts',(4.06818591989252,1.40516939421034,-9.13258282274659));
#19316=CARTESIAN_POINT('Ctrl Pts',(5.00524778055251,0.325006389032079,-9.21158265859414));
#19317=CARTESIAN_POINT('Ctrl Pts',(4.61258899038759,-1.05000519434651,-9.2905824944417));
#19318=CARTESIAN_POINT('Ctrl Pts',(3.24643280010204,-1.4724433834297,-9.36958233028927));
#19319=CARTESIAN_POINT('Ctrl Pts',(2.14616661581982,-0.559070207925378,
-9.44858216613683));
#19320=CARTESIAN_POINT('Ctrl Pts',(2.30996096862398,0.861497434581703,-9.52758200198439));
#19321=CARTESIAN_POINT('Ctrl Pts',(3.58921955536611,1.50050482606178,-9.60658183783196));
#19322=CARTESIAN_POINT('Ctrl Pts',(4.82339042649041,0.778248192078537,-9.68558167367951));
#19323=CARTESIAN_POINT('Ctrl Pts',(4.89282125529856,-0.650052216874333,
-9.76458150952707));
#19324=CARTESIAN_POINT('Ctrl Pts',(3.73452921733139,-1.48859941037392,-9.84358134537464));
#19325=CARTESIAN_POINT('Ctrl Pts',(2.39931573273156,-0.976716979064629,
-9.9225811812222));
#19326=CARTESIAN_POINT('Ctrl Pts',(2.0985163780543,0.421325791869091,-10.0015810170698));
#19327=CARTESIAN_POINT('Ctrl Pts',(3.10498175317381,1.43699579380393,-10.0805808529173));
#19328=CARTESIAN_POINT('Ctrl Pts',(4.50570881864875,1.14928337390154,-10.1595806887649));
#19329=CARTESIAN_POINT('Ctrl Pts',(5.02981337122874,-0.181584487549335,
-10.2385805246125));
#19330=CARTESIAN_POINT('Ctrl Pts',(4.20207775601229,-1.34673274122706,-10.31758036046));
#19331=CARTESIAN_POINT('Ctrl Pts',(2.77294702678338,-1.29200713072568,-10.3965801963076));
#19332=CARTESIAN_POINT('Ctrl Pts',(2.03980150600681,-0.0612985784366647,
-10.4755861633928));
#19333=CARTESIAN_POINT('Ctrl Pts',(2.45742857131213,0.790662874763801,-10.528258851862));
#19334=CARTESIAN_POINT('Ctrl Pts',(2.80013759513739,1.03538613273742,-10.5545982617154));
#19335=CARTESIAN_POINT('Ctrl Pts',(2.94652770548266,-1.23370775336577,0.0546623923631346));
#19336=CARTESIAN_POINT('Ctrl Pts',(2.53827686050373,-1.03747877046718,0.0283291137472804));
#19337=CARTESIAN_POINT('Ctrl Pts',(1.93863701974394,-0.211567058731892,
-0.0243374434844277));
#19338=CARTESIAN_POINT('Ctrl Pts',(2.48865976187493,1.22804653526214,-0.10333727933199));
#19339=CARTESIAN_POINT('Ctrl Pts',(3.99336348781746,1.54968339598036,-0.182337115179553));
#19340=CARTESIAN_POINT('Ctrl Pts',(5.08565120465648,0.467383005740241,-0.261336951027115));
#19341=CARTESIAN_POINT('Ctrl Pts',(4.7756338693668,-1.03994395941763,-0.340336786874677));
#19342=CARTESIAN_POINT('Ctrl Pts',(3.34401536059709,-1.60329424846109,-0.41933662272224));
#19343=CARTESIAN_POINT('Ctrl Pts',(2.08985820999061,-0.712402630041443,
-0.498336458569803));
#19344=CARTESIAN_POINT('Ctrl Pts',(2.15079277181453,0.824933038812594,-0.577336294417365));
#19345=CARTESIAN_POINT('Ctrl Pts',(3.47161804821771,1.61380580079035,-0.656336130264928));
#19346=CARTESIAN_POINT('Ctrl Pts',(4.85402927675347,0.938661847712682,-0.73533596611249));
#19347=CARTESIAN_POINT('Ctrl Pts',(5.04391406293652,-0.58806483806614,-0.814335801960053));
#19348=CARTESIAN_POINT('Ctrl Pts',(3.86899590992078,-1.58128326838601,-0.893335637807615));
#19349=CARTESIAN_POINT('Ctrl Pts',(2.39517585181685,-1.13995500042024,-0.972335473655178));
#19350=CARTESIAN_POINT('Ctrl Pts',(1.95951182982654,0.33555249490115,-1.05133530950274));
#19351=CARTESIAN_POINT('Ctrl Pts',(2.95724334074437,1.50664250195448,-1.1303351453503));
#19352=CARTESIAN_POINT('Ctrl Pts',(4.48321964348532,1.31089545946468,-1.20933498119787));
#19353=CARTESIAN_POINT('Ctrl Pts',(5.15306351860538,-0.0741066866975193,
-1.28833481704543));
#19354=CARTESIAN_POINT('Ctrl Pts',(4.35908709996481,-1.39187842788788,-1.36733465289299));
#19355=CARTESIAN_POINT('Ctrl Pts',(2.82159215628832,-1.44692725593814,-1.44633448874055));
#19356=CARTESIAN_POINT('Ctrl Pts',(1.93540610437903,-0.18931225173771,-1.52533432458812));
#19357=CARTESIAN_POINT('Ctrl Pts',(2.50448392357404,1.24004827912987,-1.60433416043568));
#19358=CARTESIAN_POINT('Ctrl Pts',(4.01255372972948,1.54442729337894,-1.68333399628324));
#19359=CARTESIAN_POINT('Ctrl Pts',(5.0914827642871,0.447689731903192,-1.76233383213081));
#19360=CARTESIAN_POINT('Ctrl Pts',(4.76245813103416,-1.05519546426293,-1.84133366797837));
#19361=CARTESIAN_POINT('Ctrl Pts',(3.32397356320997,-1.60079905330219,-1.92033350382593));
#19362=CARTESIAN_POINT('Ctrl Pts',(2.081033553192,-0.694145171564268,-1.99933333967349));
#19363=CARTESIAN_POINT('Ctrl Pts',(2.1612430374211,0.842242658980785,-2.07833317552106));
#19364=CARTESIAN_POINT('Ctrl Pts',(3.49183534166855,1.61454133704232,-2.15733301136862));
#19365=CARTESIAN_POINT('Ctrl Pts',(4.86568668094492,0.922115437806592,-2.23633284721618));
#19366=CARTESIAN_POINT('Ctrl Pts',(5.03642833373058,-0.606860826239594,
-2.31533268306374));
#19367=CARTESIAN_POINT('Ctrl Pts',(3.84916213214399,-1.58528818417442,-2.3943325189113));
#19368=CARTESIAN_POINT('Ctrl Pts',(2.38098529573147,-1.12552965493881,-2.47333235475887));
#19369=CARTESIAN_POINT('Ctrl Pts',(1.96383937749262,0.355318214031296,-2.55233219060643));
#19370=CARTESIAN_POINT('Ctrl Pts',(2.97616242955291,1.51381860955616,-2.63133202645399));
#19371=CARTESIAN_POINT('Ctrl Pts',(4.49956703110903,1.29897087715313,-2.71033186230156));
#19372=CARTESIAN_POINT('Ctrl Pts',(5.1520085670309,-0.0943134335168294,
-2.78933169814912));
#19373=CARTESIAN_POINT('Ctrl Pts',(4.34158695346446,-1.40203585682528,-2.86833153399668));
#19374=CARTESIAN_POINT('Ctrl Pts',(2.80352304104103,-1.43782034311876,-2.94733136984424));
#19375=CARTESIAN_POINT('Ctrl Pts',(1.93316048680112,-0.16920292548062,-3.0263312056918));
#19376=CARTESIAN_POINT('Ctrl Pts',(2.52009903336545,1.25291671460437,-3.10533104153937));
#19377=CARTESIAN_POINT('Ctrl Pts',(4.03186342310285,1.53838047426604,-3.18433087738693));
#19378=CARTESIAN_POINT('Ctrl Pts',(5.09696913243742,0.428213389498532,-3.2633307132345));
#19379=CARTESIAN_POINT('Ctrl Pts',(4.74914389947359,-1.0704322442228,-3.34233054908206));
#19380=CARTESIAN_POINT('Ctrl Pts',(3.30393750641121,-1.59797334177813,-3.42133038492961));
#19381=CARTESIAN_POINT('Ctrl Pts',(2.07245253968059,-0.675820477620115,
-3.50033022077719));
#19382=CARTESIAN_POINT('Ctrl Pts',(2.17190182976842,0.859442029855187,-3.57933005662473));
#19383=CARTESIAN_POINT('Ctrl Pts',(3.51206419990799,1.61501198017097,-3.65832989247232));
#19384=CARTESIAN_POINT('Ctrl Pts',(4.87713382598905,0.905430382249195,-3.73732972831986));
#19385=CARTESIAN_POINT('Ctrl Pts',(5.0287088257587,-0.625564767188955,-3.81632956416744));
#19386=CARTESIAN_POINT('Ctrl Pts',(3.82927916937608,-1.58904264838199,-3.89532940001498));
#19387=CARTESIAN_POINT('Ctrl Pts',(2.36697685810663,-1.11092856302756,-3.97432923586257));
#19388=CARTESIAN_POINT('Ctrl Pts',(1.96841402960207,0.375028636858347,-4.05332907171011));
#19389=CARTESIAN_POINT('Ctrl Pts',(2.99517001108918,1.52075691295122,-4.13232890755768));
#19390=CARTESIAN_POINT('Ctrl Pts',(4.51576371486808,1.28684257780627,-4.21132874340524));
#19391=CARTESIAN_POINT('Ctrl Pts',(5.15070059434344,-0.114505447218352,
-4.2903285792528));
#19392=CARTESIAN_POINT('Ctrl Pts',(4.32396092742136,-1.41197323151816,-4.36932841510037));
#19393=CARTESIAN_POINT('Ctrl Pts',(2.78556943085473,-1.42848781446165,-4.44832825094793));
#19394=CARTESIAN_POINT('Ctrl Pts',(1.93116694859041,-0.149067036742727,
-4.52732808679549));
#19395=CARTESIAN_POINT('Ctrl Pts',(2.53587412064685,1.26558852706842,-4.60632792264306));
#19396=CARTESIAN_POINT('Ctrl Pts',(4.05109585284088,1.53209224269965,-4.68532775849062));
#19397=CARTESIAN_POINT('Ctrl Pts',(5.10221109337554,0.408669846949035,-4.76432759433818));
#19398=CARTESIAN_POINT('Ctrl Pts',(4.73563984349293,-1.08550104251369,-4.84332743018574));
#19399=CARTESIAN_POINT('Ctrl Pts',(3.28393841912083,-1.59489686369236,-4.92232726603331));
#19400=CARTESIAN_POINT('Ctrl Pts',(2.06410175008772,-0.65738972823123,-5.00132710188086));
#19401=CARTESIAN_POINT('Ctrl Pts',(2.18277523975565,0.876506529997589,-5.08032693772843));
#19402=CARTESIAN_POINT('Ctrl Pts',(3.5322973665653,1.61522918256043,-5.15932677357599));
#19403=CARTESIAN_POINT('Ctrl Pts',(4.88837106166974,0.88860323917268,-5.23832660942356));
#19404=CARTESIAN_POINT('Ctrl Pts',(5.02075562202712,-0.644170539418693,
-5.31732644527111));
#19405=CARTESIAN_POINT('Ctrl Pts',(3.80935073509997,-1.59254774711999,-5.39632628111868));
#19406=CARTESIAN_POINT('Ctrl Pts',(2.35315242532392,-1.09615313517937,-5.47532611696624));
#19407=CARTESIAN_POINT('Ctrl Pts',(1.97323523227201,0.394680207143594,-5.55432595281381));
#19408=CARTESIAN_POINT('Ctrl Pts',(3.01426301629724,1.5274565668218,-5.63332578866137));
#19409=CARTESIAN_POINT('Ctrl Pts',(4.53180719838599,1.27451233667028,-5.71232562450893));
#19410=CARTESIAN_POINT('Ctrl Pts',(5.14913978196271,-0.134679491794805,
-5.79132546035649));
#19411=CARTESIAN_POINT('Ctrl Pts',(4.30621180038808,-1.42168902790432,-5.87032529620406));
#19412=CARTESIAN_POINT('Ctrl Pts',(2.76773413656592,-1.41893111589506,-5.94932513205162));
#19413=CARTESIAN_POINT('Ctrl Pts',(1.92942580605385,-0.128907755194804,
-6.02832496789918));
#19414=CARTESIAN_POINT('Ctrl Pts',(2.55180670804179,1.27806173310228,-6.10732480374674));
#19415=CARTESIAN_POINT('Ctrl Pts',(4.07024800179228,1.52556358277557,-6.1863246395943));
#19416=CARTESIAN_POINT('Ctrl Pts',(5.1072078239868,0.389062172608119,-6.26532447544188));
#19417=CARTESIAN_POINT('Ctrl Pts',(4.72194808252306,-1.10039949516504,-6.34432431128942));
#19418=CARTESIAN_POINT('Ctrl Pts',(3.26397943961881,-1.59157010143771,-6.42332414713699));
#19419=CARTESIAN_POINT('Ctrl Pts',(2.05598249496029,-0.638855815907156,
-6.50232398298456));
#19420=CARTESIAN_POINT('Ctrl Pts',(2.19386156100051,0.893433481616711,-6.58132381883211));
#19421=CARTESIAN_POINT('Ctrl Pts',(3.5525316665079,1.61519291006839,-6.66032365467969));
#19422=CARTESIAN_POINT('Ctrl Pts',(4.89939662453803,0.871636649259046,-6.73932349052724));
#19423=CARTESIAN_POINT('Ctrl Pts',(5.01256997062284,-0.66267522317572,-6.81832332637481));
#19424=CARTESIAN_POINT('Ctrl Pts',(3.78937995664444,-1.59580293033154,-6.89732316222237));
#19425=CARTESIAN_POINT('Ctrl Pts',(2.33951416682715,-1.08120569007876,-6.97632299806993));
#19426=CARTESIAN_POINT('Ctrl Pts',(1.97830222891934,0.414269841005327,-7.05532283391749));
#19427=CARTESIAN_POINT('Ctrl Pts',(3.03343844894807,1.53391651980261,-7.13432266976506));
#19428=CARTESIAN_POINT('Ctrl Pts',(4.54769496398879,1.26198208870742,-7.21332250561261));
#19429=CARTESIAN_POINT('Ctrl Pts',(5.14732637482417,-0.154832401371615,
-7.29232234146019));
#19430=CARTESIAN_POINT('Ctrl Pts',(4.28834235770175,-1.43118172130189,-7.37132217730774));
#19431=CARTESIAN_POINT('Ctrl Pts',(2.75001995703389,-1.40915174713386,-7.45032201315531));
#19432=CARTESIAN_POINT('Ctrl Pts',(1.92793733242564,-0.108728244394972,
-7.52932184900287));
#19433=CARTESIAN_POINT('Ctrl Pts',(2.56789429527925,1.29033437530905,-7.60832168485043));
#19434=CARTESIAN_POINT('Ctrl Pts',(4.08931686444629,1.51879551902432,-7.68732152069799));
#19435=CARTESIAN_POINT('Ctrl Pts',(5.1119585401436,0.369393443470953,-7.76632135654555));
#19436=CARTESIAN_POINT('Ctrl Pts',(4.70807076518642,-1.11512526418998,-7.84532119239312));
#19437=CARTESIAN_POINT('Ctrl Pts',(3.24406370003013,-1.58799357707798,-7.92432102824068));
#19438=CARTESIAN_POINT('Ctrl Pts',(2.04809604843815,-0.620221649137555,
-8.00332086408824));
#19439=CARTESIAN_POINT('Ctrl Pts',(2.20515905374669,0.910220228393272,-8.08232069993581));
#19440=CARTESIAN_POINT('Ctrl Pts',(3.57276392440657,1.61490316839571,-8.16132053578336));
#19441=CARTESIAN_POINT('Ctrl Pts',(4.9102087843703,0.854533275026842,-8.24032037163093));
#19442=CARTESIAN_POINT('Ctrl Pts',(5.00415315610998,-0.681075914523366,
-8.31932020747849));
#19443=CARTESIAN_POINT('Ctrl Pts',(3.76936996797612,-1.59880768724664,-8.39832004332606));
#19444=CARTESIAN_POINT('Ctrl Pts',(2.3260642228619,-1.06608857328652,-8.47731987917361));
#19445=CARTESIAN_POINT('Ctrl Pts',(1.98361422435313,0.433794464062913,-8.55631971502118));
#19446=CARTESIAN_POINT('Ctrl Pts',(3.05269329994679,1.54013575855648,-8.63531955086874));
#19447=CARTESIAN_POINT('Ctrl Pts',(4.56342451830662,1.24925379948397,-8.71431938671631));
#19448=CARTESIAN_POINT('Ctrl Pts',(5.1452606577547,-0.174961011903223,-8.79331922256386));
#19449=CARTESIAN_POINT('Ctrl Pts',(4.27035540310055,-1.44044982486908,-8.87231905841144));
#19450=CARTESIAN_POINT('Ctrl Pts',(2.73242967302428,-1.39915123745589,-8.95131889425898));
#19451=CARTESIAN_POINT('Ctrl Pts',(1.92670175955322,-0.0885316813087181,
-9.03031873010657));
#19452=CARTESIAN_POINT('Ctrl Pts',(2.58413436106606,1.30240454722827,-9.10931856595411));
#19453=CARTESIAN_POINT('Ctrl Pts',(4.1082994420825,1.51178907652922,-9.18831840180168));
#19454=CARTESIAN_POINT('Ctrl Pts',(5.11646250826858,0.349666816517182,-9.26731823764924));
#19455=CARTESIAN_POINT('Ctrl Pts',(4.6940100465082,-1.12967617260413,-9.34631807349681));
#19456=CARTESIAN_POINT('Ctrl Pts',(3.22419436889937,-1.58416759719399,-9.42531790934437));
#19457=CARTESIAN_POINT('Ctrl Pts',(2.04044356595287,-0.601490636528902,
-9.50431774519193));
#19458=CARTESIAN_POINT('Ctrl Pts',(2.21666610139006,0.926865057284047,-9.58331758103949));
#19459=CARTESIAN_POINT('Ctrl Pts',(3.59299066799492,1.61435825080319,-9.66231741688706));
#19460=CARTESIAN_POINT('Ctrl Pts',(4.92080640980075,0.837299133087174,-9.74131725273461));
#19461=CARTESIAN_POINT('Ctrl Pts',(4.99550542402567,-0.699376064333139,
-9.82031708858218));
#19462=CARTESIAN_POINT('Ctrl Pts',(3.749325954387,-1.60154949090376,-9.89931692442974));
#19463=CARTESIAN_POINT('Ctrl Pts',(2.31280081430815,-1.05082708596875,-9.97831676027731));
#19464=CARTESIAN_POINT('Ctrl Pts',(1.98917778316202,0.45329462229403,-10.0573165961249));
#19465=CARTESIAN_POINT('Ctrl Pts',(3.07201047670045,1.54603035978594,-10.1363164319724));
#19466=CARTESIAN_POINT('Ctrl Pts',(4.57902015504166,1.23648725745083,-10.21531626782));
#19467=CARTESIAN_POINT('Ctrl Pts',(5.14289205604824,-0.195362527731759,
-10.2943161036676));
#19468=CARTESIAN_POINT('Ctrl Pts',(4.25235055514854,-1.44891844042438,-10.3733159395151));
#19469=CARTESIAN_POINT('Ctrl Pts',(2.71478203545085,-1.39004042863217,-10.4523157753627));
#19470=CARTESIAN_POINT('Ctrl Pts',(1.92600781763548,-0.0659497151511775,
-10.5313217424478));
#19471=CARTESIAN_POINT('Ctrl Pts',(2.37532306602683,0.850655801506997,-10.5839944309171));
#19472=CARTESIAN_POINT('Ctrl Pts',(2.74403573567487,1.11394786415904,-10.6103338407705));
#19473=CARTESIAN_POINT('Ctrl Pts',(2.90470669367821,-1.32071561099641,-0.00107318669196121));
#19474=CARTESIAN_POINT('Ctrl Pts',(2.46766375324505,-1.11064748073047,-0.0274064653078154));
#19475=CARTESIAN_POINT('Ctrl Pts',(1.82573401218097,-0.226487931584689,
-0.0800730225395237));
#19476=CARTESIAN_POINT('Ctrl Pts',(2.41454738386776,1.31465513264865,-0.159072858387086));
#19477=CARTESIAN_POINT('Ctrl Pts',(4.02537109422792,1.65897559417085,-0.238072694234649));
#19478=CARTESIAN_POINT('Ctrl Pts',(5.19469294974294,0.500345426468717,-0.317072530082211));
#19479=CARTESIAN_POINT('Ctrl Pts',(4.86281148650372,-1.11328652836719,-0.396072365929774));
#19480=CARTESIAN_POINT('Ctrl Pts',(3.33022736488723,-1.71636737889213,-0.475072201777336));
#19481=CARTESIAN_POINT('Ctrl Pts',(1.98762015266065,-0.762645182575647,
-0.554072037624899));
#19482=CARTESIAN_POINT('Ctrl Pts',(2.05285215499711,0.883111854824721,-0.63307187347246));
#19483=CARTESIAN_POINT('Ctrl Pts',(3.46682929600573,1.72762026371771,-0.712071709320024));
#19484=CARTESIAN_POINT('Ctrl Pts',(4.94673576928749,1.00486144497247,-0.791071545167586));
#19485=CARTESIAN_POINT('Ctrl Pts',(5.15001227518484,-0.629538405504167,
-0.870071381015148));
#19486=CARTESIAN_POINT('Ctrl Pts',(3.89223243056803,-1.69280406341553,-0.949071216862711));
#19487=CARTESIAN_POINT('Ctrl Pts',(2.31447047419945,-1.22035089816125,-1.02807105271027));
#19488=CARTESIAN_POINT('Ctrl Pts',(1.84808102870693,0.35921750278029,-1.10707088855784));
#19489=CARTESIAN_POINT('Ctrl Pts',(2.91617805448732,1.61289921952204,-1.1860707244054));
#19490=CARTESIAN_POINT('Ctrl Pts',(4.54977460078626,1.4033470187538,-1.26507056025296));
#19491=CARTESIAN_POINT('Ctrl Pts',(5.26685955091959,-0.0793330979185393,
-1.34407039610052));
#19492=CARTESIAN_POINT('Ctrl Pts',(4.41688754741972,-1.49004135161307,-1.42307023194808));
#19493=CARTESIAN_POINT('Ctrl Pts',(2.77096000226024,-1.5489725258516,-1.50207006779565));
#19494=CARTESIAN_POINT('Ctrl Pts',(1.82227523489064,-0.202663593173311,
-1.58106990364321));
#19495=CARTESIAN_POINT('Ctrl Pts',(2.43148755250165,1.32750330551783,-1.66006973949077));
#19496=CARTESIAN_POINT('Ctrl Pts',(4.04591473756878,1.65334880229916,-1.73906957533833));
#19497=CARTESIAN_POINT('Ctrl Pts',(5.20093578303924,0.479263274624201,-1.8180694111859));
#19498=CARTESIAN_POINT('Ctrl Pts',(4.84870652262159,-1.12961365323564,-1.89706924703346));
#19499=CARTESIAN_POINT('Ctrl Pts',(3.3087721096946,-1.71369620884407,-1.97606908288102));
#19500=CARTESIAN_POINT('Ctrl Pts',(1.97817313251846,-0.743100107688879,
-2.05506891872859));
#19501=CARTESIAN_POINT('Ctrl Pts',(2.06403943082317,0.90164224463072,-2.13406875457615));
#19502=CARTESIAN_POINT('Ctrl Pts',(3.48847242420994,1.7284076740325,-2.21306859042371));
#19503=CARTESIAN_POINT('Ctrl Pts',(4.95921531775214,0.987148091214824,-2.29206842627127));
#19504=CARTESIAN_POINT('Ctrl Pts',(5.14199861117487,-0.649659990163954,
-2.37106826211884));
#19505=CARTESIAN_POINT('Ctrl Pts',(3.870999865673,-1.69709142789714,-2.4500680979664));
#19506=CARTESIAN_POINT('Ctrl Pts',(2.29927912203395,-1.20490819795988,-2.52906793381396));
#19507=CARTESIAN_POINT('Ctrl Pts',(1.85271377884109,0.38037720915851,-2.60806776966152));
#19508=CARTESIAN_POINT('Ctrl Pts',(2.93643142151619,1.62058142570894,-2.68706760550909));
#19509=CARTESIAN_POINT('Ctrl Pts',(4.56727489611532,1.39058144929823,-2.76606744135665));
#19510=CARTESIAN_POINT('Ctrl Pts',(5.26573019835659,-0.100964935684744,
-2.84506727720421));
#19511=CARTESIAN_POINT('Ctrl Pts',(4.39815319431651,-1.5009151383171,-2.92406711305178));
#19512=CARTESIAN_POINT('Ctrl Pts',(2.75161655360403,-1.53922334344132,-3.00306694889933));
#19513=CARTESIAN_POINT('Ctrl Pts',(1.81987124400756,-0.181136046603304,
-3.0820667847469));
#19514=CARTESIAN_POINT('Ctrl Pts',(2.44820392573725,1.34127929385372,-3.16106662059446));
#19515=CARTESIAN_POINT('Ctrl Pts',(4.06658625674519,1.6468755282377,-3.24006645644202));
#19516=CARTESIAN_POINT('Ctrl Pts',(5.20680908005306,0.458413353410064,-3.31906629228959));
#19517=CARTESIAN_POINT('Ctrl Pts',(4.83445329820725,-1.14592501473873,-3.39806612813715));
#19518=CARTESIAN_POINT('Ctrl Pts',(3.28732299994818,-1.71067121259855,-3.47706596398471));
#19519=CARTESIAN_POINT('Ctrl Pts',(1.96898693872843,-0.723483055520123,
-3.55606579983227));
#19520=CARTESIAN_POINT('Ctrl Pts',(2.07544993984288,0.920054609756227,-3.63506563567983));
#19521=CARTESIAN_POINT('Ctrl Pts',(3.51012793281527,1.72891150950368,-3.7140654715274));
#19522=CARTESIAN_POINT('Ctrl Pts',(4.97146977843772,0.969286313751825,-3.79306530737496));
#19523=CARTESIAN_POINT('Ctrl Pts',(5.1337346810343,-0.669683035923036,-3.87206514322252));
#19524=CARTESIAN_POINT('Ctrl Pts',(3.84971464699072,-1.70111067757465,-3.95106497907008));
#19525=CARTESIAN_POINT('Ctrl Pts',(2.2842827323247,-1.18927735672363,-4.03006481491765));
#19526=CARTESIAN_POINT('Ctrl Pts',(1.85761106058333,0.401477719434146,-4.10906465076521));
#19527=CARTESIAN_POINT('Ctrl Pts',(2.95677952226676,1.62800905642836,-4.18806448661277));
#19528=CARTESIAN_POINT('Ctrl Pts',(4.58461385911411,1.37759779556131,-4.26706432246033));
#19529=CARTESIAN_POINT('Ctrl Pts',(5.26432998023981,-0.122581001272642,
-4.3460641583079));
#19530=CARTESIAN_POINT('Ctrl Pts',(4.37928408395269,-1.51155335134072,-4.42506399415546));
#19531=CARTESIAN_POINT('Ctrl Pts',(2.73239675606114,-1.52923263352329,-4.50406383000302));
#19532=CARTESIAN_POINT('Ctrl Pts',(1.81773711051539,-0.159580064220224,
-4.58306366585058));
#19533=CARTESIAN_POINT('Ctrl Pts',(2.46509155895553,1.35484479224281,-4.66206350169815));
#19534=CARTESIAN_POINT('Ctrl Pts',(4.08717506322962,1.64014381598848,-4.74106333754571));
#19535=CARTESIAN_POINT('Ctrl Pts',(5.21242073291358,0.437491492727194,-4.82006317339327));
#19536=CARTESIAN_POINT('Ctrl Pts',(4.81999686191041,-1.16205654758144,-4.89906300924083));
#19537=CARTESIAN_POINT('Ctrl Pts',(3.26591346700327,-1.70737776435388,-4.9780628450884));
#19538=CARTESIAN_POINT('Ctrl Pts',(1.96004720551417,-0.70375246829324,-5.05706268093596));
#19539=CARTESIAN_POINT('Ctrl Pts',(2.08709020251914,0.938322592323762,-5.13606251678353));
#19540=CARTESIAN_POINT('Ctrl Pts',(3.53178805369179,1.72914403020051,-5.21506235263108));
#19541=CARTESIAN_POINT('Ctrl Pts',(4.9834995257968,0.95127242797621,-5.29406218847865));
#19542=CARTESIAN_POINT('Ctrl Pts',(5.1252205736235,-0.689600989564341,-5.37306202432621));
#19543=CARTESIAN_POINT('Ctrl Pts',(3.82838074989931,-1.70486297515788,-5.45206186017377));
#19544=CARTESIAN_POINT('Ctrl Pts',(2.2694833244913,-1.17345988442113,-5.53106169602134));
#19545=CARTESIAN_POINT('Ctrl Pts',(1.86277228098792,0.422515226562972,-5.6100615318689));
#19546=CARTESIAN_POINT('Ctrl Pts',(2.97721907123637,1.63518120674598,-5.68906136771646));
#19547=CARTESIAN_POINT('Ctrl Pts',(4.60178881734799,1.3643979579894,-5.76806120356402));
#19548=CARTESIAN_POINT('Ctrl Pts',(5.26265909078364,-0.144177830453919,
-5.84706103941159));
#19549=CARTESIAN_POINT('Ctrl Pts',(4.36028319083968,-1.5219543591365,-5.92606087525914));
#19550=CARTESIAN_POINT('Ctrl Pts',(2.71330361870369,-1.51900194400053,-6.00506071110672));
#19551=CARTESIAN_POINT('Ctrl Pts',(1.81587317302879,-0.137999039237464,
-6.08406054695427));
#19552=CARTESIAN_POINT('Ctrl Pts',(2.4821478000618,1.36819767738369,-6.16306038280184));
#19553=CARTESIAN_POINT('Ctrl Pts',(4.10767792708472,1.63315471905114,-6.24206021864939));
#19554=CARTESIAN_POINT('Ctrl Pts',(5.21776986045553,0.416500977326176,-6.32106005449696));
#19555=CARTESIAN_POINT('Ctrl Pts',(4.80533948263594,-1.17800572107301,-6.40005989034452));
#19556=CARTESIAN_POINT('Ctrl Pts',(3.24454687046858,-1.70381638052387,-6.47905972619209));
#19557=CARTESIAN_POINT('Ctrl Pts',(1.95135533584957,-0.683911442513464,
-6.55805956203965));
#19558=CARTESIAN_POINT('Ctrl Pts',(2.09895839212617,0.956443325689477,-6.63705939788721));
#19559=CARTESIAN_POINT('Ctrl Pts',(3.55344938777911,1.72910519957279,-6.71605923373477));
#19560=CARTESIAN_POINT('Ctrl Pts',(4.99530267201232,0.933109260805396,-6.79505906958234));
#19561=CARTESIAN_POINT('Ctrl Pts',(5.11645762505132,-0.709410725417731,
-6.87405890542989));
#19562=CARTESIAN_POINT('Ctrl Pts',(3.80700152228402,-1.70834773179691,-6.95305874127746));
#19563=CARTESIAN_POINT('Ctrl Pts',(2.25488322097866,-1.15745826326325,-7.03205857712502));
#19564=CARTESIAN_POINT('Ctrl Pts',(1.86819663011334,0.443486429170971,-7.11105841297258));
#19565=CARTESIAN_POINT('Ctrl Pts',(2.99774686088548,1.64209675114843,-7.19005824882015));
#19566=CARTESIAN_POINT('Ctrl Pts',(4.61879707558276,1.35098400800889,-7.26905808466771));
#19567=CARTESIAN_POINT('Ctrl Pts',(5.26071779219779,-0.165752034079112,
-7.34805792051527));
#19568=CARTESIAN_POINT('Ctrl Pts',(4.34115349675186,-1.53211652949359,-7.42705775636284));
#19569=CARTESIAN_POINT('Ctrl Pts',(2.69434013778197,-1.50853288035613,-7.5060575922104));
#19570=CARTESIAN_POINT('Ctrl Pts',(1.81427972405195,-0.116396358324663,
-7.58505742805796));
#19571=CARTESIAN_POINT('Ctrl Pts',(2.49936997245213,1.38133585383303,-7.66405726390553));
#19572=CARTESIAN_POINT('Ctrl Pts',(4.12809163083458,1.62590933421174,-7.74305709975308));
#19573=CARTESIAN_POINT('Ctrl Pts',(5.22285562325029,0.395445101208801,-7.82205693560065));
#19574=CARTESIAN_POINT('Ctrl Pts',(4.79048346053894,-1.19377003233889,-7.90105677144821));
#19575=CARTESIAN_POINT('Ctrl Pts',(3.22322656336381,-1.69998761999115,-7.98005660729577));
#19576=CARTESIAN_POINT('Ctrl Pts',(1.94291269373384,-0.66396309179314,-8.05905644314334));
#19577=CARTESIAN_POINT('Ctrl Pts',(2.11105264621048,0.974413966195839,-8.13805627899089));
#19578=CARTESIAN_POINT('Ctrl Pts',(3.57510853580632,1.72879502372344,-8.21705611483847));
#19579=CARTESIAN_POINT('Ctrl Pts',(5.00687736483572,0.914799662533391,-8.29605595068602));
#19580=CARTESIAN_POINT('Ctrl Pts',(5.10744721047652,-0.729109134744952,
-8.37505578653359));
#19581=CARTESIAN_POINT('Ctrl Pts',(3.785580319136,-1.7115644006994,-8.45405562238115));
#19582=CARTESIAN_POINT('Ctrl Pts',(2.24048471297425,-1.14127500423266,-8.53305545822871));
#19583=CARTESIAN_POINT('Ctrl Pts',(1.87388325668743,0.464388036055279,-8.61205529407627));
#19584=CARTESIAN_POINT('Ctrl Pts',(3.01835966990126,1.64875460483247,-8.69105512992383));
#19585=CARTESIAN_POINT('Ctrl Pts',(4.63563596460239,1.33735804980865,-8.77005496577141));
#19586=CARTESIAN_POINT('Ctrl Pts',(5.25850638939668,-0.187300224956761,
-8.84905480161895));
#19587=CARTESIAN_POINT('Ctrl Pts',(4.3218980031625,-1.54203827070995,-8.92805463746653));
#19588=CARTESIAN_POINT('Ctrl Pts',(2.67550929017646,-1.49782707972093,-9.00705447331408));
#19589=CARTESIAN_POINT('Ctrl Pts',(1.81295701178344,-0.0947754225043939,
-9.08605430916166));
#19590=CARTESIAN_POINT('Ctrl Pts',(2.51675537701794,1.39425728067634,-9.1650541450092));
#19591=CARTESIAN_POINT('Ctrl Pts',(4.14841296427251,1.6184087588481,-9.24405398085678));
#19592=CARTESIAN_POINT('Ctrl Pts',(5.22767723598463,0.374327244002286,-9.32305381670433));
#19593=CARTESIAN_POINT('Ctrl Pts',(4.77543110262881,-1.20934715086173,-9.4020536525519));
#19594=CARTESIAN_POINT('Ctrl Pts',(3.20195593769669,-1.69589181095829,-9.48105348839945));
#19595=CARTESIAN_POINT('Ctrl Pts',(1.93472051608591,-0.643911065132426,
-9.56005332424703));
#19596=CARTESIAN_POINT('Ctrl Pts',(2.12337123415615,0.992232679986391,-9.63905316009459));
#19597=CARTESIAN_POINT('Ctrl Pts',(3.59676178062372,1.72821167554459,-9.71805299594214));
#19598=CARTESIAN_POINT('Ctrl Pts',(5.0182223931111,0.896350074095812,-9.79705283178971));
#19599=CARTESIAN_POINT('Ctrl Pts',(5.09818959275277,-0.748699911791949,
-9.87605266763726));
#19600=CARTESIAN_POINT('Ctrl Pts',(3.76412269144261,-1.71449957143361,-9.95505250348484));
#19601=CARTESIAN_POINT('Ctrl Pts',(2.22628589588474,-1.12493719287287,-10.0340523393324));
#19602=CARTESIAN_POINT('Ctrl Pts',(1.87983918826973,0.48526345271897,-10.11305217518));
#19603=CARTESIAN_POINT('Ctrl Pts',(3.03903920022708,1.65506492576796,-10.1920520110275));
#19604=CARTESIAN_POINT('Ctrl Pts',(4.65233149143457,1.32369114100012,-10.2710518468751));
#19605=CARTESIAN_POINT('Ctrl Pts',(5.25597074086776,-0.209140567914182,
-10.3500516827227));
#19606=CARTESIAN_POINT('Ctrl Pts',(4.30262335428479,-1.5511041396217,-10.4290515185703));
#19607=CARTESIAN_POINT('Ctrl Pts',(2.65661704411831,-1.48807372653865,-10.5080513544178));
#19608=CARTESIAN_POINT('Ctrl Pts',(1.81221412926416,-0.0706008518656905,
-10.5870573215029));
#19609=CARTESIAN_POINT('Ctrl Pts',(2.29321756074153,0.910648728250192,-10.6397300099722));
#19610=CARTESIAN_POINT('Ctrl Pts',(2.68793387621235,1.19250959558065,-10.6660694198255));
#19611=CARTESIAN_POINT('Ctrl Pts',(2.90397937668593,-1.32076737590681,-10.5));
#19612=CARTESIAN_POINT('Ctrl Pts',(2.86727944188692,-1.29893471207351,-10.5));
#19613=CARTESIAN_POINT('Ctrl Pts',(2.83169802649736,-1.27545802809138,-10.5));
#19614=CARTESIAN_POINT('Ctrl Pts',(2.79735929175741,-1.25033824989213,-10.5));
#19615=CARTESIAN_POINT('Ctrl Pts',(2.75114791045458,-1.21653328714673,-10.5));
#19616=CARTESIAN_POINT('Ctrl Pts',(2.70718528420868,-1.17975351331922,-10.5));
#19617=CARTESIAN_POINT('Ctrl Pts',(2.66560257997516,-1.1403158632289,-10.5));
#19618=CARTESIAN_POINT('Ctrl Pts',(2.62355743994437,-1.10043963220698,-10.5));
#19619=CARTESIAN_POINT('Ctrl Pts',(2.58394493340546,-1.05784496331721,-10.5));
#19620=CARTESIAN_POINT('Ctrl Pts',(2.5469462583716,-1.01283383699425,-10.5));
#19621=CARTESIAN_POINT('Ctrl Pts',(2.5370259142128,-1.00076513821813,-10.5));
#19622=CARTESIAN_POINT('Ctrl Pts',(2.52729375930872,-0.988522626584723,
-10.5));
#19623=CARTESIAN_POINT('Ctrl Pts',(2.51775390963644,-0.976111975007932,
-10.5));
#19624=CARTESIAN_POINT('Ctrl Pts',(2.511245118406,-0.967644510328506,-10.5));
#19625=CARTESIAN_POINT('Ctrl Pts',(2.5048258504571,-0.959098775995798,-10.5));
#19626=CARTESIAN_POINT('Ctrl Pts',(2.49849748762295,-0.9504765680643,-10.5));
#19627=CARTESIAN_POINT('Ctrl Pts',(2.49201582400825,-0.941645492335477,
-10.5));
#19628=CARTESIAN_POINT('Ctrl Pts',(2.4856340766425,-0.932740308072392,-10.5));
#19629=CARTESIAN_POINT('Ctrl Pts',(2.47935728107968,-0.923769104127284,
-10.5));
#19630=CARTESIAN_POINT('Ctrl Pts',(2.4467581478561,-0.877176305356714,-10.5));
#19631=CARTESIAN_POINT('Ctrl Pts',(2.41695002133948,-0.82875554916227,-10.5));
#19632=CARTESIAN_POINT('Ctrl Pts',(2.39006706139692,-0.778810652111408,
-10.5));
#19633=CARTESIAN_POINT('Ctrl Pts',(2.36362934736646,-0.729692961636386,
-10.5));
#19634=CARTESIAN_POINT('Ctrl Pts',(2.34002048016728,-0.679100081706049,
-10.5));
#19635=CARTESIAN_POINT('Ctrl Pts',(2.31941557933448,-0.62730817924926,-10.5));
#19636=CARTESIAN_POINT('Ctrl Pts',(2.30117769346663,-0.581465939407855,
-10.5));
#19637=CARTESIAN_POINT('Ctrl Pts',(2.28529375648752,-0.534683695016422,
-10.5));
#19638=CARTESIAN_POINT('Ctrl Pts',(2.27191932854041,-0.487154532944957,
-10.5));
#19639=CARTESIAN_POINT('Ctrl Pts',(2.26791530106224,-0.472925283536962,
-10.5));
#19640=CARTESIAN_POINT('Ctrl Pts',(2.26413503174816,-0.458622787410054,
-10.5));
#19641=CARTESIAN_POINT('Ctrl Pts',(2.26059128056392,-0.444286805968637,
-10.5));
#19642=CARTESIAN_POINT('Ctrl Pts',(2.24768137294169,-0.392060736343278,
-10.5));
#19643=CARTESIAN_POINT('Ctrl Pts',(2.23788480709244,-0.339323391333285,
-10.5));
#19644=CARTESIAN_POINT('Ctrl Pts',(2.23134948683768,-0.286330333482162,
-10.5));
#19645=CARTESIAN_POINT('Ctrl Pts',(2.22490254378003,-0.234053901249509,
-10.5));
#19646=CARTESIAN_POINT('Ctrl Pts',(2.22162908761336,-0.18152772715788,-10.5));
#19647=CARTESIAN_POINT('Ctrl Pts',(2.22172052929498,-0.129002563547201,
-10.5));
#19648=CARTESIAN_POINT('Ctrl Pts',(2.22176330894542,-0.104429435641195,
-10.5));
#19649=CARTESIAN_POINT('Ctrl Pts',(2.2225432872073,-0.0798566892928238,
-10.5));
#19650=CARTESIAN_POINT('Ctrl Pts',(2.22408399749618,-0.0553112432975004,
-10.5));
#19651=CARTESIAN_POINT('Ctrl Pts',(2.22555857229785,-0.0318194185062761,
-10.5));
#19652=CARTESIAN_POINT('Ctrl Pts',(2.22773004647856,-0.00835259134640754,
-10.5));
#19653=CARTESIAN_POINT('Ctrl Pts',(2.23058759941273,0.0150644752044568,
-10.5));
#19654=CARTESIAN_POINT('Ctrl Pts',(2.23213148334798,0.0277162908283425,
-10.5));
#19655=CARTESIAN_POINT('Ctrl Pts',(2.23387629223041,0.0403574166494886,
-10.5));
#19656=CARTESIAN_POINT('Ctrl Pts',(2.23581806955776,0.0529688042131,-10.5));
#19657=CARTESIAN_POINT('Ctrl Pts',(2.23897614296403,0.0734797490674775,
-10.5));
#19658=CARTESIAN_POINT('Ctrl Pts',(2.24265154618475,0.0938916833615652,
-10.5));
#19659=CARTESIAN_POINT('Ctrl Pts',(2.24683171282339,0.114191366177429,-10.5));
#19660=CARTESIAN_POINT('Ctrl Pts',(2.25746540461127,0.16583059234145,-10.5));
#19661=CARTESIAN_POINT('Ctrl Pts',(2.27136188653188,0.216742631762888,-10.5));
#19662=CARTESIAN_POINT('Ctrl Pts',(2.28834566774239,0.266665394582686,-10.5));
#19663=CARTESIAN_POINT('Ctrl Pts',(2.30534672793287,0.316638947883617,-10.5));
#19664=CARTESIAN_POINT('Ctrl Pts',(2.3254421275876,0.365622165690229,-10.5));
#19665=CARTESIAN_POINT('Ctrl Pts',(2.34849751348331,0.41332218547471,-10.5));
#19666=CARTESIAN_POINT('Ctrl Pts',(2.35585489053263,0.42854409641569,-10.5));
#19667=CARTESIAN_POINT('Ctrl Pts',(2.36351397167454,0.443635044630669,-10.5));
#19668=CARTESIAN_POINT('Ctrl Pts',(2.37147109168874,0.458584629107004,-10.5));
#19669=CARTESIAN_POINT('Ctrl Pts',(2.37981195901927,0.47425518585883,-10.5));
#19670=CARTESIAN_POINT('Ctrl Pts',(2.3884803057648,0.489770423174206,-10.5));
#19671=CARTESIAN_POINT('Ctrl Pts',(2.39747223867455,0.505117767236418,-10.5));
#19672=CARTESIAN_POINT('Ctrl Pts',(2.40328124679998,0.515032526082609,-10.5));
#19673=CARTESIAN_POINT('Ctrl Pts',(2.409220878025,0.524869543178701,-10.5));
#19674=CARTESIAN_POINT('Ctrl Pts',(2.41528654831792,0.534621100868321,-10.5));
#19675=CARTESIAN_POINT('Ctrl Pts',(2.44252213382478,0.578406761884308,-10.5));
#19676=CARTESIAN_POINT('Ctrl Pts',(2.47231467151112,0.620504165307216,-10.5));
#19677=CARTESIAN_POINT('Ctrl Pts',(2.50453063857843,0.660637211715554,-10.5));
#19678=CARTESIAN_POINT('Ctrl Pts',(2.52964140926431,0.691918958533218,-10.5));
#19679=CARTESIAN_POINT('Ctrl Pts',(2.556225371933,0.722006721374281,-10.5));
#19680=CARTESIAN_POINT('Ctrl Pts',(2.58423075837921,0.750750430600732,-10.5));
#19681=CARTESIAN_POINT('Ctrl Pts',(2.59504794536868,0.761852797571121,-10.5));
#19682=CARTESIAN_POINT('Ctrl Pts',(2.60608091248154,0.772757625787352,-10.5));
#19683=CARTESIAN_POINT('Ctrl Pts',(2.61730509025834,0.783435451842213,-10.5));
#19684=CARTESIAN_POINT('Ctrl Pts',(2.65308565292733,0.817474348224813,-10.5));
#19685=CARTESIAN_POINT('Ctrl Pts',(2.69084286268129,0.849248709423217,-10.5));
#19686=CARTESIAN_POINT('Ctrl Pts',(2.73046767024449,0.878489839539784,-10.5));
#19687=CARTESIAN_POINT('Ctrl Pts',(2.7700924778077,0.907730969656352,-10.5));
#19688=CARTESIAN_POINT('Ctrl Pts',(2.8115855332062,0.934439564031336,-10.5));
#19689=CARTESIAN_POINT('Ctrl Pts',(2.85485462588355,0.95829519891841,-10.5));
#19690=CARTESIAN_POINT('',(2.85417850162344,0.958898071501409,0.000498685380349388));
#19691=CARTESIAN_POINT('Ctrl Pts',(2.85340124062148,0.959453028700747,1.346579098227E-16));
#19692=CARTESIAN_POINT('Ctrl Pts',(2.82282123135218,0.942844416454162,2.85745455358478E-16));
#19693=CARTESIAN_POINT('Ctrl Pts',(2.79311110010296,0.924851703347499,1.79905765899949E-15));
#19694=CARTESIAN_POINT('Ctrl Pts',(2.76437680446153,0.905503479527772,1.65145674912992E-15));
#19695=CARTESIAN_POINT('Ctrl Pts',(2.72398476848259,0.878305521992729,1.46763134221225E-15));
#19696=CARTESIAN_POINT('Ctrl Pts',(2.68551952020721,0.848431625036211,-6.61741344488266E-17));
#19697=CARTESIAN_POINT('Ctrl Pts',(2.64904553316328,0.816198607929121,-9.40220123979429E-16));
#19698=CARTESIAN_POINT('Ctrl Pts',(2.61505513991653,0.786160407672056,-1.75475040453543E-15));
#19699=CARTESIAN_POINT('Ctrl Pts',(2.58279383214052,0.75407239651815,1.19466269310647E-15));
#19700=CARTESIAN_POINT('Ctrl Pts',(2.55233048054817,0.720153874898648,1.35655375821386E-15));
#19701=CARTESIAN_POINT('Ctrl Pts',(2.53991532102457,0.706330581180162,1.44941899268915E-15));
#19702=CARTESIAN_POINT('Ctrl Pts',(2.52779900822753,0.692202886525742,6.75371079343568E-16));
#19703=CARTESIAN_POINT('Ctrl Pts',(2.51598720874143,0.677784246701662,5.55111512312578E-17));
#19704=CARTESIAN_POINT('Ctrl Pts',(2.50622350289069,0.665865710650002,-4.56868864520839E-16));
#19705=CARTESIAN_POINT('Ctrl Pts',(2.49666446159073,0.653743392170785,-9.49057168119929E-16));
#19706=CARTESIAN_POINT('Ctrl Pts',(2.48733805546213,0.641458137644336,-7.35522753814166E-16));
#19707=CARTESIAN_POINT('Ctrl Pts',(2.46849049126708,0.616631090639603,-3.03994947069626E-16));
#19708=CARTESIAN_POINT('Ctrl Pts',(2.45057636777883,0.591120920027303,-3.48031265324085E-16));
#19709=CARTESIAN_POINT('Ctrl Pts',(2.43360906387558,0.565001421693496,5.55111512312578E-17));
#19710=CARTESIAN_POINT('Ctrl Pts',(2.40527139199654,0.521378358321186,7.29481079207401E-16));
#19711=CARTESIAN_POINT('Ctrl Pts',(2.37957461447215,0.476059956151351,7.91024143821084E-16));
#19712=CARTESIAN_POINT('Ctrl Pts',(2.35661191998427,0.429363332514691,1.06165076729781E-15));
#19713=CARTESIAN_POINT('Ctrl Pts',(2.33337865186161,0.382116474009215,1.33546623384434E-15));
#19714=CARTESIAN_POINT('Ctrl Pts',(2.31294353384136,0.333457798512449,1.04920881821834E-15));
#19715=CARTESIAN_POINT('Ctrl Pts',(2.29544081289486,0.283679223188047,1.02001740387436E-15));
#19716=CARTESIAN_POINT('Ctrl Pts',(2.28937407302452,0.266425124894886,1.00989916466954E-15));
#19717=CARTESIAN_POINT('Ctrl Pts',(2.28366002281829,0.249036224651675,6.65784231122416E-16));
#19718=CARTESIAN_POINT('Ctrl Pts',(2.27830555103768,0.231523994364829,9.36750677027476E-16));
#19719=CARTESIAN_POINT('Ctrl Pts',(2.27541733157404,0.222077840488457,1.12794527297599E-15));
#19720=CARTESIAN_POINT('Ctrl Pts',(2.27263638189792,0.212604328404696,7.26586891309585E-16));
#19721=CARTESIAN_POINT('Ctrl Pts',(2.26996417256006,0.203108804611541,7.49400541621981E-16));
#19722=CARTESIAN_POINT('Ctrl Pts',(2.2552174363151,0.150707227047437,8.66263172620935E-16));
#19723=CARTESIAN_POINT('Ctrl Pts',(2.24376949101641,0.0976065262008687,
4.08534101287946E-17));
#19724=CARTESIAN_POINT('Ctrl Pts',(2.23572379087075,0.0441418535747884,
-4.30211422042248E-16));
#19725=CARTESIAN_POINT('Ctrl Pts',(2.22776565223313,-0.00874096199995714,
-8.96149646665323E-16));
#19726=CARTESIAN_POINT('Ctrl Pts',(2.22313553231218,-0.0619809771007474,
-2.8965713559225E-15));
#19727=CARTESIAN_POINT('Ctrl Pts',(2.22197643437771,-0.11527988813662,-3.05311331771918E-16));
#19728=CARTESIAN_POINT('Ctrl Pts',(2.22156081320029,-0.134391436437367,
6.84947814620585E-16));
#19729=CARTESIAN_POINT('Ctrl Pts',(2.22159192280362,-0.153510722380135,
-2.249679686016E-15));
#19730=CARTESIAN_POINT('Ctrl Pts',(2.22207794087312,-0.172624402843412,
-1.95676808090184E-15));
#19731=CARTESIAN_POINT('Ctrl Pts',(2.22254868025268,-0.19113721676339,-1.69646123182782E-15));
#19732=CARTESIAN_POINT('Ctrl Pts',(2.22344617954617,-0.209644777811353,
-7.8653483386481E-16));
#19733=CARTESIAN_POINT('Ctrl Pts',(2.22476297375739,-0.228137688022508,
-8.46545056276682E-16));
#19734=CARTESIAN_POINT('Ctrl Pts',(2.22566358113939,-0.240785717083357,
-9.08251614191495E-16));
#19735=CARTESIAN_POINT('Ctrl Pts',(2.22676034036135,-0.253426894133299,
1.47785297643783E-15));
#19736=CARTESIAN_POINT('Ctrl Pts',(2.22805107762706,-0.266058211650706,
1.2490009027033E-15));
#19737=CARTESIAN_POINT('Ctrl Pts',(2.229054816298,-0.275880924757348,1.05749732675775E-15));
#19738=CARTESIAN_POINT('Ctrl Pts',(2.23017537077975,-0.285692245157826,
-1.19694993143268E-15));
#19739=CARTESIAN_POINT('Ctrl Pts',(2.23141023118955,-0.295482958015865,
-1.11022302462516E-15));
#19740=CARTESIAN_POINT('Ctrl Pts',(2.23807405618757,-0.348317753409599,
-1.00747358571781E-15));
#19741=CARTESIAN_POINT('Ctrl Pts',(2.24806925032871,-0.400620352965406,
-1.83995180019013E-15));
#19742=CARTESIAN_POINT('Ctrl Pts',(2.26115510042849,-0.452165650093407,
-6.80011602582908E-16));
#19743=CARTESIAN_POINT('Ctrl Pts',(2.27469329060466,-0.505492719399986,
5.20024380441516E-16));
#19744=CARTESIAN_POINT('Ctrl Pts',(2.29153956097441,-0.558010093520958,
1.70050696717714E-15));
#19745=CARTESIAN_POINT('Ctrl Pts',(2.31148387864684,-0.609475073754277,
1.0547118733939E-15));
#19746=CARTESIAN_POINT('Ctrl Pts',(2.33139955447925,-0.660866145631631,
4.09844199643771E-16));
#19747=CARTESIAN_POINT('Ctrl Pts',(2.35440479749347,-0.711208818186421,
1.40927671219343E-15));
#19748=CARTESIAN_POINT('Ctrl Pts',(2.38034178509477,-0.760253836071474,
-1.37390099297363E-15));
#19749=CARTESIAN_POINT('Ctrl Pts',(2.38536182807648,-0.769746383995935,
-1.94096119465944E-15));
#19750=CARTESIAN_POINT('Ctrl Pts',(2.39049176520819,-0.779189910459008,
-1.05786827234693E-15));
#19751=CARTESIAN_POINT('Ctrl Pts',(2.39572358819186,-0.788570541648585,
-1.09634523681734E-15));
#19752=CARTESIAN_POINT('Ctrl Pts',(2.42367023236854,-0.838678728188221,
-1.88936709962824E-15));
#19753=CARTESIAN_POINT('Ctrl Pts',(2.45456608382348,-0.887081973696992,
3.65232473515907E-16));
#19754=CARTESIAN_POINT('Ctrl Pts',(2.48819247431748,-0.933519435542038,
2.77555756156289E-17));
#19755=CARTESIAN_POINT('Ctrl Pts',(2.51600207204131,-0.971924007494446,
-2.51343567462733E-16));
#19756=CARTESIAN_POINT('Ctrl Pts',(2.54568038471531,-1.00898433996931,-4.3693060571794E-16));
#19757=CARTESIAN_POINT('Ctrl Pts',(2.57712943690931,-1.04454500585365,2.4980018054066E-16));
#19758=CARTESIAN_POINT('Ctrl Pts',(2.58576841395081,-1.05431343303106,3.77772073805713E-16));
#19759=CARTESIAN_POINT('Ctrl Pts',(2.5945411341515,-1.06396863366007,-8.59691604797718E-16));
#19760=CARTESIAN_POINT('Ctrl Pts',(2.60344584338375,-1.07350722294854,1.66533453693773E-16));
#19761=CARTESIAN_POINT('Ctrl Pts',(2.61835241085208,-1.0894749116257,2.03691117354429E-15));
#19762=CARTESIAN_POINT('Ctrl Pts',(2.6336097141709,-1.10509519388837,4.91596122024362E-17));
#19763=CARTESIAN_POINT('Ctrl Pts',(2.64920051209182,-1.12034810033449,-6.66133814775094E-16));
#19764=CARTESIAN_POINT('Ctrl Pts',(2.69083818446211,-1.16108338049909,-2.5764371560264E-15));
#19765=CARTESIAN_POINT('Ctrl Pts',(2.73486472145526,-1.19921459067702,2.67919633695607E-16));
#19766=CARTESIAN_POINT('Ctrl Pts',(2.78109411133917,-1.23446584252596,-5.55111512312578E-17));
#19767=CARTESIAN_POINT('Ctrl Pts',(2.82095928310699,-1.26486419330493,-3.34416493233204E-16));
#19768=CARTESIAN_POINT('Ctrl Pts',(2.8624634969724,-1.29312108144354,-1.56006819163429E-15));
#19769=CARTESIAN_POINT('Ctrl Pts',(2.90551195584779,-1.31904027763685,-2.77555756156289E-17));
#19770=CARTESIAN_POINT('Ctrl Pts',(2.8546922928873,0.958179197573794,0.000498685380349445));
#19771=CARTESIAN_POINT('Ctrl Pts',(2.85850481197628,0.960904068967743,0.000332456920233391));
#19772=CARTESIAN_POINT('Ctrl Pts',(2.86233359432805,0.963606185523634,0.000166228460117303));
#19773=CARTESIAN_POINT('Ctrl Pts',(2.86617836717395,0.966285354738298,1.2490009027033E-15));
#19774=CARTESIAN_POINT('Ctrl Pts',(4.39104028268295,1.19243523336309,0.166013505999356));
#19775=CARTESIAN_POINT('Ctrl Pts',(4.78573455009837,0.910593977022875,0.139673936462541));
#19776=CARTESIAN_POINT('Ctrl Pts',(5.26671040851744,-0.0705935126856522,
0.0870010883098722));
#19777=CARTESIAN_POINT('Ctrl Pts',(4.42236229737626,-1.48797440454215,0.00799496154134886));
#19778=CARTESIAN_POINT('Ctrl Pts',(2.77646556351823,-1.55100085572438,-0.0710048743062135));
#19779=CARTESIAN_POINT('Ctrl Pts',(1.8231817769065,-0.209126570759914,-0.150004710153776));
#19780=CARTESIAN_POINT('Ctrl Pts',(2.4267807654254,1.3236028845817,-0.229004546001338));
#19781=CARTESIAN_POINT('Ctrl Pts',(4.03996554970546,1.65495464231977,-0.308004381848901));
#19782=CARTESIAN_POINT('Ctrl Pts',(5.19908829746563,0.485231098250064,-0.387004217696463));
#19783=CARTESIAN_POINT('Ctrl Pts',(4.85266468272742,-1.12486221135666,-0.466004053544026));
#19784=CARTESIAN_POINT('Ctrl Pts',(3.31493037813578,-1.71438530937678,-0.545003889391588));
#19785=CARTESIAN_POINT('Ctrl Pts',(1.98095238924354,-0.748650010516562,
-0.624003725239151));
#19786=CARTESIAN_POINT('Ctrl Pts',(2.06091425900795,0.896290333456293,-0.703003561086713));
#19787=CARTESIAN_POINT('Ctrl Pts',(3.48228013532258,1.7280964959961,-0.782003396934276));
#19788=CARTESIAN_POINT('Ctrl Pts',(4.95557248446353,0.992166550039036,-0.861003232781839));
#19789=CARTESIAN_POINT('Ctrl Pts',(5.14421062951873,-0.643868150032796,
-0.9400030686294));
#19790=CARTESIAN_POINT('Ctrl Pts',(3.87705966552992,-1.6957787847533,-1.01900290447696));
#19791=CARTESIAN_POINT('Ctrl Pts',(2.30368936823014,-1.20926655124093,-1.09800274032452));
#19792=CARTESIAN_POINT('Ctrl Pts',(1.85147337579044,0.374302296113376,-1.17700257617209));
#19793=CARTESIAN_POINT('Ctrl Pts',(2.93066571761574,1.61830089654537,-1.25600241201965));
#19794=CARTESIAN_POINT('Ctrl Pts',(4.56221455954657,1.394164357391,-1.33500224786721));
#19795=CARTESIAN_POINT('Ctrl Pts',(5.26596601862656,-0.0947691059850859,
-1.41400208371477));
#19796=CARTESIAN_POINT('Ctrl Pts',(4.40347122688333,-1.49772725382214,-1.49300191956234));
#19797=CARTESIAN_POINT('Ctrl Pts',(2.75719224100921,-1.54193549825478,-1.5720017554099));
#19798=CARTESIAN_POINT('Ctrl Pts',(1.82064627705295,-0.187287741932202,
-1.65100159125746));
#19799=CARTESIAN_POINT('Ctrl Pts',(2.44347518930979,1.33726891870949,-1.73000142710503));
#19800=CARTESIAN_POINT('Ctrl Pts',(4.06064369715841,1.64864472003992,-1.80900126295258));
#19801=CARTESIAN_POINT('Ctrl Pts',(5.20504383428331,0.464357085917297,-1.88800109880015));
#19802=CARTESIAN_POINT('Ctrl Pts',(4.83846681093798,-1.14119894150869,-1.96700093464771));
#19803=CARTESIAN_POINT('Ctrl Pts',(3.29347418099175,-1.71145032981342,-2.04600077049527));
#19804=CARTESIAN_POINT('Ctrl Pts',(1.97169538830959,-0.729060541700552,
-2.12500060634284));
#19805=CARTESIAN_POINT('Ctrl Pts',(2.07225853125702,0.914738693744935,-2.2040004421904));
#19806=CARTESIAN_POINT('Ctrl Pts',(3.50393193697739,1.72867980446563,-2.28300027803796));
#19807=CARTESIAN_POINT('Ctrl Pts',(4.96789025142369,0.974349024284007,-2.36200011388552));
#19808=CARTESIAN_POINT('Ctrl Pts',(5.13601899785199,-0.663918840546727,
-2.44099994973308));
#19809=CARTESIAN_POINT('Ctrl Pts',(3.85579045748996,-1.69987432066465,-2.51999978558065));
#19810=CARTESIAN_POINT('Ctrl Pts',(2.28863801351722,-1.19369047097085,-2.59899962142821));
#19811=CARTESIAN_POINT('Ctrl Pts',(1.85629466717739,0.395418745920643,-2.67799945727578));
#19812=CARTESIAN_POINT('Ctrl Pts',(2.95098569669531,1.62580097199172,-2.75699929312333));
#19813=CARTESIAN_POINT('Ctrl Pts',(4.57959880542434,1.38124379173793,-2.8359991289709));
#19814=CARTESIAN_POINT('Ctrl Pts',(5.26464339451333,-0.11638860083937,-2.91499896481845));
#19815=CARTESIAN_POINT('Ctrl Pts',(4.38464163429993,-1.508432340942,-2.99399880066603));
#19816=CARTESIAN_POINT('Ctrl Pts',(2.73793803074369,-1.53201441829649,-3.07299863651358));
#19817=CARTESIAN_POINT('Ctrl Pts',(1.81843502163546,-0.165740987178738,
-3.15199847236115));
#19818=CARTESIAN_POINT('Ctrl Pts',(2.46031295606552,1.35089396877779,-3.23099830820871));
#19819=CARTESIAN_POINT('Ctrl Pts',(4.08125513238924,1.64198731008323,-3.30999814405628));
#19820=CARTESIAN_POINT('Ctrl Pts',(5.21073008185995,0.443456872065259,-3.38899797990383));
#19821=CARTESIAN_POINT('Ctrl Pts',(4.82406926255307,-1.1573811219711,-3.4679978157514));
#19822=CARTESIAN_POINT('Ctrl Pts',(3.27205440550583,-1.7082338752928,-3.54699765159896));
#19823=CARTESIAN_POINT('Ctrl Pts',(1.96268557425322,-0.709363445216102,
-3.62599748744653));
#19824=CARTESIAN_POINT('Ctrl Pts',(2.08383245266016,0.933047071734419,-3.70499732329408));
#19825=CARTESIAN_POINT('Ctrl Pts',(3.52558964148418,1.72898995964266,-3.78399715914165));
#19826=CARTESIAN_POINT('Ctrl Pts',(4.97998369946044,0.956379581469577,-3.86299699498921));
#19827=CARTESIAN_POINT('Ctrl Pts',(5.12757691841429,-0.683865861766359,
-3.94199683083677));
#19828=CARTESIAN_POINT('Ctrl Pts',(3.83447157132285,-1.7037028260214,-4.02099666668433));
#19829=CARTESIAN_POINT('Ctrl Pts',(2.27378298153172,-1.17792721035138,-4.0999965025319));
#19830=CARTESIAN_POINT('Ctrl Pts',(1.86138009102058,0.416473218723921,-4.17899633837946));
#19831=CARTESIAN_POINT('Ctrl Pts',(2.97139803993003,1.63304587394689,-4.25799617422703));
#19832=CARTESIAN_POINT('Ctrl Pts',(4.59681983000601,1.36810649091058,-4.33699601007458));
#19833=CARTESIAN_POINT('Ctrl Pts',(5.26305005173533,-0.137989841995099,
-4.41599584592215));
#19834=CARTESIAN_POINT('Ctrl Pts',(4.36567941724011,-1.51890070685318,-4.49499568176971));
#19835=CARTESIAN_POINT('Ctrl Pts',(2.71880961159543,-1.52185292521907,-4.57399551761728));
#19836=CARTESIAN_POINT('Ctrl Pts',(1.81649385243162,-0.144168221412696,
-4.65299535346484));
#19837=CARTESIAN_POINT('Ctrl Pts',(2.47732008074839,1.36430702475679,-4.7319951893124));
#19838=CARTESIAN_POINT('Ctrl Pts',(4.1017815539197,1.63507222658209,-4.81099502515996));
#19839=CARTESIAN_POINT('Ctrl Pts',(5.21615406946798,0.422487067128113,-4.88999486100753));
#19840=CARTESIAN_POINT('Ctrl Pts',(4.8094701320957,-1.17338167666657,-4.96899469685509));
#19841=CARTESIAN_POINT('Ctrl Pts',(3.25067660275509,-1.70474935090286,-5.04799453270265));
#19842=CARTESIAN_POINT('Ctrl Pts',(1.95392320970657,-0.689555029625102,
-5.12699436855021));
#19843=CARTESIAN_POINT('Ctrl Pts',(2.09563481222965,0.951209028381946,-5.20599420439778));
#19844=CARTESIAN_POINT('Ctrl Pts',(3.54724953190536,1.72902878768242,-5.28499404024534));
#19845=CARTESIAN_POINT('Ctrl Pts',(4.9918510980865,0.938260055799061,-5.3639938760929));
#19846=CARTESIAN_POINT('Ctrl Pts',(5.11888562803801,-0.703705565198355,
-5.44299371194047));
#19847=CARTESIAN_POINT('Ctrl Pts',(3.81310639881089,-1.70726397249534,-5.52199354778801));
#19848=CARTESIAN_POINT('Ctrl Pts',(2.25912657912977,-1.16197909982672,-5.60099338363559));
#19849=CARTESIAN_POINT('Ctrl Pts',(1.86672886205842,0.43746233516695,-5.67999321948314));
#19850=CARTESIAN_POINT('Ctrl Pts',(2.99189953732774,1.64003450508086,-5.75899305533072));
#19851=CARTESIAN_POINT('Ctrl Pts',(4.61387493436243,1.35475449570142,-5.83799289117827));
#19852=CARTESIAN_POINT('Ctrl Pts',(5.26118623847484,-0.159569428664093,
-5.91699272702583));
#19853=CARTESIAN_POINT('Ctrl Pts',(4.34658755238584,-1.52913071452965,-5.99599256287339));
#19854=CARTESIAN_POINT('Ctrl Pts',(2.69980998483775,-1.5114526106208,-6.07499239872097));
#19855=CARTESIAN_POINT('Ctrl Pts',(1.81482307433549,-0.122572831598478,
-6.15399223456852));
#19856=CARTESIAN_POINT('Ctrl Pts',(2.49449389432028,1.37750598259717,-6.23299207041608));
#19857=CARTESIAN_POINT('Ctrl Pts',(4.12221974065168,1.62790055426783,-6.31199190626365));
#19858=CARTESIAN_POINT('Ctrl Pts',(5.22131494589194,0.401450962089136,-6.39099174211121));
#19859=CARTESIAN_POINT('Ctrl Pts',(4.79467171060061,-1.18919809477965,-6.46999157795877));
#19860=CARTESIAN_POINT('Ctrl Pts',(3.22934412750707,-1.70099730339957,-6.54899141380633));
#19861=CARTESIAN_POINT('Ctrl Pts',(1.94540966973674,-0.669638403458603,
-6.62799124965391));
#19862=CARTESIAN_POINT('Ctrl Pts',(2.10766375784038,0.969221713583442,-6.70699108550145));
#19863=CARTESIAN_POINT('Ctrl Pts',(3.56890820919659,1.72879628248244,-6.78599092134903));
#19864=CARTESIAN_POINT('Ctrl Pts',(5.00349058497245,0.919993290740459,-6.86499075719659));
#19865=CARTESIAN_POINT('Ctrl Pts',(5.10994649063147,-0.723434837437879,
-6.94399059304415));
#19866=CARTESIAN_POINT('Ctrl Pts',(3.79169829275028,-1.71055720124108,-7.02299042889171));
#19867=CARTESIAN_POINT('Ctrl Pts',(2.24467110631318,-1.14584864210466,-7.10199026473928));
#19868=CARTESIAN_POINT('Ctrl Pts',(1.87234014091828,0.458382801467482,-7.18099010058684));
#19869=CARTESIAN_POINT('Ctrl Pts',(3.01248697162693,1.64676576868065,-7.2599899364344));
#19870=CARTESIAN_POINT('Ctrl Pts',(4.63076144206815,1.34118990141411,-7.33898977228196));
#19871=CARTESIAN_POINT('Ctrl Pts',(5.25905224721656,-0.181123974402424,
-7.41798960812953));
#19872=CARTESIAN_POINT('Ctrl Pts',(4.32736903578763,-1.53912075859537,-7.49698944397708));
#19873=CARTESIAN_POINT('Ctrl Pts',(2.68094213204631,-1.50081510660373,-7.57598927982465));
#19874=CARTESIAN_POINT('Ctrl Pts',(1.81342294953926,-0.100958206659705,
-7.6549891156722));
#19875=CARTESIAN_POINT('Ctrl Pts',(2.51183170172664,1.3904887710106,-7.73398895151979));
#19876=CARTESIAN_POINT('Ctrl Pts',(4.14256648525937,1.62047341857881,-7.81298878736733));
#19877=CARTESIAN_POINT('Ctrl Pts',(5.22621190124433,0.380351858102332,-7.89198862321491));
#19878=CARTESIAN_POINT('Ctrl Pts',(4.77967632035796,-1.20482789426491,-7.97098845906245));
#19879=CARTESIAN_POINT('Ctrl Pts',(3.20806032742391,-1.69697832159357,-8.04998829491003));
#19880=CARTESIAN_POINT('Ctrl Pts',(1.93714629036355,-0.649616692178436,
-8.12898813075759));
#19881=CARTESIAN_POINT('Ctrl Pts',(2.11991740180112,0.987082300609951,-8.20798796660515));
#19882=CARTESIAN_POINT('Ctrl Pts',(3.590562274524,1.72829248059039,-8.28698780245271));
#19883=CARTESIAN_POINT('Ctrl Pts',(5.01490033351429,0.901582152746688,-8.36598763830028));
#19884=CARTESIAN_POINT('Ctrl Pts',(5.100760909075,-0.743050582186251,-8.44498747414783));
#19885=CARTESIAN_POINT('Ctrl Pts',(3.77025061252596,-1.71358199587885,-8.52398730999541));
#19886=CARTESIAN_POINT('Ctrl Pts',(2.23041883183543,-1.12953836770797,-8.60298714584296));
#19887=CARTESIAN_POINT('Ctrl Pts',(1.87821304649392,0.479231333095078,-8.68198698169053));
#19888=CARTESIAN_POINT('Ctrl Pts',(3.03315711310502,1.65323861131456,-8.76098681753808));
#19889=CARTESIAN_POINT('Ctrl Pts',(4.64747670120603,1.32741483121271,-8.83998665338566));
#19890=CARTESIAN_POINT('Ctrl Pts',(5.25664841655105,-0.202650086230401,
-8.9189864892332));
#19891=CARTESIAN_POINT('Ctrl Pts',(4.30802687631991,-1.54886929123672,-8.99798632508078));
#19892=CARTESIAN_POINT('Ctrl Pts',(2.6622090275294,-1.48994204463143,-9.07698616092833));
#19893=CARTESIAN_POINT('Ctrl Pts',(1.81229367225287,-0.0793278105488914,
-9.15598599677591));
#19894=CARTESIAN_POINT('Ctrl Pts',(2.52933083069636,1.40325348959643,-9.23498583262345));
#19895=CARTESIAN_POINT('Ctrl Pts',(4.16281850248374,1.61279172453447,-9.31398566847103));
#19896=CARTESIAN_POINT('Ctrl Pts',(5.23084434257772,0.359193561697825,-9.39298550431858));
#19897=CARTESIAN_POINT('Ctrl Pts',(4.76448598072016,-1.22026956478995,-9.47198534016615));
#19898=CARTESIAN_POINT('Ctrl Pts',(3.18682917751138,-1.69269124367719,-9.55098517601371));
#19899=CARTESIAN_POINT('Ctrl Pts',(1.92913316060619,-0.629496447108055,
-9.62998501186127));
#19900=CARTESIAN_POINT('Ctrl Pts',(2.13239611830123,1.00479447126442,-9.70898484770884));
#19901=CARTESIAN_POINT('Ctrl Pts',(3.61220396058553,1.7275051272171,-9.7879846835564));
#19902=CARTESIAN_POINT('Ctrl Pts',(5.02608686342242,0.883052990217761,-9.86698451940395));
#19903=CARTESIAN_POINT('Ctrl Pts',(5.09131451863736,-0.762594341224724,
-9.94598435525153));
#19904=CARTESIAN_POINT('Ctrl Pts',(3.7487967880808,-1.71625301028161,-10.0249841910991));
#19905=CARTESIAN_POINT('Ctrl Pts',(2.21631480459542,-1.11321229367821,-10.1039840269467));
#19906=CARTESIAN_POINT('Ctrl Pts',(1.88445547370457,0.500312018724167,-10.1829838627942));
#19907=CARTESIAN_POINT('Ctrl Pts',(3.05369936202752,1.65886512673652,-10.2619836986418));
#19908=CARTESIAN_POINT('Ctrl Pts',(4.66441579808227,1.31456735634548,-10.3409835344894));
#19909=CARTESIAN_POINT('Ctrl Pts',(5.25318976192693,-0.226472583690619,
-10.4199833703369));
#19910=CARTESIAN_POINT('Ctrl Pts',(4.61130290174357,-1.11057344913152,-10.4726499275686));
#19911=CARTESIAN_POINT('Ctrl Pts',(4.17428909295502,-1.32062757704312,-10.4989832061845));
#19912=CARTESIAN_POINT('Ctrl Pts',(4.33494771810971,1.113885518109,0.110286691365708));
#19913=CARTESIAN_POINT('Ctrl Pts',(4.70364214800736,0.850610092275097,0.083947121828893));
#19914=CARTESIAN_POINT('Ctrl Pts',(5.15293451061394,-0.065943280819724,
0.0312742736762238));
#19915=CARTESIAN_POINT('Ctrl Pts',(4.36420644645715,-1.38995653110804,-0.0477318530922994));
#19916=CARTESIAN_POINT('Ctrl Pts',(2.82673046046441,-1.44883121818993,-0.126731688939862));
#19917=CARTESIAN_POINT('Ctrl Pts',(1.9362426797905,-0.195350700904968,-0.205731524787425));
#19918=CARTESIAN_POINT('Ctrl Pts',(2.50008057491893,1.23641271543502,-0.284731360634987));
#19919=CARTESIAN_POINT('Ctrl Pts',(4.00699945736041,1.54593721959065,-0.363731196482549));
#19920=CARTESIAN_POINT('Ctrl Pts',(5.0897668952189,0.453267295492844,-0.442731032330112));
#19921=CARTESIAN_POINT('Ctrl Pts',(4.76616336792331,-1.050763758099,-0.521730868177675));
#19922=CARTESIAN_POINT('Ctrl Pts',(3.32972478856904,-1.60145298892903,-0.600730704025237));
#19923=CARTESIAN_POINT('Ctrl Pts',(2.08362041180346,-0.69933391895392,-0.6797305398728));
#19924=CARTESIAN_POINT('Ctrl Pts',(2.15831492454466,0.837248677768694,-0.758730375720361));
#19925=CARTESIAN_POINT('Ctrl Pts',(3.4860506549758,1.61426097361787,-0.837730211567926));
#19926=CARTESIAN_POINT('Ctrl Pts',(4.86229228700177,0.926809205833092,-0.916730047415487));
#19927=CARTESIAN_POINT('Ctrl Pts',(5.03850420364174,-0.601454391674104,
-0.99572988326305));
#19928=CARTESIAN_POINT('Ctrl Pts',(3.85482473111879,-1.58407213859808,-1.07472971911061));
#19929=CARTESIAN_POINT('Ctrl Pts',(2.38509762162855,-1.12960810052711,-1.15372955495818));
#19930=CARTESIAN_POINT('Ctrl Pts',(1.96267061599973,0.349645746259735,-1.23272939080574));
#19931=CARTESIAN_POINT('Ctrl Pts',(2.97077293231841,1.51169797920237,-1.3117292266533));
#19932=CARTESIAN_POINT('Ctrl Pts',(4.49484617023228,1.30232606695269,-1.39072906250087));
#19933=CARTESIAN_POINT('Ctrl Pts',(5.15223915618622,-0.08852634656157,-1.46972889834842));
#19934=CARTESIAN_POINT('Ctrl Pts',(4.3465597942492,-1.3990669274376,-1.54872873419599));
#19935=CARTESIAN_POINT('Ctrl Pts',(2.80872673646503,-1.44036302627531,-1.62772857004355));
#19936=CARTESIAN_POINT('Ctrl Pts',(1.93387420183125,-0.174950469107858,
-1.70672840589111));
#19937=CARTESIAN_POINT('Ctrl Pts',(2.5156752810109,1.24917852197866,-1.78572824173868));
#19938=CARTESIAN_POINT('Ctrl Pts',(4.02631546576466,1.5400429530919,-1.86472807758624));
#19939=CARTESIAN_POINT('Ctrl Pts',(5.09533012081654,0.433768324486494,-1.9437279134338));
#19940=CARTESIAN_POINT('Ctrl Pts',(4.75290075765169,-1.06602433294655,-2.02272774928136));
#19941=CARTESIAN_POINT('Ctrl Pts',(3.30968198322101,-1.59871134633068,-2.10172758512893));
#19942=CARTESIAN_POINT('Ctrl Pts',(2.07497320062339,-0.681034874266973,
-2.18072742097649));
#19943=CARTESIAN_POINT('Ctrl Pts',(2.16891191146536,0.854481782580953,-2.25972725682405));
#19944=CARTESIAN_POINT('Ctrl Pts',(3.50627617970828,1.61480585759867,-2.33872709267161));
#19945=CARTESIAN_POINT('Ctrl Pts',(4.87379864126613,0.910165380364193,-2.41772692851917));
#19946=CARTESIAN_POINT('Ctrl Pts',(5.03085218227572,-0.620184275836084,
-2.49672676436674));
#19947=CARTESIAN_POINT('Ctrl Pts',(3.8349565972743,-1.58789788779847,-2.5757266002143));
#19948=CARTESIAN_POINT('Ctrl Pts',(2.37103775022121,-1.1150580689981,-2.65472643606186));
#19949=CARTESIAN_POINT('Ctrl Pts',(1.96717431272409,0.369371184569583,-2.73372627190943));
#19950=CARTESIAN_POINT('Ctrl Pts',(2.98975436610342,1.51870399947977,-2.81272610775699));
#19951=CARTESIAN_POINT('Ctrl Pts',(4.51108525742519,1.29025662237067,-2.89172594360455));
#19952=CARTESIAN_POINT('Ctrl Pts',(5.15100365776719,-0.108721692651017,
-2.97072577945211));
#19953=CARTESIAN_POINT('Ctrl Pts',(4.32897057019432,-1.40906683450114,-3.04972561529968));
#19954=CARTESIAN_POINT('Ctrl Pts',(2.79074086572141,-1.43109548118747,-3.12872545114724));
#19955=CARTESIAN_POINT('Ctrl Pts',(1.93180860923765,-0.154823071484393,
-3.2077252869948));
#19956=CARTESIAN_POINT('Ctrl Pts',(2.53140388749766,1.2619060442205,-3.28672512284236));
#19957=CARTESIAN_POINT('Ctrl Pts',(4.045569156505,1.53382408909712,-3.36572495868993));
#19958=CARTESIAN_POINT('Ctrl Pts',(5.10064179616025,0.41424487794298,-3.44472479453749));
#19959=CARTESIAN_POINT('Ctrl Pts',(4.73945162415284,-1.08114053881181,-3.52372463038505));
#19960=CARTESIAN_POINT('Ctrl Pts',(3.28967320031411,-1.59570677047621,-3.60272446623261));
#19961=CARTESIAN_POINT('Ctrl Pts',(2.06655689329076,-0.662635291707721,
-3.68172430208018));
#19962=CARTESIAN_POINT('Ctrl Pts',(2.17972341977875,0.871584126198421,-3.76072413792774));
#19963=CARTESIAN_POINT('Ctrl Pts',(3.52650721845205,1.6150955818121,-3.8397239737753));
#19964=CARTESIAN_POINT('Ctrl Pts',(4.88509545324823,0.893379645123019,-3.91872380962286));
#19965=CARTESIAN_POINT('Ctrl Pts',(5.02296621097492,-0.638817319748494,
-3.99772364547043));
#19966=CARTESIAN_POINT('Ctrl Pts',(3.81504205776779,-1.59147419664407,-4.07672348131799));
#19967=CARTESIAN_POINT('Ctrl Pts',(2.35716126910365,-1.10033318731819,-4.15572331716555));
#19968=CARTESIAN_POINT('Ctrl Pts',(1.97192474261234,0.389038728508927,-4.23472315301311));
#19969=CARTESIAN_POINT('Ctrl Pts',(3.00882207970637,1.52547165540118,-4.31372298886068));
#19970=CARTESIAN_POINT('Ctrl Pts',(4.52717187525719,1.2779847196885,-4.39272282470824));
#19971=CARTESIAN_POINT('Ctrl Pts',(5.1495152738314,-0.128899987474363,-4.4717226605558));
#19972=CARTESIAN_POINT('Ctrl Pts',(4.31125745808291,-1.41884561397736,-4.55072249640336));
#19973=CARTESIAN_POINT('Ctrl Pts',(2.77287249981153,-1.42160335980039,-4.62972233225093));
#19974=CARTESIAN_POINT('Ctrl Pts',(1.92999531137135,-0.13467137628114,-4.70872216809848));
#19975=CARTESIAN_POINT('Ctrl Pts',(2.54729069573586,1.27443553713597,-4.78772200394605));
#19976=CARTESIAN_POINT('Ctrl Pts',(4.06474343368305,1.52736452538001,-4.86672183979361));
#19977=CARTESIAN_POINT('Ctrl Pts',(5.10570848748063,0.394656424512951,-4.94572167564119));
#19978=CARTESIAN_POINT('Ctrl Pts',(4.72581418746994,-1.09608708320963,-5.02472151148873));
#19979=CARTESIAN_POINT('Ctrl Pts',(3.26970362525728,-1.59245178341539,-5.10372134733631));
#19980=CARTESIAN_POINT('Ctrl Pts',(2.05837173513724,-0.644131723005486,
-5.18272118318386));
#19981=CARTESIAN_POINT('Ctrl Pts',(2.19074831826896,0.888549693739684,-5.26172101903143));
#19982=CARTESIAN_POINT('Ctrl Pts',(3.54674029911668,1.61513185211844,-5.34072085487899));
#19983=CARTESIAN_POINT('Ctrl Pts',(4.89618110645381,0.876453713487748,-5.41972069072655));
#19984=CARTESIAN_POINT('Ctrl Pts',(5.01484744509737,-0.657350115256517,
-5.49872052657412));
#19985=CARTESIAN_POINT('Ctrl Pts',(3.79508428095349,-1.59480075843476,-5.57772036242167));
#19986=CARTESIAN_POINT('Ctrl Pts',(2.34347033317158,-1.08543563241745,-5.65672019826925));
#19987=CARTESIAN_POINT('Ctrl Pts',(1.97692117213072,0.408645221331059,-5.73572003411679));
#19988=CARTESIAN_POINT('Ctrl Pts',(3.02797307458803,1.53199992192143,-5.81471986996437));
#19989=CARTESIAN_POINT('Ctrl Pts',(4.54310350258665,1.26551226526479,-5.89371970581192));
#19990=CARTESIAN_POINT('Ctrl Pts',(5.14777423621256,-0.149058054264775,
-5.97271954165949));
#19991=CARTESIAN_POINT('Ctrl Pts',(4.29342323851284,-1.42840173667663,-6.05171937750705));
#19992=CARTESIAN_POINT('Ctrl Pts',(2.75512444230473,-1.41188814886847,-6.13071921335461));
#19993=CARTESIAN_POINT('Ctrl Pts',(1.92843459304201,-0.114498547351779,
-6.20971904920218));
#19994=CARTESIAN_POINT('Ctrl Pts',(2.56333321250591,1.28676503527658,-6.28871888504973));
#19995=CARTESIAN_POINT('Ctrl Pts',(4.08383528838526,1.52066527521701,-6.3677187208973));
#19996=CARTESIAN_POINT('Ctrl Pts',(5.11052939963465,0.37500603839156,-6.44671855674487));
#19997=CARTESIAN_POINT('Ctrl Pts',(4.71199058771956,-1.11086162072043,-6.52571839259242));
#19998=CARTESIAN_POINT('Ctrl Pts',(3.24977639182829,-1.58894689588755,-6.60471822843999));
#19999=CARTESIAN_POINT('Ctrl Pts',(2.05041901064964,-0.625527071921937,
-6.68371806428756));
#20000=CARTESIAN_POINT('Ctrl Pts',(2.20198487681655,0.905375822846601,-6.7627179001351));
#20001=CARTESIAN_POINT('Ctrl Pts',(3.5669722465643,1.61491466281716,-6.84171773598269));
#20002=CARTESIAN_POINT('Ctrl Pts',(4.90705386123136,0.859390241617592,-6.92071757183023));
#20003=CARTESIAN_POINT('Ctrl Pts',(5.00649715870617,-0.675779754045749,
-6.99971740767781));
#20004=CARTESIAN_POINT('Ctrl Pts',(3.77508639876763,-1.59787705113819,-7.07871724352536));
#20005=CARTESIAN_POINT('Ctrl Pts',(2.32996709091799,-1.07036774214185,-7.15771707937293));
#20006=CARTESIAN_POINT('Ctrl Pts',(1.98216281719889,0.428187586226241,-7.23671691522048));
#20007=CARTESIAN_POINT('Ctrl Pts',(3.04720434541876,1.53828777457171,-7.31571675106806));
#20008=CARTESIAN_POINT('Ctrl Pts',(4.55887763929323,1.25284121637851,-7.3947165869156));
#20009=CARTESIAN_POINT('Ctrl Pts',(5.14578081812842,-0.169192729654759,
-7.47371642276319));
#20010=CARTESIAN_POINT('Ctrl Pts',(4.27547071017476,-1.43773370297445,-7.55271625861073));
#20011=CARTESIAN_POINT('Ctrl Pts',(2.73749947837029,-1.40195137298167,-7.6317160944583));
#20012=CARTESIAN_POINT('Ctrl Pts',(1.92712669917035,-0.0943077503801438,
-7.71071593030587));
#20013=CARTESIAN_POINT('Ctrl Pts',(2.57952892028556,1.29889260379668,-7.78971576615342));
#20014=CARTESIAN_POINT('Ctrl Pts',(4.10284172456313,1.51372738991008,-7.868715602001));
#20015=CARTESIAN_POINT('Ctrl Pts',(5.11510377608481,0.355296803274704,-7.94771543784854));
#20016=CARTESIAN_POINT('Ctrl Pts',(4.69798299421482,-1.12546183279944,-8.02671527369611));
#20017=CARTESIAN_POINT('Ctrl Pts',(3.2298946271675,-1.58519265791639,-8.10571510954367));
#20018=CARTESIAN_POINT('Ctrl Pts',(2.04269996783968,-0.606824258034226,
-8.18471494539124));
#20019=CARTESIAN_POINT('Ctrl Pts',(2.21343133207891,0.922059872996347,-8.2637147812388));
#20020=CARTESIAN_POINT('Ctrl Pts',(3.58719988585365,1.61444404804845,-8.34271461708637));
#20021=CARTESIAN_POINT('Ctrl Pts',(4.91771201130145,0.842191907142578,-8.42171445293392));
#20022=CARTESIAN_POINT('Ctrl Pts',(4.99791666226923,-0.69410334378111,-8.50071428878149));
#20023=CARTESIAN_POINT('Ctrl Pts',(3.75505154930119,-1.60070259239024,-8.57971412462905));
#20024=CARTESIAN_POINT('Ctrl Pts',(2.31665366164594,-1.05513188032014,-8.65871396047662));
#20025=CARTESIAN_POINT('Ctrl Pts',(1.98764885475204,0.44766275502708,-8.73771379632417));
#20026=CARTESIAN_POINT('Ctrl Pts',(3.06651287522861,1.5443342293134,-8.81671363217174));
#20027=CARTESIAN_POINT('Ctrl Pts',(4.57449180815055,1.23997355633378,-8.8957134680193));
#20028=CARTESIAN_POINT('Ctrl Pts',(5.1435353358654,-0.189300844171595,-8.97471330386686));
#20029=CARTESIAN_POINT('Ctrl Pts',(4.2574026837384,-1.44684006701688,-9.05371313971443));
#20030=CARTESIAN_POINT('Ctrl Pts',(2.72000038638879,-1.3917945561336,-9.13271297556199));
#20031=CARTESIAN_POINT('Ctrl Pts',(1.92607181117305,-0.0741022211365624,
-9.21171281140954));
#20032=CARTESIAN_POINT('Ctrl Pts',(2.59587532283516,1.31081646748141,-9.29071264725712));
#20033=CARTESIAN_POINT('Ctrl Pts',(4.12175967336872,1.50655171486196,-9.36971248310467));
#20034=CARTESIAN_POINT('Ctrl Pts',(5.11943106294313,0.335532274943578,-9.44871231895224));
#20035=CARTESIAN_POINT('Ctrl Pts',(4.68379329328662,-1.13988630860492,-9.52771215479979));
#20036=CARTESIAN_POINT('Ctrl Pts',(3.21006204443369,-1.58118798422641,-9.60671199064737));
#20037=CARTESIAN_POINT('Ctrl Pts',(2.03521468986255,-0.588029401108125,
-9.68571182649492));
#20038=CARTESIAN_POINT('Ctrl Pts',(2.22508803359624,0.938605283459143,-9.76471166234249));
#20039=CARTESIAN_POINT('Ctrl Pts',(3.60741596134095,1.61370856028727,-9.84371149819005));
#20040=CARTESIAN_POINT('Ctrl Pts',(4.92816164689921,0.824883322805087,-9.92271133403761));
#20041=CARTESIAN_POINT('Ctrl Pts',(4.9890925373084,-0.712359689747145,-10.0017111698852));
#20042=CARTESIAN_POINT('Ctrl Pts',(3.7350109603544,-1.60319765810002,-10.0807110057327));
#20043=CARTESIAN_POINT('Ctrl Pts',(2.30347871406799,-1.03988125964027,-10.1597108415803));
#20044=CARTESIAN_POINT('Ctrl Pts',(1.99348007230855,0.467354785065328,-10.2387106774279));
#20045=CARTESIAN_POINT('Ctrl Pts',(3.0857019371952,1.54959010726013,-10.3177105132754));
#20046=CARTESIAN_POINT('Ctrl Pts',(4.59031506980232,1.22797238780195,-10.396710349123));
#20047=CARTESIAN_POINT('Ctrl Pts',(5.14030451444203,-0.211554073683514,
-10.4757101849706));
#20048=CARTESIAN_POINT('Ctrl Pts',(4.54070089839809,-1.03741624465007,-10.5283767422023));
#20049=CARTESIAN_POINT('Ctrl Pts',(4.1324746575059,-1.23363340140067,-10.5547100208181));
#20050=CARTESIAN_POINT('Ctrl Pts',(4.27885515353647,1.0353358028549,0.0545598767320594));
#20051=CARTESIAN_POINT('Ctrl Pts',(4.62154974591635,0.790626207527318,0.0282203071952445));
#20052=CARTESIAN_POINT('Ctrl Pts',(5.03915861271046,-0.0612930489537958,
-0.0244525409574245));
#20053=CARTESIAN_POINT('Ctrl Pts',(4.30605059553801,-1.29193865767393,-0.103458667725947));
#20054=CARTESIAN_POINT('Ctrl Pts',(2.87699535741062,-1.34666158065549,-0.18245850357351));
#20055=CARTESIAN_POINT('Ctrl Pts',(2.04930358267447,-0.181574831050025,
-0.261458339421073));
#20056=CARTESIAN_POINT('Ctrl Pts',(2.57338038441246,1.14922254628835,-0.340458175268635));
#20057=CARTESIAN_POINT('Ctrl Pts',(3.97403336501536,1.4369197968615,-0.419458011116198));
#20058=CARTESIAN_POINT('Ctrl Pts',(4.9804454929722,0.421303492735624,-0.498457846963761));
#20059=CARTESIAN_POINT('Ctrl Pts',(4.67966205311918,-0.976665304841327,
-0.577457682811322));
#20060=CARTESIAN_POINT('Ctrl Pts',(3.3445191990023,-1.48852066848128,-0.656457518658885));
#20061=CARTESIAN_POINT('Ctrl Pts',(2.18628843436339,-0.650017827391278,
-0.735457354506447));
#20062=CARTESIAN_POINT('Ctrl Pts',(2.25571559008138,0.778207022081096,-0.814457190354011));
#20063=CARTESIAN_POINT('Ctrl Pts',(3.48982117462903,1.50042545123965,-0.893457026201572));
#20064=CARTESIAN_POINT('Ctrl Pts',(4.76901208954002,0.861451861627147,-0.972456862049136));
#20065=CARTESIAN_POINT('Ctrl Pts',(4.93279777776475,-0.559040633315412,
-1.0514566978967));
#20066=CARTESIAN_POINT('Ctrl Pts',(3.83258979670766,-1.47236549244286,-1.13045653374427));
#20067=CARTESIAN_POINT('Ctrl Pts',(2.46650587502695,-1.04994964981329,-1.20945636959183));
#20068=CARTESIAN_POINT('Ctrl Pts',(2.07386785620901,0.324989196406094,-1.28845620543939));
#20069=CARTESIAN_POINT('Ctrl Pts',(3.01088014702108,1.40509506185938,-1.36745604128694));
#20070=CARTESIAN_POINT('Ctrl Pts',(4.42747778091797,1.21048777651438,-1.44645587713451));
#20071=CARTESIAN_POINT('Ctrl Pts',(5.0385122937459,-0.0822835871380551,
-1.52545571298208));
#20072=CARTESIAN_POINT('Ctrl Pts',(4.28964836161505,-1.30040660105306,-1.60445554882964));
#20073=CARTESIAN_POINT('Ctrl Pts',(2.86026123192082,-1.33879055429585,-1.68345538467719));
#20074=CARTESIAN_POINT('Ctrl Pts',(2.04710212660955,-0.162613196283514,
-1.76245522052476));
#20075=CARTESIAN_POINT('Ctrl Pts',(2.58787537271199,1.16108812524782,-1.84145505637233));
#20076=CARTESIAN_POINT('Ctrl Pts',(3.99198723437091,1.43144118614388,-1.92045489221988));
#20077=CARTESIAN_POINT('Ctrl Pts',(4.98561640734979,0.40317956305569,-1.99945472806744));
#20078=CARTESIAN_POINT('Ctrl Pts',(4.6673347043654,-0.990849724384406,-2.078454563915));
#20079=CARTESIAN_POINT('Ctrl Pts',(3.32588978545028,-1.48597236284793,-2.15745439976257));
#20080=CARTESIAN_POINT('Ctrl Pts',(2.17825101293718,-0.633009206833395,
-2.23645423561013));
#20081=CARTESIAN_POINT('Ctrl Pts',(2.26556529167371,0.79422487141697,-2.31545407145769));
#20082=CARTESIAN_POINT('Ctrl Pts',(3.50862042243917,1.50093191073172,-2.39445390730526));
#20083=CARTESIAN_POINT('Ctrl Pts',(4.77970703110856,0.84598173644438,-2.47345374315282));
#20084=CARTESIAN_POINT('Ctrl Pts',(4.92568536669948,-0.576449711125441,
-2.55245357900038));
#20085=CARTESIAN_POINT('Ctrl Pts',(3.81412273705863,-1.47592145493228,-2.63145341484794));
#20086=CARTESIAN_POINT('Ctrl Pts',(2.4534374869252,-1.03642566702533,-2.71045325069551));
#20087=CARTESIAN_POINT('Ctrl Pts',(2.07805395827079,0.343323623218521,-2.78945308654307));
#20088=CARTESIAN_POINT('Ctrl Pts',(3.02852303551155,1.4116070269678,-2.86845292239064));
#20089=CARTESIAN_POINT('Ctrl Pts',(4.44257170942605,1.1992694530034,-2.9474527582382));
#20090=CARTESIAN_POINT('Ctrl Pts',(5.03736392102105,-0.101054784462667,
-3.02645259408576));
#20091=CARTESIAN_POINT('Ctrl Pts',(4.27329950608871,-1.30970132806027,-3.10545242993333));
#20092=CARTESIAN_POINT('Ctrl Pts',(2.84354370069912,-1.33017654407844,-3.18445226578088));
#20093=CARTESIAN_POINT('Ctrl Pts',(2.04518219683984,-0.143905155790045,
-3.26345210162845));
#20094=CARTESIAN_POINT('Ctrl Pts',(2.60249481892977,1.17291811966321,-3.34245193747601));
#20095=CARTESIAN_POINT('Ctrl Pts',(4.00988318062076,1.42566086811101,-3.42145177332358));
#20096=CARTESIAN_POINT('Ctrl Pts',(4.99055351046055,0.385032883820701,-3.50045160917113));
#20097=CARTESIAN_POINT('Ctrl Pts',(4.65483398575262,-1.00489995565251,-3.5794514450187));
#20098=CARTESIAN_POINT('Ctrl Pts',(3.30729199512237,-1.48317966565961,-3.65845128086626));
#20099=CARTESIAN_POINT('Ctrl Pts',(2.1704282123283,-0.615907138199342,-3.73745111671383));
#20100=CARTESIAN_POINT('Ctrl Pts',(2.27561438689736,0.810121180662424,-3.81645095256139));
#20101=CARTESIAN_POINT('Ctrl Pts',(3.52742479541991,1.50120120398156,-3.89545078840895));
#20102=CARTESIAN_POINT('Ctrl Pts',(4.79020720703601,0.830379708776461,-3.97445062425652));
#20103=CARTESIAN_POINT('Ctrl Pts',(4.91835550353555,-0.59376877773063,-4.05345046010407));
#20104=CARTESIAN_POINT('Ctrl Pts',(3.79561254421272,-1.47924556726675,-4.13245029595163));
#20105=CARTESIAN_POINT('Ctrl Pts',(2.44053955667557,-1.02273916428501,-4.21145013179919));
#20106=CARTESIAN_POINT('Ctrl Pts',(2.08246939420409,0.361604238293931,-4.29044996764677));
#20107=CARTESIAN_POINT('Ctrl Pts',(3.04624611948272,1.41789743685548,-4.36944980349431));
#20108=CARTESIAN_POINT('Ctrl Pts',(4.45752392050836,1.18786294846641,-4.4484496393419));
#20109=CARTESIAN_POINT('Ctrl Pts',(5.03598049592748,-0.11981013295363,-4.52744947518944));
#20110=CARTESIAN_POINT('Ctrl Pts',(4.25683549892569,-1.31879052110152,-4.60644931103702));
#20111=CARTESIAN_POINT('Ctrl Pts',(2.82693538802763,-1.32135379438171,-4.68544914688457));
#20112=CARTESIAN_POINT('Ctrl Pts',(2.04349677031109,-0.125174531149584,
-4.76444898273215));
#20113=CARTESIAN_POINT('Ctrl Pts',(2.61726131072331,1.18456404951518,-4.84344881857968));
#20114=CARTESIAN_POINT('Ctrl Pts',(4.02770531344641,1.41965682417793,-4.92244865442727));
#20115=CARTESIAN_POINT('Ctrl Pts',(4.99526290549326,0.366825781897791,-5.00144849027483));
#20116=CARTESIAN_POINT('Ctrl Pts',(4.64215824284418,-1.0187924897527,-5.08044832612239));
#20117=CARTESIAN_POINT('Ctrl Pts',(3.28873064775948,-1.48015421592793,-5.15944816196995));
#20118=CARTESIAN_POINT('Ctrl Pts',(2.1628202605679,-0.598708416385872,-5.23844799781751));
#20119=CARTESIAN_POINT('Ctrl Pts',(2.28586182430827,0.825890359097424,-5.31744783366508));
#20120=CARTESIAN_POINT('Ctrl Pts',(3.54623106632798,1.50123491655445,-5.39644766951263));
#20121=CARTESIAN_POINT('Ctrl Pts',(4.80051111482114,0.814647371176435,-5.47544750536019));
#20122=CARTESIAN_POINT('Ctrl Pts',(4.91080926215673,-0.610994665314678,
-5.55444734120777));
#20123=CARTESIAN_POINT('Ctrl Pts',(3.77706216309608,-1.4823375443742,-5.63344717705533));
#20124=CARTESIAN_POINT('Ctrl Pts',(2.42781408721338,-1.00889216500817,-5.71244701290288));
#20125=CARTESIAN_POINT('Ctrl Pts',(2.08711348220302,0.37982810749517,-5.79144684875045));
#20126=CARTESIAN_POINT('Ctrl Pts',(3.06404661184834,1.42396533876201,-5.87044668459801));
#20127=CARTESIAN_POINT('Ctrl Pts',(4.47233207081086,1.17627003482815,-5.94944652044556));
#20128=CARTESIAN_POINT('Ctrl Pts',(5.03436223395028,-0.138546679865455,
-6.02844635629314));
#20129=CARTESIAN_POINT('Ctrl Pts',(4.24025892463984,-1.32767275882361,-6.1074461921407));
#20130=CARTESIAN_POINT('Ctrl Pts',(2.81043889977172,-1.31232368711613,-6.18644602798827));
#20131=CARTESIAN_POINT('Ctrl Pts',(2.04204611174854,-0.106424263105081,
-6.26544586383582));
#20132=CARTESIAN_POINT('Ctrl Pts',(2.63217253069154,1.19602408795599,-6.34444569968339));
#20133=CARTESIAN_POINT('Ctrl Pts',(4.04545083611885,1.41342999616619,-6.42344553553094));
#20134=CARTESIAN_POINT('Ctrl Pts',(4.99974385337733,0.348561114693986,-6.5024453713785));
#20135=CARTESIAN_POINT('Ctrl Pts',(4.62930946483854,-1.03252514666121,-6.58144520722607));
#20136=CARTESIAN_POINT('Ctrl Pts',(3.2702086561495,-1.47689648837554,-6.66044504307363));
#20137=CARTESIAN_POINT('Ctrl Pts',(2.15542835156255,-0.581415740385269,
-6.7394448789212));
#20138=CARTESIAN_POINT('Ctrl Pts',(2.29630599579274,0.84152993210976,-6.81844471476877));
#20139=CARTESIAN_POINT('Ctrl Pts',(3.56503628393201,1.50103304315188,-6.89744455061633));
#20140=CARTESIAN_POINT('Ctrl Pts',(4.8106171374903,0.798787192494724,-6.97644438646388));
#20141=CARTESIAN_POINT('Ctrl Pts',(4.90304782678089,-0.62812467065362,-7.05544422231144));
#20142=CARTESIAN_POINT('Ctrl Pts',(3.75847450478497,-1.48519690103531,-7.134444058159));
#20143=CARTESIAN_POINT('Ctrl Pts',(2.4152630755228,-0.994886842179035,-7.21344389400658));
#20144=CARTESIAN_POINT('Ctrl Pts',(2.0919854934795,0.397992370984998,-7.29244372985414));
#20145=CARTESIAN_POINT('Ctrl Pts',(3.08192171921059,1.42980978046278,-7.3714435657017));
#20146=CARTESIAN_POINT('Ctrl Pts',(4.48699383651834,1.16449253134292,-7.45044340154927));
#20147=CARTESIAN_POINT('Ctrl Pts',(5.03250938904027,-0.157261484907092,
-7.5294432373968));
#20148=CARTESIAN_POINT('Ctrl Pts',(4.22357238456189,-1.33634664735353,-7.60844307324441));
#20149=CARTESIAN_POINT('Ctrl Pts',(2.79405682469425,-1.30308763935961,-7.68744290909193));
#20150=CARTESIAN_POINT('Ctrl Pts',(2.04083044880146,-0.087657294100584,
-7.76644274493952));
#20151=CARTESIAN_POINT('Ctrl Pts',(2.64722613884448,1.20729643658276,-7.84544258078706));
#20152=CARTESIAN_POINT('Ctrl Pts',(4.06311696386691,1.40698136124133,-7.92444241663464));
#20153=CARTESIAN_POINT('Ctrl Pts',(5.00399565092529,0.330241748447076,-8.00344225248219));
#20154=CARTESIAN_POINT('Ctrl Pts',(4.61628966807169,-1.04609577133396,-8.08244208832976));
#20155=CARTESIAN_POINT('Ctrl Pts',(3.25172892691107,-1.47340699423921,-8.16144192417732));
#20156=CARTESIAN_POINT('Ctrl Pts',(2.14825364531581,-0.564031823890016,
-8.24044176002488));
#20157=CARTESIAN_POINT('Ctrl Pts',(2.3069452623567,0.857037445382742,-8.31944159587245));
#20158=CARTESIAN_POINT('Ctrl Pts',(3.58383749718331,1.50059561550652,-8.39844143172001));
#20159=CARTESIAN_POINT('Ctrl Pts',(4.82052368908861,0.782801661538469,-8.47744126756757));
#20160=CARTESIAN_POINT('Ctrl Pts',(4.89507241546346,-0.645156105375968,
-8.55644110341514));
#20161=CARTESIAN_POINT('Ctrl Pts',(3.73985248607643,-1.48782318890163,-8.6354409392627));
#20162=CARTESIAN_POINT('Ctrl Pts',(2.40288849145644,-0.980725392932309,
-8.71444077511025));
#20163=CARTESIAN_POINT('Ctrl Pts',(2.09708466301015,0.416094176959081,-8.79344061095783));
#20164=CARTESIAN_POINT('Ctrl Pts',(3.09986863735219,1.43542984731223,-8.87244044680538));
#20165=CARTESIAN_POINT('Ctrl Pts',(4.50150691509507,1.15253228145486,-8.95144028265294));
#20166=CARTESIAN_POINT('Ctrl Pts',(5.03042225517976,-0.17595160211279,-9.0304401185005));
#20167=CARTESIAN_POINT('Ctrl Pts',(4.20677849115691,-1.34481084279703,-9.10943995434808));
#20168=CARTESIAN_POINT('Ctrl Pts',(2.77779174524815,-1.29364706763578,-9.18843979019563));
#20169=CARTESIAN_POINT('Ctrl Pts',(2.03984995009324,-0.0688766317242347,
-9.2674396260432));
#20170=CARTESIAN_POINT('Ctrl Pts',(2.66241981497398,1.21837944536639,-9.34643946189075));
#20171=CARTESIAN_POINT('Ctrl Pts',(4.08070084425368,1.40031170518944,-9.42543929773831));
#20172=CARTESIAN_POINT('Ctrl Pts',(5.00801778330857,0.311870988189331,-9.50443913358589));
#20173=CARTESIAN_POINT('Ctrl Pts',(4.60310060585307,-1.05950305241988,-9.58343896943344));
#20174=CARTESIAN_POINT('Ctrl Pts',(3.233294911356,-1.46968472477563,-9.662438805281));
#20175=CARTESIAN_POINT('Ctrl Pts',(2.1412962191189,-0.546562355108196,-9.74143864112856));
#20176=CARTESIAN_POINT('Ctrl Pts',(2.31777994889124,0.872416095653864,-9.82043847697613));
#20177=CARTESIAN_POINT('Ctrl Pts',(3.6026279620964,1.49991199335744,-9.89943831282369));
#20178=CARTESIAN_POINT('Ctrl Pts',(4.83023643037598,0.766713655392416,-9.97843814867126));
#20179=CARTESIAN_POINT('Ctrl Pts',(4.88687055597945,-0.662125038269567,
-10.0574379845188));
#20180=CARTESIAN_POINT('Ctrl Pts',(3.72122513262798,-1.49014230591843,-10.1364378203663));
#20181=CARTESIAN_POINT('Ctrl Pts',(2.39064262354056,-0.966550225602336,
-10.2154376562139));
#20182=CARTESIAN_POINT('Ctrl Pts',(2.10250467091252,0.434397551406489,-10.2944374920615));
#20183=CARTESIAN_POINT('Ctrl Pts',(3.11770451236289,1.44031508778373,-10.373437327909));
#20184=CARTESIAN_POINT('Ctrl Pts',(4.51621434152236,1.14137741925843,-10.4524371637566));
#20185=CARTESIAN_POINT('Ctrl Pts',(5.02741926695713,-0.196635563676407,
-10.5314369996042));
#20186=CARTESIAN_POINT('Ctrl Pts',(4.47009889505261,-0.964259040168617,
-10.5841035568359));
#20187=CARTESIAN_POINT('Ctrl Pts',(4.09066022205677,-1.14663922575821,-10.6104368354517));
#20188=CARTESIAN_POINT('Ctrl Pts',(4.22276258896322,0.956786087600807,-0.00116693790158886));
#20189=CARTESIAN_POINT('Ctrl Pts',(4.53945734382533,0.730642322779539,-0.0275065074384037));
#20190=CARTESIAN_POINT('Ctrl Pts',(4.92538271480697,-0.0566428170878688,
-0.0801793555910728));
#20191=CARTESIAN_POINT('Ctrl Pts',(4.24789474461888,-1.19392078423981,-0.159185482359595));
#20192=CARTESIAN_POINT('Ctrl Pts',(2.92726025435682,-1.24449194312104,-0.238185318207158));
#20193=CARTESIAN_POINT('Ctrl Pts',(2.16236448555846,-0.167798961195079,
-0.317185154054721));
#20194=CARTESIAN_POINT('Ctrl Pts',(2.64668019390599,1.06203237714166,-0.396184989902284));
#20195=CARTESIAN_POINT('Ctrl Pts',(3.94106727267031,1.32790237413237,-0.475184825749846));
#20196=CARTESIAN_POINT('Ctrl Pts',(4.87112409072546,0.389339689978404,-0.554184661597408));
#20197=CARTESIAN_POINT('Ctrl Pts',(4.59316073831506,-0.902566851583658,
-0.633184497444971));
#20198=CARTESIAN_POINT('Ctrl Pts',(3.35931360943555,-1.37558834803353,-0.712184333292533));
#20199=CARTESIAN_POINT('Ctrl Pts',(2.28895645692331,-0.600701735828637,
-0.791184169140097));
#20200=CARTESIAN_POINT('Ctrl Pts',(2.35311625561809,0.719165366393499,-0.870184004987657));
#20201=CARTESIAN_POINT('Ctrl Pts',(3.49359169428227,1.38658992886142,-0.949183840835221));
#20202=CARTESIAN_POINT('Ctrl Pts',(4.67573189207826,0.796094517421205,-1.02818367668278));
#20203=CARTESIAN_POINT('Ctrl Pts',(4.82709135188776,-0.516626874956721,
-1.10718351253034));
#20204=CARTESIAN_POINT('Ctrl Pts',(3.81035486229653,-1.36065884628765,-1.18618334837791));
#20205=CARTESIAN_POINT('Ctrl Pts',(2.54791412842535,-0.970291199099466,
-1.26518318422547));
#20206=CARTESIAN_POINT('Ctrl Pts',(2.1850650964183,0.300332646552455,-1.34418302007303));
#20207=CARTESIAN_POINT('Ctrl Pts',(3.05098736172375,1.29849214451639,-1.42318285592059));
#20208=CARTESIAN_POINT('Ctrl Pts',(4.36010939160367,1.11864948607607,-1.50218269176816));
#20209=CARTESIAN_POINT('Ctrl Pts',(4.92478543130558,-0.0760408277145407,
-1.58118252761572));
#20210=CARTESIAN_POINT('Ctrl Pts',(4.23273692898091,-1.20174627466853,-1.66018236346328));
#20211=CARTESIAN_POINT('Ctrl Pts',(2.91179572737664,-1.2372180823164,-1.73918219931084));
#20212=CARTESIAN_POINT('Ctrl Pts',(2.16033005138785,-0.15027592345917,-1.81818203515841));
#20213=CARTESIAN_POINT('Ctrl Pts',(2.6600754644131,1.072997728517,-1.89718187100597));
#20214=CARTESIAN_POINT('Ctrl Pts',(3.95765900297715,1.32283941919587,-1.97618170685353));
#20215=CARTESIAN_POINT('Ctrl Pts',(4.87590269388304,0.372590801624887,-2.0551815427011));
#20216=CARTESIAN_POINT('Ctrl Pts',(4.5817686510791,-0.915675115822265,-2.13418137854866));
#20217=CARTESIAN_POINT('Ctrl Pts',(3.34209758767953,-1.37323337936518,-2.21318121439622));
#20218=CARTESIAN_POINT('Ctrl Pts',(2.28152882525099,-0.584983539399816,
-2.29218105024378));
#20219=CARTESIAN_POINT('Ctrl Pts',(2.36221867188204,0.733967960252988,-2.37118088609134));
#20220=CARTESIAN_POINT('Ctrl Pts',(3.51096466517007,1.38705796386476,-2.45018072193891));
#20221=CARTESIAN_POINT('Ctrl Pts',(4.68561542095099,0.781798092524566,-2.52918055778647));
#20222=CARTESIAN_POINT('Ctrl Pts',(4.82051855112322,-0.532715146414797,
-2.60818039363403));
#20223=CARTESIAN_POINT('Ctrl Pts',(3.79328887684296,-1.3639450220661,-2.6871802294816));
#20224=CARTESIAN_POINT('Ctrl Pts',(2.5358372236292,-0.957793265052575,-2.76618006532916));
#20225=CARTESIAN_POINT('Ctrl Pts',(2.18893360381748,0.317276061867459,-2.84517990117672));
#20226=CARTESIAN_POINT('Ctrl Pts',(3.06729170491967,1.30451005445585,-2.92417973702428));
#20227=CARTESIAN_POINT('Ctrl Pts',(4.3740581614269,1.10828228363614,-3.00317957287185));
#20228=CARTESIAN_POINT('Ctrl Pts',(4.92372418427492,-0.093387876274314,
-3.0821794087194));
#20229=CARTESIAN_POINT('Ctrl Pts',(4.21762844198311,-1.21033582161941,-3.16117924456697));
#20230=CARTESIAN_POINT('Ctrl Pts',(2.89634653567684,-1.22925760696942,-3.24017908041453));
#20231=CARTESIAN_POINT('Ctrl Pts',(2.15855578444204,-0.132987240095699,
-3.31917891626209));
#20232=CARTESIAN_POINT('Ctrl Pts',(2.6735857503619,1.08393019510593,-3.39817875210966));
#20233=CARTESIAN_POINT('Ctrl Pts',(3.97419720473653,1.31749764712491,-3.47717858795722));
#20234=CARTESIAN_POINT('Ctrl Pts',(4.88046522476084,0.355820889698422,-3.55617842380478));
#20235=CARTESIAN_POINT('Ctrl Pts',(4.57021634735239,-0.928659372493224,
-3.63517825965234));
#20236=CARTESIAN_POINT('Ctrl Pts',(3.32491078993065,-1.37065256084301,-3.71417809549991));
#20237=CARTESIAN_POINT('Ctrl Pts',(2.27429953136583,-0.569178984690962,
-3.79317793134746));
#20238=CARTESIAN_POINT('Ctrl Pts',(2.37150535401595,0.748658235126427,-3.87217776719504));
#20239=CARTESIAN_POINT('Ctrl Pts',(3.52834237238777,1.38730682615101,-3.95117760304259));
#20240=CARTESIAN_POINT('Ctrl Pts',(4.6953189608238,0.767379772429904,-4.03017743889016));
#20241=CARTESIAN_POINT('Ctrl Pts',(4.81374479609618,-0.548720235712767,
-4.10917727473772));
#20242=CARTESIAN_POINT('Ctrl Pts',(3.77618303065766,-1.36701693788942,-4.18817711058528));
#20243=CARTESIAN_POINT('Ctrl Pts',(2.52391784424749,-0.94514514125183,-4.26717694643284));
#20244=CARTESIAN_POINT('Ctrl Pts',(2.19301404579585,0.334169748078935,-4.34617678228041));
#20245=CARTESIAN_POINT('Ctrl Pts',(3.08367015925906,1.31032321830978,-4.42517661812797));
#20246=CARTESIAN_POINT('Ctrl Pts',(4.38787596575953,1.09774117724432,-4.50417645397553));
#20247=CARTESIAN_POINT('Ctrl Pts',(4.92244571802357,-0.110720278432897,
-4.58317628982309));
#20248=CARTESIAN_POINT('Ctrl Pts',(4.20241353976848,-1.21873542822569,-4.66217612567066));
#20249=CARTESIAN_POINT('Ctrl Pts',(2.88099827624373,-1.22110422896304,-4.74117596151822));
#20250=CARTESIAN_POINT('Ctrl Pts',(2.15699822925082,-0.115677686018026,
-4.82017579736578));
#20251=CARTESIAN_POINT('Ctrl Pts',(2.68723192571078,1.09469256189437,-4.89917563321335));
#20252=CARTESIAN_POINT('Ctrl Pts',(3.99066719320976,1.31194912297586,-4.9781754690609));
#20253=CARTESIAN_POINT('Ctrl Pts',(4.88481732350589,0.33899513928263,-5.05717530490847));
#20254=CARTESIAN_POINT('Ctrl Pts',(4.55850229821843,-0.94149789629576,-5.13617514075603));
#20255=CARTESIAN_POINT('Ctrl Pts',(3.30775767026166,-1.36785664844046,-5.2151749766036));
#20256=CARTESIAN_POINT('Ctrl Pts',(2.26726878599858,-0.553285109766257,
-5.29417481245115));
#20257=CARTESIAN_POINT('Ctrl Pts',(2.38097533034757,0.763231024455163,-5.37317464829872));
#20258=CARTESIAN_POINT('Ctrl Pts',(3.5457218335393,1.38733798099046,-5.45217448414627));
#20259=CARTESIAN_POINT('Ctrl Pts',(4.70484112318846,0.752841028865123,-5.53117431999385));
#20260=CARTESIAN_POINT('Ctrl Pts',(4.80677107921609,-0.564639215372841,
-5.6101741558414));
#20261=CARTESIAN_POINT('Ctrl Pts',(3.75904004523867,-1.36987433031362,-5.68917399168897));
#20262=CARTESIAN_POINT('Ctrl Pts',(2.5121578412552,-0.932348697598894,-5.76817382753653));
#20263=CARTESIAN_POINT('Ctrl Pts',(2.19730579227532,0.351010993659279,-5.84717366338409));
#20264=CARTESIAN_POINT('Ctrl Pts',(3.10012014910864,1.3159307556026,-5.92617349923167));
#20265=CARTESIAN_POINT('Ctrl Pts',(4.40156063903508,1.08702780439152,-6.00517333507921));
#20266=CARTESIAN_POINT('Ctrl Pts',(4.92095023168801,-0.128035305466137,
-6.08417317092679));
#20267=CARTESIAN_POINT('Ctrl Pts',(4.18709461076685,-1.22694378097059,-6.16317300677434));
#20268=CARTESIAN_POINT('Ctrl Pts',(2.86575335723871,-1.21275922536378,-6.24217284262192));
#20269=CARTESIAN_POINT('Ctrl Pts',(2.15565763045507,-0.0983499788583807,
-6.32117267846946));
#20270=CARTESIAN_POINT('Ctrl Pts',(2.70101184887717,1.1052831406354,-6.40017251431704));
#20271=CARTESIAN_POINT('Ctrl Pts',(4.00706638385242,1.30619471711537,-6.47917235016458));
#20272=CARTESIAN_POINT('Ctrl Pts',(4.88895830712003,0.322116190996409,-6.55817218601216));
#20273=CARTESIAN_POINT('Ctrl Pts',(4.5466283419575,-0.954188672601991,-6.63717202185972));
#20274=CARTESIAN_POINT('Ctrl Pts',(3.29064092047072,-1.36484608086353,-6.71617185770728));
#20275=CARTESIAN_POINT('Ctrl Pts',(2.26043769247546,-0.537304408848601,
-6.79517169355484));
#20276=CARTESIAN_POINT('Ctrl Pts',(2.39062711476892,0.777684041372917,-6.87417152940241));
#20277=CARTESIAN_POINT('Ctrl Pts',(3.56310032129972,1.3871514234866,-6.95317136524997));
#20278=CARTESIAN_POINT('Ctrl Pts',(4.71418041374923,0.738184143371853,-7.03217120109753));
#20279=CARTESIAN_POINT('Ctrl Pts',(4.79959849485559,-0.580469587261487,
-7.11117103694509));
#20280=CARTESIAN_POINT('Ctrl Pts',(3.74186261080232,-1.37251675093242,-7.19017087279266));
#20281=CARTESIAN_POINT('Ctrl Pts',(2.50055906012761,-0.91940594221622,-7.26917070864021));
#20282=CARTESIAN_POINT('Ctrl Pts',(2.20180816976011,0.367797155743754,-7.34817054448779));
#20283=CARTESIAN_POINT('Ctrl Pts',(3.1166390930024,1.32133178635383,-7.42717038033534));
#20284=CARTESIAN_POINT('Ctrl Pts',(4.41511003374343,1.07614384630731,-7.50617021618291));
#20285=CARTESIAN_POINT('Ctrl Pts',(4.91923795995212,-0.145330240159424,
-7.58517005203047));
#20286=CARTESIAN_POINT('Ctrl Pts',(4.17167405894901,-1.23495959173261,-7.66416988787803));
#20287=CARTESIAN_POINT('Ctrl Pts',(2.85061417101823,-1.20422390573755,-7.74316972372559));
#20288=CARTESIAN_POINT('Ctrl Pts',(2.15453419843256,-0.0810068378210246,
-7.82216955957316));
#20289=CARTESIAN_POINT('Ctrl Pts',(2.7149233574034,1.11570026936884,-7.90116939542071));
#20290=CARTESIAN_POINT('Ctrl Pts',(4.02339220317067,1.30023533257259,-7.98016923126829));
#20291=CARTESIAN_POINT('Ctrl Pts',(4.89288752576577,0.305186693619449,-8.05916906711584));
#20292=CARTESIAN_POINT('Ctrl Pts',(4.53459634192857,-0.966729709868482,
-8.1381689029634));
#20293=CARTESIAN_POINT('Ctrl Pts',(3.27356322665466,-1.36162133056204,-8.21716873881097));
#20294=CARTESIAN_POINT('Ctrl Pts',(2.25380732279195,-0.521239389745805,
-8.29616857465853));
#20295=CARTESIAN_POINT('Ctrl Pts',(2.40045919263447,0.792015017769138,-8.37516841050609));
#20296=CARTESIAN_POINT('Ctrl Pts',(3.58047510851297,1.38674718296458,-8.45416824635366));
#20297=CARTESIAN_POINT('Ctrl Pts',(4.72333536687576,0.723411415934357,-8.53316808220121));
#20298=CARTESIAN_POINT('Ctrl Pts',(4.7922281686577,-0.596208866970824,-8.61216791804879));
#20299=CARTESIAN_POINT('Ctrl Pts',(3.72465342285165,-1.37494378541303,-8.69116775389634));
#20300=CARTESIAN_POINT('Ctrl Pts',(2.48912332126697,-0.906318905544476,
-8.77016758974391));
#20301=CARTESIAN_POINT('Ctrl Pts',(2.20652047126826,0.384525598891084,-8.84916742559147));
#20302=CARTESIAN_POINT('Ctrl Pts',(3.13322439947578,1.32652546531105,-8.92816726143904));
#20303=CARTESIAN_POINT('Ctrl Pts',(4.42852202203957,1.06509100657593,-9.00716709728659));
#20304=CARTESIAN_POINT('Ctrl Pts',(4.91730917449412,-0.162602360053987,
-9.08616693313416));
#20305=CARTESIAN_POINT('Ctrl Pts',(4.15615429857538,-1.24278161857717,-9.16516676898172));
#20306=CARTESIAN_POINT('Ctrl Pts',(2.83558310410754,-1.19549957913796,-9.24416660482928));
#20307=CARTESIAN_POINT('Ctrl Pts',(2.15362808901342,-0.0636510423119035,
-9.32316644067685));
#20308=CARTESIAN_POINT('Ctrl Pts',(2.72896430711279,1.12594242325137,-9.4021662765244));
#20309=CARTESIAN_POINT('Ctrl Pts',(4.03964201513864,1.29407169551693,-9.48116611237197));
#20310=CARTESIAN_POINT('Ctrl Pts',(4.896604503674,0.288209701435084,-9.56016594821952));
#20311=CARTESIAN_POINT('Ctrl Pts',(4.52240791841949,-0.979119796234855,
-9.6391657840671));
#20312=CARTESIAN_POINT('Ctrl Pts',(3.25652777827833,-1.35818146532484,-9.71816561991465));
#20313=CARTESIAN_POINT('Ctrl Pts',(2.24737774837526,-0.505095309108265,
-9.79716545576223));
#20314=CARTESIAN_POINT('Ctrl Pts',(2.41047186418625,0.806226907848581,-9.87616529160978));
#20315=CARTESIAN_POINT('Ctrl Pts',(3.59783996285183,1.38611542642761,-9.95516512745734));
#20316=CARTESIAN_POINT('Ctrl Pts',(4.73231121385275,0.708543987979741,-10.0341649633049));
#20317=CARTESIAN_POINT('Ctrl Pts',(4.78464857465049,-0.611890386791985,
-10.1131647991525));
#20318=CARTESIAN_POINT('Ctrl Pts',(3.70743930490157,-1.37708695373684,-10.1921646350001));
#20319=CARTESIAN_POINT('Ctrl Pts',(2.47780653301313,-0.8932191915644,-10.2711644708476));
#20320=CARTESIAN_POINT('Ctrl Pts',(2.21152926951652,0.401440317747649,-10.3501643066952));
#20321=CARTESIAN_POINT('Ctrl Pts',(3.14970708753058,1.33104006830733,-10.4291641425427));
#20322=CARTESIAN_POINT('Ctrl Pts',(4.44211361324239,1.05478245071491,-10.5081639783903));
#20323=CARTESIAN_POINT('Ctrl Pts',(4.91453401947221,-0.181717053669302,
-10.5871638142379));
#20324=CARTESIAN_POINT('Ctrl Pts',(4.39949689170713,-0.891101835687162,
-10.6398303714696));
#20325=CARTESIAN_POINT('Ctrl Pts',(4.04884578660764,-1.05964505011576,-10.6661636500854));
#20326=CARTESIAN_POINT('',(4.22506707917393,0.958749515186979,-10.500517058265));
#20327=CARTESIAN_POINT('Ctrl Pts',(4.22563688151301,0.959452996237738,-10.5));
#20328=CARTESIAN_POINT('Ctrl Pts',(4.2562168906156,0.942844384233757,-10.5));
#20329=CARTESIAN_POINT('Ctrl Pts',(4.28592702146003,0.924851671966296,-10.5));
#20330=CARTESIAN_POINT('Ctrl Pts',(4.31466131642553,0.90550344967816,-10.5));
#20331=CARTESIAN_POINT('Ctrl Pts',(4.35457535570847,0.878627352478251,-10.5));
#20332=CARTESIAN_POINT('Ctrl Pts',(4.39260790499763,0.849138177160262,-10.5));
#20333=CARTESIAN_POINT('Ctrl Pts',(4.42869685663605,0.817341922666849,-10.5));
#20334=CARTESIAN_POINT('Ctrl Pts',(4.46599521848368,0.784480114505271,-10.5));
#20335=CARTESIAN_POINT('Ctrl Pts',(4.50121824244792,0.74915350101323,-10.5));
#20336=CARTESIAN_POINT('Ctrl Pts',(4.53427434865288,0.71164930909598,-10.5));
#20337=CARTESIAN_POINT('Ctrl Pts',(4.54834774946247,0.695682167605729,-10.5));
#20338=CARTESIAN_POINT('Ctrl Pts',(4.56202803905104,0.679319759554166,-10.5));
#20339=CARTESIAN_POINT('Ctrl Pts',(4.57530644205088,0.66258198317025,-10.5));
#20340=CARTESIAN_POINT('Ctrl Pts',(4.58155620710802,0.654703989861894,-10.5));
#20341=CARTESIAN_POINT('Ctrl Pts',(4.58771180447156,0.646749202455899,-10.5));
#20342=CARTESIAN_POINT('Ctrl Pts',(4.59376918906261,0.638724849112881,-10.5));
#20343=CARTESIAN_POINT('Ctrl Pts',(4.62474005444643,0.597697048509672,-10.5));
#20344=CARTESIAN_POINT('Ctrl Pts',(4.65317519747177,0.554817087484474,-10.5));
#20345=CARTESIAN_POINT('Ctrl Pts',(4.67900095039148,0.5104163567665,-10.5));
#20346=CARTESIAN_POINT('Ctrl Pts',(4.7054689829035,0.464911391708797,-10.5));
#20347=CARTESIAN_POINT('Ctrl Pts',(4.7291969971767,0.41780829539787,-10.5));
#20348=CARTESIAN_POINT('Ctrl Pts',(4.75007397342937,0.369418834636001,-10.5));
#20349=CARTESIAN_POINT('Ctrl Pts',(4.76945845021146,0.324488746711177,-10.5));
#20350=CARTESIAN_POINT('Ctrl Pts',(4.78638508274871,0.278448543884407,-10.5));
#20351=CARTESIAN_POINT('Ctrl Pts',(4.80073253596587,0.231524038388971,-10.5));
#20352=CARTESIAN_POINT('Ctrl Pts',(4.8036207521087,0.222077894030463,-10.5));
#20353=CARTESIAN_POINT('Ctrl Pts',(4.80640169864761,0.212604391535165,-10.5));
#20354=CARTESIAN_POINT('Ctrl Pts',(4.80907390505575,0.20310887732277,-10.5));
#20355=CARTESIAN_POINT('Ctrl Pts',(4.82382063804542,0.150707306746792,-10.5));
#20356=CARTESIAN_POINT('Ctrl Pts',(4.83526858041764,0.097606612097567,-10.5));
#20357=CARTESIAN_POINT('Ctrl Pts',(4.84331427811994,0.0441419444719137,
-10.5));
#20358=CARTESIAN_POINT('Ctrl Pts',(4.85127241447955,-0.00874086707904043,
-10.5));
#20359=CARTESIAN_POINT('Ctrl Pts',(4.85590253247874,-0.06198087933818,-10.5));
#20360=CARTESIAN_POINT('Ctrl Pts',(4.85706162899042,-0.115279789094187,
-10.5));
#20361=CARTESIAN_POINT('Ctrl Pts',(4.85747724957996,-0.134391333363179,
-10.5));
#20362=CARTESIAN_POINT('Ctrl Pts',(4.85744613961991,-0.153510615472189,
-10.5));
#20363=CARTESIAN_POINT('Ctrl Pts',(4.85696012143623,-0.172624292325265,
-10.5));
#20364=CARTESIAN_POINT('Ctrl Pts',(4.85648938188235,-0.191137105254633,
-10.5));
#20365=CARTESIAN_POINT('Ctrl Pts',(4.85559188252653,-0.209644665520278,
-10.5));
#20366=CARTESIAN_POINT('Ctrl Pts',(4.85427508835799,-0.228137575142134,
-10.5));
#20367=CARTESIAN_POINT('Ctrl Pts',(4.85337448116019,-0.240785601623099,
-10.5));
#20368=CARTESIAN_POINT('Ctrl Pts',(4.85227772223906,-0.253426776185862,
-10.5));
#20369=CARTESIAN_POINT('Ctrl Pts',(4.85098698538755,-0.266058091305494,
-10.5));
#20370=CARTESIAN_POINT('Ctrl Pts',(4.84998324704724,-0.275880802464079,
-10.5));
#20371=CARTESIAN_POINT('Ctrl Pts',(4.84886269296499,-0.285692120985615,
-10.5));
#20372=CARTESIAN_POINT('Ctrl Pts',(4.84762783302268,-0.295482832018067,
-10.5));
#20373=CARTESIAN_POINT('Ctrl Pts',(4.8409806354647,-0.348185805234636,-10.5));
#20374=CARTESIAN_POINT('Ctrl Pts',(4.83101865061774,-0.400359240847176,
-10.5));
#20375=CARTESIAN_POINT('Ctrl Pts',(4.81798085892437,-0.451779699261908,
-10.5));
#20376=CARTESIAN_POINT('Ctrl Pts',(4.80449726831377,-0.50495836836319,-10.5));
#20377=CARTESIAN_POINT('Ctrl Pts',(4.78772387104494,-0.557332542920654,
-10.5));
#20378=CARTESIAN_POINT('Ctrl Pts',(4.76786911240598,-0.608661600473398,
-10.5));
#20379=CARTESIAN_POINT('Ctrl Pts',(4.75361695127058,-0.645506671847593,
-10.5));
#20380=CARTESIAN_POINT('Ctrl Pts',(4.73777586561183,-0.68181341338085,-10.5));
#20381=CARTESIAN_POINT('Ctrl Pts',(4.72040658847988,-0.717490842063492,
-10.5));
#20382=CARTESIAN_POINT('Ctrl Pts',(4.71341635861835,-0.731849149865565,
-10.5));
#20383=CARTESIAN_POINT('Ctrl Pts',(4.70617846932405,-0.746105493624825,
-10.5));
#20384=CARTESIAN_POINT('Ctrl Pts',(4.69869630293336,-0.760253747426929,
-10.5));
#20385=CARTESIAN_POINT('Ctrl Pts',(4.69367625902796,-0.769746299658832,
-10.5));
#20386=CARTESIAN_POINT('Ctrl Pts',(4.68854632090072,-0.779189830422629,
-10.5));
#20387=CARTESIAN_POINT('Ctrl Pts',(4.68331449686019,-0.788570465878601,
-10.5));
#20388=CARTESIAN_POINT('Ctrl Pts',(4.65536785501926,-0.838678660897688,
-10.5));
#20389=CARTESIAN_POINT('Ctrl Pts',(4.62447200580773,-0.887081914965809,
-10.5));
#20390=CARTESIAN_POINT('Ctrl Pts',(4.59084561731805,-0.933519384991513,
-10.5));
#20391=CARTESIAN_POINT('Ctrl Pts',(4.5630360211261,-0.971923963883094,-10.5));
#20392=CARTESIAN_POINT('Ctrl Pts',(4.53335770980376,-1.00898430302673,-10.5));
#20393=CARTESIAN_POINT('Ctrl Pts',(4.50190865869827,-1.04454497505135,-10.5));
#20394=CARTESIAN_POINT('Ctrl Pts',(4.49326968388208,-1.05431340173732,-10.5));
#20395=CARTESIAN_POINT('Ctrl Pts',(4.48449696594651,-1.06396860188547,-10.5));
#20396=CARTESIAN_POINT('Ctrl Pts',(4.4755922590162,-1.07350719070055,-10.5));
#20397=CARTESIAN_POINT('Ctrl Pts',(4.46697989294738,-1.08273262835935,-10.5));
#20398=CARTESIAN_POINT('Ctrl Pts',(4.45824953647072,-1.09184305726326,-10.5));
#20399=CARTESIAN_POINT('Ctrl Pts',(4.44940666939404,-1.10083236703997,-10.5));
#20400=CARTESIAN_POINT('Ctrl Pts',(4.40811313745869,-1.1428097423779,-10.5));
#20401=CARTESIAN_POINT('Ctrl Pts',(4.36434749913231,-1.18217192728758,-10.5));
#20402=CARTESIAN_POINT('Ctrl Pts',(4.3183086417908,-1.21863823117122,-10.5));
#20403=CARTESIAN_POINT('Ctrl Pts',(4.27226978444943,-1.25510453505477,-10.5));
#20404=CARTESIAN_POINT('Ctrl Pts',(4.22395717313442,-1.28867608466361,-10.5));
#20405=CARTESIAN_POINT('Ctrl Pts',(4.1735261449982,-1.31904027763685,-10.5));
#20406=CARTESIAN_POINT('Ctrl Pts',(4.21285985862019,0.966285267670136,-10.5));
#20407=CARTESIAN_POINT('Ctrl Pts',(4.21677432467609,0.963557533091195,-10.500172352755));
#20408=CARTESIAN_POINT('Ctrl Pts',(4.22067221525924,0.960806011697469,-10.50034470551));
#20409=CARTESIAN_POINT('Ctrl Pts',(4.22455324251919,0.95803090668261,-10.500517058265));
#20410=CARTESIAN_POINT('Ctrl Pts',(4.17505875713847,-1.32076734070061,3.60605642568679E-16));
#20411=CARTESIAN_POINT('Ctrl Pts',(4.21175869148079,-1.29893467734339,2.81168414804524E-15));
#20412=CARTESIAN_POINT('Ctrl Pts',(4.24734010600691,-1.27545799450025,1.12858061007627E-15));
#20413=CARTESIAN_POINT('Ctrl Pts',(4.28167883941674,-1.25033821821112,1.58033308661487E-15));
#20414=CARTESIAN_POINT('Ctrl Pts',(4.32789021929204,-1.21653325777111,2.12731127463373E-15));
#20415=CARTESIAN_POINT('Ctrl Pts',(4.37185284323022,-1.17975348759852,2.30323139873742E-15));
#20416=CARTESIAN_POINT('Ctrl Pts',(4.41343554449499,-1.14031584215013,1.65492619608187E-15));
#20417=CARTESIAN_POINT('Ctrl Pts',(4.45548068146681,-1.100439615876,9.99411277230459E-16));
#20418=CARTESIAN_POINT('Ctrl Pts',(4.49509318427713,-1.05784495275133,1.62667307186133E-15));
#20419=CARTESIAN_POINT('Ctrl Pts',(4.53209185513524,-1.01283383283948,1.56125112837913E-15));
#20420=CARTESIAN_POINT('Ctrl Pts',(4.54201219813825,-1.00076513582634,1.54370973826388E-15));
#20421=CARTESIAN_POINT('Ctrl Pts',(4.55174435185581,-0.988522626003564,
1.56237023283978E-15));
#20422=CARTESIAN_POINT('Ctrl Pts',(4.56128420031517,-0.976111976277783,
1.79023462720806E-15));
#20423=CARTESIAN_POINT('Ctrl Pts',(4.56823205005158,-0.967073328568305,
1.9869967211788E-15));
#20424=CARTESIAN_POINT('Ctrl Pts',(4.57507846805373,-0.95794470700848,2.05160167689976E-15));
#20425=CARTESIAN_POINT('Ctrl Pts',(4.58181998349954,-0.948730743276248,
2.21350715534641E-15));
#20426=CARTESIAN_POINT('Ctrl Pts',(4.5878624474001,-0.940472207983901,2.35862408293951E-15));
#20427=CARTESIAN_POINT('Ctrl Pts',(4.59381742463971,-0.932149464021884,
2.4118579661099E-15));
#20428=CARTESIAN_POINT('Ctrl Pts',(4.59968082387781,-0.923769113033705,
2.13024042849952E-15));
#20429=CARTESIAN_POINT('Ctrl Pts',(4.63227995240401,-0.877176321401323,
8.03406007810654E-16));
#20430=CARTESIAN_POINT('Ctrl Pts',(4.66208807399467,-0.828755572706594,
2.02916507695729E-15));
#20431=CARTESIAN_POINT('Ctrl Pts',(4.68897102900036,-0.778810683153279,
1.83880688453542E-15));
#20432=CARTESIAN_POINT('Ctrl Pts',(4.715408739606,-0.729692997394368,1.6516014675121E-15));
#20433=CARTESIAN_POINT('Ctrl Pts',(4.73901760306379,-0.679100122019099,
4.5266924147842E-16));
#20434=CARTESIAN_POINT('Ctrl Pts',(4.75962250001883,-0.627308223650069,
1.29757316003065E-15));
#20435=CARTESIAN_POINT('Ctrl Pts',(4.77786038072504,-0.581465991773642,
2.04541756363981E-15));
#20436=CARTESIAN_POINT('Ctrl Pts',(4.79374431288129,-0.534683755159472,
2.37654961231099E-15));
#20437=CARTESIAN_POINT('Ctrl Pts',(4.80711873651456,-0.487154600398972,
1.58206781009085E-15));
#20438=CARTESIAN_POINT('Ctrl Pts',(4.81112276225609,-0.472925354761761,
1.37998562811125E-15));
#20439=CARTESIAN_POINT('Ctrl Pts',(4.81490302992813,-0.458622862382454,
7.62743180822846E-16));
#20440=CARTESIAN_POINT('Ctrl Pts',(4.81844677957601,-0.444286884642647,
1.01307850997046E-15));
#20441=CARTESIAN_POINT('Ctrl Pts',(4.8314764555538,-0.391576291814387,1.94800769444789E-15));
#20442=CARTESIAN_POINT('Ctrl Pts',(4.84133483345071,-0.338344892022729,
-1.36320875843642E-15));
#20443=CARTESIAN_POINT('Ctrl Pts',(4.84786961538125,-0.284855426792769,
-1.81799020282369E-15));
#20444=CARTESIAN_POINT('Ctrl Pts',(4.85419670205816,-0.23306601952435,-1.58832042192958E-15));
#20445=CARTESIAN_POINT('Ctrl Pts',(4.85740809979461,-0.181033825930539,
-1.15722930975132E-15));
#20446=CARTESIAN_POINT('Ctrl Pts',(4.85731751599618,-0.129002639121944,
-4.16333634234434E-16));
#20447=CARTESIAN_POINT('Ctrl Pts',(4.85727473537566,-0.104429520122545,
-3.46124443849845E-16));
#20448=CARTESIAN_POINT('Ctrl Pts',(4.856494756818,-0.0798567823844845,3.76639887157404E-16));
#20449=CARTESIAN_POINT('Ctrl Pts',(4.85495404695298,-0.0553113446397769,
7.63278329429795E-16));
#20450=CARTESIAN_POINT('Ctrl Pts',(4.85315804114454,-0.0266987227821337,
1.1759601691976E-15));
#20451=CARTESIAN_POINT('Ctrl Pts',(4.85032828424195,0.00187688481085785,
1.38058548014164E-15));
#20452=CARTESIAN_POINT('Ctrl Pts',(4.8464840467839,0.0303705085563297,-4.57966997657877E-16));
#20453=CARTESIAN_POINT('Ctrl Pts',(4.8449279844867,0.0419040972341098,-1.17936797381194E-15));
#20454=CARTESIAN_POINT('Ctrl Pts',(4.84320517044147,0.0534263312481266,
1.71590219105396E-15));
#20455=CARTESIAN_POINT('Ctrl Pts',(4.84132080768837,0.0649121098521592,
1.36002320516582E-15));
#20456=CARTESIAN_POINT('Ctrl Pts',(4.83280402732952,0.116824542031136,-3.53615764954016E-16));
#20457=CARTESIAN_POINT('Ctrl Pts',(4.82097943108821,0.16809263458422,9.08710747336598E-16));
#20458=CARTESIAN_POINT('Ctrl Pts',(4.80603635446104,0.218463194567921,4.16333634234434E-16));
#20459=CARTESIAN_POINT('Ctrl Pts',(4.79103253706761,0.269038501304066,-7.80448982467912E-17));
#20460=CARTESIAN_POINT('Ctrl Pts',(4.77288409654513,0.318709937008753,-1.91585121700684E-16));
#20461=CARTESIAN_POINT('Ctrl Pts',(4.7517374255193,0.367195857426411,-6.52256026967279E-16));
#20462=CARTESIAN_POINT('Ctrl Pts',(4.73115375517605,0.414390907699223,-1.10066221057683E-15));
#20463=CARTESIAN_POINT('Ctrl Pts',(4.70772855633126,0.460463414084556,-1.80544295475632E-15));
#20464=CARTESIAN_POINT('Ctrl Pts',(4.68156583033195,0.50511771381136,-1.94289029309402E-16));
#20465=CARTESIAN_POINT('Ctrl Pts',(4.67575682331076,0.515032473483056,-4.95920238020822E-17));
#20466=CARTESIAN_POINT('Ctrl Pts',(4.66981719320886,0.524869491416437,-2.32356906808459E-16));
#20467=CARTESIAN_POINT('Ctrl Pts',(4.66375152405354,0.534621049953091,-4.9960036108132E-16));
#20468=CARTESIAN_POINT('Ctrl Pts',(4.63663984781298,0.578207518505316,-1.5147220868618E-15));
#20469=CARTESIAN_POINT('Ctrl Pts',(4.60699440856623,0.620121024458588,-2.06711395355149E-15));
#20470=CARTESIAN_POINT('Ctrl Pts',(4.57494698409233,0.660089312547657,-9.71445146547012E-16));
#20471=CARTESIAN_POINT('Ctrl Pts',(4.54970696039761,0.691567677969098,-1.08514439810198E-16));
#20472=CARTESIAN_POINT('Ctrl Pts',(4.52297617472456,0.721838929845157,8.87735236017173E-16));
#20473=CARTESIAN_POINT('Ctrl Pts',(4.49480733225647,0.750750410734639,5.27355936696949E-16));
#20474=CARTESIAN_POINT('Ctrl Pts',(4.48399014602072,0.761852779370735,3.51819881515091E-16));
#20475=CARTESIAN_POINT('Ctrl Pts',(4.47295717962163,0.772757609187209,-1.45592073936577E-15));
#20476=CARTESIAN_POINT('Ctrl Pts',(4.46173300251126,0.783435436762616,-1.27675647831893E-15));
#20477=CARTESIAN_POINT('Ctrl Pts',(4.42595244233202,0.817474337644931,-6.13637071966557E-16));
#20478=CARTESIAN_POINT('Ctrl Pts',(4.38819523463332,0.849248702584587,-1.66910301889349E-15));
#20479=CARTESIAN_POINT('Ctrl Pts',(4.34857042848663,0.878489835334903,-1.4432899320127E-15));
#20480=CARTESIAN_POINT('Ctrl Pts',(4.30894562233994,0.907730968085219,-1.25272571723038E-15));
#20481=CARTESIAN_POINT('Ctrl Pts',(4.26745256771982,0.934439563987207,-1.0624151382049E-17));
#20482=CARTESIAN_POINT('Ctrl Pts',(4.22418347496246,0.958295198918397,4.71844785465692E-16));
#20483=CARTESIAN_POINT('Origin',(3.53951905042299,8.32667268468867E-16,
-10.5));
#20484=CARTESIAN_POINT('Origin',(3.53951905042299,8.32667268468867E-16,
0.));
#40721=UNCERTAINTY_MEASURE_WITH_UNIT(LENGTH_MEASURE(0.01),#40735,
'DISTANCE_ACCURACY_VALUE',
'Maximum model space distance between geometric entities at asserted c
onnectivities');
#40724=UNCERTAINTY_MEASURE_WITH_UNIT(LENGTH_MEASURE(0.01),#40735,
'DISTANCE_ACCURACY_VALUE',
'Maximum model space distance between geometric entities at asserted c
onnectivities');
#40731=(
GEOMETRIC_REPRESENTATION_CONTEXT(3)
GLOBAL_UNCERTAINTY_ASSIGNED_CONTEXT((#40721))
GLOBAL_UNIT_ASSIGNED_CONTEXT((#40735,#40737,#40738))
REPRESENTATION_CONTEXT('','3D')
);
#40734=(
GEOMETRIC_REPRESENTATION_CONTEXT(3)
GLOBAL_UNCERTAINTY_ASSIGNED_CONTEXT((#40724))
GLOBAL_UNIT_ASSIGNED_CONTEXT((#40735,#40737,#40738))
REPRESENTATION_CONTEXT('','3D')
);
#40735=(
LENGTH_UNIT()
NAMED_UNIT(*)
SI_UNIT(.MILLI.,.METRE.)
);
#40737=(
NAMED_UNIT(*)
PLANE_ANGLE_UNIT()
SI_UNIT($,.RADIAN.)
);
#40738=(
NAMED_UNIT(*)
SI_UNIT($,.STERADIAN.)
SOLID_ANGLE_UNIT()
);
#40745=SHAPE_DEFINITION_REPRESENTATION(#40754,#40771);
#40754=PRODUCT_DEFINITION_SHAPE('',$,#40781);
#40771=SHAPE_REPRESENTATION('',(#3351),#40731);
#40774=PRODUCT_DEFINITION_CONTEXT('part definition',#40803,'design');
#40781=PRODUCT_DEFINITION('Screw','Screw',#40790,#40774);
#40790=PRODUCT_DEFINITION_FORMATION('',$,#40811);
#40803=APPLICATION_CONTEXT(
'Core Data for Automotive Mechanical Design Process');
#40804=PRODUCT_CONTEXT('part definition',#40803,'mechanical');
#40811=PRODUCT('Screw','Screw',$,(#40804));
#40815=PRESENTATION_STYLE_ASSIGNMENT((#40818));
#40818=SURFACE_STYLE_USAGE(.BOTH.,#40821);
#40821=SURFACE_SIDE_STYLE('',(#40824));
#40824=SURFACE_STYLE_FILL_AREA(#40827);
#40827=FILL_AREA_STYLE('Opaque(203,203,203)',(#40830));
#40830=FILL_AREA_STYLE_COLOUR('Opaque(203,203,203)',#40833);
#40833=COLOUR_RGB('Opaque(203,203,203)', 0.09019608, 0.27058824, 0.51372549);
ENDSEC;
END-ISO-10303-21;
